ISO-10303-21;
HEADER;
FILE_DESCRIPTION (('STEP AP214'),
    '1' );
FILE_NAME ('motion translator_ISO - Spur gear 0.25M 58T 20PA 2FW ---S58B6H18L3.0N.step',
    '2026-10-09T15:17:24',
    ( '' ),
    ( '' ),
    'SwSTEP 2.0',
    'SolidWorks 2026',
    '' );
FILE_SCHEMA (( 'AUTOMOTIVE_DESIGN' ));
ENDSEC;

DATA;
#9=DIRECTION ( 'NONE',  ( -1.000000000000000000, 0.000000000000000000, 0.000000000000000000 ) ) ;
#19=DIRECTION ( 'NONE',  ( 1.000000000000000000, 0.000000000000000000, 0.000000000000000000 ) ) ;
#21=EDGE_LOOP ( 'NONE', ( #48561, #59529, #5133, #41435 ) ) ;
#34=EDGE_CURVE ( 'NONE', #6901, #57938, #39765, .T. ) ;
#35=CIRCLE ( 'NONE', #8525, 2.899999999999994582 ) ;
#37=ORIENTED_EDGE ( 'NONE', *, *, #2591, .T. ) ;
#40=CARTESIAN_POINT ( 'NONE',  ( -22.27721056931765631, -3.610969226755186057, 0.7178530073137494583 ) ) ;
#50=ORIENTED_EDGE ( 'NONE', *, *, #19511, .T. ) ;
#55=CARTESIAN_POINT ( 'NONE',  ( -22.30078715814471835, 0.2606204736987125514, 3.743307663037636956 ) ) ;
#59=VERTEX_POINT ( 'NONE', #24459 ) ;
#60=DIRECTION ( 'NONE',  ( -1.000000000000000000, 0.000000000000000000, 0.000000000000000000 ) ) ;
#67=DIRECTION ( 'NONE',  ( -1.000000000000000000, 0.000000000000000000, 0.000000000000000000 ) ) ;
#70=CARTESIAN_POINT ( 'NONE',  ( -25.62834777364930616, 3.789932915281918113, 0.3208481691297681571 ) ) ;
#71=LINE ( 'NONE', #60932, #20822 ) ;
#74=DIRECTION ( 'NONE',  ( 0.000000000000000000, 0.000000000000000000, -1.000000000000000000 ) ) ;
#78=CARTESIAN_POINT ( 'NONE',  ( -22.30625920655495165, -3.783486345733982237, 0.2529928606556808846 ) ) ;
#89=CARTESIAN_POINT ( 'NONE',  ( -27.09229696323321335, -2.225368503508849294, 0.6397626223479151442 ) ) ;
#100=CARTESIAN_POINT ( 'NONE',  ( -22.30625920655495165, 0.8854385781085528651, -3.687109008463846926 ) ) ;
#101=EDGE_CURVE ( 'NONE', #9709, #46803, #31331, .T. ) ;
#104=ORIENTED_EDGE ( 'NONE', *, *, #19181, .T. ) ;
#106=AXIS2_PLACEMENT_3D ( 'NONE', #32837, #48187, #63433 ) ;
#117=CARTESIAN_POINT ( 'NONE',  ( 2.000000000000001776, -6.441884263200823746, -2.217201541069834914 ) ) ;
#125=VERTEX_POINT ( 'NONE', #10810 ) ;
#126=CARTESIAN_POINT ( 'NONE',  ( -22.28506771379528573, 3.622079238249921840, 0.8783543640076683090 ) ) ;
#128=CARTESIAN_POINT ( 'NONE',  ( -22.29570301036918778, 3.588849529203733457, -1.042190670255880525 ) ) ;
#135=EDGE_LOOP ( 'NONE', ( #15997, #3702, #27078, #2033 ) ) ;
#138=AXIS2_PLACEMENT_3D ( 'NONE', #35736, #56035, #531 ) ;
#157=CARTESIAN_POINT ( 'NONE',  ( -22.29018399051993882, -0.9010028109495024085, 3.609810019245832002 ) ) ;
#164=FACE_OUTER_BOUND ( 'NONE', #34592, .T. ) ;
#165=AXIS2_PLACEMENT_3D ( 'NONE', #42783, #38794, #59092 ) ;
#175=CARTESIAN_POINT ( 'NONE',  ( -27.08579483061202708, -2.287150433979698416, 0.2015567301747388795 ) ) ;
#178=EDGE_CURVE ( 'NONE', #56217, #10069, #62087, .T. ) ;
#179=FACE_OUTER_BOUND ( 'NONE', #65053, .T. ) ;
#180=DIRECTION ( 'NONE',  ( -1.000000000000000000, 0.000000000000000000, 0.000000000000000000 ) ) ;
#181=EDGE_CURVE ( 'NONE', #43273, #6060, #21747, .T. ) ;
#186=VECTOR ( 'NONE', #14671, 1000.000000000000000 ) ;
#191=B_SPLINE_CURVE_WITH_KNOTS ( 'NONE', 3,
 ( #18911, #33216, #7968, #28236, #58853, #48528 ),
 .UNSPECIFIED., .F., .F.,
 ( 4, 2, 4 ),
 ( 0.0002637379172017313396, 0.0009975831966478583904, 0.001731428476093985116 ),
 .UNSPECIFIED. ) ;
#194=CARTESIAN_POINT ( 'NONE',  ( -27.15511094194037867, -2.499833641087594760, 0.1446243978645337658 ) ) ;
#195=CARTESIAN_POINT ( 'NONE',  ( -35.04709527796842394, 0.01012471662513447779, 0.007095259204982495849 ) ) ;
#199=CARTESIAN_POINT ( 'NONE',  ( -27.08421860617808363, -2.116856729767840228, -0.8768262158915675064 ) ) ;
#201=CARTESIAN_POINT ( 'NONE',  ( -27.32343372485683730, 2.534722478175136740, 1.625341394141078144 ) ) ;
#206=EDGE_CURVE ( 'NONE', #57207, #22857, #45089, .T. ) ;
#214=CIRCLE ( 'NONE', #62853, 6.936499999999993449 ) ;
#226=DIRECTION ( 'NONE',  ( -1.000000000000000000, 0.000000000000000000, 0.000000000000000000 ) ) ;
#228=FACE_OUTER_BOUND ( 'NONE', #46876, .T. ) ;
#233=CARTESIAN_POINT ( 'NONE',  ( 2.000000000000001776, -2.562706407243573459, -6.312399813420393357 ) ) ;
#236=EDGE_CURVE ( 'NONE', #36605, #55598, #2693, .T. ) ;
#241=EDGE_CURVE ( 'NONE', #20405, #8903, #32353, .T. ) ;
#244=LINE ( 'NONE', #9870, #20494 ) ;
#247=CARTESIAN_POINT ( 'NONE',  ( 2.000000000000001776, -0.7281529553921466391, -7.464569195442808613 ) ) ;
#251=CARTESIAN_POINT ( 'NONE',  ( -22.27721056931765631, -1.183805672860815283, 3.486117586310720995 ) ) ;
#258=CARTESIAN_POINT ( 'NONE',  ( -27.09483304420799143, 2.317106154747425872, -0.1669215111592681211 ) ) ;
#262=CARTESIAN_POINT ( 'NONE',  ( -35.04834644901396956, -0.01383120537648091335, 0.0002835132723572086118 ) ) ;
#263=FACE_OUTER_BOUND ( 'NONE', #15822, .T. ) ;
#267=AXIS2_PLACEMENT_3D ( 'NONE', #40883, #20912, #26243 ) ;
#290=CARTESIAN_POINT ( 'NONE',  ( 2.000000000000001776, 3.155844197800189210, -6.177028383390422484 ) ) ;
#291=AXIS2_PLACEMENT_3D ( 'NONE', #33597, #54208, #9283 ) ;
#293=CARTESIAN_POINT ( 'NONE',  ( -27.28573687977896611, -0.4470060700698409994, 2.862048090118440857 ) ) ;
#294=VECTOR ( 'NONE', #14164, 1000.000000000000000 ) ;
#296=EDGE_CURVE ( 'NONE', #24592, #42057, #62639, .T. ) ;
#298=ORIENTED_EDGE ( 'NONE', *, *, #33062, .T. ) ;
#299=CARTESIAN_POINT ( 'NONE',  ( -27.08702828306202193, -0.5765135930295117728, 2.226264228965860070 ) ) ;
#304=CIRCLE ( 'NONE', #21567, 6.936499999999989008 ) ;
#305=CARTESIAN_POINT ( 'NONE',  ( -22.27218376572352554, -3.547715993389675582, 0.9890213205919727857 ) ) ;
#307=VECTOR ( 'NONE', #56220, 1000.000000000000000 ) ;
#313=DIRECTION ( 'NONE',  ( 0.000000000000000000, 0.000000000000000000, 1.000000000000000000 ) ) ;
#319=ADVANCED_FACE ( 'NONE', ( #1518 ), #2557, .F. ) ;
#320=CARTESIAN_POINT ( 'NONE',  ( 2.000000000000001776, -4.962980376314093611, 4.846014654777763830 ) ) ;
#321=EDGE_LOOP ( 'NONE', ( #20951, #13092, #29653, #40953 ) ) ;
#331=CARTESIAN_POINT ( 'NONE',  ( -27.09125059358652976, -2.243253600381622803, -0.5611156659262992452 ) ) ;
#332=VERTEX_POINT ( 'NONE', #63974 ) ;
#334=CARTESIAN_POINT ( 'NONE',  ( 0.000000000000000000, 0.000000000000000000, 0.000000000000000000 ) ) ;
#340=EDGE_LOOP ( 'NONE', ( #633, #26710, #31623, #29348 ) ) ;
#345=AXIS2_PLACEMENT_3D ( 'NONE', #43283, #37319, #57631 ) ;
#348=LINE ( 'NONE', #20626, #43001 ) ;
#349=EDGE_LOOP ( 'NONE', ( #5413, #53685, #34393, #20305 ) ) ;
#353=CARTESIAN_POINT ( 'NONE',  ( -22.27706485742869091, 2.625261754997705310, -2.580541389029900934 ) ) ;
#362=AXIS2_PLACEMENT_3D ( 'NONE', #13702, #44294, #38671 ) ;
#375=CIRCLE ( 'NONE', #17362, 2.899999999999995026 ) ;
#383=VECTOR ( 'NONE', #63975, 1000.000000000000000 ) ;
#384=AXIS2_PLACEMENT_3D ( 'NONE', #29738, #61009, #5154 ) ;
#390=LINE ( 'NONE', #40941, #307 ) ;
#392=DIRECTION ( 'NONE',  ( 0.000000000000000000, 0.000000000000000000, 1.000000000000000000 ) ) ;
#393=AXIS2_PLACEMENT_3D ( 'NONE', #15543, #5604, #5260 ) ;
#399=ORIENTED_EDGE ( 'NONE', *, *, #28460, .T. ) ;
#408=AXIS2_PLACEMENT_3D ( 'NONE', #57980, #3109, #2452 ) ;
#419=CARTESIAN_POINT ( 'NONE',  ( -22.66110217412718697, 4.192227617777429138, 2.622110956932540038 ) ) ;
#420=CARTESIAN_POINT ( 'NONE',  ( 2.000000000000001776, 0.000000000000000000, 0.000000000000000000 ) ) ;
#421=FACE_OUTER_BOUND ( 'NONE', #30596, .T. ) ;
#423=AXIS2_PLACEMENT_3D ( 'NONE', #17587, #51850, #16598 ) ;
#440=CARTESIAN_POINT ( 'NONE',  ( -27.20102706715913143, -0.8206313329275967128, -2.512061365242614919 ) ) ;
#441=CIRCLE ( 'NONE', #54549, 6.936499999999987232 ) ;
#447=ORIENTED_EDGE ( 'NONE', *, *, #54741, .T. ) ;
#451=VERTEX_POINT ( 'NONE', #48384 ) ;
#455=EDGE_CURVE ( 'NONE', #51352, #10755, #51524, .T. ) ;
#456=CARTESIAN_POINT ( 'NONE',  ( -35.04709527796842394, 0.001003525937978352878, -0.01232256164996822778 ) ) ;
#475=CARTESIAN_POINT ( 'NONE',  ( -22.28284753389937478, 3.563226652211057388, -0.9912969289936535144 ) ) ;
#479=ORIENTED_EDGE ( 'NONE', *, *, #27553, .F. ) ;
#497=DIRECTION ( 'NONE',  ( -1.000000000000000000, 0.000000000000000000, 0.000000000000000000 ) ) ;
#500=CARTESIAN_POINT ( 'NONE',  ( -22.29978294495153790, -0.8878583829805396510, 3.642708310327676280 ) ) ;
#509=DIRECTION ( 'NONE',  ( 1.000000000000000000, -0.000000000000000000, -0.000000000000000000 ) ) ;
#512=CARTESIAN_POINT ( 'NONE',  ( 2.000000000000001776, 0.000000000000000000, 0.000000000000000000 ) ) ;
#514=CARTESIAN_POINT ( 'NONE',  ( -22.29978294495153790, 0.8878583829805657412, -3.642708310327676280 ) ) ;
#520=CARTESIAN_POINT ( 'NONE',  ( -22.27721698446158172, -0.6951119527727915859, -3.615509722105072044 ) ) ;
#522=CARTESIAN_POINT ( 'NONE',  ( 2.000000000000001776, -3.979254915827311390, -5.681598592373819478 ) ) ;
#530=VECTOR ( 'NONE', #52703, 1000.000000000000227 ) ;
#531=DIRECTION ( 'NONE',  ( 0.000000000000000000, 0.9985334138511239299, -0.05413890858541457046 ) ) ;
#534=CARTESIAN_POINT ( 'NONE',  ( 2.000000000000001776, 6.250523986464036064, -3.007653927006531447 ) ) ;
#551=DIRECTION ( 'NONE',  ( 0.000000000000000000, 0.000000000000000000, 1.000000000000000000 ) ) ;
#554=LINE ( 'NONE', #31449, #3124 ) ;
#557=CARTESIAN_POINT ( 'NONE',  ( -27.09125059358652265, 2.243253600381615698, 0.5611156659262670487 ) ) ;
#563=CARTESIAN_POINT ( 'NONE',  ( -27.08871896697694837, 1.309412067288143078, 1.896680818244922850 ) ) ;
#570=MECHANICAL_DESIGN_GEOMETRIC_PRESENTATION_REPRESENTATION('',(#52641),#64299);
#580=AXIS2_PLACEMENT_3D ( 'NONE', #12761, #33050, #53357 ) ;
#581=DIRECTION ( 'NONE',  ( 0.000000000000000000, 0.000000000000000000, 1.000000000000000000 ) ) ;
#588=CARTESIAN_POINT ( 'NONE',  ( -27.08485414902839494, 0.5917839443972588986, -2.215517476308472400 ) ) ;
#589=CARTESIAN_POINT ( 'NONE',  ( -27.08871896697731785, 2.297279805116092977, -0.1856437051692902407 ) ) ;
#596=ORIENTED_EDGE ( 'NONE', *, *, #56050, .F. ) ;
#609=CARTESIAN_POINT ( 'NONE',  ( 0.000000000000000000, -1.779948802829851129, 6.576141558201223702 ) ) ;
#610=ORIENTED_EDGE ( 'NONE', *, *, #32209, .F. ) ;
#611=CARTESIAN_POINT ( 'NONE',  ( -22.29677679919927868, -3.730758197825073008, 0.2674217835790752007 ) ) ;
#620=CARTESIAN_POINT ( 'NONE',  ( -22.71097035706202405, 4.089776368546564456, 2.846599994298306679 ) ) ;
#622=CARTESIAN_POINT ( 'NONE',  ( 0.000000000000000000, 0.000000000000000000, 0.000000000000000000 ) ) ;
#625=CARTESIAN_POINT ( 'NONE',  ( -27.09229696323388836, -0.5586335684078734820, 2.247106967996828963 ) ) ;
#633=ORIENTED_EDGE ( 'NONE', *, *, #3467, .F. ) ;
#634=VERTEX_POINT ( 'NONE', #46897 ) ;
#638=DIRECTION ( 'NONE',  ( 0.000000000000000000, 0.1081190184239353008, 0.9941379571543603744 ) ) ;
#640=CARTESIAN_POINT ( 'NONE',  ( -22.27721038036499479, -3.438655654856782373, -1.315315479297514134 ) ) ;
#648=VERTEX_POINT ( 'NONE', #32243 ) ;
#662=VERTEX_POINT ( 'NONE', #42878 ) ;
#663=LINE ( 'NONE', #10958, #26308 ) ;
#666=VERTEX_POINT ( 'NONE', #2338 ) ;
#672=CARTESIAN_POINT ( 'NONE',  ( -22.31328051695926007, -2.608921479762108753, 2.748895659348124187 ) ) ;
#680=CARTESIAN_POINT ( 'NONE',  ( -27.08776759928964850, 0.6183458186125572187, 2.217308861843124035 ) ) ;
#687=CARTESIAN_POINT ( 'NONE',  ( 0.000000000000000000, -6.750946897830688798, -1.593658756657146292 ) ) ;
#693=CARTESIAN_POINT ( 'NONE',  ( 1.000000000000000888, 7.414200355365252015, 1.131208685655162638 ) ) ;
#702=CARTESIAN_POINT ( 'NONE',  ( 0.000000000000000000, 6.250523986463984549, 3.007653927006597172 ) ) ;
#703=CARTESIAN_POINT ( 'NONE',  ( -35.04683013664716640, -0.009445816769442809055, -0.007968230201772305218 ) ) ;
#704=CARTESIAN_POINT ( 'NONE',  ( -27.08429572838383947, 2.279961732801592422, -0.2296550094122856711 ) ) ;
#708=EDGE_CURVE ( 'NONE', #10609, #56404, #22264, .T. ) ;
#709=CIRCLE ( 'NONE', #32531, 7.499999999999988454 ) ;
#719=EDGE_LOOP ( 'NONE', ( #21137, #14630, #27756, #54283 ) ) ;
#721=CARTESIAN_POINT ( 'NONE',  ( -22.27713295444592845, 0.8543895091636684036, 3.580881989303308810 ) ) ;
#725=VERTEX_POINT ( 'NONE', #38552 ) ;
#741=DIRECTION ( 'NONE',  ( 0.9606638835031803270, 0.02862840969242944761, 0.2762341707520462042 ) ) ;
#745=ADVANCED_FACE ( 'NONE', ( #17946 ), #38208, .T. ) ;
#752=CARTESIAN_POINT ( 'NONE',  ( -27.09569413923794912, -2.232620870184085060, 0.6513788562879397892 ) ) ;
#756=EDGE_CURVE ( 'NONE', #28947, #52648, #34539, .T. ) ;
#760=EDGE_LOOP ( 'NONE', ( #46114, #4042, #25768, #55762 ) ) ;
#772=CARTESIAN_POINT ( 'NONE',  ( -22.76187086591099984, -0.9059972289356940101, -5.055065309934924755 ) ) ;
#776=EDGE_LOOP ( 'NONE', ( #11721, #57798, #2709, #5498 ) ) ;
#788=ORIENTED_EDGE ( 'NONE', *, *, #27671, .T. ) ;
#789=EDGE_CURVE ( 'NONE', #16747, #25350, #24974, .T. ) ;
#790=CARTESIAN_POINT ( 'NONE',  ( -27.20164183316782669, -1.409601201084045297, -2.237540722393188020 ) ) ;
#793=CARTESIAN_POINT ( 'NONE',  ( 2.000000000000001776, -6.338823199656649088, -2.816798305433765748 ) ) ;
#806=ORIENTED_EDGE ( 'NONE', *, *, #17340, .T. ) ;
#811=ORIENTED_EDGE ( 'NONE', *, *, #53682, .F. ) ;
#821=EDGE_CURVE ( 'NONE', #21537, #33192, #25015, .T. ) ;
#824=DIRECTION ( 'NONE',  ( -1.000000000000000000, 0.000000000000000000, 0.000000000000000000 ) ) ;
#825=CARTESIAN_POINT ( 'NONE',  ( 0.000000000000000000, 6.539067737394526958, -2.314222412769764148 ) ) ;
#827=B_SPLINE_CURVE_WITH_KNOTS ( 'NONE', 3,
 ( #32126, #1238, #21517, #12180, #16839, #26824, #2566, #37452 ),
 .UNSPECIFIED., .F., .F.,
 ( 4, 2, 2, 4 ),
 ( 0.000000000000000000, 0.0003639104015149979571, 0.0007278208030299959143, 0.001455641606059991829 ),
 .UNSPECIFIED. ) ;
#839=CIRCLE ( 'NONE', #57095, 2.899999999999996358 ) ;
#847=ORIENTED_EDGE ( 'NONE', *, *, #52308, .T. ) ;
#852=CARTESIAN_POINT ( 'NONE',  ( 2.000000000000001776, 6.253963800348318003, -4.139799123620975685 ) ) ;
#858=DIRECTION ( 'NONE',  ( -1.000000000000000000, 0.000000000000000000, 0.000000000000000000 ) ) ;
#862=ORIENTED_EDGE ( 'NONE', *, *, #20137, .F. ) ;
#863=CARTESIAN_POINT ( 'NONE',  ( -27.08850691366480490, 2.232573186527712306, 0.5697889027535342210 ) ) ;
#868=CARTESIAN_POINT ( 'NONE',  ( -22.30625920655495165, 3.150098859949344909, -2.110841417170892242 ) ) ;
#869=AXIS2_PLACEMENT_3D ( 'NONE', #36595, #26608, #21289 ) ;
#877=ORIENTED_EDGE ( 'NONE', *, *, #53294, .F. ) ;
#898=DIRECTION ( 'NONE',  ( -1.000000000000000000, 0.000000000000000000, 0.000000000000000000 ) ) ;
#901=CARTESIAN_POINT ( 'NONE',  ( 0.000000000000000000, 0.000000000000000000, 0.000000000000000000 ) ) ;
#903=ADVANCED_FACE ( 'NONE', ( #35516 ), #11835, .F. ) ;
#907=AXIS2_PLACEMENT_3D ( 'NONE', #20849, #15201, #35484 ) ;
#915=CARTESIAN_POINT ( 'NONE',  ( 2.000000000000001776, -4.962980376314023445, -4.846014654777856201 ) ) ;
#918=VERTEX_POINT ( 'NONE', #36152 ) ;
#923=AXIS2_PLACEMENT_3D ( 'NONE', #20101, #14440, #41031 ) ;
#927=EDGE_CURVE ( 'NONE', #35439, #25961, #34586, .T. ) ;
#941=ORIENTED_EDGE ( 'NONE', *, *, #51723, .F. ) ;
#942=CARTESIAN_POINT ( 'NONE',  ( -22.27384469013076185, 3.564715702084495952, -0.9224151068931343289 ) ) ;
#961=ORIENTED_EDGE ( 'NONE', *, *, #65675, .T. ) ;
#962=EDGE_CURVE ( 'NONE', #2752, #28450, #1679, .T. ) ;
#965=CIRCLE ( 'NONE', #16908, 6.936499999999989896 ) ;
#968=FACE_BOUND ( 'NONE', #43387, .T. ) ;
#969=ADVANCED_FACE ( 'NONE', ( #40500 ), #46804, .T. ) ;
#972=CARTESIAN_POINT ( 'NONE',  ( -22.27715526084302056, 3.652257391294508881, -0.4651416883073660746 ) ) ;
#973=CIRCLE ( 'NONE', #5195, 2.899999999999995914 ) ;
#983=VERTEX_POINT ( 'NONE', #45830 ) ;
#998=EDGE_CURVE ( 'NONE', #52904, #10633, #38823, .T. ) ;
#999=CARTESIAN_POINT ( 'NONE',  ( -27.09030469827879628, 0.6314616953885330286, 2.221523195520524574 ) ) ;
#1002=DIRECTION ( 'NONE',  ( 0.000000000000000000, 0.000000000000000000, 1.000000000000000000 ) ) ;
#1006=AXIS2_PLACEMENT_3D ( 'NONE', #6026, #45915, #46251 ) ;
#1008=CARTESIAN_POINT ( 'NONE',  ( 2.000000000000001776, 1.058508696394974358, 6.730038252034905355 ) ) ;
#1017=CARTESIAN_POINT ( 'NONE',  ( -22.30625920655495165, -1.076742202099160606, -3.635849356906424745 ) ) ;
#1021=FACE_OUTER_BOUND ( 'NONE', #10782, .T. ) ;
#1037=DIRECTION ( 'NONE',  ( -1.000000000000000000, 0.000000000000000000, 0.000000000000000000 ) ) ;
#1043=ORIENTED_EDGE ( 'NONE', *, *, #24378, .F. ) ;
#1049=DIRECTION ( 'NONE',  ( -1.000000000000000000, 0.000000000000000000, 0.000000000000000000 ) ) ;
#1052=CARTESIAN_POINT ( 'NONE',  ( -22.29479313954897890, 0.2707859422896981005, 3.724550806388638780 ) ) ;
#1058=EDGE_CURVE ( 'NONE', #16108, #50142, #55821, .T. ) ;
#1061=LINE ( 'NONE', #57586, #15991 ) ;
#1065=CARTESIAN_POINT ( 'NONE',  ( -24.22918518688384282, 4.353569350872102284, 0.3685645067157813370 ) ) ;
#1068=CARTESIAN_POINT ( 'NONE',  ( -27.28573687977896611, -2.255103317860393197, -1.818142657385574790 ) ) ;
#1073=CARTESIAN_POINT ( 'NONE',  ( -35.04709527796842394, 0.01117341439754726551, -0.005292201869334239861 ) ) ;
#1075=DIRECTION ( 'NONE',  ( -1.000000000000000000, 0.000000000000000000, 0.000000000000000000 ) ) ;
#1082=CARTESIAN_POINT ( 'NONE',  ( -35.04643116707788408, 0.01204777744935082995, -0.001845126042314057524 ) ) ;
#1084=CARTESIAN_POINT ( 'NONE',  ( 2.000000000000001776, 0.000000000000000000, 0.000000000000000000 ) ) ;
#1087=EDGE_CURVE ( 'NONE', #56385, #30158, #48430, .T. ) ;
#1088=ORIENTED_EDGE ( 'NONE', *, *, #19961, .F. ) ;
#1089=CARTESIAN_POINT ( 'NONE',  ( -35.04683013664716640, -0.01065093278703673797, 0.006266879427257444207 ) ) ;
#1096=( GEOMETRIC_REPRESENTATION_CONTEXT ( 3 ) GLOBAL_UNCERTAINTY_ASSIGNED_CONTEXT ( ( #2439 ) ) GLOBAL_UNIT_ASSIGNED_CONTEXT ( ( #30433, #21104, #11150 ) ) REPRESENTATION_CONTEXT ( 'NONE', 'WORKASPACE' ) );
#1099=CARTESIAN_POINT ( 'NONE',  ( -28.66013792860432119, 1.673433383655442697, 0.7552004871165165500 ) ) ;
#1102=DIRECTION ( 'NONE',  ( -1.000000000000000000, 0.000000000000000000, 0.000000000000000000 ) ) ;
#1111=CARTESIAN_POINT ( 'NONE',  ( -22.27720412283625961, 3.493592264983219398, 1.161733799004142309 ) ) ;
#1119=ORIENTED_EDGE ( 'NONE', *, *, #35766, .T. ) ;
#1121=CARTESIAN_POINT ( 'NONE',  ( -27.08417473062937120, -1.729223128152646671, 1.503027223283678548 ) ) ;
#1126=CIRCLE ( 'NONE', #7463, 7.499999999999988454 ) ;
#1128=ORIENTED_EDGE ( 'NONE', *, *, #56050, .T. ) ;
#1131=CYLINDRICAL_SURFACE ( 'NONE', #46206, 7.499999999999988454 ) ;
#1137=ORIENTED_EDGE ( 'NONE', *, *, #46137, .F. ) ;
#1142=EDGE_CURVE ( 'NONE', #5306, #8685, #3822, .T. ) ;
#1144=CIRCLE ( 'NONE', #29776, 6.936499999999989008 ) ;
#1146=VECTOR ( 'NONE', #37888, 1000.000000000000000 ) ;
#1148=AXIS2_PLACEMENT_3D ( 'NONE', #55835, #61145, #51522 ) ;
#1150=CYLINDRICAL_SURFACE ( 'NONE', #57509, 7.499999999999988454 ) ;
#1167=( BOUNDED_SURFACE ( )  B_SPLINE_SURFACE ( 3, 1, ( 
 ( #31988, #5779 ),
 ( #45999, #51654 ),
 ( #36332, #46982 ),
 ( #456, #57625 ) ),
 .UNSPECIFIED., .F., .F., .F. ) 
 B_SPLINE_SURFACE_WITH_KNOTS ( ( 4, 4 ),
 ( 2, 2 ),
 ( 0.000000000000000000, 1.000000000000000000 ),
 ( 0.000000000000000000, 1.000000000000000000 ),
 .UNSPECIFIED. ) 
 GEOMETRIC_REPRESENTATION_ITEM ( )  RATIONAL_B_SPLINE_SURFACE ( (
 ( 1.000000000000000000, 1.000000000000000000),
 ( 0.8716676215708681896, 0.8964445200148167814),
 ( 0.8716676215708681896, 0.8964445200148167814),
 ( 1.000000000000000000, 1.000000000000000000) ) ) 
 REPRESENTATION_ITEM ( '' )  SURFACE ( )  );
#1169=AXIS2_PLACEMENT_3D ( 'NONE', #39836, #34520, #50801 ) ;
#1176=CIRCLE ( 'NONE', #2225, 2.899999999999994582 ) ;
#1179=CARTESIAN_POINT ( 'NONE',  ( 0.000000000000000000, 2.315790869867065283, 7.133520354428103616 ) ) ;
#1180=ORIENTED_EDGE ( 'NONE', *, *, #57328, .T. ) ;
#1181=CYLINDRICAL_SURFACE ( 'NONE', #21717, 6.936499999999988120 ) ;
#1186=AXIS2_PLACEMENT_3D ( 'NONE', #32629, #36666, #57626 ) ;
#1195=ORIENTED_EDGE ( 'NONE', *, *, #16801, .F. ) ;
#1200=DIRECTION ( 'NONE',  ( -0.3162277663656185012, 0.1673616205762862574, 0.9338040949457712125 ) ) ;
#1201=VERTEX_POINT ( 'NONE', #15147 ) ;
#1202=CARTESIAN_POINT ( 'NONE',  ( -27.08935880048752409, 2.235999130317591010, 0.5666837974575442693 ) ) ;
#1203=CIRCLE ( 'NONE', #58554, 2.899999999999995470 ) ;
#1222=ORIENTED_EDGE ( 'NONE', *, *, #6307, .F. ) ;
#1227=ORIENTED_EDGE ( 'NONE', *, *, #18704, .T. ) ;
#1230=CARTESIAN_POINT ( 'NONE',  ( -22.27718150314433387, -1.117371044661075841, 3.507884203786634458 ) ) ;
#1231=ORIENTED_EDGE ( 'NONE', *, *, #38538, .T. ) ;
#1238=CARTESIAN_POINT ( 'NONE',  ( -22.35190811654612375, 3.252894036332518723, -2.161847148103698935 ) ) ;
#1240=CARTESIAN_POINT ( 'NONE',  ( -27.08579483061179261, 0.9690219683526832828, -2.081508743190604083 ) ) ;
#1243=LINE ( 'NONE', #20853, #12880 ) ;
#1260=CIRCLE ( 'NONE', #23566, 6.936499999999989008 ) ;
#1263=AXIS2_PLACEMENT_3D ( 'NONE', #9918, #44836, #55139 ) ;
#1264=ORIENTED_EDGE ( 'NONE', *, *, #30145, .F. ) ;
#1265=CARTESIAN_POINT ( 'NONE',  ( -22.29479313954897890, -3.724550806388635227, 0.2707859422896675139 ) ) ;
#1267=AXIS2_PLACEMENT_3D ( 'NONE', #42009, #42317, #47666 ) ;
#1271=DIRECTION ( 'NONE',  ( 0.000000000000000000, 0.000000000000000000, 1.000000000000000000 ) ) ;
#1275=DIRECTION ( 'NONE',  ( 0.000000000000000000, 0.000000000000000000, 1.000000000000000000 ) ) ;
#1276=EDGE_CURVE ( 'NONE', #40046, #47952, #60886, .T. ) ;
#1279=CARTESIAN_POINT ( 'NONE',  ( -28.66013792860432119, 0.4872053345172169814, -1.770123732198267463 ) ) ;
#1282=DIRECTION ( 'NONE',  ( 0.000000000000000000, 0.000000000000000000, 1.000000000000000000 ) ) ;
#1283=ORIENTED_EDGE ( 'NONE', *, *, #51389, .T. ) ;
#1285=CARTESIAN_POINT ( 'NONE',  ( 0.000000000000000000, 0.000000000000000000, 0.000000000000000000 ) ) ;
#1289=CYLINDRICAL_SURFACE ( 'NONE', #23548, 6.936499999999988120 ) ;
#1292=ORIENTED_EDGE ( 'NONE', *, *, #30703, .T. ) ;
#1302=EDGE_CURVE ( 'NONE', #3684, #16346, #11158, .T. ) ;
#1304=DIRECTION ( 'NONE',  ( 0.000000000000000000, 0.9985334138511240409, -0.05413890858541454271 ) ) ;
#1319=AXIS2_PLACEMENT_3D ( 'NONE', #334, #15284, #14603 ) ;
#1327=ORIENTED_EDGE ( 'NONE', *, *, #32180, .F. ) ;
#1334=CARTESIAN_POINT ( 'NONE',  ( -22.59983133926798615, -3.996991822164155383, -2.378226455340851420 ) ) ;
#1338=CARTESIAN_POINT ( 'NONE',  ( -22.27711351828769892, 2.657880562424700610, -2.547249869018249235 ) ) ;
#1347=DIRECTION ( 'NONE',  ( 1.000000000000000000, 0.000000000000000000, 0.000000000000000000 ) ) ;
#1368=DIRECTION ( 'NONE',  ( 0.000000000000000000, 0.2149704402110177992, 0.9766205557100881007 ) ) ;
#1369=VERTEX_POINT ( 'NONE', #17121 ) ;
#1371=ORIENTED_EDGE ( 'NONE', *, *, #30278, .F. ) ;
#1373=CARTESIAN_POINT ( 'NONE',  ( 2.000000000000001776, 1.836970198721030181E-16, -1.500000000000000222 ) ) ;
#1374=CARTESIAN_POINT ( 'NONE',  ( 2.000000000000001776, 6.586971819220387658, -3.586335490831350725 ) ) ;
#1380=CIRCLE ( 'NONE', #59751, 2.899999999999994582 ) ;
#1384=EDGE_CURVE ( 'NONE', #9803, #36432, #16619, .T. ) ;
#1385=AXIS2_PLACEMENT_3D ( 'NONE', #65031, #20479, #15478 ) ;
#1400=ORIENTED_EDGE ( 'NONE', *, *, #54116, .T. ) ;
#1406=CARTESIAN_POINT ( 'NONE',  ( 2.000000000000001776, -6.767909380267593811, 0.7805499053120233954 ) ) ;
#1411=EDGE_LOOP ( 'NONE', ( #9726, #61869, #50151, #56073 ) ) ;
#1426=ORIENTED_EDGE ( 'NONE', *, *, #42084, .F. ) ;
#1429=CARTESIAN_POINT ( 'NONE',  ( 1.000000000000000888, -7.414200355365233364, -1.131208685655244350 ) ) ;
#1434=EDGE_CURVE ( 'NONE', #33641, #15285, #25060, .T. ) ;
#1444=ADVANCED_FACE ( 'NONE', ( #44036 ), #64307, .T. ) ;
#1447=CARTESIAN_POINT ( 'NONE',  ( 0.000000000000000000, 0.000000000000000000, 0.000000000000000000 ) ) ;
#1460=VERTEX_POINT ( 'NONE', #19429 ) ;
#1471=CARTESIAN_POINT ( 'NONE',  ( -22.28169757117798966, -3.561623073126547911, 0.9841724999439861454 ) ) ;
#1477=CARTESIAN_POINT ( 'NONE',  ( 2.000000000000001776, 7.203928197742132333, -2.086484728383096510 ) ) ;
#1479=VERTEX_POINT ( 'NONE', #9411 ) ;
#1480=EDGE_CURVE ( 'NONE', #50535, #50607, #4897, .T. ) ;
#1481=FACE_OUTER_BOUND ( 'NONE', #57483, .T. ) ;
#1482=VERTEX_POINT ( 'NONE', #63983 ) ;
#1483=AXIS2_PLACEMENT_3D ( 'NONE', #18572, #34782, #53801 ) ;
#1489=DIRECTION ( 'NONE',  ( 0.000000000000000000, 0.000000000000000000, 1.000000000000000000 ) ) ;
#1498=EDGE_LOOP ( 'NONE', ( #10895, #64421, #21344, #12911 ) ) ;
#1500=ORIENTED_EDGE ( 'NONE', *, *, #63507, .F. ) ;
#1505=DIRECTION ( 'NONE',  ( -1.000000000000000000, 0.000000000000000000, 0.000000000000000000 ) ) ;
#1511=CARTESIAN_POINT ( 'NONE',  ( 2.000000000000001776, 6.201547234537079234, -2.820401998297854096 ) ) ;
#1517=EDGE_CURVE ( 'NONE', #63755, #61730, #59022, .T. ) ;
#1518=FACE_OUTER_BOUND ( 'NONE', #51247, .T. ) ;
#1525=EDGE_CURVE ( 'NONE', #15504, #38810, #44342, .T. ) ;
#1526=DIRECTION ( 'NONE',  ( -1.000000000000000000, 0.000000000000000000, 0.000000000000000000 ) ) ;
#1531=EDGE_CURVE ( 'NONE', #662, #48402, #34379, .T. ) ;
#1538=CARTESIAN_POINT ( 'NONE',  ( -22.30625920655495165, 3.783486345733975131, -0.2529928606556600679 ) ) ;
#1541=CYLINDRICAL_SURFACE ( 'NONE', #57609, 7.499999999999988454 ) ;
#1542=B_SPLINE_CURVE_WITH_KNOTS ( 'NONE', 3,
 ( #51876, #51564, #50572, #60863, #26268, #61497, #680, #20290, #6013, #999, #20936, #40568, #50886, #25607, #46542, #21267, #41542, #36573, #45900 ),
 .UNSPECIFIED., .F., .F.,
 ( 4, 3, 3, 3, 3, 3, 4 ),
 ( 0.000000000000000000, 2.832085443540684365E-05, 4.217789847394754410E-05, 5.603488375046140088E-05, 6.989180858579403647E-05, 9.821094829919064780E-05, 0.0001178165571465091021 ),
 .UNSPECIFIED. ) ;
#1550=EDGE_CURVE ( 'NONE', #14567, #26639, #62212, .T. ) ;
#1554=FACE_OUTER_BOUND ( 'NONE', #54024, .T. ) ;
#1555=CARTESIAN_POINT ( 'NONE',  ( -22.27722019117890540, 0.6494988092404053726, 3.623917154020592335 ) ) ;
#1556=AXIS2_PLACEMENT_3D ( 'NONE', #41594, #52585, #31301 ) ;
#1562=ORIENTED_EDGE ( 'NONE', *, *, #47404, .F. ) ;
#1564=CARTESIAN_POINT ( 'NONE',  ( 0.000000000000000000, 6.470132594555819239, 2.133363481234098469 ) ) ;
#1570=CARTESIAN_POINT ( 'NONE',  ( 2.000000000000001776, 0.000000000000000000, 0.000000000000000000 ) ) ;
#1598=ADVANCED_FACE ( 'NONE', ( #60629 ), #60302, .T. ) ;
#1614=VERTEX_POINT ( 'NONE', #41003 ) ;
#1620=CARTESIAN_POINT ( 'NONE',  ( -35.04643116707788408, 0.01156612771643569793, 0.003844232202706091006 ) ) ;
#1625=VERTEX_POINT ( 'NONE', #11083 ) ;
#1630=DIRECTION ( 'NONE',  ( 0.000000000000000000, 0.000000000000000000, -1.000000000000000000 ) ) ;
#1636=CARTESIAN_POINT ( 'NONE',  ( -27.35552965826137140, 1.320216934008397569, 2.810569013793730697 ) ) ;
#1644=DIRECTION ( 'NONE',  ( 0.000000000000000000, 0.3193015301359806712, -0.9476531711828022342 ) ) ;
#1654=ORIENTED_EDGE ( 'NONE', *, *, #24018, .F. ) ;
#1658=DIRECTION ( 'NONE',  ( 0.000000000000000000, -0.2149704402110115264, -0.9766205557100894330 ) ) ;
#1662=CARTESIAN_POINT ( 'NONE',  ( -27.28563798457900091, 1.483130241384917891, -2.487904455214884347 ) ) ;
#1665=CARTESIAN_POINT ( 'NONE',  ( -22.71097035706202405, -4.089776368546547580, -2.846599994298351977 ) ) ;
#1668=LINE ( 'NONE', #56531, #27445 ) ;
#1676=ORIENTED_EDGE ( 'NONE', *, *, #56782, .T. ) ;
#1679=CIRCLE ( 'NONE', #36735, 2.899999999999994582 ) ;
#1680=ORIENTED_EDGE ( 'NONE', *, *, #29933, .T. ) ;
#1685=CARTESIAN_POINT ( 'NONE',  ( -27.08702828306175903, -0.6138566972905382668, -2.216258174335471232 ) ) ;
#1687=EDGE_LOOP ( 'NONE', ( #43716, #4623, #55256, #11570 ) ) ;
#1689=CARTESIAN_POINT ( 'NONE',  ( -22.71097035706202760, 2.846599994298365743, -4.089776368546553798 ) ) ;
#1714=FACE_OUTER_BOUND ( 'NONE', #2932, .T. ) ;
#1720=ORIENTED_EDGE ( 'NONE', *, *, #27553, .T. ) ;
#1733=CARTESIAN_POINT ( 'NONE',  ( 0.000000000000000000, -5.217815162096861137, 5.387430271863535403 ) ) ;
#1739=ORIENTED_EDGE ( 'NONE', *, *, #46333, .F. ) ;
#1750=DIRECTION ( 'NONE',  ( 0.000000000000000000, 0.000000000000000000, -1.000000000000000000 ) ) ;
#1754=CARTESIAN_POINT ( 'NONE',  ( 0.000000000000000000, 0.000000000000000000, 0.000000000000000000 ) ) ;
#1757=B_SPLINE_CURVE_WITH_KNOTS ( 'NONE', 3,
 ( #44467, #64747, #17915, #23229, #28868, #48842, #59148, #63769, #64429, #13259, #13560, #53512, #14220, #7956, #33843, #28223, #3289, #38177, #58489 ),
 .UNSPECIFIED., .F., .F.,
 ( 4, 3, 3, 3, 3, 3, 4 ),
 ( 0.000000000000000000, 2.832085443685227149E-05, 4.217789847592207954E-05, 5.603488375296408508E-05, 6.989180858882511338E-05, 9.821094830335176152E-05, 0.0001178165571463577204 ),
 .UNSPECIFIED. ) ;
#1759=EDGE_CURVE ( 'NONE', #13124, #60470, #2769, .T. ) ;
#1762=CARTESIAN_POINT ( 'NONE',  ( -22.70624764888619751, -1.907540768355087124, -4.891815784104558418 ) ) ;
#1766=CARTESIAN_POINT ( 'NONE',  ( 2.000000000000001776, 5.457833520448658327, 4.281014542496528463 ) ) ;
#1773=DIRECTION ( 'NONE',  ( 0.000000000000000000, 0.5155538571770230671, -0.8568571761675883858 ) ) ;
#1778=CARTESIAN_POINT ( 'NONE',  ( -35.04834644901396956, -0.01046409687784406219, -0.009049049589502401736 ) ) ;
#1784=ADVANCED_FACE ( 'NONE', ( #7730 ), #18376, .T. ) ;
#1785=ORIENTED_EDGE ( 'NONE', *, *, #13728, .F. ) ;
#1789=DIRECTION ( 'NONE',  ( -1.000000000000000000, 0.000000000000000000, 0.000000000000000000 ) ) ;
#1797=ORIENTED_EDGE ( 'NONE', *, *, #8646, .F. ) ;
#1800=VERTEX_POINT ( 'NONE', #38642 ) ;
#1802=DIRECTION ( 'NONE',  ( 0.000000000000000000, 0.000000000000000000, 1.000000000000000000 ) ) ;
#1803=CARTESIAN_POINT ( 'NONE',  ( 0.000000000000000000, 5.107597897712347290, 4.693343793638412365 ) ) ;
#1805=ORIENTED_EDGE ( 'NONE', *, *, #54412, .T. ) ;
#1807=EDGE_CURVE ( 'NONE', #32874, #52513, #58953, .T. ) ;
#1820=DIRECTION ( 'NONE',  ( -1.000000000000000000, 0.000000000000000000, 0.000000000000000000 ) ) ;
#1823=CARTESIAN_POINT ( 'NONE',  ( -22.27706485742869091, -0.9221835209182183135, -3.563814065926679042 ) ) ;
#1825=DIRECTION ( 'NONE',  ( -1.000000000000000000, 0.000000000000000000, 0.000000000000000000 ) ) ;
#1830=CARTESIAN_POINT ( 'NONE',  ( 2.000000000000001776, 4.376687952327412034, -5.220963330856592144 ) ) ;
#1837=CARTESIAN_POINT ( 'NONE',  ( -27.08419642509983305, 0.4837273216075048676, 2.239682169453929284 ) ) ;
#1840=CARTESIAN_POINT ( 'NONE',  ( 2.000000000000001776, 1.145812388885126820, 6.715725538143592743 ) ) ;
#1853=VERTEX_POINT ( 'NONE', #19017 ) ;
#1856=DIRECTION ( 'NONE',  ( 0.000000000000000000, 0.000000000000000000, 1.000000000000000000 ) ) ;
#1858=DIRECTION ( 'NONE',  ( 0.000000000000000000, 0.000000000000000000, -1.000000000000000000 ) ) ;
#1863=CARTESIAN_POINT ( 'NONE',  ( 1.000000000000000888, 7.414200355365271555, -1.131208685655096691 ) ) ;
#1865=DIRECTION ( 'NONE',  ( 0.000000000000000000, 0.000000000000000000, 1.000000000000000000 ) ) ;
#1867=CARTESIAN_POINT ( 'NONE',  ( -22.27722019094931483, 2.374181302999014420, 2.813874087059979878 ) ) ;
#1872=DIRECTION ( 'NONE',  ( -1.000000000000000000, 0.000000000000000000, 0.000000000000000000 ) ) ;
#1886=CIRCLE ( 'NONE', #64523, 7.499999999999988454 ) ;
#1892=DIRECTION ( 'NONE',  ( 0.000000000000000000, 0.000000000000000000, 1.000000000000000000 ) ) ;
#1897=FACE_OUTER_BOUND ( 'NONE', #12593, .T. ) ;
#1901=B_SPLINE_CURVE_WITH_KNOTS ( 'NONE', 3,
 ( #15994, #36282, #35629, #11028, #35937, #45955, #4754, #50619, #16350, #31309, #51611, #40624, #26315, #15010, #1052, #36621, #55, #56927, #11347, #60574, #30326, #35296 ),
 .UNSPECIFIED., .F., .F.,
 ( 4, 3, 3, 3, 3, 3, 3, 4 ),
 ( 0.000000000000000000, 4.447697177976342209E-05, 6.624143997791237092E-05, 8.800576886944197236E-05, 0.0001097699864780881258, 0.0001315341395364363788, 0.0001760120188223247427, 0.0001867971373174718945 ),
 .UNSPECIFIED. ) ;
#1907=CARTESIAN_POINT ( 'NONE',  ( -27.09048036756592026, 0.1785511875143080684, 2.303144499688032809 ) ) ;
#1909=ORIENTED_EDGE ( 'NONE', *, *, #42296, .F. ) ;
#1926=CARTESIAN_POINT ( 'NONE',  ( -35.04683013664716640, -0.01075274317999010479, -0.006090538653967201080 ) ) ;
#1935=ORIENTED_EDGE ( 'NONE', *, *, #12328, .T. ) ;
#1939=CARTESIAN_POINT ( 'NONE',  ( -35.04643116707788408, -0.01204777744936991191, 0.001845126042312322800 ) ) ;
#1940=CARTESIAN_POINT ( 'NONE',  ( 0.000000000000000000, 5.769711778877324448, 4.791703871138532023 ) ) ;
#1947=B_SPLINE_CURVE_WITH_KNOTS ( 'NONE', 3,
 ( #30120, #4868, #25454, #199, #45403, #20141, #40407, #60711, #40755, #61043, #56037, #35738, #14158, #34450, #11155, #57361 ),
 .UNSPECIFIED., .F., .F.,
 ( 4, 3, 3, 3, 3, 4 ),
 ( 1.371419323662639293E-18, 6.991367980366453884E-05, 0.0001398269368981367756, 0.0002097400188389093086, 0.0002811534801551364318, 0.0003526297678872523478 ),
 .UNSPECIFIED. ) ;
#1953=CARTESIAN_POINT ( 'NONE',  ( -27.09569413923886572, 1.680421072128821303, 1.607816962455205889 ) ) ;
#1956=CARTESIAN_POINT ( 'NONE',  ( -22.38932658256920405, 1.810630688302315550, -3.587092141214307528 ) ) ;
#1983=CARTESIAN_POINT ( 'NONE',  ( 0.000000000000000000, 1.145812388885215194, -6.715725538143608730 ) ) ;
#1985=DIRECTION ( 'NONE',  ( -1.000000000000000000, 0.000000000000000000, 0.000000000000000000 ) ) ;
#1991=CARTESIAN_POINT ( 'NONE',  ( 2.000000000000001776, 5.107597897712416568, -4.693343793638371508 ) ) ;
#1994=DIRECTION ( 'NONE',  ( 0.000000000000000000, 0.000000000000000000, 1.000000000000000000 ) ) ;
#2005=PRODUCT_DEFINITION_CONTEXT ( 'detailed design', #20477, 'design' ) ;
#2033=ORIENTED_EDGE ( 'NONE', *, *, #20320, .F. ) ;
#2041=AXIS2_PLACEMENT_3D ( 'NONE', #13469, #8488, #3540 ) ;
#2047=ADVANCED_FACE ( 'NONE', ( #61865 ), #13980, .F. ) ;
#2048=CARTESIAN_POINT ( 'NONE',  ( 2.000000000000001776, -5.997115278587647147, 3.485633455389469226 ) ) ;
#2053=ORIENTED_EDGE ( 'NONE', *, *, #21061, .T. ) ;
#2061=CIRCLE ( 'NONE', #26445, 7.499999999999988454 ) ;
#2064=CARTESIAN_POINT ( 'NONE',  ( -27.08429572838383947, 2.089332284968718145, 0.9410937941433747955 ) ) ;
#2065=FACE_OUTER_BOUND ( 'NONE', #44955, .T. ) ;
#2067=EDGE_LOOP ( 'NONE', ( #8310, #48829, #48406, #37613 ) ) ;
#2075=CARTESIAN_POINT ( 'NONE',  ( 2.000000000000001776, 1.058508696395052517, -6.730038252034905355 ) ) ;
#2086=EDGE_CURVE ( 'NONE', #28230, #52659, #42461, .T. ) ;
#2091=EDGE_CURVE ( 'NONE', #2794, #25335, #38473, .T. ) ;
#2095=VERTEX_POINT ( 'NONE', #63401 ) ;
#2097=CARTESIAN_POINT ( 'NONE',  ( -27.08426571771018487, -1.845988025802333787, 1.357728109767515345 ) ) ;
#2105=ORIENTED_EDGE ( 'NONE', *, *, #26511, .T. ) ;
#2123=CARTESIAN_POINT ( 'NONE',  ( -22.29018399051993526, -3.609810019245839108, -0.9010028109495191728 ) ) ;
#2126=( BOUNDED_SURFACE ( )  B_SPLINE_SURFACE ( 3, 1, ( 
 ( #44053, #14106 ),
 ( #55002, #3517 ),
 ( #18790, #14429 ),
 ( #39053, #59343 ) ),
 .UNSPECIFIED., .F., .F., .F. ) 
 B_SPLINE_SURFACE_WITH_KNOTS ( ( 4, 4 ),
 ( 2, 2 ),
 ( 0.000000000000000000, 1.000000000000000000 ),
 ( 0.000000000000000000, 1.000000000000000000 ),
 .UNSPECIFIED. ) 
 GEOMETRIC_REPRESENTATION_ITEM ( )  RATIONAL_B_SPLINE_SURFACE ( (
 ( 1.000000000000000000, 1.000000000000000000),
 ( 0.8716676215708681896, 0.8964445200148167814),
 ( 0.8716676215708681896, 0.8964445200148167814),
 ( 1.000000000000000000, 1.000000000000000000) ) ) 
 REPRESENTATION_ITEM ( '' )  SURFACE ( )  );
#2131=ORIENTED_EDGE ( 'NONE', *, *, #7041, .F. ) ;
#2132=LINE ( 'NONE', #16763, #49799 ) ;
#2137=DIRECTION ( 'NONE',  ( 0.000000000000000000, 0.000000000000000000, -1.000000000000000000 ) ) ;
#2138=AXIS2_PLACEMENT_3D ( 'NONE', #59492, #54521, #3333 ) ;
#2146=EDGE_CURVE ( 'NONE', #58714, #32257, #64385, .T. ) ;
#2167=CARTESIAN_POINT ( 'NONE',  ( -22.70624764888619751, -0.08990180771016251238, 5.249808673991983810 ) ) ;
#2173=ORIENTED_EDGE ( 'NONE', *, *, #50269, .F. ) ;
#2175=FACE_OUTER_BOUND ( 'NONE', #40364, .T. ) ;
#2176=VECTOR ( 'NONE', #45492, 999.9999999999998863 ) ;
#2179=CIRCLE ( 'NONE', #46744, 7.499999999999988454 ) ;
#2187=ADVANCED_FACE ( 'NONE', ( #54097 ), #54782, .F. ) ;
#2191=DIRECTION ( 'NONE',  ( -1.000000000000000000, 0.000000000000000000, 0.000000000000000000 ) ) ;
#2194=DIRECTION ( 'NONE',  ( -1.000000000000000000, 0.000000000000000000, 0.000000000000000000 ) ) ;
#2213=VECTOR ( 'NONE', #3653, 1000.000000000000000 ) ;
#2215=FACE_OUTER_BOUND ( 'NONE', #44117, .T. ) ;
#2221=CARTESIAN_POINT ( 'NONE',  ( -22.27706485742869091, 0.9221835209182547288, 3.563814065926663499 ) ) ;
#2223=CARTESIAN_POINT ( 'NONE',  ( -27.08429572838383947, -1.859677275556421927, 1.338867938658193424 ) ) ;
#2225=AXIS2_PLACEMENT_3D ( 'NONE', #29351, #65559, #9712 ) ;
#2226=ORIENTED_EDGE ( 'NONE', *, *, #55583, .F. ) ;
#2229=AXIS2_PLACEMENT_3D ( 'NONE', #23782, #33074, #27763 ) ;
#2232=DIRECTION ( 'NONE',  ( 0.000000000000000000, 0.000000000000000000, 1.000000000000000000 ) ) ;
#2236=EDGE_CURVE ( 'NONE', #28622, #44459, #25071, .T. ) ;
#2237=CIRCLE ( 'NONE', #35086, 2.899999999999995026 ) ;
#2242=DIRECTION ( 'NONE',  ( 1.000000000000000000, 0.000000000000000000, 0.000000000000000000 ) ) ;
#2248=CARTESIAN_POINT ( 'NONE',  ( -23.41523303002442091, -0.3963225057404748397, 4.681453266967022131 ) ) ;
#2250=CARTESIAN_POINT ( 'NONE',  ( -22.71097035706202405, 0.4203397252017515573, -4.965150228107761521 ) ) ;
#2256=CARTESIAN_POINT ( 'NONE',  ( 2.000000000000001776, -1.865193240757054394, -6.552473556515217012 ) ) ;
#2265=AXIS2_PLACEMENT_3D ( 'NONE', #52763, #53431, #48444 ) ;
#2278=CARTESIAN_POINT ( 'NONE',  ( 0.000000000000000000, -5.457833520448623688, -4.281014542496604847 ) ) ;
#2285=ORIENTED_EDGE ( 'NONE', *, *, #6769, .F. ) ;
#2292=CARTESIAN_POINT ( 'NONE',  ( -22.31213670151049300, -1.669817926839913147, 3.398324501467281156 ) ) ;
#2307=CARTESIAN_POINT ( 'NONE',  ( -22.27720412283625961, -2.752887114864230877, 2.444672752438195928 ) ) ;
#2334=CARTESIAN_POINT ( 'NONE',  ( 0.000000000000000000, 0.000000000000000000, 0.000000000000000000 ) ) ;
#2336=DIRECTION ( 'NONE',  ( 0.000000000000000000, -0.6051742151937558045, -0.7960930657056509707 ) ) ;
#2338=CARTESIAN_POINT ( 'NONE',  ( -22.27722019117889474, -0.6494988092404023750, -3.623917154020615428 ) ) ;
#2345=CYLINDRICAL_SURFACE ( 'NONE', #59473, 2.899999999999994582 ) ;
#2358=ORIENTED_EDGE ( 'NONE', *, *, #39553, .T. ) ;
#2360=CARTESIAN_POINT ( 'NONE',  ( 2.000000000000001776, -1.956810415765224187, 6.654767106875530303 ) ) ;
#2364=CARTESIAN_POINT ( 'NONE',  ( -22.31213670151048944, -2.108126385153791471, -3.145266995071696936 ) ) ;
#2365=ORIENTED_EDGE ( 'NONE', *, *, #45022, .T. ) ;
#2366=AXIS2_PLACEMENT_3D ( 'NONE', #52693, #43023, #28390 ) ;
#2373=AXIS2_PLACEMENT_3D ( 'NONE', #61023, #56020, #35404 ) ;
#2376=CARTESIAN_POINT ( 'NONE',  ( -22.27706485742869091, 0.9832726768967819941, -3.547445275915930285 ) ) ;
#2381=LINE ( 'NONE', #57244, #29962 ) ;
#2387=DIRECTION ( 'NONE',  ( -1.000000000000000000, 0.000000000000000000, 0.000000000000000000 ) ) ;
#2397=CARTESIAN_POINT ( 'NONE',  ( -28.67667724226168602, 1.695959153103731465, 0.8389685652161870122 ) ) ;
#2399=EDGE_LOOP ( 'NONE', ( #12021, #54011, #25735, #54477 ) ) ;
#2402=CARTESIAN_POINT ( 'NONE',  ( -35.04683013664716640, -0.0001018103929411406472, -0.01235741808123163275 ) ) ;
#2403=CIRCLE ( 'NONE', #33181, 6.936499999999989008 ) ;
#2413=CARTESIAN_POINT ( 'NONE',  ( -27.08418322526030408, 2.134267017050455184, 0.8335872080609374457 ) ) ;
#2416=CARTESIAN_POINT ( 'NONE',  ( 2.000000000000001776, 3.786546189469266466, -5.663561025469129540 ) ) ;
#2425=ADVANCED_FACE ( 'NONE', ( #35755 ), #19838, .T. ) ;
#2427=CARTESIAN_POINT ( 'NONE',  ( -22.29382655386184453, -2.689927793811001333, -2.586160974799840417 ) ) ;
#2431=CIRCLE ( 'NONE', #34264, 7.499999999999988454 ) ;
#2436=LINE ( 'NONE', #28027, #11062 ) ;
#2437=CARTESIAN_POINT ( 'NONE',  ( -22.46509356695200310, 3.157489876851330646, 2.840174833751751393 ) ) ;
#2439=UNCERTAINTY_MEASURE_WITH_UNIT (LENGTH_MEASURE( 1.000000000000000082E-05 ), #30433, 'distance_accuracy_value', 'NONE');
#2447=CARTESIAN_POINT ( 'NONE',  ( -22.49803948133827802, 0.1132714802761836531, 4.343047530463623573 ) ) ;
#2452=DIRECTION ( 'NONE',  ( 0.000000000000000000, 0.000000000000000000, 1.000000000000000000 ) ) ;
#2453=ORIENTED_EDGE ( 'NONE', *, *, #32816, .F. ) ;
#2456=CARTESIAN_POINT ( 'NONE',  ( 2.000000000000001776, 0.000000000000000000, 0.000000000000000000 ) ) ;
#2467=DIRECTION ( 'NONE',  ( 0.000000000000000000, 0.000000000000000000, 1.000000000000000000 ) ) ;
#2470=AXIS2_PLACEMENT_3D ( 'NONE', #20680, #41265, #25661 ) ;
#2477=ORIENTED_EDGE ( 'NONE', *, *, #26149, .F. ) ;
#2478=AXIS2_PLACEMENT_3D ( 'NONE', #14581, #34555, #38906 ) ;
#2482=CARTESIAN_POINT ( 'NONE',  ( -22.28350523959501217, 3.346230442873243227, 1.580062893038950200 ) ) ;
#2484=B_SPLINE_CURVE_WITH_KNOTS ( 'NONE', 3,
 ( #64919, #60270, #53981, #8425, #24054, #19058 ),
 .UNSPECIFIED., .F., .F.,
 ( 4, 2, 4 ),
 ( 0.0001654224980408428632, 0.0006219428995476552254, 0.001078463301054467588 ),
 .UNSPECIFIED. ) ;
#2485=CARTESIAN_POINT ( 'NONE',  ( -22.27878402819508352, 0.9624056734348347408, 3.558531829368139388 ) ) ;
#2486=DIRECTION ( 'NONE',  ( -1.000000000000000000, 0.000000000000000000, 0.000000000000000000 ) ) ;
#2490=LINE ( 'NONE', #54339, #47208 ) ;
#2496=ADVANCED_FACE ( 'NONE', ( #41084 ), #4216, .T. ) ;
#2499=CIRCLE ( 'NONE', #34317, 6.936499999999989896 ) ;
#2502=DIRECTION ( 'NONE',  ( 0.000000000000000000, -0.4198891015602527754, -0.9075754196709624466 ) ) ;
#2503=EDGE_CURVE ( 'NONE', #4743, #56025, #48873, .T. ) ;
#2509=VERTEX_POINT ( 'NONE', #36762 ) ;
#2517=CARTESIAN_POINT ( 'NONE',  ( 2.000000000000001776, 6.201547234537035713, 2.820401998297911383 ) ) ;
#2518=EDGE_LOOP ( 'NONE', ( #38015, #52775, #11245, #28931 ) ) ;
#2521=DIRECTION ( 'NONE',  ( -1.000000000000000000, 0.000000000000000000, 0.000000000000000000 ) ) ;
#2529=DIRECTION ( 'NONE',  ( -1.000000000000000000, 0.000000000000000000, 0.000000000000000000 ) ) ;
#2536=CARTESIAN_POINT ( 'NONE',  ( 0.000000000000000000, 6.997684042076905087, 2.698595569414227402 ) ) ;
#2544=ORIENTED_EDGE ( 'NONE', *, *, #14124, .F. ) ;
#2550=CARTESIAN_POINT ( 'NONE',  ( -22.27722019094931483, 3.623977093944217298, -0.6491642780571648119 ) ) ;
#2557=( BOUNDED_SURFACE ( )  B_SPLINE_SURFACE ( 3, 1, ( 
 ( #37386, #12116 ),
 ( #32391, #27737 ),
 ( #27406, #47702 ),
 ( #22420, #42686 ) ),
 .UNSPECIFIED., .F., .F., .F. ) 
 B_SPLINE_SURFACE_WITH_KNOTS ( ( 4, 4 ),
 ( 2, 2 ),
 ( 0.000000000000000000, 1.000000000000000000 ),
 ( 0.000000000000000000, 1.000000000000000000 ),
 .UNSPECIFIED. ) 
 GEOMETRIC_REPRESENTATION_ITEM ( )  RATIONAL_B_SPLINE_SURFACE ( (
 ( 1.000000000000000000, 1.000000000000000000),
 ( 0.9257577194822556033, 0.9980522942447415113),
 ( 0.9257577194822556033, 0.9980522942447415113),
 ( 1.000000000000000000, 1.000000000000000000) ) ) 
 REPRESENTATION_ITEM ( '' )  SURFACE ( )  );
#2559=CARTESIAN_POINT ( 'NONE',  ( 2.000000000000001776, 3.805198749487436416, 5.799611601383225512 ) ) ;
#2560=ORIENTED_EDGE ( 'NONE', *, *, #60361, .F. ) ;
#2563=DIRECTION ( 'NONE',  ( -1.000000000000000000, 0.000000000000000000, 0.000000000000000000 ) ) ;
#2564=VERTEX_POINT ( 'NONE', #26788 ) ;
#2566=CARTESIAN_POINT ( 'NONE',  ( -22.65996813707687707, 4.292955455498910666, -2.220979297960689713 ) ) ;
#2567=CARTESIAN_POINT ( 'NONE',  ( 2.000000000000001776, 5.107597897712347290, 4.693343793638412365 ) ) ;
#2568=CARTESIAN_POINT ( 'NONE',  ( -27.28573687977897677, -2.702109387930236473, 1.043905432732878946 ) ) ;
#2574=ORIENTED_EDGE ( 'NONE', *, *, #14124, .T. ) ;
#2577=EDGE_LOOP ( 'NONE', ( #65321, #31343, #61697, #48279 ) ) ;
#2591=EDGE_CURVE ( 'NONE', #8602, #8461, #30871, .T. ) ;
#2599=CARTESIAN_POINT ( 'NONE',  ( -22.27706089016750113, -2.622757446538683368, 2.583072118615359347 ) ) ;
#2608=CARTESIAN_POINT ( 'NONE',  ( -27.08417568107324058, 1.774279301226123984, -1.449568724721373325 ) ) ;
#2619=ORIENTED_EDGE ( 'NONE', *, *, #60397, .T. ) ;
#2633=CIRCLE ( 'NONE', #48298, 6.936499999999989896 ) ;
#2638=CARTESIAN_POINT ( 'NONE',  ( -22.28546858134833641, 2.587024666338670897, -2.654201075783116259 ) ) ;
#2641=DIRECTION ( 'NONE',  ( 0.000000000000000000, 0.7621620551276377942, -0.6473862847818260269 ) ) ;
#2647=ORIENTED_EDGE ( 'NONE', *, *, #17683, .T. ) ;
#2648=CARTESIAN_POINT ( 'NONE',  ( 0.000000000000000000, 1.018311147294167274, 6.861346417234447159 ) ) ;
#2654=CARTESIAN_POINT ( 'NONE',  ( -22.27721038036499834, -2.858424446490929416, 2.320305412324230154 ) ) ;
#2662=ORIENTED_EDGE ( 'NONE', *, *, #40756, .F. ) ;
#2664=CARTESIAN_POINT ( 'NONE',  ( -22.27718112499583469, 2.901898111564464422, -2.265557025479496556 ) ) ;
#2667=CARTESIAN_POINT ( 'NONE',  ( -22.27384469013076185, -3.358914544760244869, -1.508555848190776150 ) ) ;
#2670=FACE_OUTER_BOUND ( 'NONE', #15590, .T. ) ;
#2677=ORIENTED_EDGE ( 'NONE', *, *, #40477, .F. ) ;
#2681=CARTESIAN_POINT ( 'NONE',  ( -22.27706485742869091, -2.985151051101489372, 2.154081322712201096 ) ) ;
#2689=EDGE_CURVE ( 'NONE', #20437, #55446, #54310, .T. ) ;
#2693=CIRCLE ( 'NONE', #21753, 6.936499999999989008 ) ;
#2696=ADVANCED_FACE ( 'NONE', ( #43051 ), #18125, .T. ) ;
#2704=DIRECTION ( 'NONE',  ( -1.000000000000000000, 0.000000000000000000, 0.000000000000000000 ) ) ;
#2707=CARTESIAN_POINT ( 'NONE',  ( -22.28482751661422512, -2.105139449411421282, -3.048214341614495559 ) ) ;
#2709=ORIENTED_EDGE ( 'NONE', *, *, #4391, .T. ) ;
#2714=EDGE_CURVE ( 'NONE', #45191, #35989, #40850, .T. ) ;
#2717=CARTESIAN_POINT ( 'NONE',  ( -22.31099767395441091, -0.2534174342804020874, -3.774495463598473766 ) ) ;
#2721=CARTESIAN_POINT ( 'NONE',  ( 0.000000000000000000, 0.000000000000000000, 0.000000000000000000 ) ) ;
#2737=ORIENTED_EDGE ( 'NONE', *, *, #63333, .T. ) ;
#2743=ADVANCED_FACE ( 'NONE', ( #53712 ), #34054, .T. ) ;
#2748=CARTESIAN_POINT ( 'NONE',  ( -22.28506771379528573, 2.697635452840769332, 2.571716811880536024 ) ) ;
#2752=VERTEX_POINT ( 'NONE', #33729 ) ;
#2753=CYLINDRICAL_SURFACE ( 'NONE', #31137, 6.936499999999988120 ) ;
#2758=CARTESIAN_POINT ( 'NONE',  ( -27.08417473062937120, 2.166271322019585277, 0.7460375461499114680 ) ) ;
#2769=LINE ( 'NONE', #64542, #10188 ) ;
#2772=ORIENTED_EDGE ( 'NONE', *, *, #17105, .F. ) ;
#2773=CARTESIAN_POINT ( 'NONE',  ( -25.42680463514451716, 1.651747791411784627, 3.516354806212989459 ) ) ;
#2777=CARTESIAN_POINT ( 'NONE',  ( -27.10719052120871098, -1.310802520592025955, -1.962717903527680718 ) ) ;
#2782=CARTESIAN_POINT ( 'NONE',  ( 2.000000000000001776, -6.164400007374764456, -2.900694413976575792 ) ) ;
#2791=CYLINDRICAL_SURFACE ( 'NONE', #9983, 6.936499999999988120 ) ;
#2794=VERTEX_POINT ( 'NONE', #12455 ) ;
#2797=CARTESIAN_POINT ( 'NONE',  ( 2.000000000000001776, 4.472310526050767621, 6.020667617347370104 ) ) ;
#2801=VERTEX_POINT ( 'NONE', #35364 ) ;
#2803=VERTEX_POINT ( 'NONE', #19770 ) ;
#2812=ORIENTED_EDGE ( 'NONE', *, *, #59950, .F. ) ;
#2820=CARTESIAN_POINT ( 'NONE',  ( -27.10719052120871098, 2.261993590776037788, -0.6736837626858775963 ) ) ;
#2830=DIRECTION ( 'NONE',  ( 0.000000000000000000, 0.000000000000000000, 1.000000000000000000 ) ) ;
#2834=DIRECTION ( 'NONE',  ( -1.000000000000000000, 0.000000000000000000, 0.000000000000000000 ) ) ;
#2846=CARTESIAN_POINT ( 'NONE',  ( 2.000000000000001776, 0.000000000000000000, 0.000000000000000000 ) ) ;
#2861=EDGE_CURVE ( 'NONE', #51096, #54376, #29715, .T. ) ;
#2871=VERTEX_POINT ( 'NONE', #25080 ) ;
#2886=CARTESIAN_POINT ( 'NONE',  ( 0.000000000000000000, 7.493043167941616289, 0.3229614270519615693 ) ) ;
#2910=ORIENTED_EDGE ( 'NONE', *, *, #37555, .T. ) ;
#2912=CARTESIAN_POINT ( 'NONE',  ( -22.27706485742869091, -2.625261754997692876, 2.580541389029905819 ) ) ;
#2916=DIRECTION ( 'NONE',  ( -1.000000000000000000, 0.000000000000000000, 0.000000000000000000 ) ) ;
#2917=DIRECTION ( 'NONE',  ( 0.000000000000000000, -0.9868265225415245867, -0.1617819965527747539 ) ) ;
#2919=EDGE_LOOP ( 'NONE', ( #1043, #44630, #41176, #13059 ) ) ;
#2924=DIRECTION ( 'NONE',  ( 1.000000000000000000, -0.000000000000000000, -0.000000000000000000 ) ) ;
#2930=ORIENTED_EDGE ( 'NONE', *, *, #30564, .F. ) ;
#2932=EDGE_LOOP ( 'NONE', ( #26415, #12554, #11118, #10219 ) ) ;
#2942=EDGE_LOOP ( 'NONE', ( #47407, #41244, #12232, #15298 ) ) ;
#2948=CARTESIAN_POINT ( 'NONE',  ( -22.27878402819508707, 2.600576127690929162, -2.612733676624897416 ) ) ;
#2949=CARTESIAN_POINT ( 'NONE',  ( -27.10719052120871098, -0.1538293304135310291, -2.355164825213519109 ) ) ;
#2950=AXIS2_PLACEMENT_3D ( 'NONE', #52012, #10777, #1802 ) ;
#2952=DIRECTION ( 'NONE',  ( 0.000000000000000000, -0.6051742151937555825, -0.7960930657056509707 ) ) ;
#2957=ADVANCED_FACE ( 'NONE', ( #26375 ), #57302, .T. ) ;
#2965=EDGE_CURVE ( 'NONE', #42155, #13349, #34150, .T. ) ;
#2968=CARTESIAN_POINT ( 'NONE',  ( -27.08954555554413801, -2.300063521504145836, 0.1819824474943266546 ) ) ;
#2975=CARTESIAN_POINT ( 'NONE',  ( -22.27722019094931483, 2.813874087060014517, -2.374181302998998877 ) ) ;
#2978=DIRECTION ( 'NONE',  ( -1.000000000000000000, 0.000000000000000000, 0.000000000000000000 ) ) ;
#2981=CARTESIAN_POINT ( 'NONE',  ( -27.08418322526031119, 1.431535851194455145, 1.789041206975748199 ) ) ;
#3001=EDGE_CURVE ( 'NONE', #62601, #58400, #42628, .T. ) ;
#3011=ORIENTED_EDGE ( 'NONE', *, *, #23262, .F. ) ;
#3023=ORIENTED_EDGE ( 'NONE', *, *, #181, .F. ) ;
#3030=VERTEX_POINT ( 'NONE', #16415 ) ;
#3039=ADVANCED_FACE ( 'NONE', ( #36356 ), #55149, .F. ) ;
#3047=CARTESIAN_POINT ( 'NONE',  ( -22.27218376572352554, 0.9890213205919790029, 3.547715993389650713 ) ) ;
#3048=CARTESIAN_POINT ( 'NONE',  ( -22.28415773361649954, 3.586804264761564109, 0.9182279841529663589 ) ) ;
#3062=ORIENTED_EDGE ( 'NONE', *, *, #1434, .F. ) ;
#3073=ORIENTED_EDGE ( 'NONE', *, *, #46770, .F. ) ;
#3074=B_SPLINE_CURVE_WITH_KNOTS ( 'NONE', 3,
 ( #28394, #23087, #23411, #29379, #8780, #33707, #13107, #9095, #38029, #54002, #28719, #49372, #24071, #12756, #18098, #49033 ),
 .UNSPECIFIED., .F., .F.,
 ( 4, 3, 3, 3, 3, 4 ),
 ( 0.000000000000000000, 6.991367980366392898E-05, 0.0001398269368981362607, 0.0002097400188389099591, 0.0002811534801551364318, 0.0003526297678872489867 ),
 .UNSPECIFIED. ) ;
#3075=CARTESIAN_POINT ( 'NONE',  ( 2.000000000000001776, -3.224464355699781848, -6.771471746882029130 ) ) ;
#3080=DIRECTION ( 'NONE',  ( -1.000000000000000000, 0.000000000000000000, 0.000000000000000000 ) ) ;
#3082=CARTESIAN_POINT ( 'NONE',  ( -27.08418322526031119, -0.8335872080609559864, 2.134267017050457849 ) ) ;
#3086=CARTESIAN_POINT ( 'NONE',  ( -10.00000000000000178, 0.000000000000000000, 0.000000000000000000 ) ) ;
#3108=CARTESIAN_POINT ( 'NONE',  ( 2.000000000000001776, -4.604744433234713163, 5.919993978425451608 ) ) ;
#3109=DIRECTION ( 'NONE',  ( -1.000000000000000000, 0.000000000000000000, 0.000000000000000000 ) ) ;
#3115=DIRECTION ( 'NONE',  ( 1.000000000000000000, -0.000000000000000000, -0.000000000000000000 ) ) ;
#3117=DIRECTION ( 'NONE',  ( -1.000000000000000000, 0.000000000000000000, 0.000000000000000000 ) ) ;
#3120=VERTEX_POINT ( 'NONE', #4312 ) ;
#3124=VECTOR ( 'NONE', #1200, 1000.000000000000227 ) ;
#3126=DIRECTION ( 'NONE',  ( -1.000000000000000000, 0.000000000000000000, 0.000000000000000000 ) ) ;
#3129=CARTESIAN_POINT ( 'NONE',  ( -22.31328051695926007, -3.685074213229319717, -0.8849444482788241251 ) ) ;
#3146=VERTEX_POINT ( 'NONE', #18392 ) ;
#3147=DIRECTION ( 'NONE',  ( 0.000000000000000000, -0.1081190184239488317, 0.9941379571543589311 ) ) ;
#3157=VERTEX_POINT ( 'NONE', #49863 ) ;
#3159=CARTESIAN_POINT ( 'NONE',  ( 0.000000000000000000, -1.145812388885072863, -6.715725538143620277 ) ) ;
#3161=CARTESIAN_POINT ( 'NONE',  ( -27.28563798457901868, -0.04047623855282859312, 2.896153581097021590 ) ) ;
#3165=CARTESIAN_POINT ( 'NONE',  ( 2.000000000000001776, -1.865193240757054394, -6.552473556515217012 ) ) ;
#3171=VERTEX_POINT ( 'NONE', #9949 ) ;
#3173=AXIS2_PLACEMENT_3D ( 'NONE', #2721, #27614, #28942 ) ;
#3175=ORIENTED_EDGE ( 'NONE', *, *, #34362, .T. ) ;
#3188=EDGE_LOOP ( 'NONE', ( #60521, #17682, #30246, #63034 ) ) ;
#3197=AXIS2_PLACEMENT_3D ( 'NONE', #12274, #7283, #42862 ) ;
#3199=DIRECTION ( 'NONE',  ( 0.000000000000000000, 0.000000000000000000, 1.000000000000000000 ) ) ;
#3201=VERTEX_POINT ( 'NONE', #50529 ) ;
#3206=DIRECTION ( 'NONE',  ( -1.000000000000000000, 0.000000000000000000, 0.000000000000000000 ) ) ;
#3207=ORIENTED_EDGE ( 'NONE', *, *, #43430, .F. ) ;
#3208=DIRECTION ( 'NONE',  ( 0.000000000000000000, 0.000000000000000000, 1.000000000000000000 ) ) ;
#3218=CARTESIAN_POINT ( 'NONE',  ( 0.000000000000000000, -2.562706407243573459, -6.312399813420393357 ) ) ;
#3231=EDGE_CURVE ( 'NONE', #36273, #32360, #48744, .T. ) ;
#3246=CARTESIAN_POINT ( 'NONE',  ( -27.08417473062937120, 1.729223128152643341, -1.503027223283694092 ) ) ;
#3249=ORIENTED_EDGE ( 'NONE', *, *, #23214, .F. ) ;
#3252=DIRECTION ( 'NONE',  ( -1.000000000000000000, 0.000000000000000000, 0.000000000000000000 ) ) ;
#3256=AXIS2_PLACEMENT_3D ( 'NONE', #53321, #43316, #32027 ) ;
#3260=CARTESIAN_POINT ( 'NONE',  ( -22.31328051695926007, 0.8849444482788259014, -3.685074213229314388 ) ) ;
#3261=CARTESIAN_POINT ( 'NONE',  ( 0.000000000000000000, 6.906413915731199005, -0.6453518998146886565 ) ) ;
#3264=CARTESIAN_POINT ( 'NONE',  ( -22.27706485742869091, 3.358064672837120401, 1.508175983031588840 ) ) ;
#3267=DIRECTION ( 'NONE',  ( -1.000000000000000000, 0.000000000000000000, 0.000000000000000000 ) ) ;
#3273=CARTESIAN_POINT ( 'NONE',  ( -22.31328051695926007, 2.608921479762127849, -2.748895659348120635 ) ) ;
#3274=CARTESIAN_POINT ( 'NONE',  ( 2.000000000000001776, 0.000000000000000000, 0.000000000000000000 ) ) ;
#3278=CARTESIAN_POINT ( 'NONE',  ( -35.04643116707788408, 0.009112266603805360687, -0.008094444324502694799 ) ) ;
#3279=CARTESIAN_POINT ( 'NONE',  ( 2.000000000000001776, 6.470132594555819239, 2.133363481234098469 ) ) ;
#3281=ORIENTED_EDGE ( 'NONE', *, *, #55116, .F. ) ;
#3289=CARTESIAN_POINT ( 'NONE',  ( -27.10307689719148527, -1.615391801699804120, 1.703783570823879323 ) ) ;
#3292=CIRCLE ( 'NONE', #12849, 7.499999999999988454 ) ;
#3294=CARTESIAN_POINT ( 'NONE',  ( 18.00005080000000035, 0.000000000000000000, 0.000000000000000000 ) ) ;
#3300=DIRECTION ( 'NONE',  ( 0.000000000000000000, 0.000000000000000000, 1.000000000000000000 ) ) ;
#3301=CARTESIAN_POINT ( 'NONE',  ( 2.000000000000001776, 6.662861565602072211, 1.421313227905651289 ) ) ;
#3309=EDGE_CURVE ( 'NONE', #332, #61330, #6614, .T. ) ;
#3314=( BOUNDED_SURFACE ( )  B_SPLINE_SURFACE ( 3, 1, ( 
 ( #56284, #1762 ),
 ( #11077, #31021 ),
 ( #61593, #31351 ),
 ( #37653, #57950 ) ),
 .UNSPECIFIED., .F., .F., .F. ) 
 B_SPLINE_SURFACE_WITH_KNOTS ( ( 4, 4 ),
 ( 2, 2 ),
 ( 0.000000000000000000, 1.000000000000000000 ),
 ( 0.000000000000000000, 1.000000000000000000 ),
 .UNSPECIFIED. ) 
 GEOMETRIC_REPRESENTATION_ITEM ( )  RATIONAL_B_SPLINE_SURFACE ( (
 ( 1.000000000000000000, 1.000000000000000000),
 ( 0.8716676215708681896, 0.8964445200148167814),
 ( 0.8716676215708681896, 0.8964445200148167814),
 ( 1.000000000000000000, 1.000000000000000000) ) ) 
 REPRESENTATION_ITEM ( '' )  SURFACE ( )  );
#3321=DIRECTION ( 'NONE',  ( 0.000000000000000000, 0.000000000000000000, 1.000000000000000000 ) ) ;
#3327=AXIS2_PLACEMENT_3D ( 'NONE', #49266, #38937, #22667 ) ;
#3331=EDGE_CURVE ( 'NONE', #60562, #10633, #32500, .T. ) ;
#3333=DIRECTION ( 'NONE',  ( 0.000000000000000000, 0.000000000000000000, 1.000000000000000000 ) ) ;
#3336=DIRECTION ( 'NONE',  ( -1.000000000000000000, 0.000000000000000000, 0.000000000000000000 ) ) ;
#3338=DIRECTION ( 'NONE',  ( -1.000000000000000000, 0.000000000000000000, 0.000000000000000000 ) ) ;
#3344=CARTESIAN_POINT ( 'NONE',  ( 0.000000000000000000, 3.155844197800107498, 6.177028383390443800 ) ) ;
#3348=CARTESIAN_POINT ( 'NONE',  ( 2.000000000000001776, -6.796153407501424049, -1.388283512725909219 ) ) ;
#3357=CIRCLE ( 'NONE', #59640, 2.899999999999995914 ) ;
#3358=DIRECTION ( 'NONE',  ( -1.000000000000000000, 0.000000000000000000, 0.000000000000000000 ) ) ;
#3359=B_SPLINE_CURVE_WITH_KNOTS ( 'NONE', 3,
 ( #58207, #12975, #32905, #17970, #63829, #52882, #38227, #18648, #2707, #38908, #22967, #43221, #54201, #7315, #47903, #8644, #27599, #53218, #57897, #49234, #2364, #22636 ),
 .UNSPECIFIED., .F., .F.,
 ( 4, 3, 3, 3, 3, 3, 3, 4 ),
 ( 0.000000000000000000, 4.447697177976180934E-05, 6.624143997791020252E-05, 8.800576886943984461E-05, 0.0001097699864780857134, 0.0001315341395364307139, 0.0001760120188223187525, 0.0001867971373174701869 ),
 .UNSPECIFIED. ) ;
#3361=DIRECTION ( 'NONE',  ( -1.000000000000000000, 0.000000000000000000, 0.000000000000000000 ) ) ;
#3363=CARTESIAN_POINT ( 'NONE',  ( -22.28939870658739864, -0.2834927284407604553, -3.707376022556866602 ) ) ;
#3366=DIRECTION ( 'NONE',  ( 1.000000000000000000, 0.000000000000000000, 0.000000000000000000 ) ) ;
#3368=ORIENTED_EDGE ( 'NONE', *, *, #33397, .F. ) ;
#3381=CARTESIAN_POINT ( 'NONE',  ( -22.27878402819508707, 3.562981801125752135, 0.9457981527432224311 ) ) ;
#3384=VERTEX_POINT ( 'NONE', #1940 ) ;
#3386=AXIS2_PLACEMENT_3D ( 'NONE', #51473, #29829, #40816 ) ;
#3419=EDGE_CURVE ( 'NONE', #50728, #42390, #19320, .T. ) ;
#3426=EDGE_CURVE ( 'NONE', #1201, #62360, #24499, .T. ) ;
#3428=EDGE_CURVE ( 'NONE', #11425, #26907, #24627, .T. ) ;
#3432=CARTESIAN_POINT ( 'NONE',  ( -22.28629837673888048, 3.697248502489085098, -0.2936941584814282136 ) ) ;
#3437=AXIS2_PLACEMENT_3D ( 'NONE', #40793, #61375, #25826 ) ;
#3439=ORIENTED_EDGE ( 'NONE', *, *, #47419, .T. ) ;
#3455=ORIENTED_EDGE ( 'NONE', *, *, #34362, .F. ) ;
#3458=ORIENTED_EDGE ( 'NONE', *, *, #63498, .T. ) ;
#3466=AXIS2_PLACEMENT_3D ( 'NONE', #33656, #12699, #13048 ) ;
#3467=EDGE_CURVE ( 'NONE', #25430, #65138, #64947, .T. ) ;
#3475=ORIENTED_EDGE ( 'NONE', *, *, #55381, .F. ) ;
#3480=CARTESIAN_POINT ( 'NONE',  ( -22.27704833740210333, 2.142029987820972980, 2.993786163585769877 ) ) ;
#3484=AXIS2_PLACEMENT_3D ( 'NONE', #3301, #14229, #54815 ) ;
#3485=ORIENTED_EDGE ( 'NONE', *, *, #58362, .F. ) ;
#3501=EDGE_CURVE ( 'NONE', #65490, #26404, #35079, .T. ) ;
#3504=DIRECTION ( 'NONE',  ( 0.000000000000000000, 0.000000000000000000, 1.000000000000000000 ) ) ;
#3509=VECTOR ( 'NONE', #62543, 1000.000000000000227 ) ;
#3517=CARTESIAN_POINT ( 'NONE',  ( -22.66110217412718697, 0.1747008913564316313, -4.941631093908251948 ) ) ;
#3521=CARTESIAN_POINT ( 'NONE',  ( 2.000000000000001776, 5.814643797626930954, 3.550179297009575574 ) ) ;
#3525=DIRECTION ( 'NONE',  ( 1.000000000000000000, 0.000000000000000000, 0.000000000000000000 ) ) ;
#3529=ORIENTED_EDGE ( 'NONE', *, *, #43547, .T. ) ;
#3532=ORIENTED_EDGE ( 'NONE', *, *, #7872, .T. ) ;
#3539=EDGE_CURVE ( 'NONE', #60178, #37749, #16931, .T. ) ;
#3540=DIRECTION ( 'NONE',  ( 0.000000000000000000, 0.6876994588534192099, 0.7259954919231347281 ) ) ;
#3544=EDGE_CURVE ( 'NONE', #44459, #12705, #29180, .T. ) ;
#3549=DIRECTION ( 'NONE',  ( 0.000000000000000000, 0.000000000000000000, 1.000000000000000000 ) ) ;
#3551=AXIS2_PLACEMENT_3D ( 'NONE', #1830, #17113, #2502 ) ;
#3555=DIRECTION ( 'NONE',  ( 0.000000000000000000, 0.000000000000000000, 1.000000000000000000 ) ) ;
#3569=DIRECTION ( 'NONE',  ( -1.000000000000000000, 0.000000000000000000, 0.000000000000000000 ) ) ;
#3581=CARTESIAN_POINT ( 'NONE',  ( -22.31328051695926007, -2.608921479762108753, 2.748895659348124187 ) ) ;
#3591=CARTESIAN_POINT ( 'NONE',  ( -22.66110217412718697, 4.941631093908234185, 0.1747008913564567778 ) ) ;
#3593=AXIS2_PLACEMENT_3D ( 'NONE', #30922, #51571, #51885 ) ;
#3608=CARTESIAN_POINT ( 'NONE',  ( 0.000000000000000000, 0.000000000000000000, 0.000000000000000000 ) ) ;
#3609=DIRECTION ( 'NONE',  ( 0.000000000000000000, -0.9868265225415244757, -0.1617819965527746984 ) ) ;
#3615=EDGE_LOOP ( 'NONE', ( #11405, #58441, #39249, #9010 ) ) ;
#3618=VERTEX_POINT ( 'NONE', #65698 ) ;
#3622=CARTESIAN_POINT ( 'NONE',  ( -22.29115169517546136, -1.614783311161199109, 3.355084543108113326 ) ) ;
#3623=VERTEX_POINT ( 'NONE', #51102 ) ;
#3642=CARTESIAN_POINT ( 'NONE',  ( 2.000000000000001776, 1.058508696394974358, 6.730038252034905355 ) ) ;
#3649=CARTESIAN_POINT ( 'NONE',  ( 2.000000000000001776, -5.662015959325143122, -4.918493191654053298 ) ) ;
#3651=AXIS2_PLACEMENT_3D ( 'NONE', #41736, #5871, #26127 ) ;
#3652=CARTESIAN_POINT ( 'NONE',  ( -27.08588607604449550, 1.616144682268094268, -1.631236259433592073 ) ) ;
#3653=DIRECTION ( 'NONE',  ( -1.000000000000000000, 0.000000000000000000, 0.000000000000000000 ) ) ;
#3667=CARTESIAN_POINT ( 'NONE',  ( -22.27834755396594346, 3.643689482009642155, -0.5583491773602359265 ) ) ;
#3668=DIRECTION ( 'NONE',  ( 1.000000000000000000, 0.000000000000000000, 0.000000000000000000 ) ) ;
#3671=AXIS2_PLACEMENT_3D ( 'NONE', #45984, #4784, #25047 ) ;
#3672=CARTESIAN_POINT ( 'NONE',  ( 2.000000000000001776, 6.767909380267608022, -0.7805499053121014441 ) ) ;
#3674=CARTESIAN_POINT ( 'NONE',  ( 0.000000000000000000, 0.000000000000000000, 0.000000000000000000 ) ) ;
#3675=ORIENTED_EDGE ( 'NONE', *, *, #42785, .T. ) ;
#3679=CIRCLE ( 'NONE', #16418, 2.899999999999995470 ) ;
#3684=VERTEX_POINT ( 'NONE', #40108 ) ;
#3685=CARTESIAN_POINT ( 'NONE',  ( 2.000000000000001776, 0.000000000000000000, 0.000000000000000000 ) ) ;
#3700=CARTESIAN_POINT ( 'NONE',  ( 0.000000000000000000, 3.224464355699827145, 6.771471746881979392 ) ) ;
#3702=ORIENTED_EDGE ( 'NONE', *, *, #15172, .T. ) ;
#3703=CARTESIAN_POINT ( 'NONE',  ( -23.18047892478189098, 2.738168160732706191, -3.933989833240143064 ) ) ;
#3707=DIRECTION ( 'NONE',  ( -1.000000000000000000, 0.000000000000000000, 0.000000000000000000 ) ) ;
#3708=VERTEX_POINT ( 'NONE', #27440 ) ;
#3709=ORIENTED_EDGE ( 'NONE', *, *, #39769, .F. ) ;
#3711=ADVANCED_FACE ( 'NONE', ( #16506 ), #42076, .F. ) ;
#3712=ORIENTED_EDGE ( 'NONE', *, *, #47263, .T. ) ;
#3722=EDGE_CURVE ( 'NONE', #51469, #36018, #12783, .T. ) ;
#3730=DIRECTION ( 'NONE',  ( 0.000000000000000000, 0.000000000000000000, 1.000000000000000000 ) ) ;
#3737=ORIENTED_EDGE ( 'NONE', *, *, #58121, .F. ) ;
#3740=AXIS2_PLACEMENT_3D ( 'NONE', #6168, #63307, #57034 ) ;
#3750=CIRCLE ( 'NONE', #19678, 1.499999999999998224 ) ;
#3752=CARTESIAN_POINT ( 'NONE',  ( -22.65999102136915511, 4.797155153747065803, 0.5917351393134848703 ) ) ;
#3757=ADVANCED_FACE ( 'NONE', ( #21142 ), #17484, .T. ) ;
#3759=ORIENTED_EDGE ( 'NONE', *, *, #64613, .T. ) ;
#3767=PRODUCT_DEFINITION_FORMATION_WITH_SPECIFIED_SOURCE ( 'ANY', '', #33856, .NOT_KNOWN. ) ;
#3773=CARTESIAN_POINT ( 'NONE',  ( -22.27713295444592845, -2.530364014314296472, -2.673940016109019879 ) ) ;
#3774=CARTESIAN_POINT ( 'NONE',  ( 0.000000000000000000, 2.480520636974283821, -6.345145617221223944 ) ) ;
#3786=ADVANCED_FACE ( 'NONE', ( #1554 ), #37758, .T. ) ;
#3802=CARTESIAN_POINT ( 'NONE',  ( 0.000000000000000000, 6.777474576704075382, -0.6925993764990371337 ) ) ;
#3815=EDGE_CURVE ( 'NONE', #125, #10128, #57733, .T. ) ;
#3822=CIRCLE ( 'NONE', #21843, 2.899999999999994582 ) ;
#3825=VERTEX_POINT ( 'NONE', #43384 ) ;
#3835=DIRECTION ( 'NONE',  ( -1.000000000000000000, 0.000000000000000000, 0.000000000000000000 ) ) ;
#3844=ORIENTED_EDGE ( 'NONE', *, *, #16582, .F. ) ;
#3849=CARTESIAN_POINT ( 'NONE',  ( -22.28506771379528573, -3.348518833762381686, -1.636577531579577416 ) ) ;
#3867=CARTESIAN_POINT ( 'NONE',  ( -27.05874794189610455, 1.836970198720914070E-16, -1.500000000000008882 ) ) ;
#3870=DIRECTION ( 'NONE',  ( 0.000000000000000000, 0.000000000000000000, 1.000000000000000000 ) ) ;
#3871=CYLINDRICAL_SURFACE ( 'NONE', #62863, 2.899999999999994582 ) ;
#3879=EDGE_CURVE ( 'NONE', #24723, #27863, #22330, .T. ) ;
#3881=CARTESIAN_POINT ( 'NONE',  ( 2.000000000000001776, -5.769711778877296027, -4.791703871138604853 ) ) ;
#3887=CYLINDRICAL_SURFACE ( 'NONE', #165, 7.499999999999988454 ) ;
#3892=DIRECTION ( 'NONE',  ( -1.000000000000000000, 0.000000000000000000, 0.000000000000000000 ) ) ;
#3899=( BOUNDED_SURFACE ( )  B_SPLINE_SURFACE ( 3, 1, ( 
 ( #35912, #19349 ),
 ( #14982, #35606 ),
 ( #45927, #10019 ),
 ( #35271, #34615 ) ),
 .UNSPECIFIED., .F., .F., .F. ) 
 B_SPLINE_SURFACE_WITH_KNOTS ( ( 4, 4 ),
 ( 2, 2 ),
 ( 0.000000000000000000, 1.000000000000000000 ),
 ( 0.000000000000000000, 1.000000000000000000 ),
 .UNSPECIFIED. ) 
 GEOMETRIC_REPRESENTATION_ITEM ( )  RATIONAL_B_SPLINE_SURFACE ( (
 ( 1.000000000000000000, 1.000000000000000000),
 ( 0.9257577194822556033, 0.9980522942447415113),
 ( 0.9257577194822556033, 0.9980522942447415113),
 ( 1.000000000000000000, 1.000000000000000000) ) ) 
 REPRESENTATION_ITEM ( '' )  SURFACE ( )  );
#3905=DIRECTION ( 'NONE',  ( -1.000000000000000000, 0.000000000000000000, 0.000000000000000000 ) ) ;
#3907=EDGE_CURVE ( 'NONE', #5798, #48006, #44060, .T. ) ;
#3921=EDGE_CURVE ( 'NONE', #36432, #3157, #13773, .T. ) ;
#3928=ORIENTED_EDGE ( 'NONE', *, *, #5131, .F. ) ;
#3931=ORIENTED_EDGE ( 'NONE', *, *, #32100, .F. ) ;
#3935=ORIENTED_EDGE ( 'NONE', *, *, #24653, .F. ) ;
#3941=CARTESIAN_POINT ( 'NONE',  ( 2.000000000000001776, 0.000000000000000000, 7.500000000000000000 ) ) ;
#3955=CARTESIAN_POINT ( 'NONE',  ( -27.10719052120871098, 2.295785794152562787, 0.5475695427849293084 ) ) ;
#3956=DIRECTION ( 'NONE',  ( -1.000000000000000000, 0.000000000000000000, 0.000000000000000000 ) ) ;
#3958=ORIENTED_EDGE ( 'NONE', *, *, #5883, .T. ) ;
#3965=CARTESIAN_POINT ( 'NONE',  ( 2.000000000000001776, -1.018311147294196806, 6.861346417234461370 ) ) ;
#3971=EDGE_CURVE ( 'NONE', #38388, #60470, #24799, .T. ) ;
#3972=DIRECTION ( 'NONE',  ( -1.000000000000000000, 0.000000000000000000, 0.000000000000000000 ) ) ;
#3977=CARTESIAN_POINT ( 'NONE',  ( -35.04643116707788408, -0.001845126042319261694, -0.01204777744935776884 ) ) ;
#3981=LINE ( 'NONE', #25226, #21401 ) ;
#3984=ORIENTED_EDGE ( 'NONE', *, *, #6838, .F. ) ;
#3985=CARTESIAN_POINT ( 'NONE',  ( -27.08776759928964850, 2.217308861843129364, -0.6183458186125485589 ) ) ;
#3986=CYLINDRICAL_SURFACE ( 'NONE', #25527, 7.499999999999988454 ) ;
#3990=CARTESIAN_POINT ( 'NONE',  ( 2.000000000000001776, 0.000000000000000000, 0.000000000000000000 ) ) ;
#3993=EDGE_CURVE ( 'NONE', #10675, #44838, #28818, .T. ) ;
#3997=ADVANCED_FACE ( 'NONE', ( #10117 ), #30396, .T. ) ;
#3999=ORIENTED_EDGE ( 'NONE', *, *, #14250, .T. ) ;
#4002=CARTESIAN_POINT ( 'NONE',  ( -27.35552965826137140, 1.773915698030573473, -2.548625910254528559 ) ) ;
#4004=DIRECTION ( 'NONE',  ( -1.000000000000000000, 0.000000000000000000, 0.000000000000000000 ) ) ;
#4024=DIRECTION ( 'NONE',  ( -1.000000000000000000, 0.000000000000000000, 0.000000000000000000 ) ) ;
#4042=ORIENTED_EDGE ( 'NONE', *, *, #32715, .F. ) ;
#4052=CIRCLE ( 'NONE', #47574, 6.936499999999989008 ) ;
#4056=AXIS2_PLACEMENT_3D ( 'NONE', #11702, #62908, #43602 ) ;
#4059=CARTESIAN_POINT ( 'NONE',  ( -35.04660725145885891, -0.003326400506010091657, 0.01184012236745035987 ) ) ;
#4062=DIRECTION ( 'NONE',  ( 0.000000000000000000, 0.000000000000000000, -1.000000000000000000 ) ) ;
#4070=DIRECTION ( 'NONE',  ( -1.000000000000000000, 0.000000000000000000, 0.000000000000000000 ) ) ;
#4074=EDGE_LOOP ( 'NONE', ( #17907, #37943, #45108, #58361 ) ) ;
#4084=ORIENTED_EDGE ( 'NONE', *, *, #50522, .T. ) ;
#4088=LINE ( 'NONE', #14685, #22740 ) ;
#4094=ORIENTED_EDGE ( 'NONE', *, *, #17276, .T. ) ;
#4103=CARTESIAN_POINT ( 'NONE',  ( -27.35552965826136429, -1.320216934008378473, -2.810569013793753346 ) ) ;
#4105=CARTESIAN_POINT ( 'NONE',  ( -22.31213670151048944, 1.669817926839938460, -3.398324501467284708 ) ) ;
#4123=EDGE_CURVE ( 'NONE', #15834, #36605, #59828, .T. ) ;
#4146=AXIS2_PLACEMENT_3D ( 'NONE', #37457, #56432, #16197 ) ;
#4148=ADVANCED_FACE ( 'NONE', ( #22054 ), #56316, .T. ) ;
#4155=EDGE_CURVE ( 'NONE', #48840, #42334, #62600, .T. ) ;
#4158=ORIENTED_EDGE ( 'NONE', *, *, #47404, .T. ) ;
#4160=ORIENTED_EDGE ( 'NONE', *, *, #44087, .F. ) ;
#4162=ORIENTED_EDGE ( 'NONE', *, *, #23764, .T. ) ;
#4165=CARTESIAN_POINT ( 'NONE',  ( -27.35552965826137140, 2.548625910254547655, 1.773915698030531951 ) ) ;
#4173=ORIENTED_EDGE ( 'NONE', *, *, #15625, .T. ) ;
#4179=CARTESIAN_POINT ( 'NONE',  ( -22.27720412283625961, 1.161733799004190049, -3.493592264983214513 ) ) ;
#4186=VERTEX_POINT ( 'NONE', #38323 ) ;
#4187=CARTESIAN_POINT ( 'NONE',  ( -27.28563798457900091, 1.413023339712129678, 2.528380693767707577 ) ) ;
#4188=SURFACE_SIDE_STYLE ('',( #49743 ) ) ;
#4192=DIRECTION ( 'NONE',  ( -1.000000000000000000, 0.000000000000000000, 0.000000000000000000 ) ) ;
#4216=CYLINDRICAL_SURFACE ( 'NONE', #36498, 2.899999999999994582 ) ;
#4217=EDGE_CURVE ( 'NONE', #60024, #18352, #60917, .T. ) ;
#4218=B_SPLINE_CURVE_WITH_KNOTS ( 'NONE', 3,
 ( #56938, #40297, #20031, #36294, #10058, #70, #6069, #1065, #55936, #5402 ),
 .UNSPECIFIED., .F., .F.,
 ( 4, 3, 3, 4 ),
 ( 3.556024639816093331E-05, 0.0005177888728809999395, 0.002588944364542827056, 0.005045323458346599385 ),
 .UNSPECIFIED. ) ;
#4221=ADVANCED_FACE ( 'NONE', ( #52970 ), #53315, .T. ) ;
#4233=CYLINDRICAL_SURFACE ( 'NONE', #46052, 2.899999999999994582 ) ;
#4234=ADVANCED_FACE ( 'NONE', ( #18060 ), #22728, .T. ) ;
#4244=AXIS2_PLACEMENT_3D ( 'NONE', #34852, #55161, #9590 ) ;
#4247=CARTESIAN_POINT ( 'NONE',  ( -10.00000000000000178, 0.000000000000000000, 0.000000000000000000 ) ) ;
#4250=B_SPLINE_CURVE_WITH_KNOTS ( 'NONE', 3,
 ( #64876, #35277, #60551, #55587, #45269, #40262, #29004, #10026, #14989, #65527, #19994, #30306, #24997, #54621, #19022, #54915, #49312, #19355, #24016 ),
 .UNSPECIFIED., .F., .F.,
 ( 4, 3, 3, 3, 3, 3, 4 ),
 ( 0.000000000000000000, 2.836829842861096206E-05, 4.224792512343923038E-05, 5.612066614708679683E-05, 6.998859278152698427E-05, 9.832141287889580906E-05, 0.0001178161482480330561 ),
 .UNSPECIFIED. ) ;
#4254=ORIENTED_EDGE ( 'NONE', *, *, #45022, .F. ) ;
#4255=VECTOR ( 'NONE', #53500, 1000.000000000000000 ) ;
#4262=CYLINDRICAL_SURFACE ( 'NONE', #40150, 2.899999999999994582 ) ;
#4270=CARTESIAN_POINT ( 'NONE',  ( -27.09833916700336331, 1.609723001518233998, -1.689564470273829055 ) ) ;
#4271=CARTESIAN_POINT ( 'NONE',  ( 2.000000000000001776, 2.480520636974191895, 6.345145617221231049 ) ) ;
#4274=CARTESIAN_POINT ( 'NONE',  ( 2.000000000000001776, -5.585096664091960150, 4.113602740025890547 ) ) ;
#4285=EDGE_CURVE ( 'NONE', #37470, #62166, #54522, .T. ) ;
#4287=CARTESIAN_POINT ( 'NONE',  ( 2.000000000000001776, 0.000000000000000000, 0.000000000000000000 ) ) ;
#4288=CARTESIAN_POINT ( 'NONE',  ( 2.000000000000001776, -2.664846396702436948, -6.404188155573047325 ) ) ;
#4302=CARTESIAN_POINT ( 'NONE',  ( 2.000000000000001776, 6.470132594555819239, 2.133363481234098469 ) ) ;
#4303=ADVANCED_FACE ( 'NONE', ( #10351 ), #55920, .T. ) ;
#4306=CARTESIAN_POINT ( 'NONE',  ( -27.09342121492585420, 2.227768580955217903, -0.6436068655225335444 ) ) ;
#4312=CARTESIAN_POINT ( 'NONE',  ( 2.000000000000001776, 5.662015959325201742, 4.918493191653995567 ) ) ;
#4316=FACE_OUTER_BOUND ( 'NONE', #58075, .T. ) ;
#4320=ORIENTED_EDGE ( 'NONE', *, *, #41373, .F. ) ;
#4323=AXIS2_PLACEMENT_3D ( 'NONE', #2256, #63723, #2917 ) ;
#4327=VERTEX_POINT ( 'NONE', #59943 ) ;
#4330=VERTEX_POINT ( 'NONE', #20013 ) ;
#4332=B_SPLINE_CURVE_WITH_KNOTS ( 'NONE', 3,
 ( #36693, #16078, #27052, #46352, #61971, #17059, #31049, #56313, #11732, #31381, #46668, #31686, #6125, #26721, #1471, #47346, #10762, #56991, #20752, #41339, #11417, #62598 ),
 .UNSPECIFIED., .F., .F.,
 ( 4, 3, 3, 3, 3, 3, 3, 4 ),
 ( 0.000000000000000000, 4.455945684386706894E-05, 6.636307477203974396E-05, 8.816671873158892945E-05, 0.0001099660380492610182, 0.0001317545563165296125, 0.0001762613022895047734, 0.0001867992666138396194 ),
 .UNSPECIFIED. ) ;
#4334=CARTESIAN_POINT ( 'NONE',  ( -27.08588607604433562, -2.220764381377023700, -0.5840042213197168541 ) ) ;
#4340=ORIENTED_EDGE ( 'NONE', *, *, #19130, .F. ) ;
#4341=ORIENTED_EDGE ( 'NONE', *, *, #26273, .T. ) ;
#4349=ORIENTED_EDGE ( 'NONE', *, *, #18952, .T. ) ;
#4350=AXIS2_PLACEMENT_3D ( 'NONE', #42380, #52730, #27124 ) ;
#4357=AXIS2_PLACEMENT_3D ( 'NONE', #4271, #40145, #44482 ) ;
#4358=VERTEX_POINT ( 'NONE', #9697 ) ;
#4362=CYLINDRICAL_SURFACE ( 'NONE', #65194, 7.499999999999988454 ) ;
#4368=CARTESIAN_POINT ( 'NONE',  ( 0.000000000000000000, -0.2704997240205401221, 6.931223712253438585 ) ) ;
#4372=AXIS2_PLACEMENT_3D ( 'NONE', #63328, #12784, #43714 ) ;
#4386=FACE_OUTER_BOUND ( 'NONE', #42998, .T. ) ;
#4389=DIRECTION ( 'NONE',  ( -1.000000000000000000, 0.000000000000000000, 0.000000000000000000 ) ) ;
#4391=EDGE_CURVE ( 'NONE', #62601, #50166, #60246, .T. ) ;
#4395=AXIS2_PLACEMENT_3D ( 'NONE', #2334, #22610, #42875 ) ;
#4398=CARTESIAN_POINT ( 'NONE',  ( -22.30625920655495165, 3.150098859949344909, -2.110841417170892242 ) ) ;
#4402=CIRCLE ( 'NONE', #50061, 1.499999999999997780 ) ;
#4403=EDGE_LOOP ( 'NONE', ( #23586, #4349, #23661, #45279, #15482, #57855, #10341, #63344, #37520, #21399, #24518, #60034, #15934, #62861, #14353, #12038, #45225, #30767, #20046, #32763, #26079, #63278, #11612, #7262, #40695, #47433, #26396, #6541, #3999, #22414, #29465, #51739, #31227, #37025 ) ) ;
#4417=CARTESIAN_POINT ( 'NONE',  ( 2.000000000000001776, 7.387287142779370264, -1.295372019972111932 ) ) ;
#4419=DIRECTION ( 'NONE',  ( -1.000000000000000000, 0.000000000000000000, 0.000000000000000000 ) ) ;
#4424=DIRECTION ( 'NONE',  ( -1.000000000000000000, 0.000000000000000000, 0.000000000000000000 ) ) ;
#4430=AXIS2_PLACEMENT_3D ( 'NONE', #12364, #63241, #63556 ) ;
#4437=EDGE_LOOP ( 'NONE', ( #9980, #33598, #11430, #64585 ) ) ;
#4444=CARTESIAN_POINT ( 'NONE',  ( 0.000000000000000000, -3.152010634611648321, -6.039758645301327000 ) ) ;
#4446=LINE ( 'NONE', #19738, #26364 ) ;
#4447=AXIS2_PLACEMENT_3D ( 'NONE', #29878, #25551, #64788 ) ;
#4449=ADVANCED_FACE ( 'NONE', ( #1714 ), #20980, .T. ) ;
#4452=ORIENTED_EDGE ( 'NONE', *, *, #8794, .F. ) ;
#4457=ADVANCED_FACE ( 'NONE', ( #26978 ), #6368, .T. ) ;
#4460=B_SPLINE_CURVE_WITH_KNOTS ( 'NONE', 3,
 ( #14586, #17732, #33345, #34864, #2447, #53957, #55173, #8396 ),
 .UNSPECIFIED., .F., .F.,
 ( 4, 2, 2, 4 ),
 ( 0.000000000000000000, 0.0003639104015150018061, 0.0007278208030300036121, 0.001455641606060007224 ),
 .UNSPECIFIED. ) ;
#4469=DIRECTION ( 'NONE',  ( -1.000000000000000000, 0.000000000000000000, 0.000000000000000000 ) ) ;
#4478=CARTESIAN_POINT ( 'NONE',  ( -22.27715239060371744, 3.521735673127126542, 1.072868796692219240 ) ) ;
#4482=DIRECTION ( 'NONE',  ( -1.000000000000000000, 0.000000000000000000, 0.000000000000000000 ) ) ;
#4485=VERTEX_POINT ( 'NONE', #25999 ) ;
#4489=AXIS2_PLACEMENT_3D ( 'NONE', #45754, #40776, #47083 ) ;
#4492=DIRECTION ( 'NONE',  ( -1.000000000000000000, 0.000000000000000000, 0.000000000000000000 ) ) ;
#4493=FACE_OUTER_BOUND ( 'NONE', #2919, .T. ) ;
#4505=CARTESIAN_POINT ( 'NONE',  ( -22.30398854582848145, -0.8844201765542077931, 3.656532484463041577 ) ) ;
#4512=ORIENTED_EDGE ( 'NONE', *, *, #6769, .T. ) ;
#4515=ORIENTED_EDGE ( 'NONE', *, *, #64778, .F. ) ;
#4519=ORIENTED_EDGE ( 'NONE', *, *, #8270, .T. ) ;
#4524=CARTESIAN_POINT ( 'NONE',  ( -22.27722015946439171, 1.271715168852085132, -3.455127654605127496 ) ) ;
#4528=EDGE_CURVE ( 'NONE', #32831, #55569, #39546, .T. ) ;
#4536=VECTOR ( 'NONE', #53489, 1000.000000000000000 ) ;
#4537=AXIS2_PLACEMENT_3D ( 'NONE', #14494, #50439, #4884 ) ;
#4540=EDGE_CURVE ( 'NONE', #16636, #15834, #7017, .T. ) ;
#4547=ORIENTED_EDGE ( 'NONE', *, *, #3501, .T. ) ;
#4562=AXIS2_PLACEMENT_3D ( 'NONE', #41596, #31611, #55916 ) ;
#4564=CARTESIAN_POINT ( 'NONE',  ( 0.000000000000000000, 0.000000000000000000, 0.000000000000000000 ) ) ;
#4567=CIRCLE ( 'NONE', #41716, 2.899999999999996803 ) ;
#4568=CARTESIAN_POINT ( 'NONE',  ( 1.000000000000000888, 6.936109781200682889, 2.853135311045038591 ) ) ;
#4577=ORIENTED_EDGE ( 'NONE', *, *, #53382, .T. ) ;
#4589=EDGE_CURVE ( 'NONE', #21047, #36610, #63653, .T. ) ;
#4598=CARTESIAN_POINT ( 'NONE',  ( -27.08430792439081003, 0.6005833784282779142, -2.211452765398048914 ) ) ;
#4600=CARTESIAN_POINT ( 'NONE',  ( -10.00000000000000178, 0.000000000000000000, 0.000000000000000000 ) ) ;
#4601=CARTESIAN_POINT ( 'NONE',  ( -27.09861164373112885, 1.025570525056652693, -2.097104182796081240 ) ) ;
#4603=DIRECTION ( 'NONE',  ( -1.000000000000000000, 0.000000000000000000, 0.000000000000000000 ) ) ;
#4616=CARTESIAN_POINT ( 'NONE',  ( -27.28573687977896611, 2.862048090118431976, 0.4470060700698362810 ) ) ;
#4621=AXIS2_PLACEMENT_3D ( 'NONE', #25068, #4469, #54356 ) ;
#4623=ORIENTED_EDGE ( 'NONE', *, *, #7872, .F. ) ;
#4628=CARTESIAN_POINT ( 'NONE',  ( -22.27704833740210333, -3.663709865074144201, 0.3581593033281248450 ) ) ;
#4632=DIRECTION ( 'NONE',  ( -1.000000000000000000, 0.000000000000000000, 0.000000000000000000 ) ) ;
#4652=CARTESIAN_POINT ( 'NONE',  ( -27.09229696323321335, 2.225368503508855067, -0.6397626223479118135 ) ) ;
#4657=CYLINDRICAL_SURFACE ( 'NONE', #2478, 2.899999999999994582 ) ;
#4672=EDGE_CURVE ( 'NONE', #57650, #65336, #43827, .T. ) ;
#4676=CARTESIAN_POINT ( 'NONE',  ( 2.000000000000001776, 2.664846396702499121, 6.404188155572998475 ) ) ;
#4678=B_SPLINE_CURVE_WITH_KNOTS ( 'NONE', 3,
 ( #27486, #11542, #18187, #22855, #53443, #43106, #37803, #42116, #43428, #27173, #1907, #38115, #63383, #6902, #22175, #7888, #62400, #48131, #37136 ),
 .UNSPECIFIED., .F., .F.,
 ( 4, 3, 3, 3, 3, 3, 4 ),
 ( 0.000000000000000000, 2.836829842860724867E-05, 4.224792512343544923E-05, 5.612066614708095569E-05, 6.998859278152062813E-05, 9.832141287889069976E-05, 0.0001178161482480190834 ),
 .UNSPECIFIED. ) ;
#4681=ORIENTED_EDGE ( 'NONE', *, *, #50536, .F. ) ;
#4685=ADVANCED_FACE ( 'NONE', ( #30247 ), #36899, .F. ) ;
#4688=ORIENTED_EDGE ( 'NONE', *, *, #24378, .T. ) ;
#4690=VERTEX_POINT ( 'NONE', #34872 ) ;
#4696=CARTESIAN_POINT ( 'NONE',  ( -22.46509356695198889, -2.840174833751764272, 3.157489876851286681 ) ) ;
#4697=ORIENTED_EDGE ( 'NONE', *, *, #30812, .F. ) ;
#4698=DIRECTION ( 'NONE',  ( -1.000000000000000000, 0.000000000000000000, 0.000000000000000000 ) ) ;
#4703=DIRECTION ( 'NONE',  ( -1.000000000000000000, 0.000000000000000000, 0.000000000000000000 ) ) ;
#4713=ORIENTED_EDGE ( 'NONE', *, *, #42221, .T. ) ;
#4715=CARTESIAN_POINT ( 'NONE',  ( 0.000000000000000000, 0.000000000000000000, 0.000000000000000000 ) ) ;
#4722=CIRCLE ( 'NONE', #32255, 2.899999999999995914 ) ;
#4728=CARTESIAN_POINT ( 'NONE',  ( 1.000000000000000888, 0.7281529553922073683, 7.464569195442786409 ) ) ;
#4731=DIRECTION ( 'NONE',  ( -1.000000000000000000, 0.000000000000000000, 0.000000000000000000 ) ) ;
#4741=CARTESIAN_POINT ( 'NONE',  ( 0.000000000000000000, -6.586971819220299729, -3.586335490831473738 ) ) ;
#4743=VERTEX_POINT ( 'NONE', #14923 ) ;
#4754=CARTESIAN_POINT ( 'NONE',  ( -22.28236030719477512, 0.3108070568283993751, 3.683993210674375351 ) ) ;
#4760=EDGE_CURVE ( 'NONE', #21349, #55219, #36712, .T. ) ;
#4761=EDGE_CURVE ( 'NONE', #53826, #28860, #59728, .T. ) ;
#4767=CARTESIAN_POINT ( 'NONE',  ( 2.000000000000001776, 3.979254915827449945, -5.681598592373734213 ) ) ;
#4774=CARTESIAN_POINT ( 'NONE',  ( -27.08954555554413446, -0.1819824474943325943, -2.300063521504153830 ) ) ;
#4777=ORIENTED_EDGE ( 'NONE', *, *, #63713, .F. ) ;
#4778=VERTEX_POINT ( 'NONE', #35856 ) ;
#4784=DIRECTION ( 'NONE',  ( -1.000000000000000000, 0.000000000000000000, 0.000000000000000000 ) ) ;
#4794=CYLINDRICAL_SURFACE ( 'NONE', #25416, 2.899999999999994582 ) ;
#4807=EDGE_CURVE ( 'NONE', #5728, #41912, #37402, .T. ) ;
#4815=ORIENTED_EDGE ( 'NONE', *, *, #46436, .T. ) ;
#4816=VERTEX_POINT ( 'NONE', #1803 ) ;
#4820=ORIENTED_EDGE ( 'NONE', *, *, #4761, .F. ) ;
#4826=DIRECTION ( 'NONE',  ( 0.000000000000000000, 0.000000000000000000, -1.000000000000000000 ) ) ;
#4827=CARTESIAN_POINT ( 'NONE',  ( 0.000000000000000000, 1.956810415765277922, -6.654767106875532967 ) ) ;
#4833=ORIENTED_EDGE ( 'NONE', *, *, #48499, .T. ) ;
#4834=ORIENTED_EDGE ( 'NONE', *, *, #18181, .T. ) ;
#4837=EDGE_CURVE ( 'NONE', #9689, #50060, #25745, .T. ) ;
#4843=ORIENTED_EDGE ( 'NONE', *, *, #56908, .F. ) ;
#4847=VERTEX_POINT ( 'NONE', #21765 ) ;
#4850=DIRECTION ( 'NONE',  ( 0.000000000000000000, -0.1081190184239489566, 0.9941379571543588201 ) ) ;
#4860=DIRECTION ( 'NONE',  ( 0.000000000000000000, 0.000000000000000000, 1.000000000000000000 ) ) ;
#4864=CARTESIAN_POINT ( 'NONE',  ( -22.51237073810381162, -4.218051923713588280, 1.333315726166073967 ) ) ;
#4868=CARTESIAN_POINT ( 'NONE',  ( -27.08426571771018487, -2.098821047392069428, -0.9198084705429488972 ) ) ;
#4883=CARTESIAN_POINT ( 'NONE',  ( 0.000000000000000000, 5.888698556700818543, -3.665823448873358981 ) ) ;
#4884=DIRECTION ( 'NONE',  ( 0.000000000000000000, 0.8276889981568879007, 0.5611870653623863836 ) ) ;
#4887=ORIENTED_EDGE ( 'NONE', *, *, #36857, .T. ) ;
#4890=EDGE_CURVE ( 'NONE', #20337, #30460, #16750, .T. ) ;
#4895=CARTESIAN_POINT ( 'NONE',  ( -27.08954555554373300, 1.307633183325747739, 1.900922216191343717 ) ) ;
#4897=CIRCLE ( 'NONE', #35670, 2.899999999999995914 ) ;
#4916=VERTEX_POINT ( 'NONE', #7418 ) ;
#4919=DIRECTION ( 'NONE',  ( -1.000000000000000000, 0.000000000000000000, 0.000000000000000000 ) ) ;
#4920=CARTESIAN_POINT ( 'NONE',  ( -27.08588607604433562, 0.5840042213197134124, -2.220764381377025476 ) ) ;
#4921=DIRECTION ( 'NONE',  ( 1.000000000000000000, -0.000000000000000000, -0.000000000000000000 ) ) ;
#4926=ORIENTED_EDGE ( 'NONE', *, *, #2714, .T. ) ;
#4930=DIRECTION ( 'NONE',  ( 0.000000000000000000, -0.8276889981568955612, 0.5611870653623749483 ) ) ;
#4935=DIRECTION ( 'NONE',  ( 1.000000000000000000, 0.000000000000000000, 0.000000000000000000 ) ) ;
#4937=ORIENTED_EDGE ( 'NONE', *, *, #35605, .T. ) ;
#4941=VERTEX_POINT ( 'NONE', #52677 ) ;
#4947=ORIENTED_EDGE ( 'NONE', *, *, #32895, .T. ) ;
#4950=CARTESIAN_POINT ( 'NONE',  ( -27.09150307427401927, 2.085162835056709518, 1.001311209615645570 ) ) ;
#4954=LINE ( 'NONE', #56821, #25524 ) ;
#4957=CARTESIAN_POINT ( 'NONE',  ( -27.08639648637162267, -0.5801562253464774832, 2.223359598375754587 ) ) ;
#4958=ORIENTED_EDGE ( 'NONE', *, *, #26947, .T. ) ;
#4962=B_SPLINE_CURVE_WITH_KNOTS ( 'NONE', 3,
 ( #42175, #12262, #46866, #62462, #37194, #37541, #21604, #37866, #2307, #58157, #32854, #53162, #7608, #57847, #26573, #2654, #22915, #17914, #38176, #62157, #16929, #8580 ),
 .UNSPECIFIED., .F., .F.,
 ( 4, 3, 3, 3, 3, 3, 3, 4 ),
 ( 0.000000000000000000, 6.990956068646398400E-05, 0.0001398191187764043859, 0.0002097286751720219781, 0.0002796382307041368601, 0.0003495477861619817792, 0.0004194573423310291168, 0.0005586102576333201340 ),
 .UNSPECIFIED. ) ;
#4963=DIRECTION ( 'NONE',  ( 0.000000000000000000, 0.000000000000000000, 1.000000000000000000 ) ) ;
#4967=ORIENTED_EDGE ( 'NONE', *, *, #10550, .T. ) ;
#4968=CARTESIAN_POINT ( 'NONE',  ( -27.09833916700227618, 2.238843247505183598, -0.6583442518269285726 ) ) ;
#4971=FACE_OUTER_BOUND ( 'NONE', #32078, .T. ) ;
#4985=ORIENTED_EDGE ( 'NONE', *, *, #1807, .T. ) ;
#5001=ORIENTED_EDGE ( 'NONE', *, *, #36863, .T. ) ;
#5007=DIRECTION ( 'NONE',  ( 0.000000000000000000, 0.9985334138511237079, 0.05413890858542116241 ) ) ;
#5012=CARTESIAN_POINT ( 'NONE',  ( 2.000000000000001776, -6.662861565602053560, -1.421313227905724341 ) ) ;
#5017=ADVANCED_FACE ( 'NONE', ( #23386 ), #45838, .F. ) ;
#5023=DIRECTION ( 'NONE',  ( -1.000000000000000000, 0.000000000000000000, 0.000000000000000000 ) ) ;
#5033=DIRECTION ( 'NONE',  ( -1.000000000000000000, 0.000000000000000000, 0.000000000000000000 ) ) ;
#5037=DIRECTION ( 'NONE',  ( 1.000000000000000000, -0.000000000000000000, -0.000000000000000000 ) ) ;
#5045=CARTESIAN_POINT ( 'NONE',  ( -35.04709527796842394, -0.001003525937983557048, 0.01232256164995608472 ) ) ;
#5047=EDGE_CURVE ( 'NONE', #36605, #9429, #15024, .T. ) ;
#5050=EDGE_CURVE ( 'NONE', #39295, #27713, #24496, .T. ) ;
#5052=ORIENTED_EDGE ( 'NONE', *, *, #31788, .T. ) ;
#5054=EDGE_CURVE ( 'NONE', #11425, #20378, #45615, .T. ) ;
#5059=ADVANCED_FACE ( 'NONE', ( #45299 ), #57297, .F. ) ;
#5069=EDGE_CURVE ( 'NONE', #26347, #4941, #25026, .T. ) ;
#5073=EDGE_LOOP ( 'NONE', ( #57638, #38829, #1222, #51521 ) ) ;
#5075=FACE_OUTER_BOUND ( 'NONE', #15166, .T. ) ;
#5076=CARTESIAN_POINT ( 'NONE',  ( -35.04834644901396956, -0.009049049589492451362, 0.01046409687783809300 ) ) ;
#5079=CARTESIAN_POINT ( 'NONE',  ( 2.000000000000001776, -3.230174184210014232, -5.998318953995379843 ) ) ;
#5083=CARTESIAN_POINT ( 'NONE',  ( -27.08417568107323703, 2.261355310631424587, -0.3682236895270699639 ) ) ;
#5084=LINE ( 'NONE', #60269, #22684 ) ;
#5093=CARTESIAN_POINT ( 'NONE',  ( -27.08419797710328325, 0.3221715127608066331, 2.268561579780434379 ) ) ;
#5100=ORIENTED_EDGE ( 'NONE', *, *, #30597, .F. ) ;
#5102=DIRECTION ( 'NONE',  ( 0.000000000000000000, 0.000000000000000000, 1.000000000000000000 ) ) ;
#5104=ORIENTED_EDGE ( 'NONE', *, *, #23948, .T. ) ;
#5107=CIRCLE ( 'NONE', #28439, 6.936499999999990784 ) ;
#5108=CIRCLE ( 'NONE', #12525, 2.899999999999994138 ) ;
#5110=CARTESIAN_POINT ( 'NONE',  ( 2.000000000000001776, 0.000000000000000000, 0.000000000000000000 ) ) ;
#5114=ORIENTED_EDGE ( 'NONE', *, *, #28984, .T. ) ;
#5118=EDGE_CURVE ( 'NONE', #24342, #58016, #42244, .T. ) ;
#5130=VERTEX_POINT ( 'NONE', #11354 ) ;
#5131=EDGE_CURVE ( 'NONE', #44216, #37286, #1061, .T. ) ;
#5133=ORIENTED_EDGE ( 'NONE', *, *, #34679, .F. ) ;
#5138=CARTESIAN_POINT ( 'NONE',  ( -22.35190811654612375, -2.161847148103705152, -3.252894036332531602 ) ) ;
#5148=CYLINDRICAL_SURFACE ( 'NONE', #6247, 7.499999999999988454 ) ;
#5154=DIRECTION ( 'NONE',  ( 0.000000000000000000, 0.1764146379942750642, 0.9843159429275485373 ) ) ;
#5163=CARTESIAN_POINT ( 'NONE',  ( -22.94572469358971034, -4.011883207821678177, -2.792384151940671799 ) ) ;
#5167=DIRECTION ( 'NONE',  ( -1.000000000000000000, 0.000000000000000000, 0.000000000000000000 ) ) ;
#5172=CARTESIAN_POINT ( 'NONE',  ( -22.27721038036499834, 1.315315479297517465, -3.438655654856780597 ) ) ;
#5175=ADVANCED_FACE ( 'NONE', ( #6380 ), #26649, .T. ) ;
#5178=DIRECTION ( 'NONE',  ( -1.000000000000000000, 0.000000000000000000, 0.000000000000000000 ) ) ;
#5180=DIRECTION ( 'NONE',  ( 0.000000000000000000, 0.8835120444460240474, -0.4684084406997880423 ) ) ;
#5181=CARTESIAN_POINT ( 'NONE',  ( -27.35552965826137140, -3.094132632038958608, -0.2619431035392160156 ) ) ;
#5185=CARTESIAN_POINT ( 'NONE',  ( 2.000000000000001776, 0.000000000000000000, 0.000000000000000000 ) ) ;
#5186=LINE ( 'NONE', #60370, #41581 ) ;
#5188=ORIENTED_EDGE ( 'NONE', *, *, #6526, .F. ) ;
#5195=AXIS2_PLACEMENT_3D ( 'NONE', #2075, #17382, #17711 ) ;
#5201=CIRCLE ( 'NONE', #56168, 2.899999999999996803 ) ;
#5202=DIRECTION ( 'NONE',  ( 0.000000000000000000, -0.7621620551276425681, 0.6473862847818204758 ) ) ;
#5204=CARTESIAN_POINT ( 'NONE',  ( -22.28073302975500880, -0.9769664947681180323, -3.560599703067835797 ) ) ;
#5208=FACE_OUTER_BOUND ( 'NONE', #19290, .T. ) ;
#5219=ORIENTED_EDGE ( 'NONE', *, *, #62885, .T. ) ;
#5221=ORIENTED_EDGE ( 'NONE', *, *, #20402, .F. ) ;
#5228=DIRECTION ( 'NONE',  ( -1.000000000000000000, 0.000000000000000000, 0.000000000000000000 ) ) ;
#5230=CIRCLE ( 'NONE', #41235, 2.899999999999994582 ) ;
#5231=CARTESIAN_POINT ( 'NONE',  ( -22.27706485742869091, -1.508175983031604606, 3.358064672837097753 ) ) ;
#5235=ORIENTED_EDGE ( 'NONE', *, *, #17726, .T. ) ;
#5241=CARTESIAN_POINT ( 'NONE',  ( 2.000000000000001776, -6.253963800348206092, -4.139799123621114241 ) ) ;
#5254=FACE_OUTER_BOUND ( 'NONE', #57256, .T. ) ;
#5255=DIRECTION ( 'NONE',  ( 0.000000000000000000, 0.000000000000000000, 1.000000000000000000 ) ) ;
#5260=DIRECTION ( 'NONE',  ( 0.000000000000000000, 0.6051742151937610226, 0.7960930657056468629 ) ) ;
#5261=ORIENTED_EDGE ( 'NONE', *, *, #10077, .T. ) ;
#5269=CARTESIAN_POINT ( 'NONE',  ( -22.27384469013076185, 2.625926801827887846, -2.581192766446249731 ) ) ;
#5272=CARTESIAN_POINT ( 'NONE',  ( -22.27706485742869091, 2.580541389029920030, 2.625261754997667119 ) ) ;
#5277=CIRCLE ( 'NONE', #32876, 6.936499999999990784 ) ;
#5278=CARTESIAN_POINT ( 'NONE',  ( -27.09125059358712306, -0.5611156659247565903, 2.243253600383845914 ) ) ;
#5287=ORIENTED_EDGE ( 'NONE', *, *, #31216, .T. ) ;
#5289=ORIENTED_EDGE ( 'NONE', *, *, #59908, .T. ) ;
#5292=CYLINDRICAL_SURFACE ( 'NONE', #27930, 2.899999999999994582 ) ;
#5293=CARTESIAN_POINT ( 'NONE',  ( -22.27721688985630166, -3.446999288411544349, -1.293557211780071103 ) ) ;
#5298=DIRECTION ( 'NONE',  ( 0.000000000000000000, -0.7621620551276425681, 0.6473862847818204758 ) ) ;
#5305=CARTESIAN_POINT ( 'NONE',  ( -27.08506889328327460, 1.872884652026870045, -1.324351020479947350 ) ) ;
#5306=VERTEX_POINT ( 'NONE', #43920 ) ;
#5315=CARTESIAN_POINT ( 'NONE',  ( 0.000000000000000000, 7.203928197742101247, 2.086484728383167564 ) ) ;
#5318=EDGE_LOOP ( 'NONE', ( #56575, #8824, #13539, #46280 ) ) ;
#5326=AXIS2_PLACEMENT_3D ( 'NONE', #41131, #14863, #55796 ) ;
#5327=CARTESIAN_POINT ( 'NONE',  ( -26.74023318801843274, 3.035730054944089762, -1.425982498898162643 ) ) ;
#5328=CARTESIAN_POINT ( 'NONE',  ( -22.28506771379528573, -1.636577531579579414, 3.348518833762379909 ) ) ;
#5331=VERTEX_POINT ( 'NONE', #11889 ) ;
#5337=ORIENTED_EDGE ( 'NONE', *, *, #31735, .T. ) ;
#5340=CARTESIAN_POINT ( 'NONE',  ( 0.000000000000000000, 0.000000000000000000, 0.000000000000000000 ) ) ;
#5345=AXIS2_PLACEMENT_3D ( 'NONE', #61447, #65770, #5633 ) ;
#5357=FACE_OUTER_BOUND ( 'NONE', #43136, .T. ) ;
#5384=DIRECTION ( 'NONE',  ( 0.000000000000000000, -0.7621620551276424571, 0.6473862847818206978 ) ) ;
#5385=CIRCLE ( 'NONE', #23416, 6.936499999999989896 ) ;
#5397=EDGE_CURVE ( 'NONE', #26006, #26098, #13846, .T. ) ;
#5402=CARTESIAN_POINT ( 'NONE',  ( -22.71097035706203116, 4.965150228107710006, 0.4203397252017151420 ) ) ;
#5410=FACE_OUTER_BOUND ( 'NONE', #61546, .T. ) ;
#5413=ORIENTED_EDGE ( 'NONE', *, *, #34278, .F. ) ;
#5418=EDGE_CURVE ( 'NONE', #46803, #44248, #30846, .T. ) ;
#5423=CARTESIAN_POINT ( 'NONE',  ( -22.28023996335807411, 1.558279384310090387, -3.345627887484357021 ) ) ;
#5425=CIRCLE ( 'NONE', #39375, 2.899999999999995026 ) ;
#5427=ORIENTED_EDGE ( 'NONE', *, *, #56706, .F. ) ;
#5428=CARTESIAN_POINT ( 'NONE',  ( 2.000000000000001776, -6.812627895098285258, 2.855765430652664971 ) ) ;
#5430=ORIENTED_EDGE ( 'NONE', *, *, #41512, .T. ) ;
#5437=DIRECTION ( 'NONE',  ( 0.000000000000000000, 0.000000000000000000, 1.000000000000000000 ) ) ;
#5439=VECTOR ( 'NONE', #19044, 1000.000000000000114 ) ;
#5442=AXIS2_PLACEMENT_3D ( 'NONE', #55382, #30112, #4860 ) ;
#5450=ORIENTED_EDGE ( 'NONE', *, *, #62567, .F. ) ;
#5456=CARTESIAN_POINT ( 'NONE',  ( 0.000000000000000000, 1.779948802829910193, -6.576141558201243242 ) ) ;
#5461=CARTESIAN_POINT ( 'NONE',  ( 1.000000000000000888, -7.248432822490255667, 1.926193556692974429 ) ) ;
#5462=CARTESIAN_POINT ( 'NONE',  ( -22.28415773361650309, 3.565377603762382108, -0.9981933716384956412 ) ) ;
#5466=CARTESIAN_POINT ( 'NONE',  ( 2.000000000000001776, 0.000000000000000000, 0.000000000000000000 ) ) ;
#5469=EDGE_LOOP ( 'NONE', ( #34415, #53575, #14295, #46360, #24275, #32953, #63104, #30932, #26037, #30852, #39708, #34775, #28048, #1088, #6110, #11929, #51609, #51790, #15018, #47170, #49594, #41111, #60627, #56449, #9267, #55526, #12707, #62761, #65333, #4820, #6437, #37804, #52289, #52245, #6691, #6662, #24756, #37032, #5993, #3249, #49660, #9529, #37534, #24678, #26274, #10519, #36822, #24634, #20118, #32559, #61475, #40950, #12251, #55104, #34347, #34884, #41993, #27796, #9534, #9830, #54822, #8695, #26749, #63070, #17139, #12597, #5967, #41778, #18055, #811, #46465, #17658, #15486, #22637, #38018, #32200, #59036, #38155, #6494, #58479, #52653, #53021, #51010, #41705, #48834, #21003, #9954, #21909, #23516, #4843, #64364, #56516, #39552, #32373, #64159, #25486, #43100, #24952, #4697, #18006, #43579, #20410, #37020, #59515, #53617, #25243, #36161, #24629, #34696, #22110, #55092, #25783, #59273, #35207, #54235, #13967, #21690, #52811, #11736, #52723, #59262, #63090, #36927, #65230, #45144, #17977, #26265, #58551, #46223, #40041, #10440, #33659, #65231, #36208, #2662, #54391, #62544, #63046, #42294, #45125, #63548, #34730, #24612, #15910, #17156, #31997, #56612, #17828, #43774, #53509, #13713, #22565, #10687, #38741, #42948, #15117, #28639, #20261, #53339, #14042, #43731, #30654, #862, #54916, #15644, #33082, #33896, #17668, #32059, #55663, #40045, #16410, #5580, #3455, #16172, #596, #54840, #54932, #13132, #36529, #48343, #33723, #26394, #11442, #6988, #58383, #7326, #33497, #17718, #23236, #27013, #52901, #10722, #46288, #56304, #46965, #19979, #55476, #64476, #20164, #51372, #57000, #30475, #51618, #4254, #35973, #7573, #65613, #20679, #16837, #27474, #15626, #54173, #50136, #37480, #21304, #45635, #12993, #8241, #27881, #60448, #47007, #26815, #45336, #15888, #59533, #7286, #54399, #11465, #44797, #26088, #54028, #51606, #10926, #54402, #13958, #23744 ) ) ;
#5477=CARTESIAN_POINT ( 'NONE',  ( 2.000000000000001776, 6.812627895098307462, 0.04423456934733380197 ) ) ;
#5486=DIRECTION ( 'NONE',  ( 0.000000000000000000, 0.000000000000000000, -1.000000000000000000 ) ) ;
#5494=CARTESIAN_POINT ( 'NONE',  ( 2.000000000000001776, 5.997115278587632936, 3.485633455389514523 ) ) ;
#5495=CARTESIAN_POINT ( 'NONE',  ( 2.000000000000001776, -1.956810415765137368, -6.654767106875568494 ) ) ;
#5498=ORIENTED_EDGE ( 'NONE', *, *, #59713, .T. ) ;
#5501=EDGE_LOOP ( 'NONE', ( #50690, #58761, #38136, #1680 ) ) ;
#5516=AXIS2_PLACEMENT_3D ( 'NONE', #5800, #6116, #46345 ) ;
#5520=AXIS2_PLACEMENT_3D ( 'NONE', #56752, #15810, #56391 ) ;
#5535=CIRCLE ( 'NONE', #14007, 2.899999999999995026 ) ;
#5536=CARTESIAN_POINT ( 'NONE',  ( 2.000000000000001776, 3.224464355699842688, 6.771471746881975839 ) ) ;
#5539=CARTESIAN_POINT ( 'NONE',  ( -27.15511094194037511, -2.237231637349085034, -1.124668417986079527 ) ) ;
#5540=CARTESIAN_POINT ( 'NONE',  ( 2.000000000000001776, 4.409940824963509698, -5.354199675985237050 ) ) ;
#5556=CARTESIAN_POINT ( 'NONE',  ( -27.08429572838383947, 1.338867938658203860, 1.859677275556406384 ) ) ;
#5565=EDGE_CURVE ( 'NONE', #20378, #32446, #965, .T. ) ;
#5571=ORIENTED_EDGE ( 'NONE', *, *, #51224, .T. ) ;
#5573=CYLINDRICAL_SURFACE ( 'NONE', #61342, 6.936499999999988120 ) ;
#5574=CARTESIAN_POINT ( 'NONE',  ( -22.27706485742869091, -0.9832726768967594566, 3.547445275915920071 ) ) ;
#5578=EDGE_CURVE ( 'NONE', #46169, #15877, #33500, .T. ) ;
#5580=ORIENTED_EDGE ( 'NONE', *, *, #59895, .F. ) ;
#5583=VECTOR ( 'NONE', #2194, 1000.000000000000000 ) ;
#5584=CARTESIAN_POINT ( 'NONE',  ( -27.10719052120871098, 2.355164825213508450, -0.1538293304135275597 ) ) ;
#5594=AXIS2_PLACEMENT_3D ( 'NONE', #30487, #34801, #9881 ) ;
#5601=FACE_OUTER_BOUND ( 'NONE', #23803, .T. ) ;
#5602=ADVANCED_FACE ( 'NONE', ( #10795 ), #62005, .T. ) ;
#5604=DIRECTION ( 'NONE',  ( -1.000000000000000000, 0.000000000000000000, 0.000000000000000000 ) ) ;
#5606=AXIS2_PLACEMENT_3D ( 'NONE', #61499, #41214, #56535 ) ;
#5608=CARTESIAN_POINT ( 'NONE',  ( -22.28482751661422512, -3.692400780723923415, 0.2989970708918304743 ) ) ;
#5623=CARTESIAN_POINT ( 'NONE',  ( -27.08588607604449194, -0.5840042213184938324, 2.220764381377819952 ) ) ;
#5633=DIRECTION ( 'NONE',  ( 0.000000000000000000, 0.000000000000000000, 1.000000000000000000 ) ) ;
#5634=VERTEX_POINT ( 'NONE', #11138 ) ;
#5637=DIRECTION ( 'NONE',  ( 0.000000000000000000, -0.9985334138511243740, 0.05413890858540761075 ) ) ;
#5638=CARTESIAN_POINT ( 'NONE',  ( -22.27720387087364884, -3.430312021254878552, -1.337073746937890828 ) ) ;
#5646=ORIENTED_EDGE ( 'NONE', *, *, #62566, .F. ) ;
#5647=CARTESIAN_POINT ( 'NONE',  ( -22.27719443589224113, 2.462030382548443974, 2.737335337013082182 ) ) ;
#5650=EDGE_CURVE ( 'NONE', #63127, #43263, #47047, .T. ) ;
#5654=LINE ( 'NONE', #40885, #19494 ) ;
#5659=ORIENTED_EDGE ( 'NONE', *, *, #65673, .T. ) ;
#5668=ORIENTED_EDGE ( 'NONE', *, *, #35610, .F. ) ;
#5681=DIRECTION ( 'NONE',  ( 0.000000000000000000, 0.000000000000000000, 1.000000000000000000 ) ) ;
#5700=FACE_BOUND ( 'NONE', #30657, .T. ) ;
#5709=CIRCLE ( 'NONE', #21649, 6.936499999999990784 ) ;
#5711=ORIENTED_EDGE ( 'NONE', *, *, #5734, .T. ) ;
#5713=ORIENTED_EDGE ( 'NONE', *, *, #49684, .F. ) ;
#5723=ORIENTED_EDGE ( 'NONE', *, *, #35881, .F. ) ;
#5728=VERTEX_POINT ( 'NONE', #825 ) ;
#5730=CARTESIAN_POINT ( 'NONE',  ( 2.000000000000001776, -0.4129979343797593461, 6.800241778083677247 ) ) ;
#5732=AXIS2_PLACEMENT_3D ( 'NONE', #34325, #49633, #29646 ) ;
#5734=EDGE_CURVE ( 'NONE', #56025, #64706, #61332, .T. ) ;
#5737=ORIENTED_EDGE ( 'NONE', *, *, #7429, .T. ) ;
#5750=CARTESIAN_POINT ( 'NONE',  ( -27.08429572838383947, 2.279961732801592422, -0.2296550094122856711 ) ) ;
#5751=LINE ( 'NONE', #26656, #64956 ) ;
#5755=DIRECTION ( 'NONE',  ( 0.000000000000000000, 0.000000000000000000, 1.000000000000000000 ) ) ;
#5756=ORIENTED_EDGE ( 'NONE', *, *, #3921, .T. ) ;
#5757=DIRECTION ( 'NONE',  ( 0.000000000000000000, 0.000000000000000000, 1.000000000000000000 ) ) ;
#5765=CARTESIAN_POINT ( 'NONE',  ( 2.000000000000001776, 2.469490258309423591, 6.482025155313315246 ) ) ;
#5774=CARTESIAN_POINT ( 'NONE',  ( 1.000000000000000888, 1.530946385938475762, -7.342084388195351252 ) ) ;
#5777=CARTESIAN_POINT ( 'NONE',  ( -27.10719052120871098, -1.044362304621479165, 2.116547233941197703 ) ) ;
#5779=CARTESIAN_POINT ( 'NONE',  ( -22.70624764888619751, -4.891815784104535325, 1.907540768355092231 ) ) ;
#5782=DIRECTION ( 'NONE',  ( -1.000000000000000000, 0.000000000000000000, 0.000000000000000000 ) ) ;
#5785=DIRECTION ( 'NONE',  ( -1.000000000000000000, 0.000000000000000000, 0.000000000000000000 ) ) ;
#5786=DIRECTION ( 'NONE',  ( 0.000000000000000000, -6.883382752675980017E-15, 1.000000000000000000 ) ) ;
#5791=DIRECTION ( 'NONE',  ( -1.000000000000000000, 0.000000000000000000, 0.000000000000000000 ) ) ;
#5796=CARTESIAN_POINT ( 'NONE',  ( -22.27722019094931483, 3.463038365117174333, 1.249795790945178897 ) ) ;
#5798=VERTEX_POINT ( 'NONE', #58328 ) ;
#5800=CARTESIAN_POINT ( 'NONE',  ( 2.000000000000001776, 1.779948802829910193, -6.576141558201243242 ) ) ;
#5812=CYLINDRICAL_SURFACE ( 'NONE', #16617, 6.936499999999988120 ) ;
#5816=AXIS2_PLACEMENT_3D ( 'NONE', #58769, #3569, #64048 ) ;
#5829=EDGE_CURVE ( 'NONE', #64384, #57499, #24917, .T. ) ;
#5838=EDGE_LOOP ( 'NONE', ( #24220, #27829, #21430, #12977 ) ) ;
#5842=EDGE_CURVE ( 'NONE', #5634, #63998, #39987, .T. ) ;
#5846=DIRECTION ( 'NONE',  ( 1.000000000000000000, -0.000000000000000000, -0.000000000000000000 ) ) ;
#5851=CARTESIAN_POINT ( 'NONE',  ( -22.27719443589224113, -0.7635131876694993824, -3.601617131804410565 ) ) ;
#5861=CARTESIAN_POINT ( 'NONE',  ( -22.46225619532222950, 2.255146441673809843, 3.586917175123511381 ) ) ;
#5871=DIRECTION ( 'NONE',  ( -1.000000000000000000, 0.000000000000000000, 0.000000000000000000 ) ) ;
#5875=EDGE_LOOP ( 'NONE', ( #52296, #29112, #39950, #36395 ) ) ;
#5883=EDGE_CURVE ( 'NONE', #45297, #20405, #61290, .T. ) ;
#5886=CARTESIAN_POINT ( 'NONE',  ( -27.10719052120871098, 2.295785794152562787, 0.5475695427849293084 ) ) ;
#5908=FACE_OUTER_BOUND ( 'NONE', #22678, .T. ) ;
#5911=AXIS2_PLACEMENT_3D ( 'NONE', #53543, #28251, #48546 ) ;
#5913=CARTESIAN_POINT ( 'NONE',  ( -22.27721701579900682, -1.205877546543695278, 3.478642907697079956 ) ) ;
#5920=CARTESIAN_POINT ( 'NONE',  ( -27.09229696323320979, 0.5586335684093801657, -2.247106967994374482 ) ) ;
#5923=CARTESIAN_POINT ( 'NONE',  ( -27.09364415740165910, 1.009938549038103206, -2.088137158971423268 ) ) ;
#5925=DIRECTION ( 'NONE',  ( 0.000000000000000000, 0.000000000000000000, 1.000000000000000000 ) ) ;
#5936=VERTEX_POINT ( 'NONE', #44636 ) ;
#5943=CARTESIAN_POINT ( 'NONE',  ( -22.31328051695926007, -3.781397440874596061, 0.2528478350593901802 ) ) ;
#5947=VERTEX_POINT ( 'NONE', #54962 ) ;
#5967=ORIENTED_EDGE ( 'NONE', *, *, #36957, .F. ) ;
#5974=CARTESIAN_POINT ( 'NONE',  ( 0.000000000000000000, 6.441884263200815752, 2.217201541069855786 ) ) ;
#5983=CARTESIAN_POINT ( 'NONE',  ( -27.08430418657510685, 1.863523114788013801, -1.333569526609269085 ) ) ;
#5984=ORIENTED_EDGE ( 'NONE', *, *, #3722, .T. ) ;
#5986=CARTESIAN_POINT ( 'NONE',  ( -27.09229696323388836, 1.666734935102336612, 1.607344345646377404 ) ) ;
#5987=CARTESIAN_POINT ( 'NONE',  ( -22.27709082389155171, 3.569727173833830758, -0.8996430462092170899 ) ) ;
#5993=ORIENTED_EDGE ( 'NONE', *, *, #8939, .F. ) ;
#5999=EDGE_LOOP ( 'NONE', ( #14846, #57002, #40623, #39808 ) ) ;
#6001=CARTESIAN_POINT ( 'NONE',  ( 2.000000000000001776, 6.796153407501467569, -1.388283512725773772 ) ) ;
#6008=LINE ( 'NONE', #57186, #36470 ) ;
#6011=CARTESIAN_POINT ( 'NONE',  ( 0.000000000000000000, 0.000000000000000000, 0.000000000000000000 ) ) ;
#6013=CARTESIAN_POINT ( 'NONE',  ( -27.08935880048752409, 0.6272370006475171955, 2.219773948423720444 ) ) ;
#6026=CARTESIAN_POINT ( 'NONE',  ( 0.000000000000000000, 0.000000000000000000, 0.000000000000000000 ) ) ;
#6043=CARTESIAN_POINT ( 'NONE',  ( 2.000000000000001776, 0.000000000000000000, 0.000000000000000000 ) ) ;
#6053=VERTEX_POINT ( 'NONE', #41293 ) ;
#6060=VERTEX_POINT ( 'NONE', #51637 ) ;
#6062=VERTEX_POINT ( 'NONE', #61918 ) ;
#6067=DIRECTION ( 'NONE',  ( 0.000000000000000000, 0.4198891015602592147, 0.9075754196709596711 ) ) ;
#6069=CARTESIAN_POINT ( 'NONE',  ( -24.98829009532795808, 4.047772734466310141, 0.3426763744735841777 ) ) ;
#6077=ORIENTED_EDGE ( 'NONE', *, *, #28984, .F. ) ;
#6088=VECTOR ( 'NONE', #11025, 1000.000000000000000 ) ;
#6093=DIRECTION ( 'NONE',  ( -1.000000000000000000, 0.000000000000000000, 0.000000000000000000 ) ) ;
#6097=DIRECTION ( 'NONE',  ( -1.000000000000000000, 0.000000000000000000, 0.000000000000000000 ) ) ;
#6110=ORIENTED_EDGE ( 'NONE', *, *, #64067, .F. ) ;
#6116=DIRECTION ( 'NONE',  ( -1.000000000000000000, 0.000000000000000000, 0.000000000000000000 ) ) ;
#6122=CIRCLE ( 'NONE', #15638, 2.899999999999995914 ) ;
#6123=VERTEX_POINT ( 'NONE', #57934 ) ;
#6125=CARTESIAN_POINT ( 'NONE',  ( -22.28415773361650309, -3.565377603762382108, 0.9981933716384869815 ) ) ;
#6128=VERTEX_POINT ( 'NONE', #17692 ) ;
#6129=CARTESIAN_POINT ( 'NONE',  ( 0.000000000000000000, 0.000000000000000000, 0.000000000000000000 ) ) ;
#6140=CARTESIAN_POINT ( 'NONE',  ( 18.00005080000000035, 1.836970198721027222E-16, -1.499999999999997780 ) ) ;
#6142=ADVANCED_FACE ( 'NONE', ( #48299 ), #12023, .T. ) ;
#6158=DIRECTION ( 'NONE',  ( 0.000000000000000000, 0.000000000000000000, 1.000000000000000000 ) ) ;
#6165=CARTESIAN_POINT ( 'NONE',  ( -22.28629837673887693, -3.055064048018810929, 2.102970853432575282 ) ) ;
#6168=CARTESIAN_POINT ( 'NONE',  ( 2.000000000000001776, 0.000000000000000000, 0.000000000000000000 ) ) ;
#6178=CARTESIAN_POINT ( 'NONE',  ( 2.000000000000001776, -6.750946897830688798, -1.593658756657146292 ) ) ;
#6182=LINE ( 'NONE', #61685, #53265 ) ;
#6184=ORIENTED_EDGE ( 'NONE', *, *, #25800, .T. ) ;
#6187=CARTESIAN_POINT ( 'NONE',  ( -22.66110217412718342, -0.6585288088159785280, 4.900671186447912220 ) ) ;
#6189=ORIENTED_EDGE ( 'NONE', *, *, #64778, .T. ) ;
#6195=CARTESIAN_POINT ( 'NONE',  ( -27.08776759928964850, 2.229418711698783806, 0.5731512436791836862 ) ) ;
#6198=CARTESIAN_POINT ( 'NONE',  ( -22.66110217412718697, 4.366928509133841452, -2.319520136975649294 ) ) ;
#6204=CARTESIAN_POINT ( 'NONE',  ( 2.000000000000001776, -2.473437528934089524, -7.080403010455012414 ) ) ;
#6216=CARTESIAN_POINT ( 'NONE',  ( 0.000000000000000000, 0.000000000000000000, 0.000000000000000000 ) ) ;
#6220=ORIENTED_EDGE ( 'NONE', *, *, #181, .T. ) ;
#6231=ADVANCED_FACE ( 'NONE', ( #39258 ), #18992, .T. ) ;
#6239=DIRECTION ( 'NONE',  ( -1.000000000000000000, 0.000000000000000000, 0.000000000000000000 ) ) ;
#6244=ORIENTED_EDGE ( 'NONE', *, *, #25082, .T. ) ;
#6245=CARTESIAN_POINT ( 'NONE',  ( 2.000000000000001776, 0.000000000000000000, 0.000000000000000000 ) ) ;
#6247=AXIS2_PLACEMENT_3D ( 'NONE', #50702, #25755, #56326 ) ;
#6248=ORIENTED_EDGE ( 'NONE', *, *, #52920, .T. ) ;
#6249=CARTESIAN_POINT ( 'NONE',  ( -22.30078715814471835, -3.743307663037635180, 0.2606204736986815207 ) ) ;
#6262=EDGE_CURVE ( 'NONE', #20337, #25571, #47734, .T. ) ;
#6265=DIRECTION ( 'NONE',  ( 0.000000000000000000, 0.000000000000000000, 1.000000000000000000 ) ) ;
#6281=CARTESIAN_POINT ( 'NONE',  ( -27.08416781016246588, -2.253489850813972240, 0.4141677382007513675 ) ) ;
#6283=CARTESIAN_POINT ( 'NONE',  ( 1.000000000000000888, -1.693411908627245221, 7.306323022404576761 ) ) ;
#6298=CARTESIAN_POINT ( 'NONE',  ( 2.000000000000001776, -0.3246585432986597852, 6.805031400696099020 ) ) ;
#6302=ORIENTED_EDGE ( 'NONE', *, *, #8939, .T. ) ;
#6307=EDGE_CURVE ( 'NONE', #28230, #52982, #40912, .T. ) ;
#6314=CARTESIAN_POINT ( 'NONE',  ( 0.000000000000000000, -6.883677378339468689, 0.8544109087185604023 ) ) ;
#6320=CARTESIAN_POINT ( 'NONE',  ( -22.27709082389155171, 2.641652894015124708, -2.563977319272113586 ) ) ;
#6334=CYLINDRICAL_SURFACE ( 'NONE', #47913, 2.899999999999994582 ) ;
#6336=VERTEX_POINT ( 'NONE', #41546 ) ;
#6347=EDGE_CURVE ( 'NONE', #58400, #9014, #27909, .T. ) ;
#6349=CARTESIAN_POINT ( 'NONE',  ( -27.08429572838383947, 1.632445743623435197, -1.608131779585709076 ) ) ;
#6365=VECTOR ( 'NONE', #45157, 1000.000000000000000 ) ;
#6366=EDGE_LOOP ( 'NONE', ( #54406, #33944, #1785, #34109 ) ) ;
#6368=CYLINDRICAL_SURFACE ( 'NONE', #41684, 2.899999999999994582 ) ;
#6372=CIRCLE ( 'NONE', #42406, 6.936499999999987232 ) ;
#6380=FACE_OUTER_BOUND ( 'NONE', #38848, .T. ) ;
#6386=CARTESIAN_POINT ( 'NONE',  ( 0.000000000000000000, 5.585096664091945939, 4.113602740025928739 ) ) ;
#6388=CARTESIAN_POINT ( 'NONE',  ( -22.70624764888619751, -4.097886656202274658, -3.282666355490689192 ) ) ;
#6393=ADVANCED_FACE ( 'NONE', ( #37210 ), #7969, .T. ) ;
#6398=CARTESIAN_POINT ( 'NONE',  ( -27.10512513516275845, -2.256292013315179812, 0.6711200423626850764 ) ) ;
#6399=CARTESIAN_POINT ( 'NONE',  ( -22.27384469013076185, -3.548341908721032389, -0.9835229356382479970 ) ) ;
#6402=ORIENTED_EDGE ( 'NONE', *, *, #46576, .T. ) ;
#6409=CARTESIAN_POINT ( 'NONE',  ( -27.09729107899804390, -1.021938248125916271, 2.094470452260984494 ) ) ;
#6414=AXIS2_PLACEMENT_3D ( 'NONE', #58363, #7827, #63647 ) ;
#6415=DIRECTION ( 'NONE',  ( 0.000000000000000000, 0.000000000000000000, 1.000000000000000000 ) ) ;
#6422=DIRECTION ( 'NONE',  ( 0.000000000000000000, -0.7621620551276288014, -0.6473862847818365740 ) ) ;
#6428=EDGE_LOOP ( 'NONE', ( #29084, #32774, #65446, #4452 ) ) ;
#6432=CARTESIAN_POINT ( 'NONE',  ( -35.04709527796842394, -0.005292201869334239861, -0.01117341439756461274 ) ) ;
#6437=ORIENTED_EDGE ( 'NONE', *, *, #38872, .F. ) ;
#6449=DIRECTION ( 'NONE',  ( 0.000000000000000000, 0.3193015301359743985, 0.9476531711828043436 ) ) ;
#6475=DIRECTION ( 'NONE',  ( 0.000000000000000000, 0.000000000000000000, 1.000000000000000000 ) ) ;
#6479=DIRECTION ( 'NONE',  ( -1.000000000000000000, 0.000000000000000000, 0.000000000000000000 ) ) ;
#6484=CARTESIAN_POINT ( 'NONE',  ( -22.27945548916780183, -3.016427163003897238, 2.122548946923907387 ) ) ;
#6490=AXIS2_PLACEMENT_3D ( 'NONE', #420, #26011, #50632 ) ;
#6494=ORIENTED_EDGE ( 'NONE', *, *, #20060, .F. ) ;
#6500=EDGE_CURVE ( 'NONE', #2095, #52731, #42513, .T. ) ;
#6503=DIRECTION ( 'NONE',  ( -1.000000000000000000, 0.000000000000000000, 0.000000000000000000 ) ) ;
#6508=CARTESIAN_POINT ( 'NONE',  ( -35.04643116707788408, -0.009511118309140503824, 0.007621814750495559121 ) ) ;
#6526=EDGE_CURVE ( 'NONE', #7525, #65358, #49822, .T. ) ;
#6531=EDGE_CURVE ( 'NONE', #52659, #48378, #31960, .T. ) ;
#6538=EDGE_CURVE ( 'NONE', #47492, #49777, #16141, .T. ) ;
#6541=ORIENTED_EDGE ( 'NONE', *, *, #51723, .T. ) ;
#6548=ORIENTED_EDGE ( 'NONE', *, *, #64067, .T. ) ;
#6562=AXIS2_PLACEMENT_3D ( 'NONE', #63639, #33065, #3504 ) ;
#6578=CARTESIAN_POINT ( 'NONE',  ( 2.000000000000001776, -3.859771122243078167, 5.613913289150019637 ) ) ;
#6580=VERTEX_POINT ( 'NONE', #20204 ) ;
#6604=AXIS2_PLACEMENT_3D ( 'NONE', #17140, #63015, #37082 ) ;
#6607=EDGE_CURVE ( 'NONE', #11283, #22582, #28658, .T. ) ;
#6614=LINE ( 'NONE', #6283, #53257 ) ;
#6622=CARTESIAN_POINT ( 'NONE',  ( -27.28573687977897677, 1.043905432732902927, 2.702109387930228479 ) ) ;
#6625=AXIS2_PLACEMENT_3D ( 'NONE', #50320, #25036, #49352 ) ;
#6634=ORIENTED_EDGE ( 'NONE', *, *, #40017, .T. ) ;
#6650=CARTESIAN_POINT ( 'NONE',  ( 2.000000000000001776, -6.441884263200823746, -2.217201541069834914 ) ) ;
#6661=VECTOR ( 'NONE', #65739, 1000.000000000000114 ) ;
#6662=ORIENTED_EDGE ( 'NONE', *, *, #19181, .F. ) ;
#6663=CARTESIAN_POINT ( 'NONE',  ( 0.000000000000000000, -1.058508696394911963, -6.730038252034928448 ) ) ;
#6682=CARTESIAN_POINT ( 'NONE',  ( 0.000000000000000000, 0.000000000000000000, 0.000000000000000000 ) ) ;
#6691=ORIENTED_EDGE ( 'NONE', *, *, #39924, .F. ) ;
#6700=ORIENTED_EDGE ( 'NONE', *, *, #11894, .T. ) ;
#6707=ORIENTED_EDGE ( 'NONE', *, *, #11273, .T. ) ;
#6708=AXIS2_PLACEMENT_3D ( 'NONE', #40916, #1347, #11625 ) ;
#6725=DIRECTION ( 'NONE',  ( -1.000000000000000000, 0.000000000000000000, 0.000000000000000000 ) ) ;
#6743=AXIS2_PLACEMENT_3D ( 'NONE', #42687, #43032, #38713 ) ;
#6769=EDGE_CURVE ( 'NONE', #53550, #47123, #38196, .T. ) ;
#6770=CARTESIAN_POINT ( 'NONE',  ( 0.000000000000000000, 6.812627895098307462, 0.04423456934733380197 ) ) ;
#6789=VECTOR ( 'NONE', #16501, 1000.000000000000000 ) ;
#6795=CIRCLE ( 'NONE', #60950, 2.899999999999994582 ) ;
#6802=EDGE_CURVE ( 'NONE', #12068, #28265, #33967, .T. ) ;
#6811=DIRECTION ( 'NONE',  ( -1.000000000000000000, 0.000000000000000000, 0.000000000000000000 ) ) ;
#6815=DIRECTION ( 'NONE',  ( -1.000000000000000000, 0.000000000000000000, 0.000000000000000000 ) ) ;
#6817=DIRECTION ( 'NONE',  ( 0.000000000000000000, 0.9985334138511237079, 0.05413890858542116241 ) ) ;
#6823=CARTESIAN_POINT ( 'NONE',  ( -22.30078715814471479, -3.111489293522209820, 2.097357782488221023 ) ) ;
#6833=CIRCLE ( 'NONE', #34441, 6.936499999999990784 ) ;
#6836=VECTOR ( 'NONE', #42805, 1000.000000000000000 ) ;
#6838=EDGE_CURVE ( 'NONE', #648, #23034, #63702, .T. ) ;
#6846=CARTESIAN_POINT ( 'NONE',  ( -10.00000000000000178, 0.000000000000000000, 7.499999999999988454 ) ) ;
#6849=AXIS2_PLACEMENT_3D ( 'NONE', #7440, #22412, #48031 ) ;
#6860=DIRECTION ( 'NONE',  ( 0.000000000000000000, 0.000000000000000000, 1.000000000000000000 ) ) ;
#6866=EDGE_LOOP ( 'NONE', ( #62178, #13749, #23359, #1119 ) ) ;
#6868=VERTEX_POINT ( 'NONE', #3881 ) ;
#6869=CYLINDRICAL_SURFACE ( 'NONE', #65517, 7.499999999999988454 ) ;
#6887=DIRECTION ( 'NONE',  ( 1.000000000000000000, -0.000000000000000000, -0.000000000000000000 ) ) ;
#6888=DIRECTION ( 'NONE',  ( -1.000000000000000000, 0.000000000000000000, 0.000000000000000000 ) ) ;
#6897=CARTESIAN_POINT ( 'NONE',  ( 0.000000000000000000, -0.4129979343796691404, -6.800241778083718991 ) ) ;
#6899=VECTOR ( 'NONE', #37014, 1000.000000000000000 ) ;
#6901=VERTEX_POINT ( 'NONE', #64366 ) ;
#6902=CARTESIAN_POINT ( 'NONE',  ( -27.08704841010922593, 0.1930432016059930034, 2.291653842312383116 ) ) ;
#6905=CARTESIAN_POINT ( 'NONE',  ( -16.00005080000000035, 0.000000000000000000, 0.000000000000000000 ) ) ;
#6907=DIRECTION ( 'NONE',  ( -1.000000000000000000, 0.000000000000000000, 0.000000000000000000 ) ) ;
#6909=ORIENTED_EDGE ( 'NONE', *, *, #10450, .F. ) ;
#6916=EDGE_CURVE ( 'NONE', #46888, #47458, #28466, .T. ) ;
#6929=ORIENTED_EDGE ( 'NONE', *, *, #8809, .F. ) ;
#6933=CARTESIAN_POINT ( 'NONE',  ( -27.08419642509982950, -2.239682169453945715, 0.4837273216074967075 ) ) ;
#6941=VERTEX_POINT ( 'NONE', #39759 ) ;
#6945=MANIFOLD_SOLID_BREP ( 'Join1', #59965 ) ;
#6948=DIRECTION ( 'NONE',  ( 0.000000000000000000, -0.9985334138511243740, 0.05413890858540768708 ) ) ;
#6956=ORIENTED_EDGE ( 'NONE', *, *, #38287, .F. ) ;
#6963=AXIS2_PLACEMENT_3D ( 'NONE', #12600, #43863, #57868 ) ;
#6973=DIRECTION ( 'NONE',  ( -1.000000000000000000, 0.000000000000000000, 0.000000000000000000 ) ) ;
#6982=DIRECTION ( 'NONE',  ( -1.000000000000000000, 0.000000000000000000, 0.000000000000000000 ) ) ;
#6988=ORIENTED_EDGE ( 'NONE', *, *, #2965, .F. ) ;
#6995=DIRECTION ( 'NONE',  ( 0.000000000000000000, 0.000000000000000000, 1.000000000000000000 ) ) ;
#7004=DIRECTION ( 'NONE',  ( -1.000000000000000000, 0.000000000000000000, 0.000000000000000000 ) ) ;
#7005=CARTESIAN_POINT ( 'NONE',  ( -27.08588607604433918, -1.631236259432285784, -1.616144682268734423 ) ) ;
#7015=CIRCLE ( 'NONE', #37815, 2.899999999999994582 ) ;
#7017=LINE ( 'NONE', #11994, #26832 ) ;
#7020=CARTESIAN_POINT ( 'NONE',  ( -27.08418322526031119, -0.3452258100746897207, -2.265123059255418347 ) ) ;
#7041=EDGE_CURVE ( 'NONE', #20378, #22014, #26576, .T. ) ;
#7050=EDGE_LOOP ( 'NONE', ( #48091, #28303, #64506, #65702, #6700, #24057, #47370, #28776, #13834, #53088, #46274, #4688, #27306, #41436, #45053, #8465, #39325, #23622, #35158, #42018, #21127, #51776, #59081, #50513, #15980, #45943, #52284, #7865, #961, #4341, #64179, #28023, #36455, #26891 ) ) ;
#7052=CARTESIAN_POINT ( 'NONE',  ( -27.08426571771018487, 2.098821047392067207, 0.9198084705429259156 ) ) ;
#7053=CARTESIAN_POINT ( 'NONE',  ( -35.04643116707788408, -0.01204777744936991191, 0.001845126042312322800 ) ) ;
#7067=CARTESIAN_POINT ( 'NONE',  ( -22.28546858134833286, -2.654201075783114927, -2.587024666338680667 ) ) ;
#7069=ORIENTED_EDGE ( 'NONE', *, *, #49496, .T. ) ;
#7070=ADVANCED_FACE ( 'NONE', ( #43946 ), #18018, .T. ) ;
#7072=CARTESIAN_POINT ( 'NONE',  ( 1.000000000000000888, -7.387287142779332960, -1.295372019972250710 ) ) ;
#7074=CARTESIAN_POINT ( 'NONE',  ( -22.27718150314433387, -3.596602356343906681, 0.7862703917636705286 ) ) ;
#7085=DIRECTION ( 'NONE',  ( -1.000000000000000000, 0.000000000000000000, 0.000000000000000000 ) ) ;
#7089=DIRECTION ( 'NONE',  ( 1.000000000000000000, -0.000000000000000000, -0.000000000000000000 ) ) ;
#7113=ORIENTED_EDGE ( 'NONE', *, *, #29459, .T. ) ;
#7114=ORIENTED_EDGE ( 'NONE', *, *, #24960, .T. ) ;
#7116=DIRECTION ( 'NONE',  ( -1.000000000000000000, 0.000000000000000000, 0.000000000000000000 ) ) ;
#7119=CARTESIAN_POINT ( 'NONE',  ( -22.30398854582848145, 1.062335901716063624, 3.608860109585115605 ) ) ;
#7125=CARTESIAN_POINT ( 'NONE',  ( -22.31213670151049300, -3.145266995071682725, 2.108126385153798132 ) ) ;
#7138=B_SPLINE_CURVE_WITH_KNOTS ( 'NONE', 3,
 ( #33118, #38778, #22837, #18170, #59075, #23480, #44088, #39085, #59379, #53429, #43092, #43757, #54735, #64038, #18522, #33766, #8502, #54411, #27810, #63368, #23827, #8843 ),
 .UNSPECIFIED., .F., .F.,
 ( 4, 3, 3, 3, 3, 3, 3, 4 ),
 ( 9.813077866771631884E-18, 4.447697177976269703E-05, 6.624143997791186948E-05, 8.800576886944293459E-05, 0.0001097699864780885595, 0.0001315341395364375715, 0.0001760120188223282935, 0.0001867971373174741171 ),
 .UNSPECIFIED. ) ;
#7145=ORIENTED_EDGE ( 'NONE', *, *, #39752, .T. ) ;
#7148=FACE_OUTER_BOUND ( 'NONE', #19959, .T. ) ;
#7149=FACE_OUTER_BOUND ( 'NONE', #8938, .T. ) ;
#7150=VERTEX_POINT ( 'NONE', #24305 ) ;
#7156=CARTESIAN_POINT ( 'NONE',  ( 2.000000000000001776, -5.997115278587605403, -3.485633455389573587 ) ) ;
#7161=DIRECTION ( 'NONE',  ( -1.000000000000000000, 0.000000000000000000, 0.000000000000000000 ) ) ;
#7166=FACE_OUTER_BOUND ( 'NONE', #42777, .T. ) ;
#7169=VERTEX_POINT ( 'NONE', #44570 ) ;
#7170=FACE_OUTER_BOUND ( 'NONE', #23356, .T. ) ;
#7176=ORIENTED_EDGE ( 'NONE', *, *, #13778, .T. ) ;
#7184=DIRECTION ( 'NONE',  ( -1.000000000000000000, 0.000000000000000000, 0.000000000000000000 ) ) ;
#7197=EDGE_CURVE ( 'NONE', #27863, #14116, #13997, .T. ) ;
#7198=FACE_OUTER_BOUND ( 'NONE', #38929, .T. ) ;
#7203=ORIENTED_EDGE ( 'NONE', *, *, #12685, .F. ) ;
#7213=CARTESIAN_POINT ( 'NONE',  ( -27.35552965826137140, 0.2619431035392177365, -3.094132632038957276 ) ) ;
#7214=CARTESIAN_POINT ( 'NONE',  ( -22.23402523511428086, 1.734723475976807094E-15, -8.673617379884035472E-15 ) ) ;
#7219=AXIS2_PLACEMENT_3D ( 'NONE', #53087, #33127, #17186 ) ;
#7222=ORIENTED_EDGE ( 'NONE', *, *, #41135, .T. ) ;
#7223=AXIS2_PLACEMENT_3D ( 'NONE', #34011, #44317, #58668 ) ;
#7227=AXIS2_PLACEMENT_3D ( 'NONE', #32054, #6815, #27084 ) ;
#7233=CYLINDRICAL_SURFACE ( 'NONE', #35009, 6.936499999999988120 ) ;
#7248=DIRECTION ( 'NONE',  ( -1.000000000000000000, 0.000000000000000000, 0.000000000000000000 ) ) ;
#7250=CARTESIAN_POINT ( 'NONE',  ( 1.000000000000000888, -5.097042323172408906, -5.501832381651512449 ) ) ;
#7251=ORIENTED_EDGE ( 'NONE', *, *, #5418, .T. ) ;
#7253=EDGE_CURVE ( 'NONE', #18329, #12876, #3292, .T. ) ;
#7255=CIRCLE ( 'NONE', #47617, 2.899999999999995026 ) ;
#7256=CARTESIAN_POINT ( 'NONE',  ( -22.27218376572352554, -3.670373711461420108, 0.3046453028544536812 ) ) ;
#7258=ORIENTED_EDGE ( 'NONE', *, *, #44253, .T. ) ;
#7262=ORIENTED_EDGE ( 'NONE', *, *, #5829, .T. ) ;
#7264=ORIENTED_EDGE ( 'NONE', *, *, #31188, .F. ) ;
#7265=EDGE_LOOP ( 'NONE', ( #1805, #60073, #40210, #40713 ) ) ;
#7267=CARTESIAN_POINT ( 'NONE',  ( 0.000000000000000000, 4.472310526050767621, 6.020667617347370104 ) ) ;
#7278=CARTESIAN_POINT ( 'NONE',  ( -22.27715239060371744, 2.689999469426704426, -2.513478159995845562 ) ) ;
#7283=DIRECTION ( 'NONE',  ( -1.000000000000000000, 0.000000000000000000, 0.000000000000000000 ) ) ;
#7286=ORIENTED_EDGE ( 'NONE', *, *, #7526, .F. ) ;
#7293=DIRECTION ( 'NONE',  ( -1.000000000000000000, 0.000000000000000000, 0.000000000000000000 ) ) ;
#7303=DIRECTION ( 'NONE',  ( -1.000000000000000000, 0.000000000000000000, 0.000000000000000000 ) ) ;
#7306=AXIS2_PLACEMENT_3D ( 'NONE', #3990, #48332, #24254 ) ;
#7312=CARTESIAN_POINT ( 'NONE',  ( -27.10719052120871098, -1.714424047991075506, -1.622102031466694072 ) ) ;
#7315=CARTESIAN_POINT ( 'NONE',  ( -22.29290468048228036, -2.097193667172395859, -3.083035815361915510 ) ) ;
#7322=EDGE_CURVE ( 'NONE', #21537, #27004, #23592, .T. ) ;
#7324=DIRECTION ( 'NONE',  ( -1.000000000000000000, 0.000000000000000000, 0.000000000000000000 ) ) ;
#7326=ORIENTED_EDGE ( 'NONE', *, *, #17485, .F. ) ;
#7327=CARTESIAN_POINT ( 'NONE',  ( 2.000000000000001776, -7.484036900328561615, -0.4890722589970097345 ) ) ;
#7342=VECTOR ( 'NONE', #61202, 1000.000000000000000 ) ;
#7344=DIRECTION ( 'NONE',  ( -1.000000000000000000, 0.000000000000000000, 0.000000000000000000 ) ) ;
#7357=CARTESIAN_POINT ( 'NONE',  ( 2.000000000000001776, -6.796153407501448029, 1.388283512725787761 ) ) ;
#7359=VERTEX_POINT ( 'NONE', #19582 ) ;
#7360=ORIENTED_EDGE ( 'NONE', *, *, #1058, .T. ) ;
#7373=LINE ( 'NONE', #38637, #54163 ) ;
#7380=B_SPLINE_CURVE_WITH_KNOTS ( 'NONE', 3,
 ( #32759, #60264, #58071, #58745, #53067, #48431, #17506, #25031, #37777, #43082, #63358, #13167, #28137 ),
 .UNSPECIFIED., .F., .F.,
 ( 4, 3, 3, 3, 4 ),
 ( 0.0002792983885906313336, 0.0002796382307041357217, 0.0003495477861619808576, 0.0004194573423310284663, 0.0005586102576333146046 ),
 .UNSPECIFIED. ) ;
#7386=VERTEX_POINT ( 'NONE', #24891 ) ;
#7394=VERTEX_POINT ( 'NONE', #34198 ) ;
#7399=FACE_OUTER_BOUND ( 'NONE', #20885, .T. ) ;
#7402=CARTESIAN_POINT ( 'NONE',  ( 0.000000000000000000, 7.387287142779349836, 1.295372019972174549 ) ) ;
#7409=CARTESIAN_POINT ( 'NONE',  ( -22.31328051695926007, -3.685074213229319717, -0.8849444482788241251 ) ) ;
#7412=CARTESIAN_POINT ( 'NONE',  ( -10.00000000000000178, 0.000000000000000000, 0.000000000000000000 ) ) ;
#7418=CARTESIAN_POINT ( 'NONE',  ( 0.000000000000000000, -4.472310526050724100, -6.020667617347421618 ) ) ;
#7419=CARTESIAN_POINT ( 'NONE',  ( 2.000000000000001776, 0.000000000000000000, 0.000000000000000000 ) ) ;
#7426=DIRECTION ( 'NONE',  ( 0.000000000000000000, -0.7621620551276423461, 0.6473862847818205868 ) ) ;
#7429=EDGE_CURVE ( 'NONE', #56470, #53254, #17081, .T. ) ;
#7440=CARTESIAN_POINT ( 'NONE',  ( -10.00000000000000178, 0.000000000000000000, 0.000000000000000000 ) ) ;
#7441=EDGE_CURVE ( 'NONE', #22102, #49356, #43819, .T. ) ;
#7443=EDGE_CURVE ( 'NONE', #39229, #52589, #56454, .T. ) ;
#7449=B_SPLINE_CURVE_WITH_KNOTS ( 'NONE', 3,
 ( #28569, #13594, #33882, #48871, #43871, #18630, #64155, #38889, #59179, #28905, #23933, #18932, #59489, #13915, #10909, #50178, #55481, #61770, #35819, #56818, #9926, #5272 ),
 .UNSPECIFIED., .F., .F.,
 ( 4, 3, 3, 3, 3, 3, 3, 4 ),
 ( 0.000000000000000000, 4.455945684386631000E-05, 6.636307477203665399E-05, 8.816671873158535159E-05, 0.0001099660380492586736, 0.0001317545563165287723, 0.0001762613022895051528, 0.0001867992666138375594 ),
 .UNSPECIFIED. ) ;
#7455=DIRECTION ( 'NONE',  ( -1.000000000000000000, 0.000000000000000000, 0.000000000000000000 ) ) ;
#7457=DIRECTION ( 'NONE',  ( 0.000000000000000000, 0.000000000000000000, 1.000000000000000000 ) ) ;
#7463=AXIS2_PLACEMENT_3D ( 'NONE', #6216, #36464, #2467 ) ;
#7468=CARTESIAN_POINT ( 'NONE',  ( 2.000000000000001776, 0.000000000000000000, 0.000000000000000000 ) ) ;
#7471=AXIS2_PLACEMENT_3D ( 'NONE', #16165, #22464, #41760 ) ;
#7472=CARTESIAN_POINT ( 'NONE',  ( -10.00000000000000178, 0.000000000000000000, 0.000000000000000000 ) ) ;
#7473=EDGE_LOOP ( 'NONE', ( #23438, #4162, #49592, #38059 ) ) ;
#7476=CYLINDRICAL_SURFACE ( 'NONE', #6604, 7.499999999999988454 ) ;
#7483=DIRECTION ( 'NONE',  ( 0.000000000000000000, -0.6051742151937555825, -0.7960930657056509707 ) ) ;
#7487=CARTESIAN_POINT ( 'NONE',  ( 1.000000000000000888, 0.7281529553923131726, -7.464569195442812166 ) ) ;
#7489=CARTESIAN_POINT ( 'NONE',  ( 2.000000000000001776, 0.000000000000000000, 0.000000000000000000 ) ) ;
#7492=DIRECTION ( 'NONE',  ( 0.000000000000000000, 0.000000000000000000, -1.000000000000000000 ) ) ;
#7493=ORIENTED_EDGE ( 'NONE', *, *, #5054, .F. ) ;
#7498=CARTESIAN_POINT ( 'NONE',  ( -22.27718150314433387, 3.596602356343910234, -0.7862703917636566509 ) ) ;
#7502=VECTOR ( 'NONE', #13494, 1000.000000000000000 ) ;
#7503=ORIENTED_EDGE ( 'NONE', *, *, #1480, .T. ) ;
#7511=DIRECTION ( 'NONE',  ( -1.000000000000000000, 0.000000000000000000, 0.000000000000000000 ) ) ;
#7519=CARTESIAN_POINT ( 'NONE',  ( -27.09364415740217780, -1.918701019215943493, 1.303410551736210898 ) ) ;
#7520=EDGE_CURVE ( 'NONE', #27787, #16234, #15226, .T. ) ;
#7522=CIRCLE ( 'NONE', #6490, 7.499999999999988454 ) ;
#7523=ORIENTED_EDGE ( 'NONE', *, *, #56226, .F. ) ;
#7524=CYLINDRICAL_SURFACE ( 'NONE', #22090, 7.499999999999988454 ) ;
#7525=VERTEX_POINT ( 'NONE', #11232 ) ;
#7526=EDGE_CURVE ( 'NONE', #725, #53268, #2237, .T. ) ;
#7533=AXIS2_PLACEMENT_3D ( 'NONE', #64959, #23100, #64312 ) ;
#7534=ORIENTED_EDGE ( 'NONE', *, *, #57543, .T. ) ;
#7539=CYLINDRICAL_SURFACE ( 'NONE', #33021, 2.999999999999995559 ) ;
#7545=CARTESIAN_POINT ( 'NONE',  ( -22.29018399051993882, -2.585196332786384055, 2.675685774027739328 ) ) ;
#7552=CIRCLE ( 'NONE', #35160, 2.899999999999994582 ) ;
#7555=DIRECTION ( 'NONE',  ( -1.000000000000000000, 0.000000000000000000, 0.000000000000000000 ) ) ;
#7558=CARTESIAN_POINT ( 'NONE',  ( -35.04643116707788408, 0.01156612771643569793, 0.003844232202706091006 ) ) ;
#7573=ORIENTED_EDGE ( 'NONE', *, *, #36863, .F. ) ;
#7574=CIRCLE ( 'NONE', #51228, 2.899999999999995914 ) ;
#7579=CARTESIAN_POINT ( 'NONE',  ( -16.00005080000000035, 0.000000000000000000, 0.000000000000000000 ) ) ;
#7590=ADVANCED_FACE ( 'NONE', ( #32792 ), #58773, .T. ) ;
#7608=CARTESIAN_POINT ( 'NONE',  ( -22.27722019094931127, -2.813874087060002527, 2.374181302998998877 ) ) ;
#7612=B_SPLINE_CURVE_WITH_KNOTS ( 'NONE', 3,
 ( #3581, #63392, #22529, #7898, #13822, #23172, #48141, #18847, #7545, #12519, #8212, #63716, #64377, #38466, #33486, #17860, #54090, #8523, #53452, #53775, #2599, #2912 ),
 .UNSPECIFIED., .F., .F.,
 ( 4, 3, 3, 3, 3, 3, 3, 4 ),
 ( 0.000000000000000000, 4.455945684386370791E-05, 6.636307477203548847E-05, 8.816671873158297989E-05, 0.0001099660380492561800, 0.0001317545563165253299, 0.0001762613022894969942, 0.0001867992666138382099 ),
 .UNSPECIFIED. ) ;
#7617=ADVANCED_FACE ( 'NONE', ( #42436 ), #17538, .T. ) ;
#7621=CARTESIAN_POINT ( 'NONE',  ( 2.000000000000001776, -1.956810415765137368, -6.654767106875568494 ) ) ;
#7632=LINE ( 'NONE', #27917, #39684 ) ;
#7643=CARTESIAN_POINT ( 'NONE',  ( -27.10128162969832744, 2.102429195189572830, 1.032914450114625016 ) ) ;
#7648=ADVANCED_FACE ( 'NONE', ( #37138 ), #7539, .T. ) ;
#7649=DIRECTION ( 'NONE',  ( -1.000000000000000000, 0.000000000000000000, 0.000000000000000000 ) ) ;
#7656=EDGE_CURVE ( 'NONE', #33192, #19282, #59573, .T. ) ;
#7662=CYLINDRICAL_SURFACE ( 'NONE', #50193, 6.936499999999988120 ) ;
#7663=CARTESIAN_POINT ( 'NONE',  ( -27.10512513516273359, -1.709353012332570643, -1.618446180705552573 ) ) ;
#7671=ORIENTED_EDGE ( 'NONE', *, *, #55042, .T. ) ;
#7676=CARTESIAN_POINT ( 'NONE',  ( 0.000000000000000000, 0.000000000000000000, 0.000000000000000000 ) ) ;
#7677=CARTESIAN_POINT ( 'NONE',  ( -22.29115169517546136, -0.2790989024812826069, -3.712980101756741202 ) ) ;
#7686=DIRECTION ( 'NONE',  ( -1.000000000000000000, 0.000000000000000000, 0.000000000000000000 ) ) ;
#7687=ORIENTED_EDGE ( 'NONE', *, *, #13163, .T. ) ;
#7692=CARTESIAN_POINT ( 'NONE',  ( 2.000000000000001776, 7.493043167941616289, 0.3229614270519615693 ) ) ;
#7693=AXIS2_PLACEMENT_3D ( 'NONE', #25885, #64775, #9252 ) ;
#7695=AXIS2_PLACEMENT_3D ( 'NONE', #2846, #2521, #22792 ) ;
#7696=DIRECTION ( 'NONE',  ( 0.000000000000000000, 0.000000000000000000, 1.000000000000000000 ) ) ;
#7711=CIRCLE ( 'NONE', #31044, 2.899999999999994582 ) ;
#7719=DIRECTION ( 'NONE',  ( -0.3162277663656185012, 0.1673616205762862574, 0.9338040949457712125 ) ) ;
#7721=EDGE_LOOP ( 'NONE', ( #42562, #63249, #65247, #14991 ) ) ;
#7729=FACE_OUTER_BOUND ( 'NONE', #21, .T. ) ;
#7730=FACE_OUTER_BOUND ( 'NONE', #14226, .T. ) ;
#7742=CARTESIAN_POINT ( 'NONE',  ( -22.28023996335807411, 3.676538434326163785, -0.3233044107360694697 ) ) ;
#7746=ORIENTED_EDGE ( 'NONE', *, *, #62517, .F. ) ;
#7747=CIRCLE ( 'NONE', #19431, 6.936499999999989008 ) ;
#7750=ORIENTED_EDGE ( 'NONE', *, *, #15493, .T. ) ;
#7752=AXIS2_PLACEMENT_3D ( 'NONE', #6043, #7004, #62510 ) ;
#7753=CARTESIAN_POINT ( 'NONE',  ( -22.27945548916780183, -3.346394890313974191, -1.551028078364850460 ) ) ;
#7756=DIRECTION ( 'NONE',  ( 0.000000000000000000, -0.9635499925192253512, 0.2675283385292119842 ) ) ;
#7762=AXIS2_PLACEMENT_3D ( 'NONE', #32448, #28783, #3549 ) ;
#7767=CARTESIAN_POINT ( 'NONE',  ( -22.30625920655495165, -3.687109008463848703, -0.8854385781085442053 ) ) ;
#7778=CARTESIAN_POINT ( 'NONE',  ( -22.28073302975500880, -3.572053042948119206, -0.9342220484185019824 ) ) ;
#7779=( BOUNDED_SURFACE ( )  B_SPLINE_SURFACE ( 3, 1, ( 
 ( #48894, #43891 ),
 ( #27948, #53563 ),
 ( #28589, #37913 ),
 ( #33592, #62854 ) ),
 .UNSPECIFIED., .F., .F., .F. ) 
 B_SPLINE_SURFACE_WITH_KNOTS ( ( 4, 4 ),
 ( 2, 2 ),
 ( 0.000000000000000000, 1.000000000000000000 ),
 ( 0.000000000000000000, 1.000000000000000000 ),
 .UNSPECIFIED. ) 
 GEOMETRIC_REPRESENTATION_ITEM ( )  RATIONAL_B_SPLINE_SURFACE ( (
 ( 1.000000000000000000, 1.000000000000000000),
 ( 0.9932032654565553509, 0.8386279382598736953),
 ( 0.9932032654565553509, 0.8386279382598736953),
 ( 1.000000000000000000, 1.000000000000000000) ) ) 
 REPRESENTATION_ITEM ( '' )  SURFACE ( )  );
#7781=DIRECTION ( 'NONE',  ( 1.000000000000000000, 0.000000000000000000, 0.000000000000000000 ) ) ;
#7784=VERTEX_POINT ( 'NONE', #28807 ) ;
#7787=CARTESIAN_POINT ( 'NONE',  ( -22.29479313954897890, 3.360948587163232304, 1.627767898183716921 ) ) ;
#7789=DIRECTION ( 'NONE',  ( -1.000000000000000000, 0.000000000000000000, 0.000000000000000000 ) ) ;
#7796=ORIENTED_EDGE ( 'NONE', *, *, #12424, .T. ) ;
#7812=LINE ( 'NONE', #23770, #50000 ) ;
#7824=CARTESIAN_POINT ( 'NONE',  ( 2.000000000000001776, 0.000000000000000000, 0.000000000000000000 ) ) ;
#7827=DIRECTION ( 'NONE',  ( -1.000000000000000000, 0.000000000000000000, 0.000000000000000000 ) ) ;
#7828=DIRECTION ( 'NONE',  ( 0.000000000000000000, 0.000000000000000000, 1.000000000000000000 ) ) ;
#7832=FACE_OUTER_BOUND ( 'NONE', #33175, .T. ) ;
#7837=LINE ( 'NONE', #18795, #40000 ) ;
#7845=LINE ( 'NONE', #32742, #44654 ) ;
#7846=ORIENTED_EDGE ( 'NONE', *, *, #33182, .T. ) ;
#7850=ORIENTED_EDGE ( 'NONE', *, *, #62771, .F. ) ;
#7851=VERTEX_POINT ( 'NONE', #16132 ) ;
#7863=CARTESIAN_POINT ( 'NONE',  ( 2.000000000000001776, -7.203928197742102135, 2.086484728383119158 ) ) ;
#7865=ORIENTED_EDGE ( 'NONE', *, *, #62645, .T. ) ;
#7866=CARTESIAN_POINT ( 'NONE',  ( 2.000000000000001776, -6.750946897830710114, 1.593658756657014397 ) ) ;
#7872=EDGE_CURVE ( 'NONE', #10610, #6941, #24578, .T. ) ;
#7873=CARTESIAN_POINT ( 'NONE',  ( -28.67667724226168602, 1.375746547601641723, 1.299025457479336287 ) ) ;
#7874=CARTESIAN_POINT ( 'NONE',  ( 0.000000000000000000, -4.604744433234713163, 5.919993978425451608 ) ) ;
#7884=CIRCLE ( 'NONE', #42890, 2.899999999999995026 ) ;
#7885=CARTESIAN_POINT ( 'NONE',  ( 2.000000000000001776, -0.2704997240204360387, -6.931223712253490987 ) ) ;
#7886=ORIENTED_EDGE ( 'NONE', *, *, #43030, .T. ) ;
#7888=CARTESIAN_POINT ( 'NONE',  ( -27.08506889328343803, 0.2104793012480555281, 2.284141197253888311 ) ) ;
#7890=CARTESIAN_POINT ( 'NONE',  ( 2.000000000000001776, -0.4129979343796691404, -6.800241778083718991 ) ) ;
#7892=CARTESIAN_POINT ( 'NONE',  ( -27.08871896697732140, -2.082324523416154261, -0.9878677378287702426 ) ) ;
#7898=CARTESIAN_POINT ( 'NONE',  ( -22.29978294495153790, -2.590262069787973243, 2.710748743830185603 ) ) ;
#7899=DIRECTION ( 'NONE',  ( 0.000000000000000000, 0.000000000000000000, 1.000000000000000000 ) ) ;
#7905=CARTESIAN_POINT ( 'NONE',  ( -27.08426504710140392, 1.649100202714206986, -1.591094357919260016 ) ) ;
#7913=DIRECTION ( 'NONE',  ( 0.000000000000000000, -0.9868265225415244757, -0.1617819965527746984 ) ) ;
#7936=EDGE_LOOP ( 'NONE', ( #31392, #42646, #11562, #5289 ) ) ;
#7941=ORIENTED_EDGE ( 'NONE', *, *, #2236, .F. ) ;
#7942=CARTESIAN_POINT ( 'NONE',  ( -22.27384469013076185, -0.9835229356382323429, 3.548341908721027060 ) ) ;
#7945=CARTESIAN_POINT ( 'NONE',  ( -35.04709527796842394, 0.007030359780627049027, -0.01016988845958279042 ) ) ;
#7947=ORIENTED_EDGE ( 'NONE', *, *, #20310, .T. ) ;
#7949=AXIS2_PLACEMENT_3D ( 'NONE', #64582, #58664, #63950 ) ;
#7956=CARTESIAN_POINT ( 'NONE',  ( -27.09569413923885861, -1.607816962455224985, 1.680421072128823967 ) ) ;
#7965=DIRECTION ( 'NONE',  ( 0.000000000000000000, 0.000000000000000000, 1.000000000000000000 ) ) ;
#7967=CARTESIAN_POINT ( 'NONE',  ( -35.05012975565874456, -0.008684292310218014177, -0.01089417657933552247 ) ) ;
#7968=CARTESIAN_POINT ( 'NONE',  ( -22.59969328935885358, 2.921971394153385138, -3.618004136135298143 ) ) ;
#7969=CYLINDRICAL_SURFACE ( 'NONE', #3197, 6.936499999999988120 ) ;
#7975=ORIENTED_EDGE ( 'NONE', *, *, #60536, .F. ) ;
#7982=LINE ( 'NONE', #28248, #49028 ) ;
#7984=EDGE_CURVE ( 'NONE', #57723, #7359, #43355, .T. ) ;
#7992=CARTESIAN_POINT ( 'NONE',  ( -10.00000000000000178, 0.000000000000000000, 0.000000000000000000 ) ) ;
#7997=FACE_OUTER_BOUND ( 'NONE', #13409, .T. ) ;
#7999=ADVANCED_FACE ( 'NONE', ( #58344 ), #63310, .T. ) ;
#8003=CARTESIAN_POINT ( 'NONE',  ( -27.08588607604433562, 2.215240480751983654, -0.6046196991082997130 ) ) ;
#8008=CARTESIAN_POINT ( 'NONE',  ( -27.08776759928965205, -1.644157618163919699, -1.611072893086249014 ) ) ;
#8022=CARTESIAN_POINT ( 'NONE',  ( -26.74023318801843985, 1.916028097164423905, -2.752802096869866766 ) ) ;
#8024=CARTESIAN_POINT ( 'NONE',  ( 2.000000000000001776, -6.767909380267593811, 0.7805499053120233954 ) ) ;
#8056=CARTESIAN_POINT ( 'NONE',  ( 0.000000000000000000, -6.935703035393428806, -0.1051458740708305362 ) ) ;
#8058=ORIENTED_EDGE ( 'NONE', *, *, #37923, .T. ) ;
#8063=CARTESIAN_POINT ( 'NONE',  ( -27.08426571771018487, -0.9198084705429405705, 2.098821047392059658 ) ) ;
#8070=AXIS2_PLACEMENT_3D ( 'NONE', #41818, #25210, #46477 ) ;
#8071=ORIENTED_EDGE ( 'NONE', *, *, #19961, .T. ) ;
#8079=VERTEX_POINT ( 'NONE', #41311 ) ;
#8080=VERTEX_POINT ( 'NONE', #61594 ) ;
#8084=CARTESIAN_POINT ( 'NONE',  ( -22.28629837673887693, -3.348758206500233925, -1.594277649056540902 ) ) ;
#8097=ORIENTED_EDGE ( 'NONE', *, *, #50130, .F. ) ;
#8101=CARTESIAN_POINT ( 'NONE',  ( -22.66110217412718697, 2.622110956932579118, -4.192227617777399828 ) ) ;
#8114=CARTESIAN_POINT ( 'NONE',  ( -22.27945548916780183, 3.346394890313977744, 1.551028078364822704 ) ) ;
#8123=AXIS2_PLACEMENT_3D ( 'NONE', #43697, #54355, #8791 ) ;
#8125=CARTESIAN_POINT ( 'NONE',  ( -22.23402523511428086, 1.734723475976807094E-15, -8.673617379884035472E-15 ) ) ;
#8135=DIRECTION ( 'NONE',  ( 0.000000000000000000, 0.000000000000000000, -1.000000000000000000 ) ) ;
#8139=ORIENTED_EDGE ( 'NONE', *, *, #24854, .F. ) ;
#8150=AXIS2_PLACEMENT_3D ( 'NONE', #59523, #20835, #10857 ) ;
#8162=ORIENTED_EDGE ( 'NONE', *, *, #34682, .F. ) ;
#8169=EDGE_CURVE ( 'NONE', #47922, #35439, #57951, .T. ) ;
#8171=FACE_OUTER_BOUND ( 'NONE', #45008, .T. ) ;
#8176=CARTESIAN_POINT ( 'NONE',  ( -22.46509356695202086, -4.038408495643994733, 1.314379028669602656 ) ) ;
#8179=DIRECTION ( 'NONE',  ( 0.000000000000000000, 0.9868265225415254749, 0.1617819965527686199 ) ) ;
#8192=FACE_OUTER_BOUND ( 'NONE', #5999, .T. ) ;
#8194=EDGE_CURVE ( 'NONE', #30859, #3157, #39424, .T. ) ;
#8199=CARTESIAN_POINT ( 'NONE',  ( 1.000000000000000888, -0.8935325819929111901, 7.446583077151331942 ) ) ;
#8212=CARTESIAN_POINT ( 'NONE',  ( -22.28694879868232803, -2.586016167700811330, 2.661377239830749808 ) ) ;
#8217=EDGE_LOOP ( 'NONE', ( #42229, #3475, #9174, #36310 ) ) ;
#8218=CARTESIAN_POINT ( 'NONE',  ( -27.08418179957658367, 1.713622993062713373, -1.521007404704320942 ) ) ;
#8235=CARTESIAN_POINT ( 'NONE',  ( -27.35552965826137140, 0.2619431035392177365, -3.094132632038957276 ) ) ;
#8241=ORIENTED_EDGE ( 'NONE', *, *, #50522, .F. ) ;
#8249=CARTESIAN_POINT ( 'NONE',  ( -22.28629837673888048, -1.594277649056518475, 3.348758206500239254 ) ) ;
#8251=CARTESIAN_POINT ( 'NONE',  ( -35.04683013664716640, 0.01065093278707341523, -0.006266879427281896002 ) ) ;
#8254=EDGE_LOOP ( 'NONE', ( #14931, #59705, #39408, #23668 ) ) ;
#8263=CARTESIAN_POINT ( 'NONE',  ( 0.000000000000000000, 0.000000000000000000, 0.000000000000000000 ) ) ;
#8266=CARTESIAN_POINT ( 'NONE',  ( -28.66013792860432119, 1.306994062650338684, -1.289369452666814020 ) ) ;
#8268=VERTEX_POINT ( 'NONE', #40222 ) ;
#8270=EDGE_CURVE ( 'NONE', #34013, #16747, #45892, .T. ) ;
#8274=FACE_OUTER_BOUND ( 'NONE', #3188, .T. ) ;
#8276=CARTESIAN_POINT ( 'NONE',  ( -22.65996813707689128, -4.292955455498915995, 2.220979297960717691 ) ) ;
#8285=EDGE_CURVE ( 'NONE', #47834, #27353, #20356, .T. ) ;
#8292=AXIS2_PLACEMENT_3D ( 'NONE', #12742, #48677, #28702 ) ;
#8293=CYLINDRICAL_SURFACE ( 'NONE', #8656, 6.936499999999988120 ) ;
#8307=ORIENTED_EDGE ( 'NONE', *, *, #36235, .F. ) ;
#8308=ORIENTED_EDGE ( 'NONE', *, *, #998, .T. ) ;
#8310=ORIENTED_EDGE ( 'NONE', *, *, #52355, .T. ) ;
#8313=CARTESIAN_POINT ( 'NONE',  ( -27.09229696323320624, -1.666734935099465131, -1.607344345646473327 ) ) ;
#8325=CARTESIAN_POINT ( 'NONE',  ( -22.27945548916780183, -0.3299677273100632968, -3.673577025288763398 ) ) ;
#8326=ORIENTED_EDGE ( 'NONE', *, *, #7656, .T. ) ;
#8330=CARTESIAN_POINT ( 'NONE',  ( -27.08429572838383947, -2.208905845566027537, -0.6096735944848257205 ) ) ;
#8343=LINE ( 'NONE', #49264, #41237 ) ;
#8350=DIRECTION ( 'NONE',  ( 0.000000000000000000, 0.000000000000000000, 1.000000000000000000 ) ) ;
#8365=CARTESIAN_POINT ( 'NONE',  ( -27.08429572838383947, 2.208905845566027537, 0.6096735944847788691 ) ) ;
#8369=VERTEX_POINT ( 'NONE', #36883 ) ;
#8372=B_SPLINE_CURVE_WITH_KNOTS ( 'NONE', 3,
 ( #9354, #29639, #56229, #24333, #65538, #45595 ),
 .UNSPECIFIED., .F., .F.,
 ( 4, 2, 4 ),
 ( 0.0001654224980408687486, 0.0006219428995476670432, 0.001078463301054465419 ),
 .UNSPECIFIED. ) ;
#8377=CARTESIAN_POINT ( 'NONE',  ( -27.08418179957658367, -0.7235373421492636847, 2.174042548349516935 ) ) ;
#8378=AXIS2_PLACEMENT_3D ( 'NONE', #20935, #36571, #10974 ) ;
#8381=CARTESIAN_POINT ( 'NONE',  ( -22.28284753389937123, -2.640101649307533549, -2.590196335759745061 ) ) ;
#8386=ADVANCED_FACE ( 'NONE', ( #12924 ), #12575, .T. ) ;
#8389=CARTESIAN_POINT ( 'NONE',  ( -22.27711351828769892, -3.575417021793780403, 0.8770428151440453624 ) ) ;
#8391=ORIENTED_EDGE ( 'NONE', *, *, #44195, .F. ) ;
#8394=EDGE_LOOP ( 'NONE', ( #34428, #34153, #46518, #33358 ) ) ;
#8396=CARTESIAN_POINT ( 'NONE',  ( -22.71097035706202405, -0.4203397252017116448, 4.965150228107737540 ) ) ;
#8399=CARTESIAN_POINT ( 'NONE',  ( 2.000000000000001776, 5.217815162096925086, -5.387430271863535403 ) ) ;
#8405=AXIS2_PLACEMENT_3D ( 'NONE', #57860, #51566, #11945 ) ;
#8411=ADVANCED_FACE ( 'NONE', ( #11609 ), #47852, .T. ) ;
#8413=ORIENTED_EDGE ( 'NONE', *, *, #33263, .F. ) ;
#8425=CARTESIAN_POINT ( 'NONE',  ( -27.20164183316781248, -2.237540722393157377, 1.409601201084047517 ) ) ;
#8427=EDGE_LOOP ( 'NONE', ( #19788, #32032, #48692, #42465 ) ) ;
#8432=CARTESIAN_POINT ( 'NONE',  ( -22.28121537037577227, 3.345440028056700488, 1.565596675942127147 ) ) ;
#8435=DIRECTION ( 'NONE',  ( 0.000000000000000000, -0.9985334138511233748, -0.05413890858542835804 ) ) ;
#8444=CARTESIAN_POINT ( 'NONE',  ( 2.000000000000001776, 6.664893814313781029, -3.439359016433444438 ) ) ;
#8453=ORIENTED_EDGE ( 'NONE', *, *, #59775, .T. ) ;
#8455=CARTESIAN_POINT ( 'NONE',  ( 0.000000000000000000, 1.865193240757184290, -6.552473556515182374 ) ) ;
#8456=CARTESIAN_POINT ( 'NONE',  ( -22.71097035706202760, -2.118550233809395777, -4.510116093748293586 ) ) ;
#8461=VERTEX_POINT ( 'NONE', #38178 ) ;
#8465=ORIENTED_EDGE ( 'NONE', *, *, #6538, .T. ) ;
#8474=DIRECTION ( 'NONE',  ( -1.000000000000000000, 0.000000000000000000, 0.000000000000000000 ) ) ;
#8488=DIRECTION ( 'NONE',  ( -1.000000000000000000, 0.000000000000000000, 0.000000000000000000 ) ) ;
#8492=LINE ( 'NONE', #28778, #11327 ) ;
#8497=B_SPLINE_CURVE_WITH_KNOTS ( 'NONE', 3,
 ( #34266, #29285, #18345, #33619, #38607, #64208, #9002, #43249 ),
 .UNSPECIFIED., .F., .F.,
 ( 4, 2, 2, 4 ),
 ( 4.010449034101563893E-18, 0.0003639104015150034324, 0.0007278208030300028532, 0.001455641606060006791 ),
 .UNSPECIFIED. ) ;
#8499=CARTESIAN_POINT ( 'NONE',  ( 0.000000000000000000, 5.457833520448658327, 4.281014542496528463 ) ) ;
#8500=DIRECTION ( 'NONE',  ( 0.000000000000000000, 0.1764146379942750364, 0.9843159429275484262 ) ) ;
#8502=CARTESIAN_POINT ( 'NONE',  ( -22.30078715814471835, 3.111489293522213373, -2.097357782488221023 ) ) ;
#8504=CARTESIAN_POINT ( 'NONE',  ( -10.00000000000000178, 0.000000000000000000, 0.000000000000000000 ) ) ;
#8507=ORIENTED_EDGE ( 'NONE', *, *, #60621, .T. ) ;
#8516=AXIS2_PLACEMENT_3D ( 'NONE', #27244, #22926, #7965 ) ;
#8520=CARTESIAN_POINT ( 'NONE',  ( 0.000000000000000000, 0.000000000000000000, -2.999999999999995559 ) ) ;
#8523=CARTESIAN_POINT ( 'NONE',  ( -22.27756824490284160, -2.608445836294056797, 2.599719761044740896 ) ) ;
#8525=AXIS2_PLACEMENT_3D ( 'NONE', #65757, #50511, #36835 ) ;
#8526=EDGE_CURVE ( 'NONE', #6060, #6053, #48550, .T. ) ;
#8529=CARTESIAN_POINT ( 'NONE',  ( -27.08416974970326052, -0.4041872645907051420, -2.255186831366117417 ) ) ;
#8531=EDGE_CURVE ( 'NONE', #8602, #1479, #20455, .T. ) ;
#8533=ORIENTED_EDGE ( 'NONE', *, *, #8643, .T. ) ;
#8550=CARTESIAN_POINT ( 'NONE',  ( -22.71097035706202405, 0.4203397252017515573, -4.965150228107761521 ) ) ;
#8554=CARTESIAN_POINT ( 'NONE',  ( 2.000000000000001776, -1.058508696394911963, -6.730038252034928448 ) ) ;
#8557=CARTESIAN_POINT ( 'NONE',  ( -22.94572469358970324, 4.011883207821686170, 2.792384151940626946 ) ) ;
#8562=VECTOR ( 'NONE', #18343, 1000.000000000000000 ) ;
#8563=ORIENTED_EDGE ( 'NONE', *, *, #53441, .F. ) ;
#8564=CARTESIAN_POINT ( 'NONE',  ( 0.000000000000000000, -2.664846396702443609, -6.404188155573042884 ) ) ;
#8567=CARTESIAN_POINT ( 'NONE',  ( -22.29290468048228036, -1.621390503294478869, 3.357740900108105109 ) ) ;
#8572=DIRECTION ( 'NONE',  ( -1.000000000000000000, 0.000000000000000000, 0.000000000000000000 ) ) ;
#8574=ORIENTED_EDGE ( 'NONE', *, *, #32100, .T. ) ;
#8576=VECTOR ( 'NONE', #41023, 1000.000000000000000 ) ;
#8580=CARTESIAN_POINT ( 'NONE',  ( -22.27706485742869091, -2.985151051101489372, 2.154081322712201096 ) ) ;
#8595=CARTESIAN_POINT ( 'NONE',  ( -27.08702828306202193, 1.612407531673552219, -1.639744581306265658 ) ) ;
#8596=CARTESIAN_POINT ( 'NONE',  ( -27.08417568107324058, 1.449568724721390645, 1.774279301226111993 ) ) ;
#8602=VERTEX_POINT ( 'NONE', #61250 ) ;
#8617=CARTESIAN_POINT ( 'NONE',  ( -27.09483304420744432, 2.090133548855283241, 1.013994808269825132 ) ) ;
#8620=VECTOR ( 'NONE', #9982, 1000.000000000000000 ) ;
#8621=DIRECTION ( 'NONE',  ( 1.000000000000000000, 0.000000000000000000, 0.000000000000000000 ) ) ;
#8631=CARTESIAN_POINT ( 'NONE',  ( -27.10719052120871098, 1.310802520592036391, 1.962717903527646079 ) ) ;
#8632=CONICAL_SURFACE ( 'NONE', #23492, 5.135612550275435062, 1.249045772030607848 ) ;
#8634=CIRCLE ( 'NONE', #21403, 7.499999999999988454 ) ;
#8643=EDGE_CURVE ( 'NONE', #24684, #21602, #11679, .T. ) ;
#8644=CARTESIAN_POINT ( 'NONE',  ( -22.29677679919927513, -2.096973157017373524, -3.097220482904039063 ) ) ;
#8645=VERTEX_POINT ( 'NONE', #6386 ) ;
#8646=EDGE_CURVE ( 'NONE', #5634, #9785, #5751, .T. ) ;
#8655=DIRECTION ( 'NONE',  ( 1.000000000000000000, -0.000000000000000000, -0.000000000000000000 ) ) ;
#8656=AXIS2_PLACEMENT_3D ( 'NONE', #44493, #28563, #3321 ) ;
#8658=CARTESIAN_POINT ( 'NONE',  ( -22.66110217412718697, -0.1747008913564180588, 4.941631093908251948 ) ) ;
#8660=CARTESIAN_POINT ( 'NONE',  ( -27.04788180060269909, 1.844972430941770103, -2.650714769830301520 ) ) ;
#8661=DIRECTION ( 'NONE',  ( -1.000000000000000000, 0.000000000000000000, 0.000000000000000000 ) ) ;
#8665=CARTESIAN_POINT ( 'NONE',  ( 2.000000000000001776, 3.341639490130761114, 6.078525953551427996 ) ) ;
#8676=CARTESIAN_POINT ( 'NONE',  ( -22.49803948133827802, -0.1132714802761562861, -4.343047530463637784 ) ) ;
#8679=CIRCLE ( 'NONE', #45836, 2.899999999999994582 ) ;
#8680=ORIENTED_EDGE ( 'NONE', *, *, #1142, .T. ) ;
#8681=DIRECTION ( 'NONE',  ( 0.9582930651793755139, 0.2568015617827278940, 0.1254087680151157735 ) ) ;
#8682=CARTESIAN_POINT ( 'NONE',  ( 2.000000000000001776, 0.000000000000000000, 0.000000000000000000 ) ) ;
#8685=VERTEX_POINT ( 'NONE', #52913 ) ;
#8688=FACE_OUTER_BOUND ( 'NONE', #760, .T. ) ;
#8695=ORIENTED_EDGE ( 'NONE', *, *, #13674, .F. ) ;
#8696=CARTESIAN_POINT ( 'NONE',  ( -35.04709527796842394, 0.005292201869334239861, 0.01117341439754379606 ) ) ;
#8698=DIRECTION ( 'NONE',  ( -1.000000000000000000, 0.000000000000000000, 0.000000000000000000 ) ) ;
#8707=VECTOR ( 'NONE', #33891, 1000.000000000000000 ) ;
#8711=AXIS2_PLACEMENT_3D ( 'NONE', #51288, #60, #16000 ) ;
#8713=LINE ( 'NONE', #65520, #13677 ) ;
#8714=B_SPLINE_CURVE_WITH_KNOTS ( 'NONE', 3,
 ( #353, #6320, #1338, #37207, #7278, #43180, #52542, #63780, #22593, #23238, #38186, #17612, #2975, #36892, #58165, #27563, #42857, #21937, #2664, #11942, #47861, #32863 ),
 .UNSPECIFIED., .F., .F.,
 ( 4, 3, 3, 3, 3, 3, 3, 4 ),
 ( 9.813077866774405223E-18, 6.990956068646504110E-05, 0.0001398191187764071506, 0.0002097286751720257728, 0.0002796382307041420643, 0.0003495477861619880676, 0.0004194573423310373568, 0.0005586102576333245792 ),
 .UNSPECIFIED. ) ;
#8719=AXIS2_PLACEMENT_3D ( 'NONE', #45720, #11451, #21786 ) ;
#8723=DIRECTION ( 'NONE',  ( 0.000000000000000000, 0.000000000000000000, 1.000000000000000000 ) ) ;
#8724=CARTESIAN_POINT ( 'NONE',  ( -22.27721688985630166, -3.631967556481315640, 0.6032462375556733036 ) ) ;
#8727=ORIENTED_EDGE ( 'NONE', *, *, #33062, .F. ) ;
#8728=CIRCLE ( 'NONE', #3437, 2.899999999999996358 ) ;
#8731=CARTESIAN_POINT ( 'NONE',  ( 0.000000000000000000, -7.484036900328550956, 0.4890722589968952150 ) ) ;
#8758=CARTESIAN_POINT ( 'NONE',  ( 2.000000000000001776, -6.767909380267597363, 2.119450094687862052 ) ) ;
#8762=AXIS2_PLACEMENT_3D ( 'NONE', #32672, #61640, #16442 ) ;
#8763=ORIENTED_EDGE ( 'NONE', *, *, #24848, .F. ) ;
#8765=ORIENTED_EDGE ( 'NONE', *, *, #22552, .T. ) ;
#8768=CARTESIAN_POINT ( 'NONE',  ( -27.08416974970326407, 0.3922151116844109220, 2.257332547928087685 ) ) ;
#8777=ADVANCED_FACE ( 'NONE', ( #13007 ), #63529, .T. ) ;
#8780=CARTESIAN_POINT ( 'NONE',  ( -27.08419797710328325, -1.413289504316732614, -1.803546201758818635 ) ) ;
#8787=DIRECTION ( 'NONE',  ( -1.000000000000000000, 0.000000000000000000, 0.000000000000000000 ) ) ;
#8788=EDGE_CURVE ( 'NONE', #62166, #8079, #40815, .T. ) ;
#8791=DIRECTION ( 'NONE',  ( 0.000000000000000000, 0.000000000000000000, 1.000000000000000000 ) ) ;
#8794=EDGE_CURVE ( 'NONE', #26744, #60178, #65802, .T. ) ;
#8802=CARTESIAN_POINT ( 'NONE',  ( -35.04643116707788408, 0.004425962698851801380, -0.01135624435145456135 ) ) ;
#8809=EDGE_CURVE ( 'NONE', #38245, #37217, #61400, .T. ) ;
#8816=CARTESIAN_POINT ( 'NONE',  ( -35.04709527796842394, 0.01117341439754726551, -0.005292201869334239861 ) ) ;
#8819=CARTESIAN_POINT ( 'NONE',  ( -22.27706485742869091, 2.154081322712221969, 2.985151051101477382 ) ) ;
#8824=ORIENTED_EDGE ( 'NONE', *, *, #44511, .F. ) ;
#8843=CARTESIAN_POINT ( 'NONE',  ( -22.31328051695926007, 3.148362328073167404, -2.109671368890616350 ) ) ;
#8848=VERTEX_POINT ( 'NONE', #20532 ) ;
#8857=DIRECTION ( 'NONE',  ( -1.000000000000000000, 0.000000000000000000, 0.000000000000000000 ) ) ;
#8858=CARTESIAN_POINT ( 'NONE',  ( -27.10422407540562517, -2.109093808474706844, -1.039355862230284533 ) ) ;
#8869=CARTESIAN_POINT ( 'NONE',  ( -27.08429572838383947, -0.5764601019425836803, -2.217805374070540125 ) ) ;
#8874=AXIS2_PLACEMENT_3D ( 'NONE', #609, #25200, #45474 ) ;
#8884=LINE ( 'NONE', #59419, #62643 ) ;
#8890=CARTESIAN_POINT ( 'NONE',  ( -27.28573687977897677, 0.4470060700698672562, -2.862048090118451960 ) ) ;
#8892=CARTESIAN_POINT ( 'NONE',  ( 2.000000000000001776, 5.450255447309811707, -4.087611905901392007 ) ) ;
#8903=VERTEX_POINT ( 'NONE', #21851 ) ;
#8915=DIRECTION ( 'NONE',  ( 1.000000000000000000, -0.000000000000000000, -0.000000000000000000 ) ) ;
#8919=DIRECTION ( 'NONE',  ( -1.000000000000000000, 0.000000000000000000, 0.000000000000000000 ) ) ;
#8923=EDGE_CURVE ( 'NONE', #52767, #51541, #827, .T. ) ;
#8933=CARTESIAN_POINT ( 'NONE',  ( -27.08776759928996825, 1.611072893085662594, -1.644157618165827728 ) ) ;
#8937=AXIS2_PLACEMENT_3D ( 'NONE', #22053, #33000, #28355 ) ;
#8938=EDGE_LOOP ( 'NONE', ( #15801, #62516, #12382, #35552 ) ) ;
#8939=EDGE_CURVE ( 'NONE', #12565, #57350, #38348, .T. ) ;
#8945=VECTOR ( 'NONE', #34723, 1000.000000000000000 ) ;
#8947=CARTESIAN_POINT ( 'NONE',  ( 2.000000000000001776, 7.493043167941614513, -0.3229614270519962638 ) ) ;
#8949=VERTEX_POINT ( 'NONE', #31791 ) ;
#8950=DIRECTION ( 'NONE',  ( 0.000000000000000000, -0.9635499925192201331, -0.2675283385292311911 ) ) ;
#8954=VECTOR ( 'NONE', #24632, 1000.000000000000000 ) ;
#8959=EDGE_LOOP ( 'NONE', ( #22183, #22202, #65004, #19500 ) ) ;
#8973=DIRECTION ( 'NONE',  ( -1.000000000000000000, 0.000000000000000000, 0.000000000000000000 ) ) ;
#8988=DIRECTION ( 'NONE',  ( 1.000000000000000000, 1.685093406416449860E-16, -1.011030131491573426E-17 ) ) ;
#8989=ORIENTED_EDGE ( 'NONE', *, *, #57420, .T. ) ;
#8995=ORIENTED_EDGE ( 'NONE', *, *, #7441, .F. ) ;
#8999=CIRCLE ( 'NONE', #40849, 6.936499999999995225 ) ;
#9002=CARTESIAN_POINT ( 'NONE',  ( -22.65996813707688062, -4.828298130757413986, -0.2230532344361538521 ) ) ;
#9010=ORIENTED_EDGE ( 'NONE', *, *, #48893, .F. ) ;
#9011=DIRECTION ( 'NONE',  ( -1.000000000000000000, -1.685093406416449860E-16, 1.011030131491573426E-17 ) ) ;
#9013=CARTESIAN_POINT ( 'NONE',  ( 2.000000000000001776, 6.338823199656720142, -2.816798305433633853 ) ) ;
#9014=VERTEX_POINT ( 'NONE', #31484 ) ;
#9018=ORIENTED_EDGE ( 'NONE', *, *, #19673, .F. ) ;
#9036=DIRECTION ( 'NONE',  ( -1.000000000000000000, 0.000000000000000000, 0.000000000000000000 ) ) ;
#9043=CARTESIAN_POINT ( 'NONE',  ( -22.27718112499583469, -3.645895996548662588, 0.5110808820053356349 ) ) ;
#9057=ORIENTED_EDGE ( 'NONE', *, *, #52214, .T. ) ;
#9059=DIRECTION ( 'NONE',  ( -1.000000000000000000, 0.000000000000000000, 0.000000000000000000 ) ) ;
#9064=CARTESIAN_POINT ( 'NONE',  ( -35.04643116707788408, 0.008094444324494021181, 0.009112266603801891240 ) ) ;
#9067=ADVANCED_FACE ( 'NONE', ( #23824 ), #12832, .T. ) ;
#9069=CARTESIAN_POINT ( 'NONE',  ( 2.000000000000001776, -5.097042323172408906, -5.501832381651512449 ) ) ;
#9074=DIRECTION ( 'NONE',  ( -1.000000000000000000, 0.000000000000000000, 0.000000000000000000 ) ) ;
#9076=CARTESIAN_POINT ( 'NONE',  ( -27.10422407540562162, -0.1544383239736460967, -2.346206748218708338 ) ) ;
#9078=CARTESIAN_POINT ( 'NONE',  ( 2.000000000000001776, 3.155844197800107498, 6.177028383390443800 ) ) ;
#9081=DIRECTION ( 'NONE',  ( 0.000000000000000000, 0.000000000000000000, 1.000000000000000000 ) ) ;
#9085=CARTESIAN_POINT ( 'NONE',  ( 0.000000000000000000, 6.935703035393450122, 0.1051458740707594125 ) ) ;
#9089=CARTESIAN_POINT ( 'NONE',  ( -22.29115169517546136, 1.614783311161212875, -3.355084543108099560 ) ) ;
#9092=ORIENTED_EDGE ( 'NONE', *, *, #14222, .F. ) ;
#9093=ADVANCED_FACE ( 'NONE', ( #54067 ), #28760, .T. ) ;
#9095=CARTESIAN_POINT ( 'NONE',  ( -27.08416813689867908, -1.467601568343275265, -1.759517419957085549 ) ) ;
#9100=EDGE_CURVE ( 'NONE', #36393, #32874, #20264, .T. ) ;
#9103=EDGE_CURVE ( 'NONE', #19030, #11939, #24615, .T. ) ;
#9112=( BOUNDED_SURFACE ( )  B_SPLINE_SURFACE ( 3, 1, ( 
 ( #14827, #35113 ),
 ( #40109, #19535 ),
 ( #9517, #44777 ),
 ( #36097, #29481 ) ),
 .UNSPECIFIED., .F., .F., .F. ) 
 B_SPLINE_SURFACE_WITH_KNOTS ( ( 4, 4 ),
 ( 2, 2 ),
 ( 0.000000000000000000, 1.000000000000000000 ),
 ( 0.000000000000000000, 1.000000000000000000 ),
 .UNSPECIFIED. ) 
 GEOMETRIC_REPRESENTATION_ITEM ( )  RATIONAL_B_SPLINE_SURFACE ( (
 ( 1.000000000000000000, 1.000000000000000000),
 ( 0.8716676215708681896, 0.8964445200148164483),
 ( 0.8716676215708681896, 0.8964445200148164483),
 ( 1.000000000000000000, 1.000000000000000000) ) ) 
 REPRESENTATION_ITEM ( '' )  SURFACE ( )  );
#9117=ORIENTED_EDGE ( 'NONE', *, *, #23838, .T. ) ;
#9127=CARTESIAN_POINT ( 'NONE',  ( 1.000000000000000888, 7.203928197742132333, -2.086484728383096510 ) ) ;
#9132=ORIENTED_EDGE ( 'NONE', *, *, #57008, .F. ) ;
#9147=AXIS2_PLACEMENT_3D ( 'NONE', #20732, #5785, #60972 ) ;
#9150=LINE ( 'NONE', #24126, #59261 ) ;
#9153=CARTESIAN_POINT ( 'NONE',  ( -22.27706485742869091, -0.9221835209182183135, -3.563814065926679042 ) ) ;
#9157=DIRECTION ( 'NONE',  ( 0.000000000000000000, 0.000000000000000000, 1.000000000000000000 ) ) ;
#9159=CARTESIAN_POINT ( 'NONE',  ( -22.27706485742869091, 1.508175983031630585, -3.358064672837109743 ) ) ;
#9160=ORIENTED_EDGE ( 'NONE', *, *, #16306, .T. ) ;
#9163=FILL_AREA_STYLE_COLOUR ( '', #43555 ) ;
#9174=ORIENTED_EDGE ( 'NONE', *, *, #22821, .F. ) ;
#9182=LINE ( 'NONE', #38805, #44641 ) ;
#9184=CARTESIAN_POINT ( 'NONE',  ( -22.51237073810381517, 4.418556976583594142, -0.2145858836691955096 ) ) ;
#9208=CARTESIAN_POINT ( 'NONE',  ( -28.67667724226168602, -1.812862320140641526, 0.5419187306520707459 ) ) ;
#9218=EDGE_CURVE ( 'NONE', #37190, #25841, #53215, .T. ) ;
#9224=CARTESIAN_POINT ( 'NONE',  ( 2.000000000000001776, 5.888698556700818543, -3.665823448873358981 ) ) ;
#9237=CARTESIAN_POINT ( 'NONE',  ( -27.08935880048797529, 1.608762129669642604, -1.653090150968472116 ) ) ;
#9239=CARTESIAN_POINT ( 'NONE',  ( 2.000000000000001776, -6.906413915731171471, -0.6453518998148326524 ) ) ;
#9248=FACE_OUTER_BOUND ( 'NONE', #12217, .T. ) ;
#9252=DIRECTION ( 'NONE',  ( 0.000000000000000000, -0.8835120444460272671, 0.4684084406997818251 ) ) ;
#9257=ORIENTED_EDGE ( 'NONE', *, *, #41690, .F. ) ;
#9267=ORIENTED_EDGE ( 'NONE', *, *, #12328, .F. ) ;
#9268=FACE_OUTER_BOUND ( 'NONE', #21409, .T. ) ;
#9274=CARTESIAN_POINT ( 'NONE',  ( 2.000000000000001776, -5.396716205731396876, -4.158041573745144603 ) ) ;
#9280=VERTEX_POINT ( 'NONE', #16459 ) ;
#9281=ORIENTED_EDGE ( 'NONE', *, *, #31984, .F. ) ;
#9283=DIRECTION ( 'NONE',  ( 0.000000000000000000, -0.1764146379942750642, -0.9843159429275485373 ) ) ;
#9284=EDGE_CURVE ( 'NONE', #54109, #26729, #11446, .T. ) ;
#9291=ORIENTED_EDGE ( 'NONE', *, *, #28278, .T. ) ;
#9315=AXIS2_PLACEMENT_3D ( 'NONE', #61660, #22407, #17441 ) ;
#9328=DIRECTION ( 'NONE',  ( -1.000000000000000000, 0.000000000000000000, 0.000000000000000000 ) ) ;
#9343=DIRECTION ( 'NONE',  ( -1.000000000000000000, 0.000000000000000000, 0.000000000000000000 ) ) ;
#9351=ORIENTED_EDGE ( 'NONE', *, *, #37764, .F. ) ;
#9354=CARTESIAN_POINT ( 'NONE',  ( -27.35552965826135008, 3.094132632038936404, 0.2619431035391969198 ) ) ;
#9383=EDGE_CURVE ( 'NONE', #54788, #22230, #52306, .T. ) ;
#9396=FACE_OUTER_BOUND ( 'NONE', #24379, .T. ) ;
#9404=CIRCLE ( 'NONE', #46587, 2.899999999999995026 ) ;
#9407=CARTESIAN_POINT ( 'NONE',  ( -35.04709527796842394, -0.01232256164996302361, -0.001003525937983557048 ) ) ;
#9411=CARTESIAN_POINT ( 'NONE',  ( 0.000000000000000000, 6.906413915731192787, 0.6453518998147528274 ) ) ;
#9417=ORIENTED_EDGE ( 'NONE', *, *, #18184, .F. ) ;
#9423=ORIENTED_EDGE ( 'NONE', *, *, #30198, .F. ) ;
#9429=VERTEX_POINT ( 'NONE', #59307 ) ;
#9439=ADVANCED_FACE ( 'NONE', ( #34016 ), #54333, .T. ) ;
#9443=ORIENTED_EDGE ( 'NONE', *, *, #34682, .T. ) ;
#9458=EDGE_CURVE ( 'NONE', #39295, #30401, #13181, .T. ) ;
#9467=CYLINDRICAL_SURFACE ( 'NONE', #43744, 2.899999999999994582 ) ;
#9468=CYLINDRICAL_SURFACE ( 'NONE', #30532, 2.899999999999994582 ) ;
#9472=ORIENTED_EDGE ( 'NONE', *, *, #30877, .T. ) ;
#9476=DIRECTION ( 'NONE',  ( 1.000000000000000000, 0.000000000000000000, 0.000000000000000000 ) ) ;
#9478=CIRCLE ( 'NONE', #40294, 2.899999999999994582 ) ;
#9490=CARTESIAN_POINT ( 'NONE',  ( 2.000000000000001776, -6.606214214351077807, 2.114938770769887455 ) ) ;
#9492=DIRECTION ( 'NONE',  ( 0.000000000000000000, 0.000000000000000000, 1.000000000000000000 ) ) ;
#9495=DIRECTION ( 'NONE',  ( -1.000000000000000000, 0.000000000000000000, 0.000000000000000000 ) ) ;
#9501=ORIENTED_EDGE ( 'NONE', *, *, #31815, .F. ) ;
#9502=CARTESIAN_POINT ( 'NONE',  ( 2.000000000000001776, 0.000000000000000000, 0.000000000000000000 ) ) ;
#9508=AXIS2_PLACEMENT_3D ( 'NONE', #54512, #55140, #29230 ) ;
#9509=AXIS2_PLACEMENT_3D ( 'NONE', #32782, #12845, #2232 ) ;
#9513=CARTESIAN_POINT ( 'NONE',  ( -27.08579483061179261, 1.318128465626146051, 1.879952013013905576 ) ) ;
#9517=CARTESIAN_POINT ( 'NONE',  ( -35.05012975565874456, 0.005092487515914018679, -0.01296790604420075023 ) ) ;
#9524=EDGE_CURVE ( 'NONE', #7525, #29429, #53548, .T. ) ;
#9525=CIRCLE ( 'NONE', #46713, 6.936499999999990784 ) ;
#9527=EDGE_CURVE ( 'NONE', #36878, #16830, #48285, .T. ) ;
#9529=ORIENTED_EDGE ( 'NONE', *, *, #17249, .F. ) ;
#9534=ORIENTED_EDGE ( 'NONE', *, *, #65400, .F. ) ;
#9535=EDGE_CURVE ( 'NONE', #45642, #7784, #25304, .T. ) ;
#9536=DIRECTION ( 'NONE',  ( 0.000000000000000000, 0.000000000000000000, 1.000000000000000000 ) ) ;
#9539=CARTESIAN_POINT ( 'NONE',  ( -27.09125059358653331, 0.5611156659263027979, -2.243253600381625024 ) ) ;
#9541=CARTESIAN_POINT ( 'NONE',  ( -27.09364415740217424, 2.313349100776208811, -0.1694361397562743343 ) ) ;
#9549=CARTESIAN_POINT ( 'NONE',  ( 2.000000000000001776, -6.201547234537033937, 2.820401998297862978 ) ) ;
#9553=DIRECTION ( 'NONE',  ( 0.000000000000000000, 0.9985334138511239299, -0.05413890858541457046 ) ) ;
#9556=EDGE_CURVE ( 'NONE', #16234, #8848, #30823, .T. ) ;
#9563=CARTESIAN_POINT ( 'NONE',  ( -27.10719052120871098, -1.714424047991075506, -1.622102031466694072 ) ) ;
#9578=CARTESIAN_POINT ( 'NONE',  ( 2.000000000000001776, -3.859771122242995123, -5.613913289150092467 ) ) ;
#9587=DIRECTION ( 'NONE',  ( 0.000000000000000000, 0.1081190184239352453, 0.9941379571543603744 ) ) ;
#9590=DIRECTION ( 'NONE',  ( 0.000000000000000000, -0.4198891015602527754, -0.9075754196709624466 ) ) ;
#9608=LINE ( 'NONE', #63836, #35284 ) ;
#9627=VECTOR ( 'NONE', #18800, 1000.000000000000114 ) ;
#9631=FACE_OUTER_BOUND ( 'NONE', #13253, .T. ) ;
#9664=EDGE_CURVE ( 'NONE', #33594, #42155, #41294, .T. ) ;
#9675=CIRCLE ( 'NONE', #21368, 7.499999999999988454 ) ;
#9680=( BOUNDED_SURFACE ( )  B_SPLINE_SURFACE ( 3, 1, ( 
 ( #51645, #60616 ),
 ( #26348, #46635 ),
 ( #1089, #45646 ),
 ( #11069, #100 ) ),
 .UNSPECIFIED., .F., .F., .F. ) 
 B_SPLINE_SURFACE_WITH_KNOTS ( ( 4, 4 ),
 ( 2, 2 ),
 ( 0.000000000000000000, 1.000000000000000000 ),
 ( 0.000000000000000000, 1.000000000000000000 ),
 .UNSPECIFIED. ) 
 GEOMETRIC_REPRESENTATION_ITEM ( )  RATIONAL_B_SPLINE_SURFACE ( (
 ( 1.000000000000000000, 1.000000000000000000),
 ( 0.9932032654565553509, 0.8386279382598740284),
 ( 0.9932032654565553509, 0.8386279382598740284),
 ( 1.000000000000000000, 1.000000000000000000) ) ) 
 REPRESENTATION_ITEM ( '' )  SURFACE ( )  );
#9685=CARTESIAN_POINT ( 'NONE',  ( 0.000000000000000000, 5.585096664091999230, -4.113602740025892324 ) ) ;
#9687=CIRCLE ( 'NONE', #58574, 7.499999999999988454 ) ;
#9689=VERTEX_POINT ( 'NONE', #32306 ) ;
#9697=CARTESIAN_POINT ( 'NONE',  ( 2.000000000000001776, -1.225832621831887792, 6.827324998361543607 ) ) ;
#9698=ORIENTED_EDGE ( 'NONE', *, *, #9218, .T. ) ;
#9703=CARTESIAN_POINT ( 'NONE',  ( -27.08702828306202193, 1.639744581306266769, 1.612407531673525796 ) ) ;
#9706=DIRECTION ( 'NONE',  ( -1.000000000000000000, 0.000000000000000000, 0.000000000000000000 ) ) ;
#9709=VERTEX_POINT ( 'NONE', #7357 ) ;
#9712=DIRECTION ( 'NONE',  ( 0.000000000000000000, -0.9289767198167949713, 0.3701381553399054614 ) ) ;
#9718=AXIS2_PLACEMENT_3D ( 'NONE', #38804, #59101, #13512 ) ;
#9722=DIRECTION ( 'NONE',  ( -1.000000000000000000, 0.000000000000000000, 0.000000000000000000 ) ) ;
#9723=ORIENTED_EDGE ( 'NONE', *, *, #29247, .T. ) ;
#9726=ORIENTED_EDGE ( 'NONE', *, *, #10190, .T. ) ;
#9732=AXIS2_PLACEMENT_3D ( 'NONE', #10861, #51114, #46130 ) ;
#9737=EDGE_CURVE ( 'NONE', #33077, #33641, #43261, .T. ) ;
#9738=ORIENTED_EDGE ( 'NONE', *, *, #16641, .T. ) ;
#9740=AXIS2_PLACEMENT_3D ( 'NONE', #25021, #9706, #26005 ) ;
#9745=CIRCLE ( 'NONE', #8719, 2.899999999999994582 ) ;
#9748=AXIS2_PLACEMENT_3D ( 'NONE', #32053, #1820, #6475 ) ;
#9754=ADVANCED_FACE ( 'NONE', ( #8688 ), #52264, .F. ) ;
#9766=CARTESIAN_POINT ( 'NONE',  ( -22.28856623400852399, 3.573466130470489333, -1.018212315222179143 ) ) ;
#9767=VERTEX_POINT ( 'NONE', #49590 ) ;
#9785=VERTEX_POINT ( 'NONE', #40235 ) ;
#9789=VERTEX_POINT ( 'NONE', #59554 ) ;
#9795=B_SPLINE_CURVE_WITH_KNOTS ( 'NONE', 3,
 ( #34720, #49717, #4505, #500, #65325, #40047, #14762, #35040, #157, #41035, #44700, #50389, #15440, #56005, #29422, #55019, #20106, #40716, #61318, #25758, #64992, #10441 ),
 .UNSPECIFIED., .F., .F.,
 ( 4, 3, 3, 3, 3, 3, 3, 4 ),
 ( 2.611104600503653083E-18, 4.455945684386675046E-05, 6.636307477204036738E-05, 8.816671873158864485E-05, 0.0001099660380492628885, 0.0001317545563165320791, 0.0001762613022895052613, 0.0001867992666138397820 ),
 .UNSPECIFIED. ) ;
#9802=CARTESIAN_POINT ( 'NONE',  ( -28.66013792860432119, 1.770123732198269240, 0.4872053345171892258 ) ) ;
#9803=VERTEX_POINT ( 'NONE', #9013 ) ;
#9807=DIRECTION ( 'NONE',  ( 0.000000000000000000, 0.000000000000000000, 1.000000000000000000 ) ) ;
#9810=AXIS2_PLACEMENT_3D ( 'NONE', #50162, #14237, #20549 ) ;
#9815=EDGE_LOOP ( 'NONE', ( #43636, #46766, #36136, #7176 ) ) ;
#9823=EDGE_CURVE ( 'NONE', #31241, #2509, #59893, .T. ) ;
#9830=ORIENTED_EDGE ( 'NONE', *, *, #27410, .F. ) ;
#9835=EDGE_CURVE ( 'NONE', #19340, #55219, #14316, .T. ) ;
#9839=VERTEX_POINT ( 'NONE', #35584 ) ;
#9844=EDGE_CURVE ( 'NONE', #18330, #3618, #63100, .T. ) ;
#9848=CARTESIAN_POINT ( 'NONE',  ( -22.30398854582848145, -1.062335901716038977, -3.608860109585141362 ) ) ;
#9859=CARTESIAN_POINT ( 'NONE',  ( -27.10719052120871098, 1.310802520592036391, 1.962717903527646079 ) ) ;
#9862=CARTESIAN_POINT ( 'NONE',  ( 2.000000000000001776, -6.812627895098285258, 2.855765430652660974 ) ) ;
#9870=CARTESIAN_POINT ( 'NONE',  ( 1.000000000000000888, -2.473437528934186780, 7.080403010454960899 ) ) ;
#9871=ADVANCED_FACE ( 'NONE', ( #50577 ), #4362, .T. ) ;
#9879=VECTOR ( 'NONE', #30650, 1000.000000000000000 ) ;
#9881=DIRECTION ( 'NONE',  ( 0.000000000000000000, 0.000000000000000000, 1.000000000000000000 ) ) ;
#9885=CARTESIAN_POINT ( 'NONE',  ( -27.09342121492585065, 0.5565043948850146860, -2.251107617621284529 ) ) ;
#9886=DIRECTION ( 'NONE',  ( 0.000000000000000000, 0.000000000000000000, 1.000000000000000000 ) ) ;
#9893=CARTESIAN_POINT ( 'NONE',  ( -28.67667724226168602, 0.1214114860980525235, 1.888227992976667213 ) ) ;
#9904=LINE ( 'NONE', #55462, #64841 ) ;
#9905=LINE ( 'NONE', #19236, #63154 ) ;
#9918=CARTESIAN_POINT ( 'NONE',  ( 0.000000000000000000, 0.000000000000000000, 0.000000000000000000 ) ) ;
#9923=DIRECTION ( 'NONE',  ( -1.000000000000000000, 0.000000000000000000, 0.000000000000000000 ) ) ;
#9926=CARTESIAN_POINT ( 'NONE',  ( -22.27706089016750113, 2.583072118615372670, 2.622757446538661608 ) ) ;
#9935=CARTESIAN_POINT ( 'NONE',  ( -27.08485414902845179, -0.5917839443963431867, 2.215517476308873412 ) ) ;
#9936=ADVANCED_FACE ( 'NONE', ( #11621 ), #37211, .T. ) ;
#9937=EDGE_LOOP ( 'NONE', ( #10465, #53987, #49166, #53153 ) ) ;
#9942=AXIS2_PLACEMENT_3D ( 'NONE', #63842, #28286, #18324 ) ;
#9949=CARTESIAN_POINT ( 'NONE',  ( -27.10719052120871098, 2.295785794152562787, 0.5475695427849293084 ) ) ;
#9950=DIRECTION ( 'NONE',  ( 0.000000000000000000, 0.9289767198167898643, 0.3701381553399182289 ) ) ;
#9954=ORIENTED_EDGE ( 'NONE', *, *, #33149, .F. ) ;
#9958=CARTESIAN_POINT ( 'NONE',  ( -22.66110217412718342, 4.573370147466346403, -1.880032915665380333 ) ) ;
#9960=CARTESIAN_POINT ( 'NONE',  ( -27.10719052120871098, 1.962717903527675611, -1.310802520592017295 ) ) ;
#9965=ADVANCED_FACE ( 'NONE', ( #59163 ), #47540, .T. ) ;
#9972=CIRCLE ( 'NONE', #55593, 2.899999999999996803 ) ;
#9978=AXIS2_PLACEMENT_3D ( 'NONE', #43785, #3892, #9492 ) ;
#9979=EDGE_CURVE ( 'NONE', #41622, #13578, #36580, .T. ) ;
#9980=ORIENTED_EDGE ( 'NONE', *, *, #28130, .F. ) ;
#9982=DIRECTION ( 'NONE',  ( -1.000000000000000000, 0.000000000000000000, 0.000000000000000000 ) ) ;
#9983=AXIS2_PLACEMENT_3D ( 'NONE', #43310, #23050, #63584 ) ;
#9989=DIRECTION ( 'NONE',  ( 0.000000000000000000, 0.9289767198167898643, 0.3701381553399182289 ) ) ;
#9998=DIRECTION ( 'NONE',  ( -1.000000000000000000, 0.000000000000000000, 0.000000000000000000 ) ) ;
#10011=DIRECTION ( 'NONE',  ( 0.000000000000000000, 0.8835120444460208278, 0.4684084406997939265 ) ) ;
#10017=CARTESIAN_POINT ( 'NONE',  ( -35.04709527796842394, -0.01231589140598780829, -0.001082316405380534530 ) ) ;
#10019=CARTESIAN_POINT ( 'NONE',  ( -22.27834755396594346, 1.162947663292851930, -3.497967921180566986 ) ) ;
#10026=CARTESIAN_POINT ( 'NONE',  ( -27.09364415740217424, -1.303410551736214229, -1.918701019215953929 ) ) ;
#10029=CARTESIAN_POINT ( 'NONE',  ( -22.27384469013076185, 2.985904959940915759, -2.154627400808017956 ) ) ;
#10030=LINE ( 'NONE', #30312, #47053 ) ;
#10032=CARTESIAN_POINT ( 'NONE',  ( 0.000000000000000000, 5.457833520448724940, -4.281014542496488495 ) ) ;
#10037=AXIS2_PLACEMENT_3D ( 'NONE', #30191, #44483, #44823 ) ;
#10038=CARTESIAN_POINT ( 'NONE',  ( -22.27719443589224113, 0.7635131876695160358, 3.601617131804383476 ) ) ;
#10040=CARTESIAN_POINT ( 'NONE',  ( 0.000000000000000000, 0.000000000000000000, 0.000000000000000000 ) ) ;
#10048=CARTESIAN_POINT ( 'NONE',  ( -27.08429572838383947, 1.608131779585724619, 1.632445743623414325 ) ) ;
#10052=AXIS2_PLACEMENT_3D ( 'NONE', #39055, #29409, #59682 ) ;
#10058=CARTESIAN_POINT ( 'NONE',  ( -26.26840407548881018, 3.532089703364137634, 0.2990196765638852838 ) ) ;
#10061=CARTESIAN_POINT ( 'NONE',  ( -27.08506889328344158, -0.2104793012480451475, -2.284141197253904298 ) ) ;
#10063=DIRECTION ( 'NONE',  ( -1.000000000000000000, 0.000000000000000000, 0.000000000000000000 ) ) ;
#10064=VERTEX_POINT ( 'NONE', #33554 ) ;
#10067=EDGE_LOOP ( 'NONE', ( #61829, #56095, #43312, #8765 ) ) ;
#10069=VERTEX_POINT ( 'NONE', #53844 ) ;
#10075=CARTESIAN_POINT ( 'NONE',  ( -27.09030469827880339, -2.221523195520537008, 0.6314616953885225925 ) ) ;
#10077=EDGE_CURVE ( 'NONE', #42334, #34961, #32331, .T. ) ;
#10079=DIRECTION ( 'NONE',  ( 1.000000000000000000, 0.000000000000000000, 0.000000000000000000 ) ) ;
#10090=CARTESIAN_POINT ( 'NONE',  ( -22.66110217412718697, 2.319520136975695479, 4.366928509133826353 ) ) ;
#10092=VERTEX_POINT ( 'NONE', #9239 ) ;
#10103=CARTESIAN_POINT ( 'NONE',  ( -22.27722015946439171, 3.455127654605130161, 1.271715168852039168 ) ) ;
#10117=FACE_OUTER_BOUND ( 'NONE', #27229, .T. ) ;
#10125=DIRECTION ( 'NONE',  ( 0.000000000000000000, -0.9289767198167949713, 0.3701381553399054614 ) ) ;
#10128=VERTEX_POINT ( 'NONE', #29847 ) ;
#10132=CARTESIAN_POINT ( 'NONE',  ( -35.04643116707788408, 0.007621814750502498015, 0.009511118309123156589 ) ) ;
#10142=EDGE_CURVE ( 'NONE', #42915, #57650, #8999, .T. ) ;
#10146=CARTESIAN_POINT ( 'NONE',  ( -22.27706485742869091, 0.9832726768967819941, -3.547445275915930285 ) ) ;
#10153=CARTESIAN_POINT ( 'NONE',  ( 1.000000000000000888, -7.203928197742085260, -2.086484728383230181 ) ) ;
#10158=CARTESIAN_POINT ( 'NONE',  ( -22.35190811654611664, 2.161847148103716698, 3.252894036332493855 ) ) ;
#10176=CARTESIAN_POINT ( 'NONE',  ( -22.71097035706203116, 4.965150228107710006, 0.4203397252017151420 ) ) ;
#10177=CARTESIAN_POINT ( 'NONE',  ( -22.28546858134833286, -1.005093225210831553, -3.567529619157811638 ) ) ;
#10188=VECTOR ( 'NONE', #28334, 1000.000000000000000 ) ;
#10190=EDGE_CURVE ( 'NONE', #14144, #53550, #9905, .T. ) ;
#10200=EDGE_CURVE ( 'NONE', #56470, #24059, #38714, .T. ) ;
#10205=DIRECTION ( 'NONE',  ( -1.000000000000000000, 0.000000000000000000, 0.000000000000000000 ) ) ;
#10215=CARTESIAN_POINT ( 'NONE',  ( 2.000000000000001776, 0.000000000000000000, 0.000000000000000000 ) ) ;
#10216=FACE_OUTER_BOUND ( 'NONE', #7473, .T. ) ;
#10219=ORIENTED_EDGE ( 'NONE', *, *, #19673, .T. ) ;
#10226=DIRECTION ( 'NONE',  ( 1.000000000000000000, -0.000000000000000000, -0.000000000000000000 ) ) ;
#10229=VERTEX_POINT ( 'NONE', #42346 ) ;
#10231=AXIS2_PLACEMENT_3D ( 'NONE', #37756, #8474, #54033 ) ;
#10233=ORIENTED_EDGE ( 'NONE', *, *, #5397, .F. ) ;
#10235=CARTESIAN_POINT ( 'NONE',  ( -22.30986928587821794, -3.771068405887398889, 0.2539257557460667392 ) ) ;
#10244=EDGE_CURVE ( 'NONE', #42103, #57333, #31179, .T. ) ;
#10251=CARTESIAN_POINT ( 'NONE',  ( -26.43258404273187168, -3.148308537883188318, 1.478864324198218450 ) ) ;
#10260=EDGE_LOOP ( 'NONE', ( #56909, #24664, #6707, #9472 ) ) ;
#10267=CARTESIAN_POINT ( 'NONE',  ( 2.000000000000001776, -6.201547234536999298, -2.820401998297984214 ) ) ;
#10274=CARTESIAN_POINT ( 'NONE',  ( -27.08579483061178905, 1.879952013013922674, -1.318128465626136059 ) ) ;
#10275=VERTEX_POINT ( 'NONE', #43027 ) ;
#10276=CARTESIAN_POINT ( 'NONE',  ( -22.27721038036499834, 3.635620891621742512, -0.5802312083658389685 ) ) ;
#10283=CARTESIAN_POINT ( 'NONE',  ( -27.10512513516277977, -2.289566223068223216, -0.5469390009826222698 ) ) ;
#10301=ADVANCED_FACE ( 'NONE', ( #57692 ), #47700, .T. ) ;
#10306=EDGE_CURVE ( 'NONE', #6062, #44602, #48321, .T. ) ;
#10312=CARTESIAN_POINT ( 'NONE',  ( -22.27384469013076185, 1.508555848190777926, -3.358914544760239540 ) ) ;
#10320=ORIENTED_EDGE ( 'NONE', *, *, #8646, .T. ) ;
#10328=AXIS2_PLACEMENT_3D ( 'NONE', #1564, #31469, #51769 ) ;
#10329=LINE ( 'NONE', #15639, #27605 ) ;
#10340=CARTESIAN_POINT ( 'NONE',  ( 2.000000000000001776, -6.164400007374764456, -2.900694413976575792 ) ) ;
#10341=ORIENTED_EDGE ( 'NONE', *, *, #9103, .T. ) ;
#10347=CARTESIAN_POINT ( 'NONE',  ( -22.39032720737627002, 1.170177197944874958, 3.847057950743270283 ) ) ;
#10351=FACE_OUTER_BOUND ( 'NONE', #44024, .T. ) ;
#10356=CARTESIAN_POINT ( 'NONE',  ( 1.000000000000000888, 2.315790869867174528, -7.133520354428103616 ) ) ;
#10359=ORIENTED_EDGE ( 'NONE', *, *, #30338, .T. ) ;
#10361=ORIENTED_EDGE ( 'NONE', *, *, #65354, .T. ) ;
#10366=DIRECTION ( 'NONE',  ( 0.000000000000000000, 0.000000000000000000, 1.000000000000000000 ) ) ;
#10370=CARTESIAN_POINT ( 'NONE',  ( -27.08429572838383947, -0.2296550094122856711, -2.279961732801603080 ) ) ;
#10381=ORIENTED_EDGE ( 'NONE', *, *, #21842, .T. ) ;
#10385=CARTESIAN_POINT ( 'NONE',  ( -22.29677679919927868, 1.633785040807725686, -3.364642266483119482 ) ) ;
#10387=ORIENTED_EDGE ( 'NONE', *, *, #48130, .F. ) ;
#10390=DIRECTION ( 'NONE',  ( -1.000000000000000000, 0.000000000000000000, 0.000000000000000000 ) ) ;
#10392=FACE_OUTER_BOUND ( 'NONE', #21931, .T. ) ;
#10394=CARTESIAN_POINT ( 'NONE',  ( 0.000000000000000000, 0.000000000000000000, 0.000000000000000000 ) ) ;
#10397=ADVANCED_FACE ( 'NONE', ( #34366 ), #24381, .T. ) ;
#10404=DIRECTION ( 'NONE',  ( -1.000000000000000000, 0.000000000000000000, 0.000000000000000000 ) ) ;
#10411=CARTESIAN_POINT ( 'NONE',  ( 0.000000000000000000, 6.812627895098307462, -0.04423456934727655609 ) ) ;
#10412=ORIENTED_EDGE ( 'NONE', *, *, #38275, .T. ) ;
#10425=ORIENTED_EDGE ( 'NONE', *, *, #35309, .F. ) ;
#10428=CARTESIAN_POINT ( 'NONE',  ( 2.000000000000001776, 1.956810415765277922, -6.654767106875532967 ) ) ;
#10440=ORIENTED_EDGE ( 'NONE', *, *, #20784, .F. ) ;
#10441=CARTESIAN_POINT ( 'NONE',  ( -22.27706485742869091, -0.9832726768967594566, 3.547445275915920071 ) ) ;
#10450=EDGE_CURVE ( 'NONE', #43107, #1369, #3074, .T. ) ;
#10463=CARTESIAN_POINT ( 'NONE',  ( 0.000000000000000000, 0.000000000000000000, 0.000000000000000000 ) ) ;
#10465=ORIENTED_EDGE ( 'NONE', *, *, #998, .F. ) ;
#10468=DIRECTION ( 'NONE',  ( -1.000000000000000000, 0.000000000000000000, 0.000000000000000000 ) ) ;
#10474=EDGE_CURVE ( 'NONE', #24723, #14755, #28084, .T. ) ;
#10497=CARTESIAN_POINT ( 'NONE',  ( 0.000000000000000000, 6.338823199656684615, 2.816798305433696470 ) ) ;
#10499=CARTESIAN_POINT ( 'NONE',  ( 2.000000000000001776, 0.000000000000000000, 0.000000000000000000 ) ) ;
#10504=CARTESIAN_POINT ( 'NONE',  ( -22.27706485742869091, -0.3729136217355977778, -3.662257305743823022 ) ) ;
#10515=LINE ( 'NONE', #60411, #49196 ) ;
#10516=CIRCLE ( 'NONE', #41317, 2.899999999999994582 ) ;
#10519=ORIENTED_EDGE ( 'NONE', *, *, #59374, .F. ) ;
#10523=ORIENTED_EDGE ( 'NONE', *, *, #6916, .T. ) ;
#10529=CARTESIAN_POINT ( 'NONE',  ( -27.09150307427447757, 2.306459590995634468, -0.1754204729056216827 ) ) ;
#10530=CARTESIAN_POINT ( 'NONE',  ( -27.10128162969832744, 1.032914450114655436, -2.102429195189573718 ) ) ;
#10533=CARTESIAN_POINT ( 'NONE',  ( -35.05012975565874456, -0.01296790604420075023, -0.005092487515917999003 ) ) ;
#10536=AXIS2_PLACEMENT_3D ( 'NONE', #9578, #3336, #43876 ) ;
#10540=DIRECTION ( 'NONE',  ( -1.000000000000000000, 0.000000000000000000, 0.000000000000000000 ) ) ;
#10548=EDGE_LOOP ( 'NONE', ( #33613, #54630, #65716, #39387 ) ) ;
#10550=EDGE_CURVE ( 'NONE', #13578, #18352, #24725, .T. ) ;
#10551=ORIENTED_EDGE ( 'NONE', *, *, #27123, .T. ) ;
#10559=CARTESIAN_POINT ( 'NONE',  ( -22.27384469013076185, 2.985904959940915759, -2.154627400808017956 ) ) ;
#10560=CARTESIAN_POINT ( 'NONE',  ( 0.000000000000000000, 4.570217215903443986, -5.218059682435596258 ) ) ;
#10561=CARTESIAN_POINT ( 'NONE',  ( 0.000000000000000000, -3.230174184210014232, -5.998318953995379843 ) ) ;
#10564=CIRCLE ( 'NONE', #61540, 2.899999999999995914 ) ;
#10565=ADVANCED_FACE ( 'NONE', ( #45006 ), #14713, .T. ) ;
#10574=CYLINDRICAL_SURFACE ( 'NONE', #45868, 2.899999999999994582 ) ;
#10576=CARTESIAN_POINT ( 'NONE',  ( 0.000000000000000000, 4.604744433234674972, 5.919993978425482695 ) ) ;
#10577=AXIS2_PLACEMENT_3D ( 'NONE', #20002, #15344, #4062 ) ;
#10587=CARTESIAN_POINT ( 'NONE',  ( -27.35552965826137140, 2.810569013793760007, -1.320216934008374920 ) ) ;
#10595=CARTESIAN_POINT ( 'NONE',  ( -22.27718150314433387, 2.479231311682841277, 2.721613812022944945 ) ) ;
#10599=CARTESIAN_POINT ( 'NONE',  ( -22.27721056931765631, 3.610969226755196715, -0.7178530073137425749 ) ) ;
#10602=DIRECTION ( 'NONE',  ( -1.000000000000000000, 0.000000000000000000, 0.000000000000000000 ) ) ;
#10609=VERTEX_POINT ( 'NONE', #55648 ) ;
#10610=VERTEX_POINT ( 'NONE', #54973 ) ;
#10614=ADVANCED_FACE ( 'NONE', ( #40005 ), #60286, .T. ) ;
#10615=AXIS2_PLACEMENT_3D ( 'NONE', #16704, #51330, #6415 ) ;
#10620=ORIENTED_EDGE ( 'NONE', *, *, #43943, .F. ) ;
#10624=CARTESIAN_POINT ( 'NONE',  ( 0.000000000000000000, -0.8935325819928070512, -7.446583077151393226 ) ) ;
#10633=VERTEX_POINT ( 'NONE', #49995 ) ;
#10650=EDGE_CURVE ( 'NONE', #1853, #1800, #40899, .T. ) ;
#10662=VERTEX_POINT ( 'NONE', #22017 ) ;
#10666=DIRECTION ( 'NONE',  ( -1.000000000000000000, 0.000000000000000000, 0.000000000000000000 ) ) ;
#10671=ORIENTED_EDGE ( 'NONE', *, *, #9100, .T. ) ;
#10675=VERTEX_POINT ( 'NONE', #31345 ) ;
#10679=DIRECTION ( 'NONE',  ( -1.000000000000000000, 0.000000000000000000, 0.000000000000000000 ) ) ;
#10687=ORIENTED_EDGE ( 'NONE', *, *, #43508, .F. ) ;
#10688=DIRECTION ( 'NONE',  ( -1.000000000000000000, 0.000000000000000000, 0.000000000000000000 ) ) ;
#10695=ADVANCED_FACE ( 'NONE', ( #41964 ), #21363, .T. ) ;
#10700=CARTESIAN_POINT ( 'NONE',  ( 1.000000000000000888, 7.387287142779352500, 1.295372019972176103 ) ) ;
#10704=VERTEX_POINT ( 'NONE', #16387 ) ;
#10712=CARTESIAN_POINT ( 'NONE',  ( -27.10719052120871098, -2.261993590776032459, 0.6736837626858792616 ) ) ;
#10713=CARTESIAN_POINT ( 'NONE',  ( -35.04582288351658548, 0.01107592729722563576, 0.006225574250530754340 ) ) ;
#10722=ORIENTED_EDGE ( 'NONE', *, *, #27939, .F. ) ;
#10728=DIRECTION ( 'NONE',  ( -1.000000000000000000, 0.000000000000000000, 0.000000000000000000 ) ) ;
#10734=AXIS2_PLACEMENT_3D ( 'NONE', #7489, #2191, #61462 ) ;
#10736=DIRECTION ( 'NONE',  ( 0.9606638835031802159, 0.2535400141108153371, 0.1133241553124300777 ) ) ;
#10746=ORIENTED_EDGE ( 'NONE', *, *, #63625, .T. ) ;
#10749=CARTESIAN_POINT ( 'NONE',  ( -22.27710395300133683, 3.562137928983405644, -0.9291085174899351706 ) ) ;
#10750=ORIENTED_EDGE ( 'NONE', *, *, #51177, .T. ) ;
#10754=EDGE_LOOP ( 'NONE', ( #1720, #1426, #29249, #23632 ) ) ;
#10755=VERTEX_POINT ( 'NONE', #11698 ) ;
#10756=CIRCLE ( 'NONE', #31975, 2.899999999999995026 ) ;
#10762=CARTESIAN_POINT ( 'NONE',  ( -22.27878402819508352, -3.558531829368155375, 0.9624056734348110931 ) ) ;
#10773=CARTESIAN_POINT ( 'NONE',  ( -27.35552965826136429, -2.810569013793742688, 1.320216934008381804 ) ) ;
#10776=B_SPLINE_CURVE_WITH_KNOTS ( 'NONE', 3,
 ( #5750, #61564, #65566, #15371, #50637, #20036, #5083, #25345, #40301, #20695, #26016, #35314, #15678, #30646, #50958, #65261 ),
 .UNSPECIFIED., .F., .F.,
 ( 4, 3, 3, 3, 3, 4 ),
 ( 0.000000000000000000, 6.991367980366403740E-05, 0.0001398269368981361522, 0.0002097400188389093899, 0.0002811534801551363776, 0.0003526297678872490952 ),
 .UNSPECIFIED. ) ;
#10777=DIRECTION ( 'NONE',  ( -1.000000000000000000, 0.000000000000000000, 0.000000000000000000 ) ) ;
#10782=EDGE_LOOP ( 'NONE', ( #21133, #52625, #46600, #36797 ) ) ;
#10783=ADVANCED_FACE ( 'NONE', ( #36326 ), #31980, .T. ) ;
#10787=ORIENTED_EDGE ( 'NONE', *, *, #41177, .T. ) ;
#10792=VERTEX_POINT ( 'NONE', #52627 ) ;
#10794=EDGE_CURVE ( 'NONE', #44565, #32207, #52173, .T. ) ;
#10795=FACE_OUTER_BOUND ( 'NONE', #32513, .T. ) ;
#10798=DIRECTION ( 'NONE',  ( -1.000000000000000000, 0.000000000000000000, 0.000000000000000000 ) ) ;
#10803=FACE_OUTER_BOUND ( 'NONE', #349, .T. ) ;
#10806=CARTESIAN_POINT ( 'NONE',  ( -35.04709527796842394, -0.01117341439755767385, 0.005292201869320362073 ) ) ;
#10810=CARTESIAN_POINT ( 'NONE',  ( 2.000000000000001776, 0.2704997240206042930, -6.931223712253475000 ) ) ;
#10812=CARTESIAN_POINT ( 'NONE',  ( -22.38932658256920760, 2.201197575855971866, 3.361598243548623799 ) ) ;
#10819=DIRECTION ( 'NONE',  ( 0.000000000000000000, 0.000000000000000000, 1.000000000000000000 ) ) ;
#10837=AXIS2_PLACEMENT_3D ( 'NONE', #46315, #10079, #11375 ) ;
#10857=DIRECTION ( 'NONE',  ( 0.000000000000000000, 0.000000000000000000, 1.000000000000000000 ) ) ;
#10861=CARTESIAN_POINT ( 'NONE',  ( -10.00000000000000178, 0.000000000000000000, 0.000000000000000000 ) ) ;
#10863=DIRECTION ( 'NONE',  ( 0.000000000000000000, -0.8835120444460178302, -0.4684084406997996441 ) ) ;
#10865=( BOUNDED_SURFACE ( )  B_SPLINE_SURFACE ( 3, 1, ( 
 ( #1082, #2667 ),
 ( #36651, #58502 ),
 ( #10713, #57266 ),
 ( #21353, #6399 ) ),
 .UNSPECIFIED., .F., .F., .F. ) 
 B_SPLINE_SURFACE_WITH_KNOTS ( ( 4, 4 ),
 ( 2, 2 ),
 ( 0.000000000000000000, 1.000000000000000000 ),
 ( 0.000000000000000000, 1.000000000000000000 ),
 .UNSPECIFIED. ) 
 GEOMETRIC_REPRESENTATION_ITEM ( )  RATIONAL_B_SPLINE_SURFACE ( (
 ( 1.000000000000000000, 1.000000000000000000),
 ( 0.9257577194822556033, 0.9980522942447415113),
 ( 0.9257577194822556033, 0.9980522942447415113),
 ( 1.000000000000000000, 1.000000000000000000) ) ) 
 REPRESENTATION_ITEM ( '' )  SURFACE ( )  );
#10867=CARTESIAN_POINT ( 'NONE',  ( -22.27711653538342773, -1.465933162149059665, 3.377206745424981449 ) ) ;
#10869=EDGE_LOOP ( 'NONE', ( #44542, #21197, #50305, #36012 ) ) ;
#10870=CARTESIAN_POINT ( 'NONE',  ( 2.000000000000001776, -5.457833520448679643, 4.281014542496493824 ) ) ;
#10871=ORIENTED_EDGE ( 'NONE', *, *, #47635, .T. ) ;
#10872=CYLINDRICAL_SURFACE ( 'NONE', #59300, 2.899999999999994582 ) ;
#10873=CARTESIAN_POINT ( 'NONE',  ( -27.08429572838383947, 0.6096735944848206135, -2.208905845566032866 ) ) ;
#10877=CIRCLE ( 'NONE', #51253, 2.899999999999995914 ) ;
#10881=DIRECTION ( 'NONE',  ( -1.000000000000000000, 0.000000000000000000, 0.000000000000000000 ) ) ;
#10895=ORIENTED_EDGE ( 'NONE', *, *, #33665, .F. ) ;
#10900=CARTESIAN_POINT ( 'NONE',  ( 2.000000000000001776, -1.058508696395003890, 6.730038252034888480 ) ) ;
#10901=LINE ( 'NONE', #57786, #35214 ) ;
#10909=CARTESIAN_POINT ( 'NONE',  ( -22.28169757117799321, 2.633129923220830282, 2.592369810060362934 ) ) ;
#10921=CARTESIAN_POINT ( 'NONE',  ( -22.27384469013075829, -3.564715702084494175, 0.9224151068931482067 ) ) ;
#10926=ORIENTED_EDGE ( 'NONE', *, *, #50048, .F. ) ;
#10935=VECTOR ( 'NONE', #42411, 1000.000000000000000 ) ;
#10940=EDGE_LOOP ( 'NONE', ( #30979, #5430, #7222, #60646 ) ) ;
#10946=CARTESIAN_POINT ( 'NONE',  ( -22.27716857039623477, 3.591587580808003555, -0.8090275962000442744 ) ) ;
#10948=LINE ( 'NONE', #4676, #48241 ) ;
#10956=EDGE_CURVE ( 'NONE', #14997, #16004, #29609, .T. ) ;
#10958=CARTESIAN_POINT ( 'NONE',  ( 2.000000000000001776, -6.796153407501448029, 1.388283512725787761 ) ) ;
#10961=ORIENTED_EDGE ( 'NONE', *, *, #9737, .T. ) ;
#10962=EDGE_LOOP ( 'NONE', ( #56045, #55764, #16608, #48414 ) ) ;
#10971=ORIENTED_EDGE ( 'NONE', *, *, #9835, .F. ) ;
#10973=ORIENTED_EDGE ( 'NONE', *, *, #48425, .F. ) ;
#10974=DIRECTION ( 'NONE',  ( 0.000000000000000000, 0.6051742151937661296, -0.7960930657056429771 ) ) ;
#10980=AXIS2_PLACEMENT_3D ( 'NONE', #31281, #21639, #57210 ) ;
#10986=AXIS2_PLACEMENT_3D ( 'NONE', #49331, #64896, #50617 ) ;
#10997=CYLINDRICAL_SURFACE ( 'NONE', #10980, 2.899999999999994582 ) ;
#11004=CIRCLE ( 'NONE', #49236, 2.899999999999994138 ) ;
#11005=AXIS2_PLACEMENT_3D ( 'NONE', #20690, #14050, #30641 ) ;
#11010=CARTESIAN_POINT ( 'NONE',  ( -22.39032720737627358, 3.847057950743288490, -1.170177197944845426 ) ) ;
#11014=AXIS2_PLACEMENT_3D ( 'NONE', #6245, #35809, #46162 ) ;
#11019=EDGE_LOOP ( 'NONE', ( #34898, #43294, #50887, #28961 ) ) ;
#11022=CARTESIAN_POINT ( 'NONE',  ( -22.27718150314433387, 0.7862703917636705286, 3.596602356343891138 ) ) ;
#11025=DIRECTION ( 'NONE',  ( -1.000000000000000000, 0.000000000000000000, 0.000000000000000000 ) ) ;
#11028=CARTESIAN_POINT ( 'NONE',  ( -22.27945548916780183, 0.3299677273100789510, 3.673577025288749187 ) ) ;
#11030=VECTOR ( 'NONE', #52451, 1000.000000000000000 ) ;
#11037=DIRECTION ( 'NONE',  ( -1.000000000000000000, 0.000000000000000000, 0.000000000000000000 ) ) ;
#11038=ORIENTED_EDGE ( 'NONE', *, *, #29967, .T. ) ;
#11050=DIRECTION ( 'NONE',  ( -1.000000000000000000, 0.000000000000000000, 0.000000000000000000 ) ) ;
#11051=ORIENTED_EDGE ( 'NONE', *, *, #55031, .F. ) ;
#11061=CARTESIAN_POINT ( 'NONE',  ( -22.66110217412718342, 3.020638270782550094, -3.914841338650321578 ) ) ;
#11062=VECTOR ( 'NONE', #48326, 1000.000000000000000 ) ;
#11069=CARTESIAN_POINT ( 'NONE',  ( -35.04709527796842394, -0.01120703303052195121, 0.005220632200989699934 ) ) ;
#11074=CIRCLE ( 'NONE', #39731, 2.899999999999995914 ) ;
#11077=CARTESIAN_POINT ( 'NONE',  ( -35.05012975565874456, 0.01039213056759654037, -0.009279204628456355630 ) ) ;
#11080=DIRECTION ( 'NONE',  ( 0.000000000000000000, 0.4198891015602592147, 0.9075754196709596711 ) ) ;
#11083=CARTESIAN_POINT ( 'NONE',  ( 0.000000000000000000, -6.796153407501448029, 1.388283512725787761 ) ) ;
#11110=ORIENTED_EDGE ( 'NONE', *, *, #62578, .F. ) ;
#11118=ORIENTED_EDGE ( 'NONE', *, *, #46953, .T. ) ;
#11120=ORIENTED_EDGE ( 'NONE', *, *, #36006, .F. ) ;
#11128=CARTESIAN_POINT ( 'NONE',  ( 2.000000000000001776, 6.936109781200682889, 2.853135311045038591 ) ) ;
#11132=DIRECTION ( 'NONE',  ( -1.000000000000000000, 0.000000000000000000, 0.000000000000000000 ) ) ;
#11135=EDGE_CURVE ( 'NONE', #38796, #60499, #41971, .T. ) ;
#11138=CARTESIAN_POINT ( 'NONE',  ( -27.08429572838383947, 0.2296550094123047669, 2.279961732801582208 ) ) ;
#11147=VERTEX_POINT ( 'NONE', #27576 ) ;
#11149=CARTESIAN_POINT ( 'NONE',  ( -22.28023996335807766, -3.022323476748280502, 2.118259050016073175 ) ) ;
#11150=( NAMED_UNIT ( * ) SI_UNIT ( $, .STERADIAN. ) SOLID_ANGLE_UNIT ( ) );
#11155=CARTESIAN_POINT ( 'NONE',  ( -27.08426504710140392, -2.202478235133281892, -0.6326154899769481643 ) ) ;
#11158=LINE ( 'NONE', #6178, #12279 ) ;
#11178=CARTESIAN_POINT ( 'NONE',  ( -23.41523303002441736, -4.681453266967030125, -0.3963225057405078133 ) ) ;
#11183=DIRECTION ( 'NONE',  ( -1.000000000000000000, 0.000000000000000000, 0.000000000000000000 ) ) ;
#11190=DIRECTION ( 'NONE',  ( -1.000000000000000000, 0.000000000000000000, 0.000000000000000000 ) ) ;
#11196=DIRECTION ( 'NONE',  ( -1.000000000000000000, 0.000000000000000000, 0.000000000000000000 ) ) ;
#11224=DIRECTION ( 'NONE',  ( -1.000000000000000000, 0.000000000000000000, 0.000000000000000000 ) ) ;
#11226=VECTOR ( 'NONE', #42122, 1000.000000000000000 ) ;
#11232=CARTESIAN_POINT ( 'NONE',  ( 2.000000000000001776, 3.341639490130849488, -6.078525953551423555 ) ) ;
#11239=CARTESIAN_POINT ( 'NONE',  ( -22.31328051695926007, 1.671726071983979711, -3.401210163132561082 ) ) ;
#11240=CIRCLE ( 'NONE', #39908, 2.899999999999996803 ) ;
#11245=ORIENTED_EDGE ( 'NONE', *, *, #40574, .T. ) ;
#11246=CARTESIAN_POINT ( 'NONE',  ( -27.08430792439084556, -0.6005833784278348242, 2.211452765398279841 ) ) ;
#11249=DIRECTION ( 'NONE',  ( 0.000000000000000000, 0.000000000000000000, 1.000000000000000000 ) ) ;
#11258=FACE_OUTER_BOUND ( 'NONE', #59544, .T. ) ;
#11262=CARTESIAN_POINT ( 'NONE',  ( -35.04643116707788408, -0.008094444324497490628, -0.009112266603826177369 ) ) ;
#11266=CARTESIAN_POINT ( 'NONE',  ( 0.000000000000000000, -3.979254915827311390, -5.681598592373819478 ) ) ;
#11273=EDGE_CURVE ( 'NONE', #50124, #53881, #46472, .T. ) ;
#11283=VERTEX_POINT ( 'NONE', #36501 ) ;
#11292=CARTESIAN_POINT ( 'NONE',  ( 2.000000000000001776, 0.000000000000000000, 0.000000000000000000 ) ) ;
#11299=AXIS2_PLACEMENT_3D ( 'NONE', #63561, #49610, #23346 ) ;
#11300=ORIENTED_EDGE ( 'NONE', *, *, #12249, .F. ) ;
#11325=CARTESIAN_POINT ( 'NONE',  ( -22.27384469013076185, -3.663183248998797659, 0.3730095848193237251 ) ) ;
#11327=VECTOR ( 'NONE', #49091, 1000.000000000000227 ) ;
#11335=DIRECTION ( 'NONE',  ( -1.000000000000000000, 0.000000000000000000, 0.000000000000000000 ) ) ;
#11347=CARTESIAN_POINT ( 'NONE',  ( -22.30986928587821794, 0.2539257557460806169, 3.771068405887386898 ) ) ;
#11354=CARTESIAN_POINT ( 'NONE',  ( 0.000000000000000000, 2.473437528934141483, 7.080403010454977775 ) ) ;
#11367=ADVANCED_FACE ( 'NONE', ( #36146 ), #56455, .T. ) ;
#11373=CARTESIAN_POINT ( 'NONE',  ( -22.70624764888619751, 2.702761586319180509, -4.501516772829864621 ) ) ;
#11375=DIRECTION ( 'NONE',  ( 0.000000000000000000, 0.000000000000000000, -1.000000000000000000 ) ) ;
#11377=AXIS2_PLACEMENT_3D ( 'NONE', #56923, #1049, #5384 ) ;
#11380=CARTESIAN_POINT ( 'NONE',  ( 0.000000000000000000, -4.604744433234619017, -5.919993978425545755 ) ) ;
#11384=CYLINDRICAL_SURFACE ( 'NONE', #25542, 2.899999999999994582 ) ;
#11394=CARTESIAN_POINT ( 'NONE',  ( 0.000000000000000000, -3.155844197800145690, 6.177028383390419819 ) ) ;
#11402=EDGE_CURVE ( 'NONE', #53826, #25430, #59091, .T. ) ;
#11405=ORIENTED_EDGE ( 'NONE', *, *, #38538, .F. ) ;
#11415=ADVANCED_FACE ( 'NONE', ( #54085 ), #22522, .T. ) ;
#11417=CARTESIAN_POINT ( 'NONE',  ( -22.27706089016750113, -3.562910635974989138, 0.9256273512588475416 ) ) ;
#11418=DIRECTION ( 'NONE',  ( 0.000000000000000000, -0.4198891015602529420, -0.9075754196709625576 ) ) ;
#11424=CARTESIAN_POINT ( 'NONE',  ( 2.000000000000001776, 0.000000000000000000, 0.000000000000000000 ) ) ;
#11425=VERTEX_POINT ( 'NONE', #38118 ) ;
#11430=ORIENTED_EDGE ( 'NONE', *, *, #7984, .F. ) ;
#11439=( BOUNDED_SURFACE ( )  B_SPLINE_SURFACE ( 3, 1, ( 
 ( #13435, #33718 ),
 ( #37733, #43360 ),
 ( #28405, #22784 ),
 ( #63315, #17782 ) ),
 .UNSPECIFIED., .F., .F., .F. ) 
 B_SPLINE_SURFACE_WITH_KNOTS ( ( 4, 4 ),
 ( 2, 2 ),
 ( 0.000000000000000000, 1.000000000000000000 ),
 ( 0.000000000000000000, 1.000000000000000000 ),
 .UNSPECIFIED. ) 
 GEOMETRIC_REPRESENTATION_ITEM ( )  RATIONAL_B_SPLINE_SURFACE ( (
 ( 1.000000000000000000, 1.000000000000000000),
 ( 0.9257577194822556033, 0.9980522942447415113),
 ( 0.9257577194822556033, 0.9980522942447415113),
 ( 1.000000000000000000, 1.000000000000000000) ) ) 
 REPRESENTATION_ITEM ( '' )  SURFACE ( )  );
#11440=ORIENTED_EDGE ( 'NONE', *, *, #37222, .T. ) ;
#11442=ORIENTED_EDGE ( 'NONE', *, *, #60204, .F. ) ;
#11445=CARTESIAN_POINT ( 'NONE',  ( 2.000000000000001776, 6.812627895098307462, 0.04423456934733380197 ) ) ;
#11446=LINE ( 'NONE', #31719, #11759 ) ;
#11447=CARTESIAN_POINT ( 'NONE',  ( -22.28546858134833286, 1.005093225210857977, 3.567529619157783660 ) ) ;
#11451=DIRECTION ( 'NONE',  ( -1.000000000000000000, 0.000000000000000000, 0.000000000000000000 ) ) ;
#11463=CARTESIAN_POINT ( 'NONE',  ( -22.27384469013076185, 2.581192766446265274, 2.625926801827853208 ) ) ;
#11465=ORIENTED_EDGE ( 'NONE', *, *, #17683, .F. ) ;
#11466=CARTESIAN_POINT ( 'NONE',  ( 2.000000000000001776, 0.000000000000000000, 0.000000000000000000 ) ) ;
#11477=CARTESIAN_POINT ( 'NONE',  ( -22.51237073810381162, -0.9543406717316460508, 4.319597983500818472 ) ) ;
#11488=DIRECTION ( 'NONE',  ( -1.000000000000000000, 0.000000000000000000, 0.000000000000000000 ) ) ;
#11498=EDGE_CURVE ( 'NONE', #53160, #21602, #20537, .T. ) ;
#11504=CARTESIAN_POINT ( 'NONE',  ( 2.000000000000001776, 5.997115278587632936, 3.485633455389514523 ) ) ;
#11510=DIRECTION ( 'NONE',  ( -1.000000000000000000, 0.000000000000000000, 0.000000000000000000 ) ) ;
#11513=CYLINDRICAL_SURFACE ( 'NONE', #26192, 7.499999999999988454 ) ;
#11535=DIRECTION ( 'NONE',  ( 0.000000000000000000, 0.000000000000000000, 1.000000000000000000 ) ) ;
#11539=ORIENTED_EDGE ( 'NONE', *, *, #28810, .F. ) ;
#11542=CARTESIAN_POINT ( 'NONE',  ( -27.10422407540562517, 0.1544383239736529800, 2.346206748218693239 ) ) ;
#11544=CIRCLE ( 'NONE', #47541, 2.899999999999996358 ) ;
#11555=DIRECTION ( 'NONE',  ( 0.000000000000000000, -0.9985334138511243740, 0.05413890858540768014 ) ) ;
#11562=ORIENTED_EDGE ( 'NONE', *, *, #59559, .F. ) ;
#11566=CARTESIAN_POINT ( 'NONE',  ( -22.28506771379528573, -1.050362426369332303, -3.575989816848478942 ) ) ;
#11570=ORIENTED_EDGE ( 'NONE', *, *, #178, .T. ) ;
#11579=VECTOR ( 'NONE', #7116, 1000.000000000000000 ) ;
#11585=CARTESIAN_POINT ( 'NONE',  ( -27.20102706715913499, 0.8206313329276082591, 2.512061365242583388 ) ) ;
#11588=VECTOR ( 'NONE', #22080, 1000.000000000000000 ) ;
#11604=AXIS2_PLACEMENT_3D ( 'NONE', #62561, #32314, #47312 ) ;
#11609=FACE_OUTER_BOUND ( 'NONE', #37259, .T. ) ;
#11612=ORIENTED_EDGE ( 'NONE', *, *, #38461, .T. ) ;
#11615=ORIENTED_EDGE ( 'NONE', *, *, #40699, .T. ) ;
#11621=FACE_OUTER_BOUND ( 'NONE', #54711, .T. ) ;
#11622=EDGE_CURVE ( 'NONE', #57938, #50060, #29150, .T. ) ;
#11625=DIRECTION ( 'NONE',  ( 0.000000000000000000, 0.000000000000000000, -1.000000000000000000 ) ) ;
#11631=DIRECTION ( 'NONE',  ( -1.000000000000000000, 0.000000000000000000, 0.000000000000000000 ) ) ;
#11632=CARTESIAN_POINT ( 'NONE',  ( 2.000000000000001776, 0.000000000000000000, 0.000000000000000000 ) ) ;
#11633=EDGE_CURVE ( 'NONE', #59691, #23443, #375, .T. ) ;
#11641=AXIS2_PLACEMENT_3D ( 'NONE', #63822, #38567, #36352 ) ;
#11663=ADVANCED_FACE ( 'NONE', ( #30439 ), #31102, .T. ) ;
#11667=CYLINDRICAL_SURFACE ( 'NONE', #37523, 2.899999999999994582 ) ;
#11674=CARTESIAN_POINT ( 'NONE',  ( -28.67667724226168602, -1.375746547601631287, -1.299025457479364043 ) ) ;
#11679=LINE ( 'NONE', #10700, #15029 ) ;
#11698=CARTESIAN_POINT ( 'NONE',  ( 2.000000000000001776, 3.795144977083718008, -6.468916029978776017 ) ) ;
#11702=CARTESIAN_POINT ( 'NONE',  ( 2.000000000000001776, -0.4129979343797593461, 6.800241778083677247 ) ) ;
#11703=EDGE_CURVE ( 'NONE', #21834, #25882, #47074, .T. ) ;
#11712=CARTESIAN_POINT ( 'NONE',  ( -22.71097035706202405, -2.846599994298329328, 4.089776368546542251 ) ) ;
#11719=CARTESIAN_POINT ( 'NONE',  ( 0.000000000000000000, 4.444115772890121718, 5.163689623839328391 ) ) ;
#11721=ORIENTED_EDGE ( 'NONE', *, *, #30605, .T. ) ;
#11722=DIRECTION ( 'NONE',  ( 0.000000000000000000, 0.2149704402110245716, -0.9766205557100865464 ) ) ;
#11723=ORIENTED_EDGE ( 'NONE', *, *, #63507, .T. ) ;
#11729=CARTESIAN_POINT ( 'NONE',  ( -27.08419797710328680, -1.803546201758814860, 1.413289504316734613 ) ) ;
#11732=CARTESIAN_POINT ( 'NONE',  ( -22.29018399051993526, -3.576688584977250951, 1.024613686459453055 ) ) ;
#11736=ORIENTED_EDGE ( 'NONE', *, *, #14244, .F. ) ;
#11754=DIRECTION ( 'NONE',  ( 0.000000000000000000, 0.5155538571770230671, -0.8568571761675883858 ) ) ;
#11759=VECTOR ( 'NONE', #5846, 1000.000000000000000 ) ;
#11762=EDGE_CURVE ( 'NONE', #18188, #648, #35368, .T. ) ;
#11782=EDGE_CURVE ( 'NONE', #42485, #29713, #5084, .T. ) ;
#11810=CARTESIAN_POINT ( 'NONE',  ( 2.000000000000001776, 0.2704997240205054276, 6.931223712253452796 ) ) ;
#11823=CARTESIAN_POINT ( 'NONE',  ( -22.27721056931765631, 2.427163553894384762, 2.768264578996945335 ) ) ;
#11833=AXIS2_PLACEMENT_3D ( 'NONE', #4600, #898, #9886 ) ;
#11835=( BOUNDED_SURFACE ( )  B_SPLINE_SURFACE ( 3, 1, ( 
 ( #41146, #10559 ),
 ( #36828, #51501 ),
 ( #61428, #15868 ),
 ( #50505, #5269 ) ),
 .UNSPECIFIED., .F., .F., .F. ) 
 B_SPLINE_SURFACE_WITH_KNOTS ( ( 4, 4 ),
 ( 2, 2 ),
 ( 0.000000000000000000, 1.000000000000000000 ),
 ( 0.000000000000000000, 1.000000000000000000 ),
 .UNSPECIFIED. ) 
 GEOMETRIC_REPRESENTATION_ITEM ( )  RATIONAL_B_SPLINE_SURFACE ( (
 ( 1.000000000000000000, 1.000000000000000000),
 ( 0.9257577194822556033, 0.9980522942447415113),
 ( 0.9257577194822556033, 0.9980522942447415113),
 ( 1.000000000000000000, 1.000000000000000000) ) ) 
 REPRESENTATION_ITEM ( '' )  SURFACE ( )  );
#11843=ORIENTED_EDGE ( 'NONE', *, *, #50547, .T. ) ;
#11845=DIRECTION ( 'NONE',  ( 0.000000000000000000, 0.5155538571770169609, 0.8568571761675920495 ) ) ;
#11850=CARTESIAN_POINT ( 'NONE',  ( -22.70624764888619751, 0.08990180771019894157, -5.249808673992000685 ) ) ;
#11853=LINE ( 'NONE', #32132, #11030 ) ;
#11856=ADVANCED_FACE ( 'NONE', ( #40280 ), #20984, .T. ) ;
#11857=ORIENTED_EDGE ( 'NONE', *, *, #20271, .T. ) ;
#11859=CARTESIAN_POINT ( 'NONE',  ( -35.04683013664716640, 0.01235741808124560595, -0.0001018103929620997795 ) ) ;
#11876=CARTESIAN_POINT ( 'NONE',  ( -22.66110217412718342, 1.880032915665426740, 4.573370147466317981 ) ) ;
#11881=DIRECTION ( 'NONE',  ( 0.000000000000000000, -0.1764146379942750642, -0.9843159429275484262 ) ) ;
#11889=CARTESIAN_POINT ( 'NONE',  ( 2.000000000000001776, 6.250523986463984549, 3.007653927006597172 ) ) ;
#11893=AXIS2_PLACEMENT_3D ( 'NONE', #45831, #60796, #40846 ) ;
#11894=EDGE_CURVE ( 'NONE', #9785, #22078, #1901, .T. ) ;
#11895=EDGE_CURVE ( 'NONE', #6336, #26369, #40757, .T. ) ;
#11901=CARTESIAN_POINT ( 'NONE',  ( -27.08417473062937120, -2.249064769433619659, 0.4370481938669266153 ) ) ;
#11911=VERTEX_POINT ( 'NONE', #7327 ) ;
#11916=CARTESIAN_POINT ( 'NONE',  ( -27.09342121492660738, 1.671264186073228464, 1.607500752098841135 ) ) ;
#11921=CYLINDRICAL_SURFACE ( 'NONE', #23383, 7.499999999999988454 ) ;
#11927=ORIENTED_EDGE ( 'NONE', *, *, #52120, .F. ) ;
#11929=ORIENTED_EDGE ( 'NONE', *, *, #13202, .F. ) ;
#11930=ORIENTED_EDGE ( 'NONE', *, *, #34321, .T. ) ;
#11932=DIRECTION ( 'NONE',  ( 0.000000000000000000, 0.000000000000000000, 1.000000000000000000 ) ) ;
#11934=CARTESIAN_POINT ( 'NONE',  ( 2.000000000000001776, 2.469490258309423591, 6.482025155313315246 ) ) ;
#11936=VERTEX_POINT ( 'NONE', #12322 ) ;
#11939=VERTEX_POINT ( 'NONE', #2376 ) ;
#11942=CARTESIAN_POINT ( 'NONE',  ( -22.27715526084302056, 2.930376837866846884, -2.228953214080618750 ) ) ;
#11945=DIRECTION ( 'NONE',  ( 0.000000000000000000, 0.000000000000000000, 1.000000000000000000 ) ) ;
#11949=ADVANCED_FACE ( 'NONE', ( #17664 ), #11667, .T. ) ;
#11964=DIRECTION ( 'NONE',  ( -1.000000000000000000, 0.000000000000000000, 0.000000000000000000 ) ) ;
#11967=CARTESIAN_POINT ( 'NONE',  ( -22.65996813707689128, -2.607318832796680752, 4.069902221062763559 ) ) ;
#11979=CARTESIAN_POINT ( 'NONE',  ( -27.09342121492585065, -1.671264186070199553, -1.607500752098762975 ) ) ;
#11983=CIRCLE ( 'NONE', #16274, 2.899999999999995470 ) ;
#11994=CARTESIAN_POINT ( 'NONE',  ( 1.000000000000000888, 4.472310526050849333, -6.020667617347339906 ) ) ;
#12009=AXIS2_PLACEMENT_3D ( 'NONE', #18872, #58129, #28504 ) ;
#12013=CARTESIAN_POINT ( 'NONE',  ( -27.10719052120871098, -1.714424047991075506, -1.622102031466694072 ) ) ;
#12018=CARTESIAN_POINT ( 'NONE',  ( -22.71097035706202760, 2.118550233809425087, 4.510116093748266053 ) ) ;
#12021=ORIENTED_EDGE ( 'NONE', *, *, #52837, .T. ) ;
#12023=CYLINDRICAL_SURFACE ( 'NONE', #25525, 7.499999999999988454 ) ;
#12037=DIRECTION ( 'NONE',  ( 0.000000000000000000, 0.000000000000000000, 1.000000000000000000 ) ) ;
#12038=ORIENTED_EDGE ( 'NONE', *, *, #20402, .T. ) ;
#12043=EDGE_CURVE ( 'NONE', #64838, #37589, #57504, .T. ) ;
#12050=CARTESIAN_POINT ( 'NONE',  ( -22.29195009621226475, -2.682867222693498643, -2.585382421603447778 ) ) ;
#12052=AXIS2_PLACEMENT_3D ( 'NONE', #25090, #59350, #29101 ) ;
#12055=EDGE_CURVE ( 'NONE', #12311, #61990, #51411, .T. ) ;
#12058=DIRECTION ( 'NONE',  ( -1.000000000000000000, 0.000000000000000000, 0.000000000000000000 ) ) ;
#12066=CARTESIAN_POINT ( 'NONE',  ( -27.08417568107323703, -1.774279301226113548, 1.449568724721383539 ) ) ;
#12068=VERTEX_POINT ( 'NONE', #48580 ) ;
#12081=ORIENTED_EDGE ( 'NONE', *, *, #24004, .F. ) ;
#12092=LINE ( 'NONE', #22393, #25949 ) ;
#12095=ORIENTED_EDGE ( 'NONE', *, *, #50102, .T. ) ;
#12113=DIRECTION ( 'NONE',  ( -1.000000000000000000, 0.000000000000000000, 0.000000000000000000 ) ) ;
#12114=CARTESIAN_POINT ( 'NONE',  ( -22.30986928587821438, -3.138878161034336145, 2.105440358094961883 ) ) ;
#12116=CARTESIAN_POINT ( 'NONE',  ( -22.27384469013076185, 0.3730095848193410446, 3.663183248998782116 ) ) ;
#12127=CARTESIAN_POINT ( 'NONE',  ( -27.35552965826136429, -1.320216934008378473, -2.810569013793753346 ) ) ;
#12129=DIRECTION ( 'NONE',  ( -1.000000000000000000, 0.000000000000000000, 0.000000000000000000 ) ) ;
#12142=DIRECTION ( 'NONE',  ( 0.000000000000000000, 0.1081190184239417817, -0.9941379571543595972 ) ) ;
#12154=CARTESIAN_POINT ( 'NONE',  ( 2.000000000000001776, 0.2704997240206042930, -6.931223712253475000 ) ) ;
#12156=AXIS2_PLACEMENT_3D ( 'NONE', #60695, #29439, #55043 ) ;
#12165=DIRECTION ( 'NONE',  ( -1.000000000000000000, 0.000000000000000000, 0.000000000000000000 ) ) ;
#12170=CARTESIAN_POINT ( 'NONE',  ( -27.08421860617808363, 0.8768262158915796078, -2.116856729767833123 ) ) ;
#12175=ORIENTED_EDGE ( 'NONE', *, *, #10650, .F. ) ;
#12179=FACE_OUTER_BOUND ( 'NONE', #50121, .T. ) ;
#12180=CARTESIAN_POINT ( 'NONE',  ( -22.46225619532221884, 3.586917175123544688, -2.255146441673786750 ) ) ;
#12182=CARTESIAN_POINT ( 'NONE',  ( 2.000000000000001776, 1.018311147294167274, 6.861346417234447159 ) ) ;
#12187=EDGE_LOOP ( 'NONE', ( #31726, #21562, #31215, #56409 ) ) ;
#12189=ORIENTED_EDGE ( 'NONE', *, *, #56288, .F. ) ;
#12192=CARTESIAN_POINT ( 'NONE',  ( -35.04643116707788408, 0.01193867652720184691, -0.002453861112635541408 ) ) ;
#12196=AXIS2_PLACEMENT_3D ( 'NONE', #56680, #50379, #4826 ) ;
#12200=DIRECTION ( 'NONE',  ( -1.000000000000000000, 0.000000000000000000, 0.000000000000000000 ) ) ;
#12201=ORIENTED_EDGE ( 'NONE', *, *, #53760, .F. ) ;
#12208=LINE ( 'NONE', #46478, #51274 ) ;
#12210=CARTESIAN_POINT ( 'NONE',  ( -22.31328051695926007, 2.109671368890633669, 3.148362328073145200 ) ) ;
#12214=DIRECTION ( 'NONE',  ( 0.000000000000000000, 0.000000000000000000, 1.000000000000000000 ) ) ;
#12217=EDGE_LOOP ( 'NONE', ( #30649, #30870, #60462, #10412 ) ) ;
#12218=EDGE_CURVE ( 'NONE', #20405, #22815, #5654, .T. ) ;
#12231=DIRECTION ( 'NONE',  ( 0.000000000000000000, 0.000000000000000000, 1.000000000000000000 ) ) ;
#12232=ORIENTED_EDGE ( 'NONE', *, *, #56078, .T. ) ;
#12233=DIRECTION ( 'NONE',  ( -1.000000000000000000, 0.000000000000000000, 0.000000000000000000 ) ) ;
#12234=DIRECTION ( 'NONE',  ( -1.000000000000000000, 0.000000000000000000, 0.000000000000000000 ) ) ;
#12244=DIRECTION ( 'NONE',  ( 0.000000000000000000, -0.8835120444460271560, 0.4684084406997820471 ) ) ;
#12246=AXIS2_PLACEMENT_3D ( 'NONE', #13162, #38762, #34422 ) ;
#12249=EDGE_CURVE ( 'NONE', #63399, #22582, #10948, .T. ) ;
#12250=CARTESIAN_POINT ( 'NONE',  ( -22.30527770659433173, -1.656864125491245066, 3.381761229713381667 ) ) ;
#12251=ORIENTED_EDGE ( 'NONE', *, *, #32527, .F. ) ;
#12262=CARTESIAN_POINT ( 'NONE',  ( -22.27709082389155171, -2.641652894015110054, 2.563977319272121580 ) ) ;
#12263=CYLINDRICAL_SURFACE ( 'NONE', #36861, 6.936499999999988120 ) ;
#12270=DIRECTION ( 'NONE',  ( -1.000000000000000000, 0.000000000000000000, 0.000000000000000000 ) ) ;
#12274=CARTESIAN_POINT ( 'NONE',  ( 2.000000000000001776, 0.000000000000000000, 0.000000000000000000 ) ) ;
#12277=VERTEX_POINT ( 'NONE', #42164 ) ;
#12279=VECTOR ( 'NONE', #62027, 1000.000000000000000 ) ;
#12293=CARTESIAN_POINT ( 'NONE',  ( -22.59983133926798615, -2.378226455340827439, 3.996991822164148278 ) ) ;
#12303=CARTESIAN_POINT ( 'NONE',  ( -27.08935880048753120, -1.653090150966153526, -1.608762129670104235 ) ) ;
#12311=VERTEX_POINT ( 'NONE', #41857 ) ;
#12316=AXIS2_PLACEMENT_3D ( 'NONE', #13086, #18746, #58663 ) ;
#12322=CARTESIAN_POINT ( 'NONE',  ( 0.000000000000000000, -6.539067737394502089, 2.314222412769776138 ) ) ;
#12328=EDGE_CURVE ( 'NONE', #42485, #21663, #16318, .T. ) ;
#12343=FACE_OUTER_BOUND ( 'NONE', #40947, .T. ) ;
#12346=CARTESIAN_POINT ( 'NONE',  ( 2.000000000000001776, -6.767909380267597363, -0.7805499053121327524 ) ) ;
#12350=ADVANCED_FACE ( 'NONE', ( #37854 ), #21592, .T. ) ;
#12351=ORIENTED_EDGE ( 'NONE', *, *, #36235, .T. ) ;
#12355=DIRECTION ( 'NONE',  ( 0.000000000000000000, 0.000000000000000000, 1.000000000000000000 ) ) ;
#12356=CARTESIAN_POINT ( 'NONE',  ( 0.000000000000000000, 0.000000000000000000, 0.000000000000000000 ) ) ;
#12364=CARTESIAN_POINT ( 'NONE',  ( 2.000000000000001776, -6.643843315911820646, 1.507714007300648307 ) ) ;
#12365=DIRECTION ( 'NONE',  ( 0.000000000000000000, -0.6876994588534294239, 0.7259954919231249582 ) ) ;
#12366=EDGE_CURVE ( 'NONE', #2801, #37153, #46850, .T. ) ;
#12374=CARTESIAN_POINT ( 'NONE',  ( -22.30527770659433173, 3.757123197210718857, -0.2559941915621641306 ) ) ;
#12382=ORIENTED_EDGE ( 'NONE', *, *, #61056, .T. ) ;
#12393=CARTESIAN_POINT ( 'NONE',  ( -22.39032720737627358, -3.916738514147019679, -0.9101257950221066650 ) ) ;
#12408=DIRECTION ( 'NONE',  ( 0.000000000000000000, -0.9289767198167871998, -0.3701381553399247792 ) ) ;
#12409=CARTESIAN_POINT ( 'NONE',  ( -22.27710395300133328, -3.549456197028680648, -0.9764373854729214708 ) ) ;
#12415=VERTEX_POINT ( 'NONE', #13866 ) ;
#12417=CARTESIAN_POINT ( 'NONE',  ( -22.27704833740210333, 3.351945466913931693, 1.521679877253146351 ) ) ;
#12420=CYLINDRICAL_SURFACE ( 'NONE', #14626, 2.899999999999994582 ) ;
#12421=CARTESIAN_POINT ( 'NONE',  ( 0.000000000000000000, -4.376687952327290354, -5.220963330856675633 ) ) ;
#12424=EDGE_CURVE ( 'NONE', #23282, #48840, #64103, .T. ) ;
#12425=ORIENTED_EDGE ( 'NONE', *, *, #6531, .F. ) ;
#12446=FACE_OUTER_BOUND ( 'NONE', #43003, .T. ) ;
#12452=CARTESIAN_POINT ( 'NONE',  ( -22.27384469013076185, 3.663183248998794106, -0.3730095848193202279 ) ) ;
#12455=CARTESIAN_POINT ( 'NONE',  ( 2.000000000000001776, -1.225832621831797420, -6.827324998361596009 ) ) ;
#12457=ORIENTED_EDGE ( 'NONE', *, *, #54665, .F. ) ;
#12458=DIRECTION ( 'NONE',  ( -1.000000000000000000, 0.000000000000000000, 0.000000000000000000 ) ) ;
#12482=CARTESIAN_POINT ( 'NONE',  ( -27.08416813689867908, 0.7899859999124485554, -2.150738950797698834 ) ) ;
#12495=CARTESIAN_POINT ( 'NONE',  ( -27.08704841010890974, 0.9786466045354205168, -2.081152044925704825 ) ) ;
#12503=EDGE_LOOP ( 'NONE', ( #37768, #53759, #35871, #46615 ) ) ;
#12510=ADVANCED_FACE ( 'NONE', ( #29495 ), #22132, .F. ) ;
#12515=CARTESIAN_POINT ( 'NONE',  ( -27.09729107899852352, -2.094470452261897542, -1.021938248127332693 ) ) ;
#12516=CARTESIAN_POINT ( 'NONE',  ( -35.05012975565874456, 0.01377677982611810216, -0.002073729464863237164 ) ) ;
#12519=CARTESIAN_POINT ( 'NONE',  ( -22.28856623400852399, -2.585606290939616692, 2.668530796663832749 ) ) ;
#12525=AXIS2_PLACEMENT_3D ( 'NONE', #3218, #43419, #48765 ) ;
#12535=B_SPLINE_CURVE_WITH_KNOTS ( 'NONE', 3,
 ( #29712, #61608, #50019, #14735, #35014, #128, #55666, #20409, #35684, #9766, #40690, #51003, #5462, #475, #41011, #61293, #15724, #36000, #56300, #10749, #31036, #51348 ),
 .UNSPECIFIED., .F., .F.,
 ( 4, 3, 3, 3, 3, 3, 3, 4 ),
 ( 0.000000000000000000, 4.455945684386670302E-05, 6.636307477203838871E-05, 8.816671873158670684E-05, 0.0001099660380492599882, 0.0001317545563165301817, 0.0001762613022895049089, 0.0001867992666138357976 ),
 .UNSPECIFIED. ) ;
#12539=EDGE_CURVE ( 'NONE', #49753, #63399, #54254, .T. ) ;
#12544=CARTESIAN_POINT ( 'NONE',  ( -27.08419797710328325, -2.268561579780436599, 0.3221715127607953644 ) ) ;
#12554=ORIENTED_EDGE ( 'NONE', *, *, #32256, .T. ) ;
#12557=VECTOR ( 'NONE', #14231, 1000.000000000000000 ) ;
#12559=ORIENTED_EDGE ( 'NONE', *, *, #56898, .F. ) ;
#12565=VERTEX_POINT ( 'NONE', #61082 ) ;
#12575=CYLINDRICAL_SURFACE ( 'NONE', #24636, 6.936499999999988120 ) ;
#12580=ADVANCED_FACE ( 'NONE', ( #45135 ), #15513, .T. ) ;
#12585=EDGE_CURVE ( 'NONE', #65358, #47259, #13865, .T. ) ;
#12587=DIRECTION ( 'NONE',  ( 0.000000000000000000, -0.5155538571770288403, 0.8568571761675849441 ) ) ;
#12593=EDGE_LOOP ( 'NONE', ( #37640, #31270, #65769, #54892 ) ) ;
#12597=ORIENTED_EDGE ( 'NONE', *, *, #49560, .F. ) ;
#12600=CARTESIAN_POINT ( 'NONE',  ( 2.000000000000001776, 0.000000000000000000, 0.000000000000000000 ) ) ;
#12607=DIRECTION ( 'NONE',  ( -1.000000000000000000, 0.000000000000000000, 0.000000000000000000 ) ) ;
#12614=CIRCLE ( 'NONE', #29605, 2.899999999999994582 ) ;
#12627=CARTESIAN_POINT ( 'NONE',  ( -22.71097035706202405, -0.4203397252017116448, 4.965150228107737540 ) ) ;
#12628=ORIENTED_EDGE ( 'NONE', *, *, #27436, .T. ) ;
#12632=DIRECTION ( 'NONE',  ( 0.000000000000000000, 0.000000000000000000, 1.000000000000000000 ) ) ;
#12634=CARTESIAN_POINT ( 'NONE',  ( 0.000000000000000000, -2.562706407243680928, 6.312399813420318750 ) ) ;
#12637=CARTESIAN_POINT ( 'NONE',  ( -22.27704833740210333, -0.3581593033281198490, -3.663709865074131766 ) ) ;
#12638=ORIENTED_EDGE ( 'NONE', *, *, #27389, .F. ) ;
#12642=ORIENTED_EDGE ( 'NONE', *, *, #33760, .F. ) ;
#12650=DIRECTION ( 'NONE',  ( 0.000000000000000000, 0.000000000000000000, 1.000000000000000000 ) ) ;
#12652=CARTESIAN_POINT ( 'NONE',  ( -22.27756824490284515, 3.555646273932183021, 0.9591204781039950333 ) ) ;
#12655=CARTESIAN_POINT ( 'NONE',  ( -27.20102706715913143, -1.966718264078098910, -1.765193291701730338 ) ) ;
#12658=LINE ( 'NONE', #2048, #18409 ) ;
#12668=B_SPLINE_CURVE_WITH_KNOTS ( 'NONE', 3,
 ( #60608, #54966, #55288, #50974, #5423, #54670, #34986, #14395, #15045, #39337, #14069, #60280, #9089, #24374, #29371, #10385, #19072, #49665, #65580, #59639, #4105, #25694 ),
 .UNSPECIFIED., .F., .F.,
 ( 4, 3, 3, 3, 3, 3, 3, 4 ),
 ( 0.000000000000000000, 4.447697177976356439E-05, 6.624143997791323828E-05, 8.800576886944330051E-05, 0.0001097699864780905381, 0.0001315341395364381678, 0.0001760120188223285103, 0.0001867971373174725450 ),
 .UNSPECIFIED. ) ;
#12673=DIRECTION ( 'NONE',  ( 0.000000000000000000, 0.000000000000000000, 1.000000000000000000 ) ) ;
#12685=EDGE_CURVE ( 'NONE', #25020, #32375, #1126, .T. ) ;
#12690=CARTESIAN_POINT ( 'NONE',  ( -27.08423805673873375, -0.6554626340706021237, 2.195702713475284895 ) ) ;
#12696=ORIENTED_EDGE ( 'NONE', *, *, #48047, .T. ) ;
#12699=DIRECTION ( 'NONE',  ( 1.000000000000000000, 0.000000000000000000, 0.000000000000000000 ) ) ;
#12700=AXIS2_PLACEMENT_3D ( 'NONE', #30819, #15851, #46154 ) ;
#12701=CARTESIAN_POINT ( 'NONE',  ( -22.29115169517546136, 3.712980101756725659, -0.2790989024812895458 ) ) ;
#12705=VERTEX_POINT ( 'NONE', #51773 ) ;
#12707=ORIENTED_EDGE ( 'NONE', *, *, #47054, .F. ) ;
#12708=ORIENTED_EDGE ( 'NONE', *, *, #58338, .F. ) ;
#12725=ORIENTED_EDGE ( 'NONE', *, *, #7984, .T. ) ;
#12729=ADVANCED_FACE ( 'NONE', ( #53330 ), #47116, .T. ) ;
#12732=CARTESIAN_POINT ( 'NONE',  ( 2.000000000000001776, -6.250523986464001425, 3.007653927006548766 ) ) ;
#12739=CARTESIAN_POINT ( 'NONE',  ( -22.29195009621226475, -3.616122380634895439, -0.8975732442595631966 ) ) ;
#12742=CARTESIAN_POINT ( 'NONE',  ( 2.000000000000001776, -5.450255447309714896, -4.087611905901492371 ) ) ;
#12752=AXIS2_PLACEMENT_3D ( 'NONE', #64223, #13666, #38281 ) ;
#12754=ORIENTED_EDGE ( 'NONE', *, *, #60266, .T. ) ;
#12756=CARTESIAN_POINT ( 'NONE',  ( -27.08423805673873375, -1.573803011992715106, -1.665498649074261373 ) ) ;
#12761=CARTESIAN_POINT ( 'NONE',  ( 2.000000000000001776, 0.000000000000000000, 0.000000000000000000 ) ) ;
#12762=LINE ( 'NONE', #33051, #383 ) ;
#12765=DIRECTION ( 'NONE',  ( -1.000000000000000000, 0.000000000000000000, 0.000000000000000000 ) ) ;
#12768=ORIENTED_EDGE ( 'NONE', *, *, #30760, .F. ) ;
#12774=CARTESIAN_POINT ( 'NONE',  ( -27.35552965826137140, -0.2619431035391951434, 3.094132632038943065 ) ) ;
#12783=CIRCLE ( 'NONE', #7471, 2.899999999999996803 ) ;
#12784=DIRECTION ( 'NONE',  ( -1.000000000000000000, 0.000000000000000000, 0.000000000000000000 ) ) ;
#12798=DIRECTION ( 'NONE',  ( 0.000000000000000000, 0.000000000000000000, 1.000000000000000000 ) ) ;
#12800=( BOUNDED_SURFACE ( )  B_SPLINE_SURFACE ( 3, 1, ( 
 ( #1620, #10921 ),
 ( #51824, #305 ),
 ( #46496, #20581 ),
 ( #36842, #47175 ) ),
 .UNSPECIFIED., .F., .F., .F. ) 
 B_SPLINE_SURFACE_WITH_KNOTS ( ( 4, 4 ),
 ( 2, 2 ),
 ( 0.000000000000000000, 1.000000000000000000 ),
 ( 0.000000000000000000, 1.000000000000000000 ),
 .UNSPECIFIED. ) 
 GEOMETRIC_REPRESENTATION_ITEM ( )  RATIONAL_B_SPLINE_SURFACE ( (
 ( 1.000000000000000000, 1.000000000000000000),
 ( 0.9932032654565553509, 0.8386279382598740284),
 ( 0.9932032654565553509, 0.8386279382598740284),
 ( 1.000000000000000000, 1.000000000000000000) ) ) 
 REPRESENTATION_ITEM ( '' )  SURFACE ( )  );
#12801=DIRECTION ( 'NONE',  ( 0.000000000000000000, 0.000000000000000000, 1.000000000000000000 ) ) ;
#12805=CARTESIAN_POINT ( 'NONE',  ( -22.27709082389155171, 2.563977319272137567, 2.641652894015082520 ) ) ;
#12832=CYLINDRICAL_SURFACE ( 'NONE', #40420, 2.899999999999994582 ) ;
#12833=FACE_OUTER_BOUND ( 'NONE', #17005, .T. ) ;
#12835=CARTESIAN_POINT ( 'NONE',  ( -27.20102706715913143, -2.512061365242607369, 0.8206313329275958246 ) ) ;
#12837=CARTESIAN_POINT ( 'NONE',  ( -27.08704841010922593, -1.888108843319752150, 1.313007237774850289 ) ) ;
#12845=DIRECTION ( 'NONE',  ( -1.000000000000000000, 0.000000000000000000, 0.000000000000000000 ) ) ;
#12849=AXIS2_PLACEMENT_3D ( 'NONE', #4715, #51243, #16308 ) ;
#12859=DIRECTION ( 'NONE',  ( -1.000000000000000000, 0.000000000000000000, 0.000000000000000000 ) ) ;
#12862=DIRECTION ( 'NONE',  ( -1.000000000000000000, 0.000000000000000000, 0.000000000000000000 ) ) ;
#12866=VECTOR ( 'NONE', #59904, 1000.000000000000000 ) ;
#12874=AXIS2_PLACEMENT_3D ( 'NONE', #48266, #43552, #12632 ) ;
#12876=VERTEX_POINT ( 'NONE', #44621 ) ;
#12879=CARTESIAN_POINT ( 'NONE',  ( -28.66013792860432119, 0.4631296695479409919, 1.776574787184017179 ) ) ;
#12880=VECTOR ( 'NONE', #52448, 1000.000000000000000 ) ;
#12902=CARTESIAN_POINT ( 'NONE',  ( 2.000000000000001776, -0.08317740279924559776, -7.499538753794370294 ) ) ;
#12903=AXIS2_PLACEMENT_3D ( 'NONE', #60634, #35356, #21042 ) ;
#12904=CARTESIAN_POINT ( 'NONE',  ( 1.000000000000000888, 5.217815162096925086, -5.387430271863535403 ) ) ;
#12906=DIRECTION ( 'NONE',  ( 0.9582930651793755139, -0.1254087680151165229, 0.2568015617827271724 ) ) ;
#12911=ORIENTED_EDGE ( 'NONE', *, *, #31598, .T. ) ;
#12924=FACE_OUTER_BOUND ( 'NONE', #19404, .T. ) ;
#12933=DIRECTION ( 'NONE',  ( -1.000000000000000000, 0.000000000000000000, 0.000000000000000000 ) ) ;
#12936=CIRCLE ( 'NONE', #46923, 2.899999999999994582 ) ;
#12938=DIRECTION ( 'NONE',  ( -1.000000000000000000, 0.000000000000000000, 0.000000000000000000 ) ) ;
#12940=EDGE_CURVE ( 'NONE', #21973, #60604, #1176, .T. ) ;
#12948=CARTESIAN_POINT ( 'NONE',  ( -35.04683013664716640, 0.0001018103929586065885, 0.01235741808121416756 ) ) ;
#12961=CARTESIAN_POINT ( 'NONE',  ( 2.000000000000001776, 5.814643797626986910, -3.550179297009520063 ) ) ;
#12974=AXIS2_PLACEMENT_3D ( 'NONE', #20269, #55189, #34573 ) ;
#12975=CARTESIAN_POINT ( 'NONE',  ( -22.27704833740210333, -2.142029987820955661, -2.993786163585799631 ) ) ;
#12977=ORIENTED_EDGE ( 'NONE', *, *, #55676, .T. ) ;
#12993=ORIENTED_EDGE ( 'NONE', *, *, #35469, .F. ) ;
#13000=DIRECTION ( 'NONE',  ( -1.000000000000000000, 0.000000000000000000, 0.000000000000000000 ) ) ;
#13001=DIRECTION ( 'NONE',  ( -1.000000000000000000, 0.000000000000000000, 0.000000000000000000 ) ) ;
#13003=CARTESIAN_POINT ( 'NONE',  ( -22.29770266787582500, 3.635870259503092949, 0.8895590726606663612 ) ) ;
#13005=CARTESIAN_POINT ( 'NONE',  ( -10.00000000000000178, 0.000000000000000000, 0.000000000000000000 ) ) ;
#13007=FACE_OUTER_BOUND ( 'NONE', #30849, .T. ) ;
#13008=B_SPLINE_CURVE_WITH_KNOTS ( 'NONE', 3,
 ( #61125, #15871, #15559, #30842, #25887, #46174, #51504, #620 ),
 .UNSPECIFIED., .F., .F.,
 ( 4, 2, 2, 4 ),
 ( 0.000000000000000000, 0.0003639104015150019687, 0.0007278208030300039374, 0.001455641606060009826 ),
 .UNSPECIFIED. ) ;
#13016=CARTESIAN_POINT ( 'NONE',  ( -27.05874794189610455, 1.734723475976807094E-15, -8.673617379884035472E-15 ) ) ;
#13018=CARTESIAN_POINT ( 'NONE',  ( -22.30625920655495165, 2.750410778797892419, 2.610366806364663450 ) ) ;
#13020=ORIENTED_EDGE ( 'NONE', *, *, #62578, .T. ) ;
#13032=ORIENTED_EDGE ( 'NONE', *, *, #15320, .F. ) ;
#13035=AXIS2_PLACEMENT_3D ( 'NONE', #6129, #36698, #56995 ) ;
#13038=DIRECTION ( 'NONE',  ( -1.000000000000000000, 0.000000000000000000, 0.000000000000000000 ) ) ;
#13043=VECTOR ( 'NONE', #19824, 1000.000000000000114 ) ;
#13048=DIRECTION ( 'NONE',  ( 0.000000000000000000, 0.000000000000000000, -1.000000000000000000 ) ) ;
#13059=ORIENTED_EDGE ( 'NONE', *, *, #64411, .F. ) ;
#13062=CARTESIAN_POINT ( 'NONE',  ( -22.31213670151049300, -3.398324501467297587, -1.669817926839923583 ) ) ;
#13063=EDGE_CURVE ( 'NONE', #47012, #6868, #7522, .T. ) ;
#13064=ORIENTED_EDGE ( 'NONE', *, *, #48523, .T. ) ;
#13076=VERTEX_POINT ( 'NONE', #25338 ) ;
#13078=ORIENTED_EDGE ( 'NONE', *, *, #60256, .F. ) ;
#13086=CARTESIAN_POINT ( 'NONE',  ( 2.000000000000001776, -6.812627895098285258, -0.04423456934733380197 ) ) ;
#13087=CARTESIAN_POINT ( 'NONE',  ( 2.000000000000001776, 6.643843315911821534, -1.507714007300717585 ) ) ;
#13088=CARTESIAN_POINT ( 'NONE',  ( -22.27706089016750113, -3.548384797797525358, -0.9798385173596375619 ) ) ;
#13092=ORIENTED_EDGE ( 'NONE', *, *, #3722, .F. ) ;
#13093=EDGE_CURVE ( 'NONE', #41782, #18208, #26659, .T. ) ;
#13095=CARTESIAN_POINT ( 'NONE',  ( 0.000000000000000000, -1.530946385938321219, -7.342084388195388556 ) ) ;
#13099=CARTESIAN_POINT ( 'NONE',  ( -22.28073302975500880, 0.9769664947681371281, 3.560599703067811816 ) ) ;
#13105=CARTESIAN_POINT ( 'NONE',  ( 0.000000000000000000, 0.000000000000000000, 0.000000000000000000 ) ) ;
#13107=CARTESIAN_POINT ( 'NONE',  ( -27.08417568107323703, -1.449568724721387092, -1.774279301226125760 ) ) ;
#13108=CARTESIAN_POINT ( 'NONE',  ( -22.28506771379528573, 2.081613609299084011, 3.091577134491921619 ) ) ;
#13110=EDGE_CURVE ( 'NONE', #24851, #49976, #14962, .T. ) ;
#13119=EDGE_CURVE ( 'NONE', #36445, #5130, #22424, .T. ) ;
#13122=LINE ( 'NONE', #33406, #64916 ) ;
#13124=VERTEX_POINT ( 'NONE', #52907 ) ;
#13132=ORIENTED_EDGE ( 'NONE', *, *, #2591, .F. ) ;
#13162=CARTESIAN_POINT ( 'NONE',  ( 0.000000000000000000, 5.450255447309811707, -4.087611905901392007 ) ) ;
#13163=EDGE_CURVE ( 'NONE', #50412, #7150, #58576, .T. ) ;
#13167=CARTESIAN_POINT ( 'NONE',  ( -22.27711653538342773, -0.4190680140413403088, -3.657713416444744237 ) ) ;
#13169=DIRECTION ( 'NONE',  ( -1.000000000000000000, 0.000000000000000000, 0.000000000000000000 ) ) ;
#13171=ORIENTED_EDGE ( 'NONE', *, *, #44204, .T. ) ;
#13180=CARTESIAN_POINT ( 'NONE',  ( 0.000000000000000000, 4.376687952327335651, 5.220963330856624118 ) ) ;
#13181=CIRCLE ( 'NONE', #49326, 2.899999999999994582 ) ;
#13184=CARTESIAN_POINT ( 'NONE',  ( -10.00000000000000178, 0.000000000000000000, 0.000000000000000000 ) ) ;
#13185=EDGE_LOOP ( 'NONE', ( #2812, #54877, #31444, #26570 ) ) ;
#13186=CARTESIAN_POINT ( 'NONE',  ( -27.32343372485686217, 1.382463360572562028, 2.674948176236182640 ) ) ;
#13189=CARTESIAN_POINT ( 'NONE',  ( 2.000000000000001776, -3.152010634611731366, 6.039758645301271933 ) ) ;
#13194=DIRECTION ( 'NONE',  ( -1.000000000000000000, 0.000000000000000000, 0.000000000000000000 ) ) ;
#13200=DIRECTION ( 'NONE',  ( 1.000000000000000000, 0.000000000000000000, 0.000000000000000000 ) ) ;
#13202=EDGE_CURVE ( 'NONE', #14676, #43944, #28794, .T. ) ;
#13203=CARTESIAN_POINT ( 'NONE',  ( -27.04788180060269553, 0.2724356095623531870, -3.218072544330549345 ) ) ;
#13205=CARTESIAN_POINT ( 'NONE',  ( -27.08421723179412410, -0.5069555058557356775, -2.234476190936522499 ) ) ;
#13209=CARTESIAN_POINT ( 'NONE',  ( -27.08421723179412055, 1.681635392574631460, -1.556274442127712820 ) ) ;
#13222=ORIENTED_EDGE ( 'NONE', *, *, #3428, .T. ) ;
#13234=LINE ( 'NONE', #15186, #45921 ) ;
#13238=ADVANCED_FACE ( 'NONE', ( #59221 ), #29926, .T. ) ;
#13240=LINE ( 'NONE', #9208, #38536 ) ;
#13242=CARTESIAN_POINT ( 'NONE',  ( -22.27786964138239867, -1.536369256421345142, 3.347945419004146661 ) ) ;
#13253=EDGE_LOOP ( 'NONE', ( #788, #39664, #9257, #30259 ) ) ;
#13258=AXIS2_PLACEMENT_3D ( 'NONE', #43727, #3525, #29413 ) ;
#13259=CARTESIAN_POINT ( 'NONE',  ( -27.09030469827931853, -1.608164674722575072, 1.657623467486013968 ) ) ;
#13269=CARTESIAN_POINT ( 'NONE',  ( 0.000000000000000000, 3.073484823194335025, 6.841322316745041654 ) ) ;
#13272=CARTESIAN_POINT ( 'NONE',  ( -10.00000000000000178, 0.000000000000000000, 0.000000000000000000 ) ) ;
#13276=ORIENTED_EDGE ( 'NONE', *, *, #36988, .F. ) ;
#13283=CARTESIAN_POINT ( 'NONE',  ( 2.000000000000001776, 3.152010634611693174, 6.039758645301271933 ) ) ;
#13285=ORIENTED_EDGE ( 'NONE', *, *, #14244, .T. ) ;
#13290=CARTESIAN_POINT ( 'NONE',  ( 2.000000000000001776, -4.444115772890066651, -5.163689623839394116 ) ) ;
#13306=DIRECTION ( 'NONE',  ( 0.000000000000000000, 0.000000000000000000, -1.000000000000000000 ) ) ;
#13308=VERTEX_POINT ( 'NONE', #61823 ) ;
#13309=ORIENTED_EDGE ( 'NONE', *, *, #37130, .F. ) ;
#13310=FACE_OUTER_BOUND ( 'NONE', #24180, .T. ) ;
#13316=EDGE_CURVE ( 'NONE', #42911, #18188, #56519, .T. ) ;
#13322=ORIENTED_EDGE ( 'NONE', *, *, #31629, .T. ) ;
#13348=EDGE_CURVE ( 'NONE', #63832, #58967, #15608, .T. ) ;
#13349=VERTEX_POINT ( 'NONE', #30571 ) ;
#13354=DIRECTION ( 'NONE',  ( -1.000000000000000000, 0.000000000000000000, 0.000000000000000000 ) ) ;
#13364=CARTESIAN_POINT ( 'NONE',  ( -22.28415773361649954, -2.647149619609361793, -2.588610893123082235 ) ) ;
#13371=DIRECTION ( 'NONE',  ( -0.9606638835031803270, 0.2674900627617600724, 0.07465901992591084113 ) ) ;
#13381=CARTESIAN_POINT ( 'NONE',  ( -22.31099767395441091, -3.395517675085600651, -1.667781795950537216 ) ) ;
#13400=CARTESIAN_POINT ( 'NONE',  ( -22.30625920655495165, 1.672644928563083333, -3.403091720605004866 ) ) ;
#13404=LINE ( 'NONE', #8758, #52695 ) ;
#13405=FACE_OUTER_BOUND ( 'NONE', #33923, .T. ) ;
#13409=EDGE_LOOP ( 'NONE', ( #30353, #61085, #23961, #55910 ) ) ;
#13411=DIRECTION ( 'NONE',  ( -1.000000000000000000, 0.000000000000000000, 0.000000000000000000 ) ) ;
#13412=CARTESIAN_POINT ( 'NONE',  ( -22.31099767395441091, 3.395517675085607756, 1.667781795950494583 ) ) ;
#13414=CARTESIAN_POINT ( 'NONE',  ( 2.000000000000001776, -2.562706407243573459, -6.312399813420393357 ) ) ;
#13419=VECTOR ( 'NONE', #43961, 1000.000000000000000 ) ;
#13421=EDGE_LOOP ( 'NONE', ( #36036, #8995, #2772, #62579 ) ) ;
#13434=CARTESIAN_POINT ( 'NONE',  ( 2.000000000000001776, 4.570217215903443986, -5.218059682435596258 ) ) ;
#13435=CARTESIAN_POINT ( 'NONE',  ( -35.04643116707788408, 0.007621814750502498015, 0.009511118309123156589 ) ) ;
#13436=EDGE_CURVE ( 'NONE', #61252, #10609, #16057, .T. ) ;
#13438=CARTESIAN_POINT ( 'NONE',  ( 1.000000000000000888, 6.253963800348250501, 4.139799123621038746 ) ) ;
#13446=ORIENTED_EDGE ( 'NONE', *, *, #41891, .T. ) ;
#13452=ORIENTED_EDGE ( 'NONE', *, *, #16777, .T. ) ;
#13454=DIRECTION ( 'NONE',  ( -1.000000000000000000, 0.000000000000000000, 0.000000000000000000 ) ) ;
#13460=ORIENTED_EDGE ( 'NONE', *, *, #14911, .F. ) ;
#13464=EDGE_LOOP ( 'NONE', ( #63820, #20664, #36368, #65197 ) ) ;
#13469=CARTESIAN_POINT ( 'NONE',  ( 2.000000000000001776, -2.480520636974233639, 6.345145617221206180 ) ) ;
#13471=CARTESIAN_POINT ( 'NONE',  ( -27.08423805673873375, 0.6554626340706067866, -2.195702713475291112 ) ) ;
#13478=ORIENTED_EDGE ( 'NONE', *, *, #30403, .T. ) ;
#13494=DIRECTION ( 'NONE',  ( -1.000000000000000000, 0.000000000000000000, 0.000000000000000000 ) ) ;
#13501=EDGE_CURVE ( 'NONE', #17594, #35944, #4962, .T. ) ;
#13502=DIRECTION ( 'NONE',  ( -1.000000000000000000, 0.000000000000000000, 0.000000000000000000 ) ) ;
#13506=EDGE_LOOP ( 'NONE', ( #42003, #47372, #22505, #2173 ) ) ;
#13508=CARTESIAN_POINT ( 'NONE',  ( 2.000000000000001776, -5.107597897712309098, -4.693343793638478978 ) ) ;
#13511=EDGE_CURVE ( 'NONE', #34813, #31213, #61723, .T. ) ;
#13512=DIRECTION ( 'NONE',  ( 0.000000000000000000, 0.4198891015602590482, 0.9075754196709594490 ) ) ;
#13529=CARTESIAN_POINT ( 'NONE',  ( -22.46509356695199955, 0.8809186187926546507, -4.154553862421312083 ) ) ;
#13531=AXIS2_PLACEMENT_3D ( 'NONE', #27903, #18907, #17611 ) ;
#13534=DIRECTION ( 'NONE',  ( -1.000000000000000000, 0.000000000000000000, 0.000000000000000000 ) ) ;
#13539=ORIENTED_EDGE ( 'NONE', *, *, #46824, .T. ) ;
#13543=( NAMED_UNIT ( * ) SI_UNIT ( $, .STERADIAN. ) SOLID_ANGLE_UNIT ( ) );
#13548=CARTESIAN_POINT ( 'NONE',  ( -22.27704833740210333, -1.521679877253162116, 3.351945466913909488 ) ) ;
#13558=VERTEX_POINT ( 'NONE', #43490 ) ;
#13560=CARTESIAN_POINT ( 'NONE',  ( -27.09125059358712306, -1.607567221344180952, 1.662156772100931157 ) ) ;
#13564=EDGE_CURVE ( 'NONE', #63687, #30290, #64746, .T. ) ;
#13571=CARTESIAN_POINT ( 'NONE',  ( -35.04709527796842394, 0.001003525937978352878, -0.01232256164996822778 ) ) ;
#13574=DIRECTION ( 'NONE',  ( 0.000000000000000000, 0.000000000000000000, 1.000000000000000000 ) ) ;
#13578=VERTEX_POINT ( 'NONE', #44805 ) ;
#13582=ORIENTED_EDGE ( 'NONE', *, *, #51358, .T. ) ;
#13587=CARTESIAN_POINT ( 'NONE',  ( 0.000000000000000000, -6.441884263200823746, -2.217201541069834914 ) ) ;
#13591=CARTESIAN_POINT ( 'NONE',  ( -35.04643116707788408, -0.009511118309140503824, 0.007621814750495559121 ) ) ;
#13594=CARTESIAN_POINT ( 'NONE',  ( -22.30861784526116054, 2.737516124790411176, 2.600591904828372325 ) ) ;
#13597=EDGE_CURVE ( 'NONE', #16004, #16830, #21385, .T. ) ;
#13598=DIRECTION ( 'NONE',  ( 0.000000000000000000, 0.000000000000000000, -1.000000000000000000 ) ) ;
#13606=DIRECTION ( 'NONE',  ( -1.000000000000000000, 0.000000000000000000, 0.000000000000000000 ) ) ;
#13607=ORIENTED_EDGE ( 'NONE', *, *, #45275, .F. ) ;
#13608=VERTEX_POINT ( 'NONE', #9224 ) ;
#13609=CARTESIAN_POINT ( 'NONE',  ( -27.09569413923794912, 2.232620870184089057, -0.6513788562879346822 ) ) ;
#13611=CARTESIAN_POINT ( 'NONE',  ( 2.000000000000001776, 0.000000000000000000, 0.000000000000000000 ) ) ;
#13615=DIRECTION ( 'NONE',  ( 0.000000000000000000, 0.000000000000000000, 1.000000000000000000 ) ) ;
#13620=B_SPLINE_CURVE_WITH_KNOTS ( 'NONE', 3,
 ( #36921, #52879, #36265, #57224, #11010, #26623 ),
 .UNSPECIFIED., .F., .F.,
 ( 4, 2, 4 ),
 ( 0.0002637379172192549199, 0.0009975831966643308908, 0.001731428476109406808 ),
 .UNSPECIFIED. ) ;
#13625=CARTESIAN_POINT ( 'NONE',  ( -22.27786964138239867, -0.3434379038477733959, -3.667590411552012597 ) ) ;
#13631=CARTESIAN_POINT ( 'NONE',  ( 0.000000000000000000, -3.979254915827401540, 5.681598592373737766 ) ) ;
#13637=CARTESIAN_POINT ( 'NONE',  ( 0.000000000000000000, -6.253963800348261159, 4.139799123620986343 ) ) ;
#13645=CARTESIAN_POINT ( 'NONE',  ( -22.28694879868232803, 3.597828382597545449, 0.9088670759107777553 ) ) ;
#13652=DIRECTION ( 'NONE',  ( -1.000000000000000000, 0.000000000000000000, 0.000000000000000000 ) ) ;
#13657=DIRECTION ( 'NONE',  ( -1.000000000000000000, 0.000000000000000000, 0.000000000000000000 ) ) ;
#13666=DIRECTION ( 'NONE',  ( -1.000000000000000000, 0.000000000000000000, 0.000000000000000000 ) ) ;
#13670=APPLICATION_CONTEXT ( 'automotive_design' ) ;
#13671=ORIENTED_EDGE ( 'NONE', *, *, #20961, .T. ) ;
#13674=EDGE_CURVE ( 'NONE', #11911, #56404, #23533, .T. ) ;
#13677=VECTOR ( 'NONE', #40256, 1000.000000000000000 ) ;
#13688=VERTEX_POINT ( 'NONE', #60427 ) ;
#13690=CARTESIAN_POINT ( 'NONE',  ( -22.27720387087364884, -3.639274226782815536, 0.5572161790459860820 ) ) ;
#13697=CIRCLE ( 'NONE', #1006, 7.499999999999988454 ) ;
#13702=CARTESIAN_POINT ( 'NONE',  ( 2.000000000000001776, 4.376687952327335651, 5.220963330856624118 ) ) ;
#13703=ADVANCED_FACE ( 'NONE', ( #35792 ), #21172, .T. ) ;
#13704=EDGE_LOOP ( 'NONE', ( #39870, #610, #56310, #65479 ) ) ;
#13706=AXIS2_PLACEMENT_3D ( 'NONE', #42512, #6973, #1002 ) ;
#13713=ORIENTED_EDGE ( 'NONE', *, *, #27678, .F. ) ;
#13728=EDGE_CURVE ( 'NONE', #26571, #725, #45798, .T. ) ;
#13732=AXIS2_PLACEMENT_3D ( 'NONE', #22652, #18327, #33272 ) ;
#13734=CARTESIAN_POINT ( 'NONE',  ( -22.29677679919927868, 2.096973157017390843, 3.097220482903997318 ) ) ;
#13736=EDGE_CURVE ( 'NONE', #24592, #19340, #25552, .T. ) ;
#13745=CIRCLE ( 'NONE', #53062, 2.899999999999995026 ) ;
#13749=ORIENTED_EDGE ( 'NONE', *, *, #32527, .T. ) ;
#13751=DIRECTION ( 'NONE',  ( 0.000000000000000000, -0.9635499925192201331, -0.2675283385292311911 ) ) ;
#13757=AXIS2_PLACEMENT_3D ( 'NONE', #24582, #50525, #29887 ) ;
#13761=CARTESIAN_POINT ( 'NONE',  ( 1.000000000000000888, -1.530946385938321219, -7.342084388195388556 ) ) ;
#13767=VERTEX_POINT ( 'NONE', #36476 ) ;
#13773=LINE ( 'NONE', #34065, #8576 ) ;
#13778=EDGE_CURVE ( 'NONE', #8079, #57809, #8679, .T. ) ;
#13792=LINE ( 'NONE', #44380, #35155 ) ;
#13812=DIRECTION ( 'NONE',  ( 0.000000000000000000, 0.000000000000000000, 1.000000000000000000 ) ) ;
#13818=CARTESIAN_POINT ( 'NONE',  ( -27.08954555554413801, -2.082904663687656921, -0.9924303381791110823 ) ) ;
#13821=DIRECTION ( 'NONE',  ( 0.000000000000000000, 0.000000000000000000, 1.000000000000000000 ) ) ;
#13822=CARTESIAN_POINT ( 'NONE',  ( -22.29770266787582500, -2.588315884842648185, 2.703976473263648206 ) ) ;
#13834=ORIENTED_EDGE ( 'NONE', *, *, #48962, .T. ) ;
#13840=AXIS2_PLACEMENT_3D ( 'NONE', #20758, #55685, #56999 ) ;
#13845=CARTESIAN_POINT ( 'NONE',  ( -22.39032720737625937, 0.9101257950221148807, -3.916738514147017902 ) ) ;
#13846=CIRCLE ( 'NONE', #38303, 6.936499999999987232 ) ;
#13853=CIRCLE ( 'NONE', #1169, 6.936499999999989008 ) ;
#13854=CARTESIAN_POINT ( 'NONE',  ( -24.42101984568203932, 3.522366633939687741, 2.451666775035081791 ) ) ;
#13862=EDGE_CURVE ( 'NONE', #23300, #27429, #7574, .T. ) ;
#13864=ORIENTED_EDGE ( 'NONE', *, *, #3907, .F. ) ;
#13865=CIRCLE ( 'NONE', #18116, 6.936499999999989896 ) ;
#13866=CARTESIAN_POINT ( 'NONE',  ( -22.23402523511428086, -7.703719777548943412E-30, -3.000000000000009326 ) ) ;
#13870=ORIENTED_EDGE ( 'NONE', *, *, #53889, .T. ) ;
#13871=DIRECTION ( 'NONE',  ( -1.000000000000000000, 0.000000000000000000, 0.000000000000000000 ) ) ;
#13878=AXIS2_PLACEMENT_3D ( 'NONE', #54018, #18778, #23427 ) ;
#13885=VERTEX_POINT ( 'NONE', #2567 ) ;
#13886=LINE ( 'NONE', #60116, #42336 ) ;
#13887=AXIS2_PLACEMENT_3D ( 'NONE', #21097, #31414, #47690 ) ;
#13905=CARTESIAN_POINT ( 'NONE',  ( -22.27945548916780183, -3.673577025288764730, 0.3299677273100650732 ) ) ;
#13907=AXIS2_PLACEMENT_3D ( 'NONE', #56443, #41132, #42110 ) ;
#13912=CARTESIAN_POINT ( 'NONE',  ( -35.04582288351658548, -0.01196488372923644808, 0.004274985098070607434 ) ) ;
#13915=CARTESIAN_POINT ( 'NONE',  ( -22.28284753389937123, 2.640101649307557974, 2.590196335759697543 ) ) ;
#13916=ADVANCED_FACE ( 'NONE', ( #49736 ), #53428, .T. ) ;
#13917=ADVANCED_FACE ( 'NONE', ( #12833 ), #3871, .T. ) ;
#13920=DIRECTION ( 'NONE',  ( -1.000000000000000000, 0.000000000000000000, 0.000000000000000000 ) ) ;
#13926=CARTESIAN_POINT ( 'NONE',  ( 2.000000000000001776, 4.604744433234674972, 5.919993978425482695 ) ) ;
#13928=VECTOR ( 'NONE', #47628, 1000.000000000000000 ) ;
#13929=AXIS2_PLACEMENT_3D ( 'NONE', #57710, #46728, #62033 ) ;
#13953=SHAPE_REPRESENTATION ( 'motion translator_ISO - Spur gear 0.25M 58T 20PA 2FW ---S58B6H18L3.0N', ( #24966 ), #29232 ) ;
#13954=CARTESIAN_POINT ( 'NONE',  ( -25.42680463514451716, 2.219378695194094142, -3.188632951113930414 ) ) ;
#13957=DIRECTION ( 'NONE',  ( 0.000000000000000000, 0.8276889981568877896, 0.5611870653623862726 ) ) ;
#13958=ORIENTED_EDGE ( 'NONE', *, *, #42702, .F. ) ;
#13960=VERTEX_POINT ( 'NONE', #24132 ) ;
#13963=ORIENTED_EDGE ( 'NONE', *, *, #42910, .F. ) ;
#13967=ORIENTED_EDGE ( 'NONE', *, *, #20806, .F. ) ;
#13972=CARTESIAN_POINT ( 'NONE',  ( 2.000000000000001776, 3.073484823194439386, -6.841322316745028331 ) ) ;
#13980=( BOUNDED_SURFACE ( )  B_SPLINE_SURFACE ( 3, 1, ( 
 ( #27846, #11325 ),
 ( #53785, #53116 ),
 ( #33152, #17871 ),
 ( #7558, #32807 ) ),
 .UNSPECIFIED., .F., .F., .F. ) 
 B_SPLINE_SURFACE_WITH_KNOTS ( ( 4, 4 ),
 ( 2, 2 ),
 ( 0.000000000000000000, 1.000000000000000000 ),
 ( 0.000000000000000000, 1.000000000000000000 ),
 .UNSPECIFIED. ) 
 GEOMETRIC_REPRESENTATION_ITEM ( )  RATIONAL_B_SPLINE_SURFACE ( (
 ( 1.000000000000000000, 1.000000000000000000),
 ( 0.9257577194822556033, 0.9980522942447415113),
 ( 0.9257577194822556033, 0.9980522942447415113),
 ( 1.000000000000000000, 1.000000000000000000) ) ) 
 REPRESENTATION_ITEM ( '' )  SURFACE ( )  );
#13989=VERTEX_POINT ( 'NONE', #59711 ) ;
#13997=LINE ( 'NONE', #65199, #47853 ) ;
#14002=CARTESIAN_POINT ( 'NONE',  ( -22.70624764888619751, -4.501516772829869950, -2.702761586319173404 ) ) ;
#14004=AXIS2_PLACEMENT_3D ( 'NONE', #60827, #51533, #21232 ) ;
#14005=AXIS2_PLACEMENT_3D ( 'NONE', #36839, #41159, #57139 ) ;
#14007=AXIS2_PLACEMENT_3D ( 'NONE', #39355, #59655, #20068 ) ;
#14012=DIRECTION ( 'NONE',  ( -1.000000000000000000, 0.000000000000000000, 0.000000000000000000 ) ) ;
#14022=ORIENTED_EDGE ( 'NONE', *, *, #15545, .F. ) ;
#14023=ADVANCED_FACE ( 'NONE', ( #29131 ), #49432, .T. ) ;
#14024=AXIS2_PLACEMENT_3D ( 'NONE', #49627, #44954, #12801 ) ;
#14031=CARTESIAN_POINT ( 'NONE',  ( -22.27716857039623477, -2.496432241075901892, -2.705892286796406587 ) ) ;
#14035=VERTEX_POINT ( 'NONE', #20781 ) ;
#14041=DIRECTION ( 'NONE',  ( -1.000000000000000000, 0.000000000000000000, 0.000000000000000000 ) ) ;
#14042=ORIENTED_EDGE ( 'NONE', *, *, #1384, .F. ) ;
#14046=AXIS2_PLACEMENT_3D ( 'NONE', #56768, #11190, #7492 ) ;
#14050=DIRECTION ( 'NONE',  ( -1.000000000000000000, 0.000000000000000000, 0.000000000000000000 ) ) ;
#14057=ADVANCED_FACE ( 'NONE', ( #55369 ), #9467, .T. ) ;
#14060=CARTESIAN_POINT ( 'NONE',  ( 0.000000000000000000, 0.000000000000000000, 0.000000000000000000 ) ) ;
#14061=ORIENTED_EDGE ( 'NONE', *, *, #58838, .T. ) ;
#14064=VERTEX_POINT ( 'NONE', #60042 ) ;
#14069=CARTESIAN_POINT ( 'NONE',  ( -22.28776923226071460, 1.601293944844132122, -3.350304995653732743 ) ) ;
#14075=PLANE ( 'NONE',  #57298 ) ;
#14077=CARTESIAN_POINT ( 'NONE',  ( 0.000000000000000000, -7.387287142779332960, -1.295372019972250710 ) ) ;
#14086=LINE ( 'NONE', #49678, #32043 ) ;
#14088=CARTESIAN_POINT ( 'NONE',  ( -22.27706485742869091, 2.625261754997705310, -2.580541389029900934 ) ) ;
#14106=CARTESIAN_POINT ( 'NONE',  ( -22.70624764888619751, 0.7939291279022951953, -5.190207123845785198 ) ) ;
#14107=EDGE_CURVE ( 'NONE', #50541, #13558, #25711, .T. ) ;
#14108=ORIENTED_EDGE ( 'NONE', *, *, #17215, .T. ) ;
#14115=DIRECTION ( 'NONE',  ( 0.000000000000000000, -0.9635499925192201331, -0.2675283385292311911 ) ) ;
#14116=VERTEX_POINT ( 'NONE', #52030 ) ;
#14124=EDGE_CURVE ( 'NONE', #21349, #36463, #62976, .T. ) ;
#14130=DIRECTION ( 'NONE',  ( 0.000000000000000000, -0.2149704402110114432, -0.9766205557100894330 ) ) ;
#14139=CARTESIAN_POINT ( 'NONE',  ( -27.35552965826136429, -2.810569013793742688, 1.320216934008381804 ) ) ;
#14144=VERTEX_POINT ( 'NONE', #47049 ) ;
#14147=CIRCLE ( 'NONE', #54525, 2.899999999999995470 ) ;
#14158=CARTESIAN_POINT ( 'NONE',  ( -27.08421723179412410, -2.188590898430375908, -0.6782017488087925816 ) ) ;
#14164=DIRECTION ( 'NONE',  ( -1.000000000000000000, 0.000000000000000000, 0.000000000000000000 ) ) ;
#14167=AXIS2_PLACEMENT_3D ( 'NONE', #38968, #24012, #28996 ) ;
#14168=EDGE_CURVE ( 'NONE', #50541, #4916, #57684, .T. ) ;
#14172=CARTESIAN_POINT ( 'NONE',  ( 1.000000000000000888, -3.224464355699781848, -6.771471746882029130 ) ) ;
#14179=DIRECTION ( 'NONE',  ( 0.000000000000000000, 0.000000000000000000, 1.000000000000000000 ) ) ;
#14194=VECTOR ( 'NONE', #60113, 1000.000000000000114 ) ;
#14195=CARTESIAN_POINT ( 'NONE',  ( -25.42680463514451716, 3.188632951113952174, 2.219378695194055062 ) ) ;
#14201=( NAMED_UNIT ( * ) PLANE_ANGLE_UNIT ( ) SI_UNIT ( $, .RADIAN. ) );
#14219=DIRECTION ( 'NONE',  ( -1.000000000000000000, 0.000000000000000000, 0.000000000000000000 ) ) ;
#14220=CARTESIAN_POINT ( 'NONE',  ( -27.09342121492660382, -1.607500752098860231, 1.671264186073233571 ) ) ;
#14222=EDGE_CURVE ( 'NONE', #26347, #46169, #54063, .T. ) ;
#14223=DIRECTION ( 'NONE',  ( 0.000000000000000000, 0.000000000000000000, 1.000000000000000000 ) ) ;
#14226=EDGE_LOOP ( 'NONE', ( #26244, #42440, #40519, #12351 ) ) ;
#14229=DIRECTION ( 'NONE',  ( -1.000000000000000000, 0.000000000000000000, 0.000000000000000000 ) ) ;
#14231=DIRECTION ( 'NONE',  ( 1.000000000000000000, -0.000000000000000000, -0.000000000000000000 ) ) ;
#14233=CARTESIAN_POINT ( 'NONE',  ( -27.08639648637162622, 1.614109828501636201, -1.635407781268143124 ) ) ;
#14234=CARTESIAN_POINT ( 'NONE',  ( -27.35552965826135008, 3.094132632038936404, 0.2619431035391969198 ) ) ;
#14237=DIRECTION ( 'NONE',  ( -1.000000000000000000, 0.000000000000000000, 0.000000000000000000 ) ) ;
#14244=EDGE_CURVE ( 'NONE', #125, #14997, #58625, .T. ) ;
#14247=CIRCLE ( 'NONE', #12156, 2.214855479030549468 ) ;
#14250=EDGE_CURVE ( 'NONE', #33968, #32845, #46063, .T. ) ;
#14251=CARTESIAN_POINT ( 'NONE',  ( 2.000000000000001776, 0.4804830611970061227, 6.919838746524539452 ) ) ;
#14278=CARTESIAN_POINT ( 'NONE',  ( 2.000000000000001776, 0.000000000000000000, 0.000000000000000000 ) ) ;
#14279=CARTESIAN_POINT ( 'NONE',  ( 1.000000000000000888, -5.662015959325143122, -4.918493191654053298 ) ) ;
#14280=ORIENTED_EDGE ( 'NONE', *, *, #24164, .F. ) ;
#14281=ORIENTED_EDGE ( 'NONE', *, *, #10794, .T. ) ;
#14282=ORIENTED_EDGE ( 'NONE', *, *, #1807, .F. ) ;
#14290=LINE ( 'NONE', #15279, #33956 ) ;
#14295=ORIENTED_EDGE ( 'NONE', *, *, #24301, .F. ) ;
#14298=EDGE_LOOP ( 'NONE', ( #43207, #30554, #50458, #26483 ) ) ;
#14304=CARTESIAN_POINT ( 'NONE',  ( 0.000000000000000000, -4.962980376314023445, -4.846014654777856201 ) ) ;
#14306=EDGE_LOOP ( 'NONE', ( #60231, #6402, #27430, #18965 ) ) ;
#14316=LINE ( 'NONE', #35246, #25958 ) ;
#14317=ORIENTED_EDGE ( 'NONE', *, *, #24848, .T. ) ;
#14325=DIRECTION ( 'NONE',  ( -1.000000000000000000, 0.000000000000000000, 0.000000000000000000 ) ) ;
#14329=AXIS2_PLACEMENT_3D ( 'NONE', #30267, #15297, #5007 ) ;
#14330=EDGE_LOOP ( 'NONE', ( #2930, #33113, #65798, #7941 ) ) ;
#14332=CARTESIAN_POINT ( 'NONE',  ( 0.000000000000000000, -4.472310526050796931, 6.020667617347345235 ) ) ;
#14340=CARTESIAN_POINT ( 'NONE',  ( 0.000000000000000000, 0.000000000000000000, 0.000000000000000000 ) ) ;
#14341=B_SPLINE_CURVE_WITH_KNOTS ( 'NONE', 3,
 ( #3129, #27074, #17086, #33370, #57332, #53670, #18080, #12739, #2123, #22749, #58665, #63951, #57998, #32042, #53334, #7778, #47367, #43662, #52360, #12409, #13088, #62963 ),
 .UNSPECIFIED., .F., .F.,
 ( 4, 3, 3, 3, 3, 3, 3, 4 ),
 ( 1.560799312097622405E-17, 4.455945684386779400E-05, 6.636307477204042159E-05, 8.816671873158962063E-05, 0.0001099660380492628749, 0.0001317545563165329193, 0.0001762613022895090831, 0.0001867992666138409204 ),
 .UNSPECIFIED. ) ;
#14342=EDGE_CURVE ( 'NONE', #53268, #14064, #18321, .T. ) ;
#14352=DIRECTION ( 'NONE',  ( 0.000000000000000000, -6.879075853011489629E-15, 1.000000000000000000 ) ) ;
#14353=ORIENTED_EDGE ( 'NONE', *, *, #8923, .T. ) ;
#14359=VERTEX_POINT ( 'NONE', #44638 ) ;
#14375=CARTESIAN_POINT ( 'NONE',  ( 2.000000000000001776, 3.152010634611693174, 6.039758645301271933 ) ) ;
#14382=CARTESIAN_POINT ( 'NONE',  ( -27.10719052120871098, -0.1538293304135310291, -2.355164825213519109 ) ) ;
#14385=ORIENTED_EDGE ( 'NONE', *, *, #25836, .T. ) ;
#14390=EDGE_CURVE ( 'NONE', #60024, #41622, #21618, .T. ) ;
#14392=CARTESIAN_POINT ( 'NONE',  ( -27.08423923533013422, 0.2759775751762021390, 2.274768056034770058 ) ) ;
#14395=CARTESIAN_POINT ( 'NONE',  ( -22.28350523959501217, 1.580062893038993499, -3.346230442873227684 ) ) ;
#14401=DIRECTION ( 'NONE',  ( -1.000000000000000000, 0.000000000000000000, 0.000000000000000000 ) ) ;
#14402=ADVANCED_FACE ( 'NONE', ( #52208 ), #27564, .T. ) ;
#14409=LINE ( 'NONE', #25379, #48968 ) ;
#14414=AXIS2_PLACEMENT_3D ( 'NONE', #43011, #16448, #12408 ) ;
#14417=DIRECTION ( 'NONE',  ( 1.000000000000000000, -0.000000000000000000, -0.000000000000000000 ) ) ;
#14420=CARTESIAN_POINT ( 'NONE',  ( -22.27709082389155171, 3.541295940224340022, 1.005749854561671652 ) ) ;
#14421=FACE_OUTER_BOUND ( 'NONE', #62794, .T. ) ;
#14429=CARTESIAN_POINT ( 'NONE',  ( -22.51237073810381517, -0.2145858836692187410, -4.418556976583602136 ) ) ;
#14432=DIRECTION ( 'NONE',  ( -1.000000000000000000, 0.000000000000000000, 0.000000000000000000 ) ) ;
#14440=DIRECTION ( 'NONE',  ( -1.000000000000000000, 0.000000000000000000, 0.000000000000000000 ) ) ;
#14456=ORIENTED_EDGE ( 'NONE', *, *, #60256, .T. ) ;
#14459=CARTESIAN_POINT ( 'NONE',  ( -22.27719381268171261, 0.9730858478814007340, -3.550654232855434689 ) ) ;
#14465=ORIENTED_EDGE ( 'NONE', *, *, #31502, .T. ) ;
#14468=DIRECTION ( 'NONE',  ( 0.000000000000000000, 0.000000000000000000, 1.000000000000000000 ) ) ;
#14478=ORIENTED_EDGE ( 'NONE', *, *, #7429, .F. ) ;
#14479=CARTESIAN_POINT ( 'NONE',  ( 2.000000000000001776, 0.000000000000000000, 0.000000000000000000 ) ) ;
#14482=AXIS2_PLACEMENT_3D ( 'NONE', #5079, #56252, #10366 ) ;
#14494=CARTESIAN_POINT ( 'NONE',  ( 2.000000000000001776, -5.860254403322033845, 3.474373880649773039 ) ) ;
#14502=CARTESIAN_POINT ( 'NONE',  ( -27.10128162969832744, 1.304299867634929999, 1.945744751330081179 ) ) ;
#14503=DIRECTION ( 'NONE',  ( -1.000000000000000000, 0.000000000000000000, 0.000000000000000000 ) ) ;
#14506=DIRECTION ( 'NONE',  ( -1.000000000000000000, 0.000000000000000000, 0.000000000000000000 ) ) ;
#14512=ORIENTED_EDGE ( 'NONE', *, *, #37244, .F. ) ;
#14526=CARTESIAN_POINT ( 'NONE',  ( -27.10307689719060065, 0.5470785519252523432, -2.283215755731191177 ) ) ;
#14532=CARTESIAN_POINT ( 'NONE',  ( 2.000000000000001776, 4.976357229393922665, -4.652926418895522609 ) ) ;
#14541=CARTESIAN_POINT ( 'NONE',  ( -22.28506771379528573, -3.091577134491930057, 2.081613609299069800 ) ) ;
#14544=CARTESIAN_POINT ( 'NONE',  ( -27.20102706715912788, 2.585824624629304402, 0.5453431011644924720 ) ) ;
#14553=CARTESIAN_POINT ( 'NONE',  ( 0.000000000000000000, 6.164400007374783108, 2.900694413976516728 ) ) ;
#14559=CARTESIAN_POINT ( 'NONE',  ( 2.000000000000001776, -4.472310526050796931, 6.020667617347345235 ) ) ;
#14560=CARTESIAN_POINT ( 'NONE',  ( -27.09252613521594455, 2.086468883257836193, 1.005681546875630383 ) ) ;
#14563=EDGE_CURVE ( 'NONE', #50060, #42450, #57624, .T. ) ;
#14567=VERTEX_POINT ( 'NONE', #28880 ) ;
#14570=CIRCLE ( 'NONE', #37986, 2.899999999999993694 ) ;
#14573=EDGE_CURVE ( 'NONE', #21425, #56181, #53350, .T. ) ;
#14577=DIRECTION ( 'NONE',  ( 0.000000000000000000, 0.000000000000000000, 1.000000000000000000 ) ) ;
#14581=CARTESIAN_POINT ( 'NONE',  ( 2.000000000000001776, -5.450255447309714896, -4.087611905901492371 ) ) ;
#14586=CARTESIAN_POINT ( 'NONE',  ( -22.31328051695926007, 0.2528478350594092761, 3.781397440874584071 ) ) ;
#14601=ORIENTED_EDGE ( 'NONE', *, *, #13163, .F. ) ;
#14603=DIRECTION ( 'NONE',  ( 0.000000000000000000, -0.9985334138511243740, 0.05413890858540761075 ) ) ;
#14612=CARTESIAN_POINT ( 'NONE',  ( -27.04788180060268843, 2.923150379392654763, -1.373100113388769694 ) ) ;
#14626=AXIS2_PLACEMENT_3D ( 'NONE', #28711, #2486, #58332 ) ;
#14630=ORIENTED_EDGE ( 'NONE', *, *, #27020, .F. ) ;
#14636=VERTEX_POINT ( 'NONE', #55792 ) ;
#14639=FACE_OUTER_BOUND ( 'NONE', #50299, .T. ) ;
#14667=DIRECTION ( 'NONE',  ( 1.000000000000000000, 0.000000000000000000, 0.000000000000000000 ) ) ;
#14671=DIRECTION ( 'NONE',  ( 1.000000000000000000, 0.000000000000000000, 0.000000000000000000 ) ) ;
#14676=VERTEX_POINT ( 'NONE', #50797 ) ;
#14685=CARTESIAN_POINT ( 'NONE',  ( 2.000000000000001776, -5.457833520448623688, -4.281014542496604847 ) ) ;
#14686=CARTESIAN_POINT ( 'NONE',  ( -22.27722019117890540, 0.6494988092404053726, 3.623917154020592335 ) ) ;
#14690=CARTESIAN_POINT ( 'NONE',  ( -27.09048036756591671, -0.1785511875142926919, -2.303144499688040803 ) ) ;
#14691=DIRECTION ( 'NONE',  ( -1.000000000000000000, 0.000000000000000000, 0.000000000000000000 ) ) ;
#14706=CARTESIAN_POINT ( 'NONE',  ( -27.08429572838383947, 0.5764601019426045525, 2.217805374070519253 ) ) ;
#14713=CYLINDRICAL_SURFACE ( 'NONE', #38760, 7.499999999999988454 ) ;
#14714=AXIS2_PLACEMENT_3D ( 'NONE', #47297, #1075, #42585 ) ;
#14721=FACE_OUTER_BOUND ( 'NONE', #63724, .T. ) ;
#14722=ORIENTED_EDGE ( 'NONE', *, *, #34, .T. ) ;
#14724=DIRECTION ( 'NONE',  ( 0.000000000000000000, 0.000000000000000000, 1.000000000000000000 ) ) ;
#14735=CARTESIAN_POINT ( 'NONE',  ( -22.29978294495153790, 3.598607126810735579, -1.052446240539692601 ) ) ;
#14748=LINE ( 'NONE', #9127, #55901 ) ;
#14755=VERTEX_POINT ( 'NONE', #41796 ) ;
#14762=CARTESIAN_POINT ( 'NONE',  ( -22.29382655386184453, -0.8947172055470686836, 3.622626291186073821 ) ) ;
#14775=CARTESIAN_POINT ( 'NONE',  ( -22.29195009621226475, 0.8975732442595634186, -3.616122380634906541 ) ) ;
#14778=CARTESIAN_POINT ( 'NONE',  ( -22.27711351828769892, 1.028167152775530724, -3.534923377568743419 ) ) ;
#14783=ORIENTED_EDGE ( 'NONE', *, *, #16713, .F. ) ;
#14787=CARTESIAN_POINT ( 'NONE',  ( 2.000000000000001776, 0.4129979343797385294, 6.800241778083691457 ) ) ;
#14789=CYLINDRICAL_SURFACE ( 'NONE', #61665, 7.499999999999988454 ) ;
#14791=DIRECTION ( 'NONE',  ( 0.000000000000000000, 0.8276889981568920085, -0.5611870653623802774 ) ) ;
#14795=CARTESIAN_POINT ( 'NONE',  ( 1.000000000000000888, -6.253963800348222968, -4.139799123621093813 ) ) ;
#14804=EDGE_CURVE ( 'NONE', #31156, #47008, #58721, .T. ) ;
#14817=CARTESIAN_POINT ( 'NONE',  ( 0.000000000000000000, 3.795144977083718008, -6.468916029978776017 ) ) ;
#14818=CIRCLE ( 'NONE', #29739, 2.899999999999996803 ) ;
#14821=ORIENTED_EDGE ( 'NONE', *, *, #28810, .T. ) ;
#14824=DIRECTION ( 'NONE',  ( 0.000000000000000000, 0.000000000000000000, 1.000000000000000000 ) ) ;
#14826=CIRCLE ( 'NONE', #46708, 2.899999999999995026 ) ;
#14827=CARTESIAN_POINT ( 'NONE',  ( -35.04709527796842394, -0.005220632201001842998, -0.01120703303053409428 ) ) ;
#14837=CARTESIAN_POINT ( 'NONE',  ( -22.27706485742869091, -3.563814065926672381, 0.9221835209182321913 ) ) ;
#14846=ORIENTED_EDGE ( 'NONE', *, *, #54746, .F. ) ;
#14847=CIRCLE ( 'NONE', #52053, 7.499999999999988454 ) ;
#14850=CARTESIAN_POINT ( 'NONE',  ( -27.09861164373156939, 2.328930759213688528, -0.1603819633258264654 ) ) ;
#14863=DIRECTION ( 'NONE',  ( -1.000000000000000000, 0.000000000000000000, 0.000000000000000000 ) ) ;
#14874=CARTESIAN_POINT ( 'NONE',  ( -22.28350523959500862, -3.687952016964556545, 0.3047406164877147772 ) ) ;
#14876=DIRECTION ( 'NONE',  ( 0.000000000000000000, 0.000000000000000000, 1.000000000000000000 ) ) ;
#14883=VECTOR ( 'NONE', #3115, 1000.000000000000000 ) ;
#14889=CARTESIAN_POINT ( 'NONE',  ( -27.08850691366518504, -0.5697889027520377514, 2.232573186529265730 ) ) ;
#14890=ORIENTED_EDGE ( 'NONE', *, *, #40699, .F. ) ;
#14891=CARTESIAN_POINT ( 'NONE',  ( 2.000000000000001776, 6.586971819220337032, 3.586335490831404460 ) ) ;
#14892=CARTESIAN_POINT ( 'NONE',  ( -23.18047892478188743, -4.338318103648297175, 2.037851053449315941 ) ) ;
#14896=FACE_OUTER_BOUND ( 'NONE', #61294, .T. ) ;
#14899=DIRECTION ( 'NONE',  ( 0.000000000000000000, 0.000000000000000000, 1.000000000000000000 ) ) ;
#14904=CARTESIAN_POINT ( 'NONE',  ( -22.27711351828769892, -3.534923377568741198, -1.028167152775526283 ) ) ;
#14905=CARTESIAN_POINT ( 'NONE',  ( -27.08416974970326763, 0.4041872645907068629, 2.255186831366090772 ) ) ;
#14910=AXIS2_PLACEMENT_3D ( 'NONE', #61707, #11183, #52075 ) ;
#14911=EDGE_CURVE ( 'NONE', #2752, #8369, #24722, .T. ) ;
#14923=CARTESIAN_POINT ( 'NONE',  ( -22.31328051695926007, -1.076152733467184985, -3.633840107626963967 ) ) ;
#14929=CARTESIAN_POINT ( 'NONE',  ( -27.09833916700227263, -2.268067253344212553, -0.5492787772350189446 ) ) ;
#14931=ORIENTED_EDGE ( 'NONE', *, *, #2146, .T. ) ;
#14950=ORIENTED_EDGE ( 'NONE', *, *, #62828, .T. ) ;
#14956=CARTESIAN_POINT ( 'NONE',  ( 2.000000000000001776, -4.915517050588423587, 4.717154614762070430 ) ) ;
#14957=CIRCLE ( 'NONE', #31950, 6.936499999999989008 ) ;
#14962=CIRCLE ( 'NONE', #30923, 2.899999999999995026 ) ;
#14966=CARTESIAN_POINT ( 'NONE',  ( 1.000000000000000888, 0.08317740279942427428, -7.499538753794372070 ) ) ;
#14975=AXIS2_PLACEMENT_3D ( 'NONE', #2517, #22788, #48057 ) ;
#14980=DIRECTION ( 'NONE',  ( -1.000000000000000000, 0.000000000000000000, 0.000000000000000000 ) ) ;
#14982=CARTESIAN_POINT ( 'NONE',  ( -35.04582288351658548, -0.002280196168880422626, 0.01249938581187134620 ) ) ;
#14984=DIRECTION ( 'NONE',  ( 0.000000000000000000, 0.000000000000000000, 1.000000000000000000 ) ) ;
#14986=AXIS2_PLACEMENT_3D ( 'NONE', #6682, #21961, #26293 ) ;
#14989=CARTESIAN_POINT ( 'NONE',  ( -27.09252613521643127, -1.304094283668831400, -1.914180209342516426 ) ) ;
#14990=VECTOR ( 'NONE', #43110, 1000.000000000000114 ) ;
#14991=ORIENTED_EDGE ( 'NONE', *, *, #40687, .T. ) ;
#14992=CARTESIAN_POINT ( 'NONE',  ( 2.000000000000001776, 6.997684042076903310, 2.698595569414223849 ) ) ;
#14994=DIRECTION ( 'NONE',  ( 0.000000000000000000, 0.6876994588534194319, 0.7259954919231345061 ) ) ;
#14995=AXIS2_PLACEMENT_3D ( 'NONE', #43992, #3117, #18068 ) ;
#14997=VERTEX_POINT ( 'NONE', #48345 ) ;
#14999=AXIS2_PLACEMENT_3D ( 'NONE', #49812, #8919, #15205 ) ;
#15010=CARTESIAN_POINT ( 'NONE',  ( -22.29290468048228036, 0.2747050847461964262, 3.718584170466863181 ) ) ;
#15018=ORIENTED_EDGE ( 'NONE', *, *, #26511, .F. ) ;
#15023=B_SPLINE_CURVE_WITH_KNOTS ( 'NONE', 3,
 ( #3273, #37849, #63429, #28516, #53810, #23884, #18884, #64412, #43472, #44148, #48184, #2638, #63751, #23211, #17898, #48497, #2948, #48823, #22899, #43821, #64101, #18232 ),
 .UNSPECIFIED., .F., .F.,
 ( 4, 3, 3, 3, 3, 3, 3, 4 ),
 ( 6.774311733015938998E-18, 4.455945684386482600E-05, 6.636307477203528518E-05, 8.816671873158391502E-05, 0.0001099660380492575894, 0.0001317545563165268478, 0.0001762613022895026863, 0.0001867992666138357976 ),
 .UNSPECIFIED. ) ;
#15024=LINE ( 'NONE', #4767, #40438 ) ;
#15029=VECTOR ( 'NONE', #51945, 1000.000000000000000 ) ;
#15033=CARTESIAN_POINT ( 'NONE',  ( -27.08430418657511751, -0.2231435303617161081, -2.280643121250633509 ) ) ;
#15036=EDGE_LOOP ( 'NONE', ( #3928, #22278, #3281, #19029 ) ) ;
#15037=CARTESIAN_POINT ( 'NONE',  ( -35.04709527796842394, 0.007030359780627049027, -0.01016988845958279042 ) ) ;
#15038=ORIENTED_EDGE ( 'NONE', *, *, #17706, .T. ) ;
#15044=CARTESIAN_POINT ( 'NONE',  ( -27.08850691366480490, -2.218359546717756814, 0.6228349286848108290 ) ) ;
#15045=CARTESIAN_POINT ( 'NONE',  ( -22.28482751661422867, 1.587261331312507240, -3.347211412506322148 ) ) ;
#15053=DIRECTION ( 'NONE',  ( 0.000000000000000000, 0.7621620551276377942, -0.6473862847818260269 ) ) ;
#15054=VECTOR ( 'NONE', #21986, 1000.000000000000000 ) ;
#15071=AXIS2_PLACEMENT_3D ( 'NONE', #37414, #2529, #58043 ) ;
#15075=DIRECTION ( 'NONE',  ( 1.000000000000000000, 0.000000000000000000, 0.000000000000000000 ) ) ;
#15076=DIRECTION ( 'NONE',  ( -1.000000000000000000, 0.000000000000000000, 0.000000000000000000 ) ) ;
#15078=DIRECTION ( 'NONE',  ( 1.000000000000000000, 0.000000000000000000, 0.000000000000000000 ) ) ;
#15079=EDGE_CURVE ( 'NONE', #22351, #14567, #18226, .T. ) ;
#15080=CARTESIAN_POINT ( 'NONE',  ( -22.27722022243424149, 3.470949075637794312, 1.227876413014556078 ) ) ;
#15094=CARTESIAN_POINT ( 'NONE',  ( -22.65996813707688062, -2.220979297960720800, -4.292955455498900896 ) ) ;
#15096=AXIS2_PLACEMENT_3D ( 'NONE', #50624, #15360, #35633 ) ;
#15101=ORIENTED_EDGE ( 'NONE', *, *, #11894, .F. ) ;
#15111=CYLINDRICAL_SURFACE ( 'NONE', #40964, 6.936499999999988120 ) ;
#15117=ORIENTED_EDGE ( 'NONE', *, *, #40473, .F. ) ;
#15120=CIRCLE ( 'NONE', #4562, 2.899999999999995026 ) ;
#15122=CARTESIAN_POINT ( 'NONE',  ( -22.28415773361650309, 0.9182279841530148756, -3.586804264761557004 ) ) ;
#15127=DIRECTION ( 'NONE',  ( -1.000000000000000000, 0.000000000000000000, 0.000000000000000000 ) ) ;
#15128=VECTOR ( 'NONE', #15342, 1000.000000000000114 ) ;
#15133=LINE ( 'NONE', #10153, #54049 ) ;
#15147=CARTESIAN_POINT ( 'NONE',  ( 2.000000000000001776, -4.409940824963369366, -5.354199675985328533 ) ) ;
#15165=CARTESIAN_POINT ( 'NONE',  ( 0.000000000000000000, 7.414200355365252015, 1.131208685655162638 ) ) ;
#15166=EDGE_LOOP ( 'NONE', ( #37111, #44033, #47519, #36067 ) ) ;
#15167=CARTESIAN_POINT ( 'NONE',  ( -27.09833916700227618, 2.268067253344194345, 0.5492787772349813080 ) ) ;
#15172=EDGE_CURVE ( 'NONE', #10704, #39168, #18733, .T. ) ;
#15173=ORIENTED_EDGE ( 'NONE', *, *, #30872, .T. ) ;
#15186=CARTESIAN_POINT ( 'NONE',  ( 1.000000000000000888, 7.248432822490286753, -1.926193556692960440 ) ) ;
#15189=CARTESIAN_POINT ( 'NONE',  ( 1.000000000000000888, 5.769711778877324448, 4.791703871138532023 ) ) ;
#15194=DIRECTION ( 'NONE',  ( 0.000000000000000000, 0.000000000000000000, 1.000000000000000000 ) ) ;
#15197=AXIS2_PLACEMENT_3D ( 'NONE', #58076, #7511, #5755 ) ;
#15201=DIRECTION ( 'NONE',  ( -1.000000000000000000, 0.000000000000000000, 0.000000000000000000 ) ) ;
#15205=DIRECTION ( 'NONE',  ( 0.000000000000000000, 0.000000000000000000, 1.000000000000000000 ) ) ;
#15219=CIRCLE ( 'NONE', #4621, 2.899999999999996358 ) ;
#15223=B_SPLINE_CURVE_WITH_KNOTS ( 'NONE', 3,
 ( #30902, #22243, #1662, #56871, #31563, #61490 ),
 .UNSPECIFIED., .F., .F.,
 ( 4, 2, 4 ),
 ( 0.0001654224980408431343, 0.0006219428995476530570, 0.001078463301054462817 ),
 .UNSPECIFIED. ) ;
#15226=LINE ( 'NONE', #61759, #63772 ) ;
#15230=CARTESIAN_POINT ( 'NONE',  ( 0.000000000000000000, -3.224464355699781848, -6.771471746882029130 ) ) ;
#15237=CARTESIAN_POINT ( 'NONE',  ( -27.15525204139121840, -0.5628609503965525951, 2.440367606305302139 ) ) ;
#15240=CARTESIAN_POINT ( 'NONE',  ( -27.28573687977897322, 1.818142657385575900, -2.255103317860381207 ) ) ;
#15246=DIRECTION ( 'NONE',  ( 0.000000000000000000, -0.9289767198167871998, -0.3701381553399246682 ) ) ;
#15253=ORIENTED_EDGE ( 'NONE', *, *, #24393, .T. ) ;
#15266=AXIS2_PLACEMENT_3D ( 'NONE', #27435, #38066, #1858 ) ;
#15271=AXIS2_PLACEMENT_3D ( 'NONE', #57372, #32080, #21125 ) ;
#15272=CARTESIAN_POINT ( 'NONE',  ( -27.09252613521594455, 1.914180209340472283, -1.304094283669201770 ) ) ;
#15273=EDGE_LOOP ( 'NONE', ( #49699, #54346, #7069, #16104 ) ) ;
#15279=CARTESIAN_POINT ( 'NONE',  ( 1.000000000000000888, -2.473437528934089524, -7.080403010455012414 ) ) ;
#15280=CARTESIAN_POINT ( 'NONE',  ( -27.08485414902839494, -2.215517476308469735, -0.5917839443972630065 ) ) ;
#15284=DIRECTION ( 'NONE',  ( -1.000000000000000000, 0.000000000000000000, 0.000000000000000000 ) ) ;
#15285=VERTEX_POINT ( 'NONE', #10624 ) ;
#15286=CARTESIAN_POINT ( 'NONE',  ( 0.000000000000000000, -1.693411908627144635, -7.306323022404617618 ) ) ;
#15287=ORIENTED_EDGE ( 'NONE', *, *, #35766, .F. ) ;
#15297=DIRECTION ( 'NONE',  ( -1.000000000000000000, 0.000000000000000000, 0.000000000000000000 ) ) ;
#15298=ORIENTED_EDGE ( 'NONE', *, *, #23302, .T. ) ;
#15301=VERTEX_POINT ( 'NONE', #51231 ) ;
#15303=AXIS2_PLACEMENT_3D ( 'NONE', #44091, #58085, #28461 ) ;
#15308=DIRECTION ( 'NONE',  ( 0.9606638835031803270, 0.2762341707520464262, -0.02862840969242635286 ) ) ;
#15309=ADVANCED_FACE ( 'NONE', ( #30272 ), #31569, .T. ) ;
#15318=CARTESIAN_POINT ( 'NONE',  ( 2.000000000000001776, 0.000000000000000000, 0.000000000000000000 ) ) ;
#15319=EDGE_CURVE ( 'NONE', #15877, #4941, #1542, .T. ) ;
#15320=EDGE_CURVE ( 'NONE', #18772, #52982, #8714, .T. ) ;
#15327=ADVANCED_FACE ( 'NONE', ( #63146 ), #57857, .T. ) ;
#15329=CARTESIAN_POINT ( 'NONE',  ( -22.27218376572352554, 0.3046453028544620634, 3.670373711461409005 ) ) ;
#15336=VERTEX_POINT ( 'NONE', #37876 ) ;
#15342=DIRECTION ( 'NONE',  ( -0.9582930651793755139, -0.1972632429577093616, 0.2067888154783157351 ) ) ;
#15344=DIRECTION ( 'NONE',  ( 1.000000000000000000, 0.000000000000000000, 0.000000000000000000 ) ) ;
#15352=DIRECTION ( 'NONE',  ( 0.000000000000000000, 0.000000000000000000, 1.000000000000000000 ) ) ;
#15360=DIRECTION ( 'NONE',  ( -1.000000000000000000, 0.000000000000000000, 0.000000000000000000 ) ) ;
#15369=CARTESIAN_POINT ( 'NONE',  ( 0.000000000000000000, -4.915517050588423587, 4.717154614762070430 ) ) ;
#15371=CARTESIAN_POINT ( 'NONE',  ( -27.08421860617808008, 2.271664812096775066, -0.2990745872176354681 ) ) ;
#15373=CARTESIAN_POINT ( 'NONE',  ( -27.35552965826137140, -2.548625910254533888, -1.773915698030580357 ) ) ;
#15374=VERTEX_POINT ( 'NONE', #7621 ) ;
#15376=ADVANCED_FACE ( 'NONE', ( #27904 ), #48214, .T. ) ;
#15377=AXIS2_PLACEMENT_3D ( 'NONE', #44101, #4192, #18834 ) ;
#15395=CARTESIAN_POINT ( 'NONE',  ( 1.000000000000000888, 6.160607635185464837, -4.277489166005534749 ) ) ;
#15396=LINE ( 'NONE', #30673, #45585 ) ;
#15398=CARTESIAN_POINT ( 'NONE',  ( -27.08704841010891329, -0.9786466045354095256, 2.081152044925695943 ) ) ;
#15399=AXIS2_PLACEMENT_3D ( 'NONE', #38367, #19079, #2830 ) ;
#15403=LINE ( 'NONE', #55968, #49815 ) ;
#15414=CARTESIAN_POINT ( 'NONE',  ( -35.04643116707788408, -0.008094444324497490628, -0.009112266603826177369 ) ) ;
#15415=CARTESIAN_POINT ( 'NONE',  ( -22.27721701579900682, 3.478642907697087505, 1.205877546543679291 ) ) ;
#15418=CARTESIAN_POINT ( 'NONE',  ( 2.000000000000001776, -4.409940824963459960, 5.354199675985231721 ) ) ;
#15425=ORIENTED_EDGE ( 'NONE', *, *, #43964, .T. ) ;
#15426=CARTESIAN_POINT ( 'NONE',  ( -28.67667724226168602, 1.574547667005687490, -1.049259427760464547 ) ) ;
#15440=CARTESIAN_POINT ( 'NONE',  ( -22.28415773361649954, -0.9182279841529923381, 3.586804264761546790 ) ) ;
#15450=ORIENTED_EDGE ( 'NONE', *, *, #50631, .F. ) ;
#15451=CARTESIAN_POINT ( 'NONE',  ( -23.41523303002442091, -3.856096202952855823, -2.683951991546297045 ) ) ;
#15466=DIRECTION ( 'NONE',  ( -1.000000000000000000, 0.000000000000000000, 0.000000000000000000 ) ) ;
#15470=CARTESIAN_POINT ( 'NONE',  ( 2.000000000000001776, 3.230174184210066191, 5.998318953995321223 ) ) ;
#15471=CARTESIAN_POINT ( 'NONE',  ( -35.05175862995318425, -0.003178856583444314432, 0.01216930940958239893 ) ) ;
#15477=CARTESIAN_POINT ( 'NONE',  ( -27.15511094194037867, 2.237231637349079261, 1.124668417986046220 ) ) ;
#15478=DIRECTION ( 'NONE',  ( 0.000000000000000000, 0.000000000000000000, 1.000000000000000000 ) ) ;
#15482=ORIENTED_EDGE ( 'NONE', *, *, #24232, .T. ) ;
#15486=ORIENTED_EDGE ( 'NONE', *, *, #41382, .F. ) ;
#15489=CARTESIAN_POINT ( 'NONE',  ( -22.28856623400852399, -1.018212315222191355, -3.573466130470484003 ) ) ;
#15493=EDGE_CURVE ( 'NONE', #8461, #45502, #28069, .T. ) ;
#15495=ORIENTED_EDGE ( 'NONE', *, *, #57069, .T. ) ;
#15496=CARTESIAN_POINT ( 'NONE',  ( -35.04834644901396956, 0.004537648929124128358, 0.01306875526353049738 ) ) ;
#15501=FACE_OUTER_BOUND ( 'NONE', #63413, .T. ) ;
#15504=VERTEX_POINT ( 'NONE', #64130 ) ;
#15508=CARTESIAN_POINT ( 'NONE',  ( 2.000000000000001776, 6.796153407501448029, 1.388283512725836388 ) ) ;
#15512=ORIENTED_EDGE ( 'NONE', *, *, #61683, .F. ) ;
#15513=CYLINDRICAL_SURFACE ( 'NONE', #52108, 2.899999999999994582 ) ;
#15514=( BOUNDED_SURFACE ( )  B_SPLINE_SURFACE ( 3, 1, ( 
 ( #64994, #30411 ),
 ( #44703, #45058 ),
 ( #61320, #19794 ),
 ( #10132, #34722 ) ),
 .UNSPECIFIED., .F., .F., .F. ) 
 B_SPLINE_SURFACE_WITH_KNOTS ( ( 4, 4 ),
 ( 2, 2 ),
 ( 0.000000000000000000, 1.000000000000000000 ),
 ( 0.000000000000000000, 1.000000000000000000 ),
 .UNSPECIFIED. ) 
 GEOMETRIC_REPRESENTATION_ITEM ( )  RATIONAL_B_SPLINE_SURFACE ( (
 ( 1.000000000000000000, 1.000000000000000000),
 ( 0.9932032654565553509, 0.8386279382598736953),
 ( 0.9932032654565553509, 0.8386279382598736953),
 ( 1.000000000000000000, 1.000000000000000000) ) ) 
 REPRESENTATION_ITEM ( '' )  SURFACE ( )  );
#15530=CARTESIAN_POINT ( 'NONE',  ( -22.39032720737625937, -1.170177197944852754, -3.847057950743297816 ) ) ;
#15535=CARTESIAN_POINT ( 'NONE',  ( 0.000000000000000000, 3.155844197800189210, -6.177028383390422484 ) ) ;
#15543=CARTESIAN_POINT ( 'NONE',  ( 0.000000000000000000, -3.152010634611731366, 6.039758645301271933 ) ) ;
#15545=EDGE_CURVE ( 'NONE', #56025, #666, #31653, .T. ) ;
#15549=CARTESIAN_POINT ( 'NONE',  ( -22.30527770659433173, -3.757123197210717525, 0.2559941915621729014 ) ) ;
#15559=CARTESIAN_POINT ( 'NONE',  ( -22.38932658256919339, 3.587092141214309748, 1.810630688302267588 ) ) ;
#15561=CARTESIAN_POINT ( 'NONE',  ( -27.32337605527166957, 1.812546145273359111, -2.404211887218399735 ) ) ;
#15562=ORIENTED_EDGE ( 'NONE', *, *, #44087, .T. ) ;
#15563=CARTESIAN_POINT ( 'NONE',  ( -27.09569413923886216, -0.5521997980573341014, 2.259195818745851181 ) ) ;
#15568=FACE_OUTER_BOUND ( 'NONE', #24849, .T. ) ;
#15590=EDGE_LOOP ( 'NONE', ( #18515, #43582, #29258, #27949 ) ) ;
#15593=ORIENTED_EDGE ( 'NONE', *, *, #28278, .F. ) ;
#15600=CARTESIAN_POINT ( 'NONE',  ( -27.08429572838383947, 1.632445743623435197, -1.608131779585709076 ) ) ;
#15605=B_SPLINE_CURVE_WITH_KNOTS ( 'NONE', 3,
 ( #25155, #51095, #36444, #11178, #55752, #16499, #30463, #31453, #25477, #46421 ),
 .UNSPECIFIED., .F., .F.,
 ( 4, 3, 3, 4 ),
 ( 5.401523115762199855E-05, 0.0008136511341527787088, 0.004068255670953081944, 0.005063778443040923075 ),
 .UNSPECIFIED. ) ;
#15608=LINE ( 'NONE', #65804, #25617 ) ;
#15623=ORIENTED_EDGE ( 'NONE', *, *, #37533, .F. ) ;
#15624=DIRECTION ( 'NONE',  ( 0.000000000000000000, 0.8276889981568920085, -0.5611870653623801664 ) ) ;
#15625=EDGE_CURVE ( 'NONE', #19640, #63755, #11074, .T. ) ;
#15626=ORIENTED_EDGE ( 'NONE', *, *, #27381, .F. ) ;
#15634=CARTESIAN_POINT ( 'NONE',  ( -28.66013792860432119, 0.7552004871165373112, -1.673433383655440920 ) ) ;
#15635=DIRECTION ( 'NONE',  ( -1.000000000000000000, 0.000000000000000000, 0.000000000000000000 ) ) ;
#15636=AXIS2_PLACEMENT_3D ( 'NONE', #57511, #36563, #57179 ) ;
#15638=AXIS2_PLACEMENT_3D ( 'NONE', #51456, #50775, #45781 ) ;
#15639=CARTESIAN_POINT ( 'NONE',  ( 1.000000000000000888, -6.253963800348261159, 4.139799123620986343 ) ) ;
#15644=ORIENTED_EDGE ( 'NONE', *, *, #48047, .F. ) ;
#15645=EDGE_CURVE ( 'NONE', #44474, #50020, #2490, .T. ) ;
#15656=CARTESIAN_POINT ( 'NONE',  ( -22.27715239060371744, 0.8317362037004401021, 3.586346956688089449 ) ) ;
#15669=ORIENTED_EDGE ( 'NONE', *, *, #64598, .T. ) ;
#15670=CARTESIAN_POINT ( 'NONE',  ( -28.67667724226168602, 0.5419187306520724112, 1.812862320140625982 ) ) ;
#15671=ADVANCED_FACE ( 'NONE', ( #48688 ), #28078, .T. ) ;
#15678=CARTESIAN_POINT ( 'NONE',  ( -27.08421723179412410, 2.234476190936505180, -0.5069555058557374538 ) ) ;
#15691=FACE_OUTER_BOUND ( 'NONE', #27372, .T. ) ;
#15693=DIRECTION ( 'NONE',  ( 0.000000000000000000, 0.000000000000000000, 1.000000000000000000 ) ) ;
#15702=DIRECTION ( 'NONE',  ( 0.000000000000000000, 0.000000000000000000, 1.000000000000000000 ) ) ;
#15705=CIRCLE ( 'NONE', #39068, 2.899999999999994582 ) ;
#15711=VECTOR ( 'NONE', #11132, 1000.000000000000000 ) ;
#15715=CARTESIAN_POINT ( 'NONE',  ( 2.000000000000001776, 6.539067737394503865, 2.314222412769824544 ) ) ;
#15721=ORIENTED_EDGE ( 'NONE', *, *, #37307, .F. ) ;
#15724=CARTESIAN_POINT ( 'NONE',  ( -22.27878402819508707, 3.558531829368145605, -0.9624056734348108710 ) ) ;
#15730=ORIENTED_EDGE ( 'NONE', *, *, #27608, .F. ) ;
#15731=CARTESIAN_POINT ( 'NONE',  ( -27.08419642509983305, -1.697757994346402510, 1.538761233743662693 ) ) ;
#15750=ORIENTED_EDGE ( 'NONE', *, *, #15079, .T. ) ;
#15770=CARTESIAN_POINT ( 'NONE',  ( 2.000000000000001776, -5.814643797626899868, -3.550179297009637747 ) ) ;
#15772=CARTESIAN_POINT ( 'NONE',  ( -22.27718112499583469, 1.380338971069160925, -3.412978993569787622 ) ) ;
#15775=CARTESIAN_POINT ( 'NONE',  ( -22.27721056931765631, -0.7178530073137546763, -3.610969226755205153 ) ) ;
#15778=DIRECTION ( 'NONE',  ( 1.000000000000000000, 0.000000000000000000, 0.000000000000000000 ) ) ;
#15792=CIRCLE ( 'NONE', #17916, 2.899999999999994582 ) ;
#15801=ORIENTED_EDGE ( 'NONE', *, *, #34370, .F. ) ;
#15802=AXIS2_PLACEMENT_3D ( 'NONE', #47457, #61408, #40822 ) ;
#15805=DIRECTION ( 'NONE',  ( 0.000000000000000000, -0.5155538571770288403, 0.8568571761675849441 ) ) ;
#15809=ORIENTED_EDGE ( 'NONE', *, *, #22626, .T. ) ;
#15810=DIRECTION ( 'NONE',  ( -1.000000000000000000, 0.000000000000000000, 0.000000000000000000 ) ) ;
#15813=ORIENTED_EDGE ( 'NONE', *, *, #16498, .F. ) ;
#15816=CARTESIAN_POINT ( 'NONE',  ( -27.32337605527168023, -2.988381643048340752, -0.3676050637290815826 ) ) ;
#15822=EDGE_LOOP ( 'NONE', ( #42286, #57999, #41698, #10973 ) ) ;
#15826=DIRECTION ( 'NONE',  ( -1.000000000000000000, 0.000000000000000000, 0.000000000000000000 ) ) ;
#15832=CIRCLE ( 'NONE', #20077, 2.899999999999994582 ) ;
#15833=CARTESIAN_POINT ( 'NONE',  ( -22.27716857039623477, -1.095155339732089894, 3.514919882996458078 ) ) ;
#15834=VERTEX_POINT ( 'NONE', #30361 ) ;
#15841=CARTESIAN_POINT ( 'NONE',  ( -27.09483304420744787, 1.013994808269859771, -2.090133548855283241 ) ) ;
#15845=CARTESIAN_POINT ( 'NONE',  ( 2.000000000000001776, 3.805198749487521681, -5.799611601383208637 ) ) ;
#15851=DIRECTION ( 'NONE',  ( -1.000000000000000000, 0.000000000000000000, 0.000000000000000000 ) ) ;
#15860=CARTESIAN_POINT ( 'NONE',  ( 0.000000000000000000, 4.472310526050849333, -6.020667617347339906 ) ) ;
#15863=CARTESIAN_POINT ( 'NONE',  ( -22.28776923226070750, -3.702096209084111855, 0.2883912626656597866 ) ) ;
#15868=CARTESIAN_POINT ( 'NONE',  ( -22.27834755396594346, 2.756126180273648085, -2.447855249718977166 ) ) ;
#15869=DIRECTION ( 'NONE',  ( 0.000000000000000000, 0.000000000000000000, 1.000000000000000000 ) ) ;
#15871=CARTESIAN_POINT ( 'NONE',  ( -22.35190811654612020, 3.498661567523018601, 1.736165297230968463 ) ) ;
#15873=ADVANCED_FACE ( 'NONE', ( #9396 ), #34671, .T. ) ;
#15877=VERTEX_POINT ( 'NONE', #14706 ) ;
#15880=CARTESIAN_POINT ( 'NONE',  ( -27.09833916700337753, -0.5492787772339994268, 2.268067253347839429 ) ) ;
#15884=DIRECTION ( 'NONE',  ( 0.000000000000000000, 0.000000000000000000, 1.000000000000000000 ) ) ;
#15888=ORIENTED_EDGE ( 'NONE', *, *, #59476, .F. ) ;
#15892=VERTEX_POINT ( 'NONE', #30024 ) ;
#15898=CARTESIAN_POINT ( 'NONE',  ( 1.000000000000000888, 1.530946385938382059, 7.342084388195351252 ) ) ;
#15910=ORIENTED_EDGE ( 'NONE', *, *, #65521, .F. ) ;
#15926=CARTESIAN_POINT ( 'NONE',  ( 0.000000000000000000, 0.000000000000000000, 0.000000000000000000 ) ) ;
#15931=CARTESIAN_POINT ( 'NONE',  ( 2.000000000000001776, 6.338823199656684615, 2.816798305433696470 ) ) ;
#15932=ORIENTED_EDGE ( 'NONE', *, *, #54329, .F. ) ;
#15934=ORIENTED_EDGE ( 'NONE', *, *, #15320, .T. ) ;
#15936=DIRECTION ( 'NONE',  ( -1.000000000000000000, 0.000000000000000000, 0.000000000000000000 ) ) ;
#15938=FACE_OUTER_BOUND ( 'NONE', #13185, .T. ) ;
#15951=CARTESIAN_POINT ( 'NONE',  ( -22.51237073810381162, -1.333315726166072190, -4.218051923713597162 ) ) ;
#15957=CARTESIAN_POINT ( 'NONE',  ( 2.000000000000001776, 6.767909380267608022, -0.7805499053121014441 ) ) ;
#15968=AXIS2_PLACEMENT_3D ( 'NONE', #57797, #7555, #12214 ) ;
#15975=CARTESIAN_POINT ( 'NONE',  ( -28.67667724226168602, 1.299025457479356938, -1.375746547601627956 ) ) ;
#15977=CARTESIAN_POINT ( 'NONE',  ( 2.000000000000001776, 0.4804830611970945520, -6.919838746524566986 ) ) ;
#15980=ORIENTED_EDGE ( 'NONE', *, *, #32209, .T. ) ;
#15981=VERTEX_POINT ( 'NONE', #5428 ) ;
#15989=CARTESIAN_POINT ( 'NONE',  ( 2.000000000000001776, -3.073484823194374993, 6.841322316745024779 ) ) ;
#15991=VECTOR ( 'NONE', #41612, 1000.000000000000000 ) ;
#15994=CARTESIAN_POINT ( 'NONE',  ( -22.27706485742869091, 0.3729136217356220917, 3.662257305743802149 ) ) ;
#15997=ORIENTED_EDGE ( 'NONE', *, *, #41018, .T. ) ;
#16000=DIRECTION ( 'NONE',  ( 0.000000000000000000, 0.000000000000000000, 1.000000000000000000 ) ) ;
#16004=VERTEX_POINT ( 'NONE', #37300 ) ;
#16008=DIRECTION ( 'NONE',  ( -1.000000000000000000, 0.000000000000000000, 0.000000000000000000 ) ) ;
#16011=CARTESIAN_POINT ( 'NONE',  ( -27.08579483061203064, -0.2015567301747530349, -2.287150433979712627 ) ) ;
#16017=CYLINDRICAL_SURFACE ( 'NONE', #50816, 2.899999999999994582 ) ;
#16020=CARTESIAN_POINT ( 'NONE',  ( 2.000000000000001776, 6.767909380267608022, -0.7805499053121014441 ) ) ;
#16034=ORIENTED_EDGE ( 'NONE', *, *, #36957, .T. ) ;
#16036=CARTESIAN_POINT ( 'NONE',  ( -27.08456565417846562, -0.9533904527919623284, 2.084650034356363424 ) ) ;
#16038=CIRCLE ( 'NONE', #23462, 2.899999999999994582 ) ;
#16042=CARTESIAN_POINT ( 'NONE',  ( 2.000000000000001776, 0.000000000000000000, 0.000000000000000000 ) ) ;
#16053=B_SPLINE_CURVE_WITH_KNOTS ( 'NONE', 3,
 ( #57895, #23278, #57559, #7005, #43219, #47901, #8008, #33589, #12303, #32261, #18308, #8313, #11979, #48891, #28271, #53876, #63184, #7663, #7312 ),
 .UNSPECIFIED., .F., .F.,
 ( 4, 3, 3, 3, 3, 3, 4 ),
 ( 0.000000000000000000, 2.832085443540691141E-05, 4.217789847394793712E-05, 5.603488375046113660E-05, 6.989180858579362990E-05, 9.821094829918940096E-05, 0.0001178165571465098204 ),
 .UNSPECIFIED. ) ;
#16057=CIRCLE ( 'NONE', #18218, 7.499999999999988454 ) ;
#16077=DIRECTION ( 'NONE',  ( -1.000000000000000000, 0.000000000000000000, 0.000000000000000000 ) ) ;
#16078=CARTESIAN_POINT ( 'NONE',  ( -22.30861784526116054, -3.620936716852757087, 1.070462554923811593 ) ) ;
#16091=ORIENTED_EDGE ( 'NONE', *, *, #20056, .F. ) ;
#16100=ADVANCED_FACE ( 'NONE', ( #47615 ), #2753, .T. ) ;
#16104=ORIENTED_EDGE ( 'NONE', *, *, #9527, .T. ) ;
#16108=VERTEX_POINT ( 'NONE', #23008 ) ;
#16113=DIRECTION ( 'NONE',  ( 0.000000000000000000, 0.000000000000000000, 1.000000000000000000 ) ) ;
#16118=CARTESIAN_POINT ( 'NONE',  ( -22.27716857039623477, -0.8090275962000452736, -3.591587580808010660 ) ) ;
#16123=AXIS2_PLACEMENT_3D ( 'NONE', #48172, #22888, #31531 ) ;
#16124=CARTESIAN_POINT ( 'NONE',  ( -22.27706485742869091, -2.985151051101489372, 2.154081322712201096 ) ) ;
#16130=CARTESIAN_POINT ( 'NONE',  ( -35.04834644901396956, 0.007161132384411757375, 0.01183641858481125804 ) ) ;
#16132=CARTESIAN_POINT ( 'NONE',  ( -27.10719052120871098, -0.5475695427849570640, 2.295785794152556125 ) ) ;
#16134=CARTESIAN_POINT ( 'NONE',  ( -35.04582288351658548, -0.009684687560356024585, -0.008224400713808234509 ) ) ;
#16141=B_SPLINE_CURVE_WITH_KNOTS ( 'NONE', 3,
 ( #54818, #33552, #64759, #64135, #29218, #49513, #8276, #23916 ),
 .UNSPECIFIED., .F., .F.,
 ( 4, 2, 2, 4 ),
 ( 0.000000000000000000, 0.0003639104015150007761, 0.0007278208030300015521, 0.001455641606060003104 ),
 .UNSPECIFIED. ) ;
#16144=AXIS2_PLACEMENT_3D ( 'NONE', #38138, #33157, #37496 ) ;
#16153=EDGE_LOOP ( 'NONE', ( #43080, #3958, #59906, #30549 ) ) ;
#16155=DIRECTION ( 'NONE',  ( 1.000000000000000000, 0.000000000000000000, 0.000000000000000000 ) ) ;
#16158=DIRECTION ( 'NONE',  ( 0.000000000000000000, 0.000000000000000000, 1.000000000000000000 ) ) ;
#16161=ORIENTED_EDGE ( 'NONE', *, *, #8531, .F. ) ;
#16165=CARTESIAN_POINT ( 'NONE',  ( 0.000000000000000000, -1.058508696395003890, 6.730038252034888480 ) ) ;
#16168=CARTESIAN_POINT ( 'NONE',  ( 2.000000000000001776, 5.217815162096836268, 5.387430271863580700 ) ) ;
#16172=ORIENTED_EDGE ( 'NONE', *, *, #31735, .F. ) ;
#16184=DIRECTION ( 'NONE',  ( 1.000000000000000000, 0.000000000000000000, 0.000000000000000000 ) ) ;
#16194=CARTESIAN_POINT ( 'NONE',  ( -27.09252613521643127, 2.309775830546442865, -0.1722886739160208736 ) ) ;
#16195=DIRECTION ( 'NONE',  ( 0.000000000000000000, 0.9289767198167924178, -0.3701381553399118451 ) ) ;
#16197=DIRECTION ( 'NONE',  ( 0.000000000000000000, 0.000000000000000000, -1.000000000000000000 ) ) ;
#16209=CARTESIAN_POINT ( 'NONE',  ( -10.00000000000000178, 0.000000000000000000, 0.000000000000000000 ) ) ;
#16216=DIRECTION ( 'NONE',  ( -0.9606638835031804380, 0.2689826995745335236, -0.06908842350339303162 ) ) ;
#16219=DIRECTION ( 'NONE',  ( -1.000000000000000000, 0.000000000000000000, 0.000000000000000000 ) ) ;
#16228=AXIS2_PLACEMENT_3D ( 'NONE', #46171, #16561, #51502 ) ;
#16234=VERTEX_POINT ( 'NONE', #33945 ) ;
#16238=AXIS2_PLACEMENT_3D ( 'NONE', #54903, #9328, #39934 ) ;
#16242=ORIENTED_EDGE ( 'NONE', *, *, #3993, .F. ) ;
#16243=ORIENTED_EDGE ( 'NONE', *, *, #54188, .F. ) ;
#16252=CARTESIAN_POINT ( 'NONE',  ( 0.000000000000000000, -5.107597897712365054, 4.693343793638375061 ) ) ;
#16260=PLANE ( 'NONE',  #31083 ) ;
#16262=CARTESIAN_POINT ( 'NONE',  ( -27.08485414902845534, 1.622802444813718381, 1.620258667553423182 ) ) ;
#16263=CARTESIAN_POINT ( 'NONE',  ( -22.27721688985630522, 3.631967556481313864, -0.6032462375556627565 ) ) ;
#16264=ORIENTED_EDGE ( 'NONE', *, *, #47054, .T. ) ;
#16274=AXIS2_PLACEMENT_3D ( 'NONE', #28926, #55506, #9950 ) ;
#16275=CIRCLE ( 'NONE', #44935, 2.899999999999995470 ) ;
#16282=ADVANCED_FACE ( 'NONE', ( #35251 ), #24666, .F. ) ;
#16287=CARTESIAN_POINT ( 'NONE',  ( -22.49803948133826381, -3.817825231362863558, -2.073427785788384270 ) ) ;
#16302=EDGE_CURVE ( 'NONE', #52904, #22369, #21616, .T. ) ;
#16306=EDGE_CURVE ( 'NONE', #16747, #44474, #46002, .T. ) ;
#16308=DIRECTION ( 'NONE',  ( 0.000000000000000000, 0.000000000000000000, 1.000000000000000000 ) ) ;
#16313=ORIENTED_EDGE ( 'NONE', *, *, #12366, .F. ) ;
#16316=DIRECTION ( 'NONE',  ( 0.000000000000000000, 0.000000000000000000, 1.000000000000000000 ) ) ;
#16318=CIRCLE ( 'NONE', #423, 2.899999999999995026 ) ;
#16321=( BOUNDED_SURFACE ( )  B_SPLINE_SURFACE ( 3, 1, ( 
 ( #10806, #56361 ),
 ( #31095, #51409 ),
 ( #17368, #32313 ),
 ( #7053, #27326 ) ),
 .UNSPECIFIED., .F., .F., .F. ) 
 B_SPLINE_SURFACE_WITH_KNOTS ( ( 4, 4 ),
 ( 2, 2 ),
 ( 0.000000000000000000, 1.000000000000000000 ),
 ( 0.000000000000000000, 1.000000000000000000 ),
 .UNSPECIFIED. ) 
 GEOMETRIC_REPRESENTATION_ITEM ( )  RATIONAL_B_SPLINE_SURFACE ( (
 ( 1.000000000000000000, 1.000000000000000000),
 ( 0.9932032654565553509, 0.8386279382598736953),
 ( 0.9932032654565553509, 0.8386279382598736953),
 ( 1.000000000000000000, 1.000000000000000000) ) ) 
 REPRESENTATION_ITEM ( '' )  SURFACE ( )  );
#16334=DIRECTION ( 'NONE',  ( -1.000000000000000000, 0.000000000000000000, 0.000000000000000000 ) ) ;
#16340=VERTEX_POINT ( 'NONE', #26932 ) ;
#16346=VERTEX_POINT ( 'NONE', #687 ) ;
#16350=CARTESIAN_POINT ( 'NONE',  ( -22.28482751661422867, 0.2989970708918424647, 3.692400780723903875 ) ) ;
#16373=ADVANCED_FACE ( 'NONE', ( #30590 ), #35895, .T. ) ;
#16382=ORIENTED_EDGE ( 'NONE', *, *, #2503, .F. ) ;
#16387=CARTESIAN_POINT ( 'NONE',  ( -22.23402523511428086, 3.673940397442055431E-16, 2.999999999999992006 ) ) ;
#16399=EDGE_CURVE ( 'NONE', #451, #2871, #63025, .T. ) ;
#16400=DIRECTION ( 'NONE',  ( 0.000000000000000000, 0.6876994588534245390, -0.7259954919231296211 ) ) ;
#16409=LINE ( 'NONE', #7072, #49009 ) ;
#16410=ORIENTED_EDGE ( 'NONE', *, *, #22766, .F. ) ;
#16412=CARTESIAN_POINT ( 'NONE',  ( -22.27706485742869091, 3.358064672837120401, 1.508175983031588840 ) ) ;
#16415=CARTESIAN_POINT ( 'NONE',  ( -22.31328051695926007, 3.633840107626944871, -1.076152733467184985 ) ) ;
#16416=VERTEX_POINT ( 'NONE', #56884 ) ;
#16418=AXIS2_PLACEMENT_3D ( 'NONE', #50752, #44762, #5202 ) ;
#16421=ORIENTED_EDGE ( 'NONE', *, *, #38232, .T. ) ;
#16424=ORIENTED_EDGE ( 'NONE', *, *, #29848, .T. ) ;
#16440=ORIENTED_EDGE ( 'NONE', *, *, #1302, .F. ) ;
#16442=DIRECTION ( 'NONE',  ( 0.000000000000000000, -0.3193015301359669600, -0.9476531711828067861 ) ) ;
#16448=DIRECTION ( 'NONE',  ( -1.000000000000000000, 0.000000000000000000, 0.000000000000000000 ) ) ;
#16449=CARTESIAN_POINT ( 'NONE',  ( 2.000000000000001776, -6.250523986463956128, -3.007653927006670003 ) ) ;
#16459=CARTESIAN_POINT ( 'NONE',  ( -22.27706485742869091, 2.580541389029920030, 2.625261754997667119 ) ) ;
#16460=CARTESIAN_POINT ( 'NONE',  ( -22.29018399051993882, 1.024613686459469930, 3.576688584977234964 ) ) ;
#16473=AXIS2_PLACEMENT_3D ( 'NONE', #58522, #33234, #18286 ) ;
#16474=DIRECTION ( 'NONE',  ( 0.000000000000000000, 0.000000000000000000, 1.000000000000000000 ) ) ;
#16476=ADVANCED_FACE ( 'NONE', ( #63156 ), #53185, .T. ) ;
#16487=CARTESIAN_POINT ( 'NONE',  ( -27.28563798457903289, -2.487904455214891897, -1.483130241384915893 ) ) ;
#16489=FACE_OUTER_BOUND ( 'NONE', #31454, .T. ) ;
#16498=EDGE_CURVE ( 'NONE', #20276, #17391, #7632, .T. ) ;
#16499=CARTESIAN_POINT ( 'NONE',  ( -25.42680463514451006, -3.871126486605853678, -0.3277218550990906309 ) ) ;
#16501=DIRECTION ( 'NONE',  ( -1.000000000000000000, 0.000000000000000000, 0.000000000000000000 ) ) ;
#16505=CARTESIAN_POINT ( 'NONE',  ( 2.000000000000001776, -3.859771122243078167, 5.613913289150019637 ) ) ;
#16506=FACE_OUTER_BOUND ( 'NONE', #8394, .T. ) ;
#16516=DIRECTION ( 'NONE',  ( 0.000000000000000000, 0.000000000000000000, 1.000000000000000000 ) ) ;
#16525=ORIENTED_EDGE ( 'NONE', *, *, #33665, .T. ) ;
#16526=LINE ( 'NONE', #10870, #10935 ) ;
#16529=ORIENTED_EDGE ( 'NONE', *, *, #756, .T. ) ;
#16538=LINE ( 'NONE', #15845, #20575 ) ;
#16541=VERTEX_POINT ( 'NONE', #62818 ) ;
#16543=CARTESIAN_POINT ( 'NONE',  ( -35.05175862995318425, 0.01212835938693528071, -0.003331684148556030012 ) ) ;
#16560=DIRECTION ( 'NONE',  ( 1.000000000000000000, 0.000000000000000000, 0.000000000000000000 ) ) ;
#16561=DIRECTION ( 'NONE',  ( -1.000000000000000000, 0.000000000000000000, 0.000000000000000000 ) ) ;
#16571=DIRECTION ( 'NONE',  ( -1.000000000000000000, 0.000000000000000000, 0.000000000000000000 ) ) ;
#16573=DIRECTION ( 'NONE',  ( 0.000000000000000000, 0.2149704402110177992, 0.9766205557100881007 ) ) ;
#16574=CARTESIAN_POINT ( 'NONE',  ( -35.04683013664716640, -0.006090538653939255552, 0.01075274317998137219 ) ) ;
#16575=B_SPLINE_CURVE_WITH_KNOTS ( 'NONE', 3,
 ( #21802, #53022, #37394, #26771, #57363, #1837, #21460, #22103, #47069, #62649 ),
 .UNSPECIFIED., .F., .F.,
 ( 4, 3, 3, 4 ),
 ( 0.0001763147164361759890, 0.0002097400188389094170, 0.0002811534801551362692, 0.0003526297678872490409 ),
 .UNSPECIFIED. ) ;
#16582=EDGE_CURVE ( 'NONE', #10662, #2752, #43859, .T. ) ;
#16597=ORIENTED_EDGE ( 'NONE', *, *, #5118, .F. ) ;
#16598=DIRECTION ( 'NONE',  ( 0.000000000000000000, 0.7621620551276333533, 0.6473862847818311339 ) ) ;
#16608=ORIENTED_EDGE ( 'NONE', *, *, #12539, .T. ) ;
#16611=EDGE_CURVE ( 'NONE', #65410, #725, #42856, .T. ) ;
#16612=DIRECTION ( 'NONE',  ( 0.000000000000000000, 0.000000000000000000, 1.000000000000000000 ) ) ;
#16617=AXIS2_PLACEMENT_3D ( 'NONE', #26386, #41680, #46031 ) ;
#16619=CIRCLE ( 'NONE', #33560, 6.936499999999988120 ) ;
#16635=LINE ( 'NONE', #36242, #57251 ) ;
#16636=VERTEX_POINT ( 'NONE', #15860 ) ;
#16639=DIRECTION ( 'NONE',  ( 0.000000000000000000, 0.000000000000000000, 1.000000000000000000 ) ) ;
#16641=EDGE_CURVE ( 'NONE', #34196, #17686, #57737, .T. ) ;
#16657=ORIENTED_EDGE ( 'NONE', *, *, #35083, .F. ) ;
#16671=EDGE_CURVE ( 'NONE', #8268, #18329, #29064, .T. ) ;
#16674=CARTESIAN_POINT ( 'NONE',  ( 2.000000000000001776, 0.000000000000000000, 0.000000000000000000 ) ) ;
#16692=DIRECTION ( 'NONE',  ( -1.000000000000000000, 0.000000000000000000, 0.000000000000000000 ) ) ;
#16696=( BOUNDED_SURFACE ( )  B_SPLINE_SURFACE ( 3, 1, ( 
 ( #8816, #59687 ),
 ( #29105, #3849 ),
 ( #49708, #64642 ),
 ( #19114, #39385 ) ),
 .UNSPECIFIED., .F., .F., .F. ) 
 B_SPLINE_SURFACE_WITH_KNOTS ( ( 4, 4 ),
 ( 2, 2 ),
 ( 0.000000000000000000, 1.000000000000000000 ),
 ( 0.000000000000000000, 1.000000000000000000 ),
 .UNSPECIFIED. ) 
 GEOMETRIC_REPRESENTATION_ITEM ( )  RATIONAL_B_SPLINE_SURFACE ( (
 ( 1.000000000000000000, 1.000000000000000000),
 ( 0.9932032654565553509, 0.8386279382598736953),
 ( 0.9932032654565553509, 0.8386279382598736953),
 ( 1.000000000000000000, 1.000000000000000000) ) ) 
 REPRESENTATION_ITEM ( '' )  SURFACE ( )  );
#16704=CARTESIAN_POINT ( 'NONE',  ( 2.000000000000001776, 1.145812388885215194, -6.715725538143608730 ) ) ;
#16712=VECTOR ( 'NONE', #10688, 1000.000000000000000 ) ;
#16713=EDGE_CURVE ( 'NONE', #29713, #25020, #37552, .T. ) ;
#16715=CARTESIAN_POINT ( 'NONE',  ( 2.000000000000001776, -6.812627895098285258, -0.04423456934733380197 ) ) ;
#16722=CARTESIAN_POINT ( 'NONE',  ( -22.51237073810381162, -2.023441661740717379, 3.933875531624984490 ) ) ;
#16730=AXIS2_PLACEMENT_3D ( 'NONE', #18742, #38997, #54314 ) ;
#16734=DIRECTION ( 'NONE',  ( 0.000000000000000000, 0.000000000000000000, -1.000000000000000000 ) ) ;
#16747=VERTEX_POINT ( 'NONE', #55804 ) ;
#16750=LINE ( 'NONE', #6140, #64878 ) ;
#16763=CARTESIAN_POINT ( 'NONE',  ( 2.000000000000001776, 6.750946897830741200, -1.593658756657007514 ) ) ;
#16770=DIRECTION ( 'NONE',  ( 0.000000000000000000, -0.7621620551276286903, -0.6473862847818365740 ) ) ;
#16773=CIRCLE ( 'NONE', #53951, 7.499999999999988454 ) ;
#16774=CARTESIAN_POINT ( 'NONE',  ( -22.27704833740210333, -2.993786163585782312, 2.142029987820952996 ) ) ;
#16777=EDGE_CURVE ( 'NONE', #25335, #56385, #9972, .T. ) ;
#16787=EDGE_CURVE ( 'NONE', #37684, #5634, #4678, .T. ) ;
#16789=EDGE_CURVE ( 'NONE', #983, #4358, #26963, .T. ) ;
#16792=EDGE_LOOP ( 'NONE', ( #62406, #25557, #3712, #20270 ) ) ;
#16801=EDGE_CURVE ( 'NONE', #63362, #3618, #46101, .T. ) ;
#16820=ORIENTED_EDGE ( 'NONE', *, *, #65400, .T. ) ;
#16825=DIRECTION ( 'NONE',  ( -1.000000000000000000, 0.000000000000000000, 0.000000000000000000 ) ) ;
#16830=VERTEX_POINT ( 'NONE', #52777 ) ;
#16831=DIRECTION ( 'NONE',  ( 0.000000000000000000, 0.000000000000000000, -1.000000000000000000 ) ) ;
#16837=ORIENTED_EDGE ( 'NONE', *, *, #29798, .F. ) ;
#16838=DIRECTION ( 'NONE',  ( 0.000000000000000000, -0.9985334138511231528, -0.05413890858542833723 ) ) ;
#16839=CARTESIAN_POINT ( 'NONE',  ( -22.49803948133827092, 3.704553751086694380, -2.269619744675233086 ) ) ;
#16842=FACE_OUTER_BOUND ( 'NONE', #21234, .T. ) ;
#16856=AXIS2_PLACEMENT_3D ( 'NONE', #2782, #58633, #49551 ) ;
#16859=ORIENTED_EDGE ( 'NONE', *, *, #29005, .F. ) ;
#16863=AXIS2_PLACEMENT_3D ( 'NONE', #43916, #7686, #48280 ) ;
#16869=CARTESIAN_POINT ( 'NONE',  ( -35.04834644901396956, 0.01183641858481722896, -0.007161132384423698344 ) ) ;
#16883=FACE_OUTER_BOUND ( 'NONE', #20577, .T. ) ;
#16908=AXIS2_PLACEMENT_3D ( 'NONE', #58448, #3252, #7913 ) ;
#16910=FACE_OUTER_BOUND ( 'NONE', #54764, .T. ) ;
#16914=CARTESIAN_POINT ( 'NONE',  ( -27.08430792439084556, 1.614882584890349637, 1.625846845508313487 ) ) ;
#16929=CARTESIAN_POINT ( 'NONE',  ( -22.27711653538342773, -2.958138731383645581, 2.191780254295684571 ) ) ;
#16931=B_SPLINE_CURVE_WITH_KNOTS ( 'NONE', 3,
 ( #54460, #33813, #18221, #8890, #38492, #8235 ),
 .UNSPECIFIED., .F., .F.,
 ( 4, 2, 4 ),
 ( 0.000000000000000000, 0.0004528561986909396394, 0.0009057123973818792789 ),
 .UNSPECIFIED. ) ;
#16945=VECTOR ( 'NONE', #47550, 1000.000000000000000 ) ;
#16956=ORIENTED_EDGE ( 'NONE', *, *, #25296, .F. ) ;
#16958=CARTESIAN_POINT ( 'NONE',  ( 1.000000000000000888, 6.936109781200720192, -2.853135311044974198 ) ) ;
#16969=ADVANCED_FACE ( 'NONE', ( #60055 ), #23840, .T. ) ;
#16975=CARTESIAN_POINT ( 'NONE',  ( 1.000000000000000888, 6.160607635185406217, 4.277489166005578269 ) ) ;
#16976=ORIENTED_EDGE ( 'NONE', *, *, #2714, .F. ) ;
#16980=EDGE_CURVE ( 'NONE', #32845, #31042, #49881, .T. ) ;
#16984=ORIENTED_EDGE ( 'NONE', *, *, #62145, .F. ) ;
#16986=DIRECTION ( 'NONE',  ( -1.000000000000000000, 0.000000000000000000, 0.000000000000000000 ) ) ;
#16988=CARTESIAN_POINT ( 'NONE',  ( -27.08416974970326052, -0.4041872645907051420, -2.255186831366117417 ) ) ;
#16993=ORIENTED_EDGE ( 'NONE', *, *, #30968, .T. ) ;
#17005=EDGE_LOOP ( 'NONE', ( #64632, #44083, #33224, #49518 ) ) ;
#17011=DIRECTION ( 'NONE',  ( 0.000000000000000000, 0.000000000000000000, 1.000000000000000000 ) ) ;
#17014=ORIENTED_EDGE ( 'NONE', *, *, #27955, .T. ) ;
#17015=B_SPLINE_CURVE_WITH_KNOTS ( 'NONE', 3,
 ( #11712, #20733, #41316, #36671, #31668, #62261, #46648, #26055, #30684, #36986 ),
 .UNSPECIFIED., .F., .F.,
 ( 4, 3, 3, 4 ),
 ( 5.401523115762567128E-05, 0.0008136511341527817446, 0.004068255670953089750, 0.005063778443040923942 ),
 .UNSPECIFIED. ) ;
#17044=CARTESIAN_POINT ( 'NONE',  ( 0.000000000000000000, 6.201547234537079234, -2.820401998297854096 ) ) ;
#17047=DIRECTION ( 'NONE',  ( 1.000000000000000000, -0.000000000000000000, -0.000000000000000000 ) ) ;
#17051=EDGE_LOOP ( 'NONE', ( #54504, #38830, #60244, #55044 ) ) ;
#17052=AXIS2_PLACEMENT_3D ( 'NONE', #34265, #29928, #55541 ) ;
#17058=CARTESIAN_POINT ( 'NONE',  ( 2.000000000000001776, 0.000000000000000000, 0.000000000000000000 ) ) ;
#17059=CARTESIAN_POINT ( 'NONE',  ( -22.29570301036918423, -3.588849529203739674, 1.042190670255894736 ) ) ;
#17066=CARTESIAN_POINT ( 'NONE',  ( -22.59969328935896726, -4.594269189967464584, -0.7214993884004354818 ) ) ;
#17068=ORIENTED_EDGE ( 'NONE', *, *, #62816, .T. ) ;
#17074=EDGE_LOOP ( 'NONE', ( #50353, #13864, #30730, #35867 ) ) ;
#17076=DIRECTION ( 'NONE',  ( -1.000000000000000000, 0.000000000000000000, 0.000000000000000000 ) ) ;
#17081=CIRCLE ( 'NONE', #22392, 2.899999999999994582 ) ;
#17086=CARTESIAN_POINT ( 'NONE',  ( -22.30398854582847790, -3.656532484463038024, -0.8844201765542353266 ) ) ;
#17103=CARTESIAN_POINT ( 'NONE',  ( -22.27718150314433387, -0.7862703917636514328, -3.596602356343918672 ) ) ;
#17105=EDGE_CURVE ( 'NONE', #6053, #22102, #61670, .T. ) ;
#17110=CARTESIAN_POINT ( 'NONE',  ( -22.28482751661422512, -3.048214341614495559, 2.105139449411428387 ) ) ;
#17113=DIRECTION ( 'NONE',  ( -1.000000000000000000, 0.000000000000000000, 0.000000000000000000 ) ) ;
#17121=CARTESIAN_POINT ( 'NONE',  ( -27.08429572838383947, -1.608131779585707299, -1.632445743623455847 ) ) ;
#17124=CIRCLE ( 'NONE', #26714, 2.899999999999994582 ) ;
#17126=VECTOR ( 'NONE', #9495, 1000.000000000000000 ) ;
#17129=DIRECTION ( 'NONE',  ( 1.000000000000000000, -0.000000000000000000, -0.000000000000000000 ) ) ;
#17139=ORIENTED_EDGE ( 'NONE', *, *, #9100, .F. ) ;
#17140=CARTESIAN_POINT ( 'NONE',  ( -10.00000000000000178, 0.000000000000000000, 0.000000000000000000 ) ) ;
#17142=CIRCLE ( 'NONE', #41532, 7.499999999999988454 ) ;
#17144=ORIENTED_EDGE ( 'NONE', *, *, #18184, .T. ) ;
#17145=CIRCLE ( 'NONE', #1263, 6.936499999999990784 ) ;
#17151=CIRCLE ( 'NONE', #63898, 2.899999999999994582 ) ;
#17156=ORIENTED_EDGE ( 'NONE', *, *, #15625, .F. ) ;
#17158=ORIENTED_EDGE ( 'NONE', *, *, #35881, .T. ) ;
#17161=ADVANCED_FACE ( 'NONE', ( #25450 ), #19998, .F. ) ;
#17163=CARTESIAN_POINT ( 'NONE',  ( -27.08429572838383947, 0.6096735944848206135, -2.208905845566032866 ) ) ;
#17164=ORIENTED_EDGE ( 'NONE', *, *, #42843, .F. ) ;
#17165=AXIS2_PLACEMENT_3D ( 'NONE', #29204, #49809, #44466 ) ;
#17167=CARTESIAN_POINT ( 'NONE',  ( -22.39032720737627002, -3.847057950743281385, 1.170177197944854530 ) ) ;
#17186=DIRECTION ( 'NONE',  ( 0.000000000000000000, -0.8276889981568840149, -0.5611870653623919347 ) ) ;
#17193=CYLINDRICAL_SURFACE ( 'NONE', #38302, 7.499999999999988454 ) ;
#17215=EDGE_CURVE ( 'NONE', #30167, #50893, #304, .T. ) ;
#17218=FACE_OUTER_BOUND ( 'NONE', #31749, .T. ) ;
#17229=AXIS2_PLACEMENT_3D ( 'NONE', #61123, #20223, #40501 ) ;
#17236=DIRECTION ( 'NONE',  ( -1.000000000000000000, 0.000000000000000000, 0.000000000000000000 ) ) ;
#17244=EDGE_LOOP ( 'NONE', ( #17858, #46218, #50579, #24514 ) ) ;
#17247=CIRCLE ( 'NONE', #3466, 2.899999999999994582 ) ;
#17249=EDGE_CURVE ( 'NONE', #14636, #44685, #7747, .T. ) ;
#17257=AXIS2_PLACEMENT_3D ( 'NONE', #59449, #13871, #38850 ) ;
#17273=ORIENTED_EDGE ( 'NONE', *, *, #45320, .F. ) ;
#17276=EDGE_CURVE ( 'NONE', #36432, #47922, #27926, .T. ) ;
#17279=DIRECTION ( 'NONE',  ( -1.000000000000000000, 0.000000000000000000, 0.000000000000000000 ) ) ;
#17282=VECTOR ( 'NONE', #12058, 1000.000000000000000 ) ;
#17290=FACE_OUTER_BOUND ( 'NONE', #55969, .T. ) ;
#17293=VECTOR ( 'NONE', #31427, 1000.000000000000227 ) ;
#17311=ORIENTED_EDGE ( 'NONE', *, *, #52586, .T. ) ;
#17322=FACE_OUTER_BOUND ( 'NONE', #52539, .T. ) ;
#17323=AXIS2_PLACEMENT_3D ( 'NONE', #23690, #9036, #14984 ) ;
#17327=CARTESIAN_POINT ( 'NONE',  ( 2.000000000000001776, 6.812627895098307462, -0.04423456934727655609 ) ) ;
#17331=DIRECTION ( 'NONE',  ( 0.000000000000000000, 0.000000000000000000, 1.000000000000000000 ) ) ;
#17335=AXIS2_PLACEMENT_3D ( 'NONE', #6663, #31895, #21626 ) ;
#17340=EDGE_CURVE ( 'NONE', #30787, #45191, #41859, .T. ) ;
#17344=CARTESIAN_POINT ( 'NONE',  ( 0.000000000000000000, -6.796153407501424049, -1.388283512725909219 ) ) ;
#17345=CARTESIAN_POINT ( 'NONE',  ( -22.31328051695926007, -3.781397440874596061, 0.2528478350593901802 ) ) ;
#17360=EDGE_CURVE ( 'NONE', #6941, #22369, #40680, .T. ) ;
#17362=AXIS2_PLACEMENT_3D ( 'NONE', #55388, #8857, #19157 ) ;
#17368=CARTESIAN_POINT ( 'NONE',  ( -35.04660725145885891, -0.01191704700713449618, 0.003039313842342893004 ) ) ;
#17371=CIRCLE ( 'NONE', #25866, 6.936499999999989896 ) ;
#17372=AXIS2_PLACEMENT_3D ( 'NONE', #30001, #65258, #59623 ) ;
#17382=DIRECTION ( 'NONE',  ( -1.000000000000000000, 0.000000000000000000, 0.000000000000000000 ) ) ;
#17385=CARTESIAN_POINT ( 'NONE',  ( -22.27878402819508352, -2.612733676624904522, -2.600576127690928718 ) ) ;
#17389=CARTESIAN_POINT ( 'NONE',  ( -27.04788180060269198, 1.373100113388795673, 2.923150379392631670 ) ) ;
#17391=VERTEX_POINT ( 'NONE', #55893 ) ;
#17392=CARTESIAN_POINT ( 'NONE',  ( -22.27706485742869091, 3.662257305743817692, -0.3729136217355926153 ) ) ;
#17403=ORIENTED_EDGE ( 'NONE', *, *, #27108, .T. ) ;
#17405=CARTESIAN_POINT ( 'NONE',  ( 0.000000000000000000, 0.000000000000000000, 0.000000000000000000 ) ) ;
#17420=FACE_OUTER_BOUND ( 'NONE', #32679, .T. ) ;
#17422=AXIS2_PLACEMENT_3D ( 'NONE', #23700, #63568, #18043 ) ;
#17425=ADVANCED_FACE ( 'NONE', ( #14639 ), #26799, .F. ) ;
#17440=CARTESIAN_POINT ( 'NONE',  ( 1.000000000000000888, -4.472310526050724100, -6.020667617347421618 ) ) ;
#17441=DIRECTION ( 'NONE',  ( 0.000000000000000000, 0.000000000000000000, 1.000000000000000000 ) ) ;
#17463=ADVANCED_FACE ( 'NONE', ( #5700, #31907 ), #56895, .F. ) ;
#17470=DIRECTION ( 'NONE',  ( -1.000000000000000000, 0.000000000000000000, 0.000000000000000000 ) ) ;
#17475=ORIENTED_EDGE ( 'NONE', *, *, #47479, .T. ) ;
#17484=CYLINDRICAL_SURFACE ( 'NONE', #14910, 6.936499999999988120 ) ;
#17485=EDGE_CURVE ( 'NONE', #4690, #9839, #26872, .T. ) ;
#17499=CARTESIAN_POINT ( 'NONE',  ( -22.27722022243424149, 3.619868281251748421, -0.6721023714405434113 ) ) ;
#17506=CARTESIAN_POINT ( 'NONE',  ( -22.27721038036499834, -0.5802312083658355268, -3.635620891621751394 ) ) ;
#17514=ORIENTED_EDGE ( 'NONE', *, *, #20860, .T. ) ;
#17521=ADVANCED_FACE ( 'NONE', ( #5357 ), #10997, .T. ) ;
#17523=EDGE_LOOP ( 'NONE', ( #47756, #53921, #18132, #47565 ) ) ;
#17529=CARTESIAN_POINT ( 'NONE',  ( -35.04709527796842394, 0.01231589140598780829, 0.001082316405371860912 ) ) ;
#17532=DIRECTION ( 'NONE',  ( -1.000000000000000000, 0.000000000000000000, 0.000000000000000000 ) ) ;
#17538=CYLINDRICAL_SURFACE ( 'NONE', #51077, 2.899999999999994582 ) ;
#17550=LINE ( 'NONE', #28180, #61643 ) ;
#17552=CARTESIAN_POINT ( 'NONE',  ( -27.08426571771018487, 1.845988025802340005, -1.357728109767518454 ) ) ;
#17560=CARTESIAN_POINT ( 'NONE',  ( 2.000000000000001776, 0.000000000000000000, 1.499999999999997780 ) ) ;
#17562=ADVANCED_FACE ( 'NONE', ( #1021 ), #26607, .T. ) ;
#17587=CARTESIAN_POINT ( 'NONE',  ( 2.000000000000001776, -1.779948802829851129, 6.576141558201223702 ) ) ;
#17589=CARTESIAN_POINT ( 'NONE',  ( -22.30625920655495165, -3.783486345733982237, 0.2529928606556808846 ) ) ;
#17594=VERTEX_POINT ( 'NONE', #58526 ) ;
#17606=B_SPLINE_CURVE_WITH_KNOTS ( 'NONE', 3,
 ( #47833, #13548, #13242, #33525, #64104, #58143, #28209, #28855, #22569, #8249, #54130, #38502, #3622, #8567, #23886, #38841, #49165, #12250, #44150, #64415, #2292, #32512 ),
 .UNSPECIFIED., .F., .F.,
 ( 4, 3, 3, 3, 3, 3, 3, 4 ),
 ( 0.000000000000000000, 4.447697177976191098E-05, 6.624143997791052778E-05, 8.800576886944171486E-05, 0.0001097699864780878276, 0.0001315341395364365415, 0.0001760120188223252577, 0.0001867971373174704037 ),
 .UNSPECIFIED. ) ;
#17611=DIRECTION ( 'NONE',  ( 0.000000000000000000, 0.000000000000000000, 1.000000000000000000 ) ) ;
#17612=CARTESIAN_POINT ( 'NONE',  ( -22.27722022243424149, 2.798846704197255342, -2.391991868237149710 ) ) ;
#17628=CARTESIAN_POINT ( 'NONE',  ( -27.10307689719060065, -0.6678239540327197687, -2.250862122746733363 ) ) ;
#17631=CARTESIAN_POINT ( 'NONE',  ( 1.000000000000000888, -7.493043167941588756, -0.3229614270520431152 ) ) ;
#17632=CARTESIAN_POINT ( 'NONE',  ( 2.000000000000001776, 3.859771122243047081, 5.613913289150030295 ) ) ;
#17634=AXIS2_PLACEMENT_3D ( 'NONE', #13087, #49013, #18079 ) ;
#17637=CARTESIAN_POINT ( 'NONE',  ( -22.35190811654613086, -1.736165297230997995, 3.498661567522999061 ) ) ;
#17651=EDGE_LOOP ( 'NONE', ( #56307, #39256, #38667, #63382 ) ) ;
#17658=ORIENTED_EDGE ( 'NONE', *, *, #45255, .F. ) ;
#17664=FACE_OUTER_BOUND ( 'NONE', #18001, .T. ) ;
#17667=DIRECTION ( 'NONE',  ( 0.000000000000000000, -0.1764146379942750642, -0.9843159429275484262 ) ) ;
#17668=ORIENTED_EDGE ( 'NONE', *, *, #45799, .F. ) ;
#17671=VERTEX_POINT ( 'NONE', #32555 ) ;
#17678=CARTESIAN_POINT ( 'NONE',  ( -22.30861784526115699, 3.671054459752226773, 0.8834205920623279251 ) ) ;
#17682=ORIENTED_EDGE ( 'NONE', *, *, #47728, .F. ) ;
#17683=EDGE_CURVE ( 'NONE', #60562, #65410, #55597, .T. ) ;
#17686=VERTEX_POINT ( 'NONE', #63476 ) ;
#17687=DIRECTION ( 'NONE',  ( -1.000000000000000000, 0.000000000000000000, 0.000000000000000000 ) ) ;
#17692=CARTESIAN_POINT ( 'NONE',  ( 2.000000000000001776, -4.570217215903394248, 5.218059682435592705 ) ) ;
#17706=EDGE_CURVE ( 'NONE', #47952, #44565, #52902, .T. ) ;
#17707=CIRCLE ( 'NONE', #60170, 2.899999999999994582 ) ;
#17711=DIRECTION ( 'NONE',  ( 0.000000000000000000, -0.8276889981568840149, -0.5611870653623919347 ) ) ;
#17712=CARTESIAN_POINT ( 'NONE',  ( 2.000000000000001776, 0.000000000000000000, 0.000000000000000000 ) ) ;
#17714=CARTESIAN_POINT ( 'NONE',  ( -22.27756824490284160, -2.599719761044739119, -2.608445836294064346 ) ) ;
#17718=ORIENTED_EDGE ( 'NONE', *, *, #3001, .F. ) ;
#17719=DIRECTION ( 'NONE',  ( -1.000000000000000000, 0.000000000000000000, 0.000000000000000000 ) ) ;
#17720=DIRECTION ( 'NONE',  ( -1.000000000000000000, 0.000000000000000000, 0.000000000000000000 ) ) ;
#17721=DIRECTION ( 'NONE',  ( -1.000000000000000000, 0.000000000000000000, 0.000000000000000000 ) ) ;
#17726=EDGE_CURVE ( 'NONE', #30167, #4485, #48159, .T. ) ;
#17732=CARTESIAN_POINT ( 'NONE',  ( -22.35190811654612375, 0.2457675311905117566, 3.898012445334706921 ) ) ;
#17734=ORIENTED_EDGE ( 'NONE', *, *, #33399, .F. ) ;
#17737=CYLINDRICAL_SURFACE ( 'NONE', #8937, 2.899999999999994582 ) ;
#17746=DIRECTION ( 'NONE',  ( 0.000000000000000000, -0.5155538571770110767, -0.8568571761675957132 ) ) ;
#17757=EDGE_LOOP ( 'NONE', ( #44383, #13870, #29298, #44948 ) ) ;
#17759=ORIENTED_EDGE ( 'NONE', *, *, #2091, .F. ) ;
#17762=EDGE_CURVE ( 'NONE', #9839, #52648, #64461, .T. ) ;
#17765=CARTESIAN_POINT ( 'NONE',  ( -22.28023996335807411, 3.345627887484369900, 1.558279384310053306 ) ) ;
#17777=CARTESIAN_POINT ( 'NONE',  ( 2.000000000000001776, 0.4129979343798200753, -6.800241778083709221 ) ) ;
#17778=CARTESIAN_POINT ( 'NONE',  ( -22.31328051695926007, -0.2528478350593797996, -3.781397440874599614 ) ) ;
#17779=ORIENTED_EDGE ( 'NONE', *, *, #34446, .T. ) ;
#17782=CARTESIAN_POINT ( 'NONE',  ( -22.27384469013076185, -0.9224151068931482067, -3.564715702084495952 ) ) ;
#17783=DIRECTION ( 'NONE',  ( 1.000000000000000000, 0.000000000000000000, 0.000000000000000000 ) ) ;
#17787=CARTESIAN_POINT ( 'NONE',  ( 0.000000000000000000, 0.000000000000000000, 0.000000000000000000 ) ) ;
#17802=ORIENTED_EDGE ( 'NONE', *, *, #57090, .T. ) ;
#17805=DIRECTION ( 'NONE',  ( -1.000000000000000000, 0.000000000000000000, 0.000000000000000000 ) ) ;
#17811=CARTESIAN_POINT ( 'NONE',  ( 2.000000000000001776, 5.814643797626986910, -3.550179297009520063 ) ) ;
#17813=CARTESIAN_POINT ( 'NONE',  ( -22.70624764888619751, -5.249808673991985586, -0.08990180771019026795 ) ) ;
#17817=CARTESIAN_POINT ( 'NONE',  ( -22.27718112499583469, 3.645895996548659035, -0.5110808820053269752 ) ) ;
#17819=VECTOR ( 'NONE', #56513, 1000.000000000000000 ) ;
#17823=EDGE_LOOP ( 'NONE', ( #54533, #15593, #46916, #22882 ) ) ;
#17828=ORIENTED_EDGE ( 'NONE', *, *, #35028, .F. ) ;
#17842=DIRECTION ( 'NONE',  ( -1.000000000000000000, 0.000000000000000000, 0.000000000000000000 ) ) ;
#17846=B_SPLINE_CURVE_WITH_KNOTS ( 'NONE', 3,
 ( #22261, #32240, #21281, #51890, #47238, #1685, #47875, #21633, #36587, #56890, #37573, #42525, #21951, #37220, #32549, #41558, #17628, #61849, #26601 ),
 .UNSPECIFIED., .F., .F.,
 ( 4, 3, 3, 3, 3, 3, 4 ),
 ( 0.000000000000000000, 2.832085443540606438E-05, 4.217789847394578227E-05, 5.603488375045981523E-05, 6.989180858579043150E-05, 9.821094829918522679E-05, 0.0001178165571465082212 ),
 .UNSPECIFIED. ) ;
#17852=ORIENTED_EDGE ( 'NONE', *, *, #62517, .T. ) ;
#17857=CARTESIAN_POINT ( 'NONE',  ( 0.000000000000000000, 6.812627895098307462, -0.04423456934727655609 ) ) ;
#17858=ORIENTED_EDGE ( 'NONE', *, *, #30703, .F. ) ;
#17860=CARTESIAN_POINT ( 'NONE',  ( -22.28073302975500880, -2.595086548180001174, 2.626377654649335813 ) ) ;
#17862=CARTESIAN_POINT ( 'NONE',  ( 2.000000000000001776, -4.376687952327290354, -5.220963330856675633 ) ) ;
#17866=CARTESIAN_POINT ( 'NONE',  ( 2.000000000000001776, 6.441884263200815752, 2.217201541069855786 ) ) ;
#17870=B_SPLINE_CURVE_WITH_KNOTS ( 'NONE', 3,
 ( #9859, #50449, #14502, #35109, #55421, #34477, #50762, #19531, #54778, #46116, #55084, #4895, #563, #41092, #9513, #61371, #40105, #39796, #5556 ),
 .UNSPECIFIED., .F., .F.,
 ( 4, 3, 3, 3, 3, 3, 4 ),
 ( 0.000000000000000000, 2.836829843012687999E-05, 4.224792512550939246E-05, 5.612066614913134463E-05, 6.998859278354717817E-05, 9.832141288087045293E-05, 0.0001178161482478527668 ),
 .UNSPECIFIED. ) ;
#17871=CARTESIAN_POINT ( 'NONE',  ( -22.27834755396593991, -3.610802913011853743, 0.7418417409069075763 ) ) ;
#17880=AXIS2_PLACEMENT_3D ( 'NONE', #41957, #16692, #12587 ) ;
#17895=CARTESIAN_POINT ( 'NONE',  ( -27.15525204139121840, 0.7327319213109966256, 2.394850816831278539 ) ) ;
#17898=CARTESIAN_POINT ( 'NONE',  ( -22.28169757117799321, 2.592369810060400237, -2.633129923220806745 ) ) ;
#17907=ORIENTED_EDGE ( 'NONE', *, *, #36135, .F. ) ;
#17909=DIRECTION ( 'NONE',  ( 1.000000000000000000, -0.000000000000000000, -0.000000000000000000 ) ) ;
#17914=CARTESIAN_POINT ( 'NONE',  ( -22.27719412087655471, -2.887588494201215994, 2.283949229175420204 ) ) ;
#17915=CARTESIAN_POINT ( 'NONE',  ( -27.08485414902845179, -1.620258667553439169, 1.622802444813708167 ) ) ;
#17916=AXIS2_PLACEMENT_3D ( 'NONE', #13180, #43761, #36999 ) ;
#17918=DIRECTION ( 'NONE',  ( 0.000000000000000000, 0.000000000000000000, 1.000000000000000000 ) ) ;
#17920=DIRECTION ( 'NONE',  ( 0.000000000000000000, 0.000000000000000000, 1.000000000000000000 ) ) ;
#17924=CARTESIAN_POINT ( 'NONE',  ( -22.23402523511428086, 1.734723475976807094E-15, -8.673617379884035472E-15 ) ) ;
#17926=CIRCLE ( 'NONE', #55073, 6.936499999999989008 ) ;
#17928=CARTESIAN_POINT ( 'NONE',  ( -35.04709527796842394, -0.01231589140598780829, -0.001082316405380534530 ) ) ;
#17931=CARTESIAN_POINT ( 'NONE',  ( -27.08416781016246588, 1.485424708116796166, 1.744495588874922509 ) ) ;
#17934=EDGE_CURVE ( 'NONE', #14755, #14116, #19478, .T. ) ;
#17936=CARTESIAN_POINT ( 'NONE',  ( 2.000000000000001776, -1.779948802829851129, 6.576141558201223702 ) ) ;
#17946=FACE_OUTER_BOUND ( 'NONE', #56994, .T. ) ;
#17954=EDGE_CURVE ( 'NONE', #29381, #37749, #58449, .T. ) ;
#17956=CARTESIAN_POINT ( 'NONE',  ( -22.27384469013076185, -1.508555848190757276, 3.358914544760229326 ) ) ;
#17961=CARTESIAN_POINT ( 'NONE',  ( -27.08485414902839494, 2.214586389210143391, -0.5952588087544573581 ) ) ;
#17965=CARTESIAN_POINT ( 'NONE',  ( -10.00000000000000178, 0.000000000000000000, 0.000000000000000000 ) ) ;
#17970=CARTESIAN_POINT ( 'NONE',  ( -22.27945548916780183, -2.122548946923912716, -3.016427163003911005 ) ) ;
#17977=ORIENTED_EDGE ( 'NONE', *, *, #52293, .F. ) ;
#17979=CARTESIAN_POINT ( 'NONE',  ( -22.28236030719477512, -0.3108070568283820556, -3.683993210674382457 ) ) ;
#17995=CARTESIAN_POINT ( 'NONE',  ( 2.000000000000001776, 3.805198749487521681, -5.799611601383208637 ) ) ;
#18001=EDGE_LOOP ( 'NONE', ( #33672, #5427, #35365, #44159 ) ) ;
#18002=AXIS2_PLACEMENT_3D ( 'NONE', #59160, #63457, #23915 ) ;
#18003=CARTESIAN_POINT ( 'NONE',  ( 2.000000000000001776, -2.562706407243680928, 6.312399813420318750 ) ) ;
#18006=ORIENTED_EDGE ( 'NONE', *, *, #28956, .F. ) ;
#18011=CIRCLE ( 'NONE', #37116, 2.899999999999994582 ) ;
#18013=EDGE_CURVE ( 'NONE', #14144, #64495, #63032, .T. ) ;
#18014=ORIENTED_EDGE ( 'NONE', *, *, #45207, .F. ) ;
#18018=CYLINDRICAL_SURFACE ( 'NONE', #12752, 7.499999999999988454 ) ;
#18022=CARTESIAN_POINT ( 'NONE',  ( 2.000000000000001776, 0.000000000000000000, 0.000000000000000000 ) ) ;
#18026=DIRECTION ( 'NONE',  ( 0.000000000000000000, 0.000000000000000000, 1.000000000000000000 ) ) ;
#18028=DIRECTION ( 'NONE',  ( 0.000000000000000000, 0.000000000000000000, -1.000000000000000000 ) ) ;
#18033=CARTESIAN_POINT ( 'NONE',  ( -22.65999102136915155, -0.5917351393135155124, 4.797155153747047152 ) ) ;
#18043=DIRECTION ( 'NONE',  ( 0.000000000000000000, 0.000000000000000000, 1.000000000000000000 ) ) ;
#18046=ADVANCED_FACE ( 'NONE', ( #54091 ), #49127, .T. ) ;
#18053=CIRCLE ( 'NONE', #26535, 2.899999999999995914 ) ;
#18054=CARTESIAN_POINT ( 'NONE',  ( -22.28023996335807411, -3.345627887484365903, -1.558279384310083282 ) ) ;
#18055=ORIENTED_EDGE ( 'NONE', *, *, #64037, .F. ) ;
#18060=FACE_OUTER_BOUND ( 'NONE', #27355, .T. ) ;
#18061=EDGE_LOOP ( 'NONE', ( #25934, #9092, #45440, #59027 ) ) ;
#18062=( BOUNDED_SURFACE ( )  B_SPLINE_SURFACE ( 3, 1, ( 
 ( #22195, #942 ),
 ( #41483, #56825 ),
 ( #1926, #31518 ),
 ( #36519, #62118 ) ),
 .UNSPECIFIED., .F., .F., .F. ) 
 B_SPLINE_SURFACE_WITH_KNOTS ( ( 4, 4 ),
 ( 2, 2 ),
 ( 0.000000000000000000, 1.000000000000000000 ),
 ( 0.000000000000000000, 1.000000000000000000 ),
 .UNSPECIFIED. ) 
 GEOMETRIC_REPRESENTATION_ITEM ( )  RATIONAL_B_SPLINE_SURFACE ( (
 ( 1.000000000000000000, 1.000000000000000000),
 ( 0.9932032654565553509, 0.8386279382598740284),
 ( 0.9932032654565553509, 0.8386279382598740284),
 ( 1.000000000000000000, 1.000000000000000000) ) ) 
 REPRESENTATION_ITEM ( '' )  SURFACE ( )  );
#18065=CARTESIAN_POINT ( 'NONE',  ( -27.05874794189610455, 0.3907329275428126913, 2.180117559290193796 ) ) ;
#18068=DIRECTION ( 'NONE',  ( 0.000000000000000000, 0.000000000000000000, 1.000000000000000000 ) ) ;
#18079=DIRECTION ( 'NONE',  ( 0.000000000000000000, 0.2149704402110246271, -0.9766205557100866574 ) ) ;
#18080=CARTESIAN_POINT ( 'NONE',  ( -22.29382655386184453, -3.622626291186075598, -0.8947172055470860030 ) ) ;
#18089=CARTESIAN_POINT ( 'NONE',  ( -22.30078715814471835, 2.097357782488240119, 3.111489293522180510 ) ) ;
#18097=CARTESIAN_POINT ( 'NONE',  ( 2.000000000000001776, 0.000000000000000000, 0.000000000000000000 ) ) ;
#18098=CARTESIAN_POINT ( 'NONE',  ( -27.08426504710140392, -1.591094357919260904, -1.649100202714224750 ) ) ;
#18103=DIRECTION ( 'NONE',  ( 0.000000000000000000, 0.000000000000000000, 1.000000000000000000 ) ) ;
#18113=ADVANCED_FACE ( 'NONE', ( #29775 ), #45098, .T. ) ;
#18116=AXIS2_PLACEMENT_3D ( 'NONE', #25842, #5228, #10863 ) ;
#18125=CYLINDRICAL_SURFACE ( 'NONE', #2229, 6.936499999999988120 ) ;
#18128=DIRECTION ( 'NONE',  ( 0.000000000000000000, -0.1764146379942750087, -0.9843159429275484262 ) ) ;
#18132=ORIENTED_EDGE ( 'NONE', *, *, #50048, .T. ) ;
#18134=CARTESIAN_POINT ( 'NONE',  ( -27.35552965826137140, -3.094132632038958608, -0.2619431035392160156 ) ) ;
#18136=DIRECTION ( 'NONE',  ( 0.000000000000000000, -0.9985334138511243740, 0.05413890858540768014 ) ) ;
#18139=CARTESIAN_POINT ( 'NONE',  ( 2.000000000000001776, 0.000000000000000000, 0.000000000000000000 ) ) ;
#18144=ORIENTED_EDGE ( 'NONE', *, *, #41135, .F. ) ;
#18170=CARTESIAN_POINT ( 'NONE',  ( -22.27945548916780183, 3.016427163003909229, -2.122548946923910940 ) ) ;
#18181=EDGE_CURVE ( 'NONE', #62557, #63186, #41817, .T. ) ;
#18184=EDGE_CURVE ( 'NONE', #9014, #28947, #47157, .T. ) ;
#18187=CARTESIAN_POINT ( 'NONE',  ( -27.10128162969864363, 0.1566844438592239763, 2.337214317750524906 ) ) ;
#18188=VERTEX_POINT ( 'NONE', #50743 ) ;
#18190=CARTESIAN_POINT ( 'NONE',  ( 2.000000000000001776, -1.145812388885072863, -6.715725538143620277 ) ) ;
#18201=CIRCLE ( 'NONE', #57456, 2.899999999999994582 ) ;
#18205=CARTESIAN_POINT ( 'NONE',  ( -27.08418322526031119, 1.789041206975757747, -1.431535851194440268 ) ) ;
#18206=AXIS2_PLACEMENT_3D ( 'NONE', #24039, #19043, #23054 ) ;
#18208=VERTEX_POINT ( 'NONE', #21463 ) ;
#18212=AXIS2_PLACEMENT_3D ( 'NONE', #25508, #35794, #56791 ) ;
#18214=CARTESIAN_POINT ( 'NONE',  ( 0.000000000000000000, -2.473437528934089524, -7.080403010455012414 ) ) ;
#18218=AXIS2_PLACEMENT_3D ( 'NONE', #15926, #31250, #36210 ) ;
#18221=CARTESIAN_POINT ( 'NONE',  ( -27.20102706715914209, 0.5453431011645279991, -2.585824624629319946 ) ) ;
#18226=CIRCLE ( 'NONE', #63867, 2.899999999999994582 ) ;
#18227=VERTEX_POINT ( 'NONE', #35433 ) ;
#18230=ORIENTED_EDGE ( 'NONE', *, *, #55344, .T. ) ;
#18232=CARTESIAN_POINT ( 'NONE',  ( -22.27706485742869091, 2.625261754997705310, -2.580541389029900934 ) ) ;
#18233=CIRCLE ( 'NONE', #55383, 2.899999999999994582 ) ;
#18234=CARTESIAN_POINT ( 'NONE',  ( -27.32343372485684796, 0.1402256980610574744, -3.007804754713670814 ) ) ;
#18237=CARTESIAN_POINT ( 'NONE',  ( 2.000000000000001776, 3.152010634611773110, -6.039758645301250617 ) ) ;
#18244=ORIENTED_EDGE ( 'NONE', *, *, #17105, .T. ) ;
#18248=ORIENTED_EDGE ( 'NONE', *, *, #13511, .T. ) ;
#18261=( BOUNDED_SURFACE ( )  B_SPLINE_SURFACE ( 3, 1, ( 
 ( #5045, #4398 ),
 ( #29324, #40265 ),
 ( #4059, #49619 ),
 ( #34307, #10029 ) ),
 .UNSPECIFIED., .F., .F., .F. ) 
 B_SPLINE_SURFACE_WITH_KNOTS ( ( 4, 4 ),
 ( 2, 2 ),
 ( 0.000000000000000000, 1.000000000000000000 ),
 ( 0.000000000000000000, 1.000000000000000000 ),
 .UNSPECIFIED. ) 
 GEOMETRIC_REPRESENTATION_ITEM ( )  RATIONAL_B_SPLINE_SURFACE ( (
 ( 1.000000000000000000, 1.000000000000000000),
 ( 0.9932032654565553509, 0.8386279382598736953),
 ( 0.9932032654565553509, 0.8386279382598736953),
 ( 1.000000000000000000, 1.000000000000000000) ) ) 
 REPRESENTATION_ITEM ( '' )  SURFACE ( )  );
#18265=AXIS2_PLACEMENT_3D ( 'NONE', #54712, #39728, #14115 ) ;
#18271=DIRECTION ( 'NONE',  ( -1.000000000000000000, 0.000000000000000000, 0.000000000000000000 ) ) ;
#18272=CIRCLE ( 'NONE', #55410, 2.899999999999995026 ) ;
#18273=CARTESIAN_POINT ( 'NONE',  ( -27.08419642509983305, 1.538761233743672241, 1.697757994346396737 ) ) ;
#18279=VERTEX_POINT ( 'NONE', #52052 ) ;
#18283=CARTESIAN_POINT ( 'NONE',  ( -22.27384469013076185, -2.581192766446256837, -2.625926801827886070 ) ) ;
#18286=DIRECTION ( 'NONE',  ( 0.000000000000000000, 0.000000000000000000, 1.000000000000000000 ) ) ;
#18288=CARTESIAN_POINT ( 'NONE',  ( -27.09729107899804745, 2.094470452260986271, 1.021938248125897397 ) ) ;
#18290=AXIS2_PLACEMENT_3D ( 'NONE', #48404, #12458, #62670 ) ;
#18296=CARTESIAN_POINT ( 'NONE',  ( 2.000000000000001776, -3.155844197800055539, -6.177028383390492650 ) ) ;
#18307=FACE_OUTER_BOUND ( 'NONE', #1498, .T. ) ;
#18308=CARTESIAN_POINT ( 'NONE',  ( -27.09125059358653331, -1.662156772098235091, -1.607567221344416986 ) ) ;
#18311=CARTESIAN_POINT ( 'NONE',  ( 2.000000000000001776, -6.470132594555817462, 2.133363481234057168 ) ) ;
#18313=ORIENTED_EDGE ( 'NONE', *, *, #20137, .T. ) ;
#18314=ORIENTED_EDGE ( 'NONE', *, *, #28077, .T. ) ;
#18315=CARTESIAN_POINT ( 'NONE',  ( 2.000000000000001776, 6.997684042076949495, -2.698595569414168338 ) ) ;
#18316=B_SPLINE_CURVE_WITH_KNOTS ( 'NONE', 3,
 ( #8550, #38488, #50112, #13529, #13845, #3260 ),
 .UNSPECIFIED., .F., .F.,
 ( 4, 2, 4 ),
 ( 0.0002637379172192615877, 0.0009975831966643347939, 0.001731428476109407675 ),
 .UNSPECIFIED. ) ;
#18321=CIRCLE ( 'NONE', #5606, 6.936499999999989008 ) ;
#18324=DIRECTION ( 'NONE',  ( 0.000000000000000000, 0.000000000000000000, 1.000000000000000000 ) ) ;
#18325=ADVANCED_FACE ( 'NONE', ( #63316 ), #62334, .T. ) ;
#18327=DIRECTION ( 'NONE',  ( -1.000000000000000000, 0.000000000000000000, 0.000000000000000000 ) ) ;
#18328=DIRECTION ( 'NONE',  ( -1.000000000000000000, 0.000000000000000000, 0.000000000000000000 ) ) ;
#18329=VERTEX_POINT ( 'NONE', #27417 ) ;
#18330=VERTEX_POINT ( 'NONE', #22786 ) ;
#18332=EDGE_CURVE ( 'NONE', #21834, #29257, #58854, .T. ) ;
#18333=ORIENTED_EDGE ( 'NONE', *, *, #37130, .T. ) ;
#18341=CARTESIAN_POINT ( 'NONE',  ( -22.29018399051993882, 3.609810019245840440, 0.9010028109494814252 ) ) ;
#18343=DIRECTION ( 'NONE',  ( -1.000000000000000000, 0.000000000000000000, 0.000000000000000000 ) ) ;
#18345=CARTESIAN_POINT ( 'NONE',  ( -22.38932658256920050, -4.011828264158258328, 0.2254938976656627458 ) ) ;
#18352=VERTEX_POINT ( 'NONE', #61257 ) ;
#18363=CARTESIAN_POINT ( 'NONE',  ( 2.000000000000001776, -4.376687952327356079, 5.220963330856582374 ) ) ;
#18369=EDGE_LOOP ( 'NONE', ( #10233, #47812, #45829, #59900 ) ) ;
#18376=CYLINDRICAL_SURFACE ( 'NONE', #11299, 6.936499999999988120 ) ;
#18387=LINE ( 'NONE', #58960, #19562 ) ;
#18390=EDGE_LOOP ( 'NONE', ( #26310, #5188, #27225, #37214 ) ) ;
#18392=CARTESIAN_POINT ( 'NONE',  ( 2.000000000000001776, 7.414200355365271555, -1.131208685655096691 ) ) ;
#18399=CARTESIAN_POINT ( 'NONE',  ( -22.27786964138240222, -3.347945419004157763, -1.536369256421360685 ) ) ;
#18402=CARTESIAN_POINT ( 'NONE',  ( -22.27722019094931127, -2.374181302998997101, -2.813874087060012741 ) ) ;
#18409=VECTOR ( 'NONE', #27305, 1000.000000000000000 ) ;
#18414=CARTESIAN_POINT ( 'NONE',  ( -22.27218376572352554, -3.566922835983774576, -0.9173404081777783992 ) ) ;
#18420=CARTESIAN_POINT ( 'NONE',  ( -22.51237073810381517, 2.023441661740732478, -3.933875531624967170 ) ) ;
#18434=CARTESIAN_POINT ( 'NONE',  ( 1.000000000000000888, 3.937687286050910895, -6.383151168292444666 ) ) ;
#18436=CARTESIAN_POINT ( 'NONE',  ( -22.28482751661422867, 3.347211412506322592, 1.587261331312464163 ) ) ;
#18437=CARTESIAN_POINT ( 'NONE',  ( -27.32337605527168378, 2.771816950947482816, -1.175835497774972982 ) ) ;
#18447=ORIENTED_EDGE ( 'NONE', *, *, #10450, .T. ) ;
#18452=FACE_OUTER_BOUND ( 'NONE', #55131, .T. ) ;
#18467=CARTESIAN_POINT ( 'NONE',  ( -27.10719052120871098, 0.1538293304135379680, 2.355164825213503121 ) ) ;
#18468=DIRECTION ( 'NONE',  ( 0.000000000000000000, -0.2149704402110317047, 0.9766205557100849921 ) ) ;
#18477=ORIENTED_EDGE ( 'NONE', *, *, #65233, .T. ) ;
#18498=EDGE_CURVE ( 'NONE', #38388, #7386, #58589, .T. ) ;
#18501=AXIS2_PLACEMENT_3D ( 'NONE', #33145, #53454, #7899 ) ;
#18507=CARTESIAN_POINT ( 'NONE',  ( 2.000000000000001776, 4.915517050588478654, -4.717154614762057108 ) ) ;
#18511=CARTESIAN_POINT ( 'NONE',  ( -22.27715526084302056, 0.4651416883073989927, 3.652257391294490230 ) ) ;
#18515=ORIENTED_EDGE ( 'NONE', *, *, #54412, .F. ) ;
#18522=CARTESIAN_POINT ( 'NONE',  ( -22.29479313954897890, 3.090162644873547748, -2.096782908204888773 ) ) ;
#18524=CARTESIAN_POINT ( 'NONE',  ( -27.08456565417852602, -1.867985369022540976, 1.328664661355674736 ) ) ;
#18540=FACE_OUTER_BOUND ( 'NONE', #50210, .T. ) ;
#18547=DIRECTION ( 'NONE',  ( -1.000000000000000000, 0.000000000000000000, 0.000000000000000000 ) ) ;
#18550=DIRECTION ( 'NONE',  ( 0.000000000000000000, 0.000000000000000000, 1.000000000000000000 ) ) ;
#18565=AXIS2_PLACEMENT_3D ( 'NONE', #41548, #26272, #46549 ) ;
#18567=VERTEX_POINT ( 'NONE', #32946 ) ;
#18571=DIRECTION ( 'NONE',  ( -1.000000000000000000, 0.000000000000000000, 0.000000000000000000 ) ) ;
#18572=CARTESIAN_POINT ( 'NONE',  ( 0.000000000000000000, 0.000000000000000000, 0.000000000000000000 ) ) ;
#18576=EDGE_LOOP ( 'NONE', ( #64451, #55677, #58964, #3175 ) ) ;
#18579=ORIENTED_EDGE ( 'NONE', *, *, #65182, .F. ) ;
#18585=LINE ( 'NONE', #58473, #60620 ) ;
#18591=VERTEX_POINT ( 'NONE', #37289 ) ;
#18615=CARTESIAN_POINT ( 'NONE',  ( 0.000000000000000000, 0.000000000000000000, 0.000000000000000000 ) ) ;
#18628=DIRECTION ( 'NONE',  ( -1.000000000000000000, 0.000000000000000000, 0.000000000000000000 ) ) ;
#18630=CARTESIAN_POINT ( 'NONE',  ( -22.29570301036918778, 2.696988360630619752, 2.586939527522273963 ) ) ;
#18634=DIRECTION ( 'NONE',  ( 0.000000000000000000, -0.6051742151937715697, 0.7960930657056388693 ) ) ;
#18640=EDGE_CURVE ( 'NONE', #7150, #18591, #16038, .T. ) ;
#18648=CARTESIAN_POINT ( 'NONE',  ( -22.28350523959500862, -2.107889123925585473, -3.041489826385515904 ) ) ;
#18650=EDGE_CURVE ( 'NONE', #6128, #42485, #39398, .T. ) ;
#18665=ORIENTED_EDGE ( 'NONE', *, *, #13597, .T. ) ;
#18668=VERTEX_POINT ( 'NONE', #35242 ) ;
#18671=EDGE_LOOP ( 'NONE', ( #4340, #50209, #14950, #60090 ) ) ;
#18672=ORIENTED_EDGE ( 'NONE', *, *, #16582, .T. ) ;
#18677=CARTESIAN_POINT ( 'NONE',  ( -22.27706089016750113, 3.548384797797536905, 0.9798385173595970388 ) ) ;
#18690=AXIS2_PLACEMENT_3D ( 'NONE', #43909, #8988, #17667 ) ;
#18692=ADVANCED_FACE ( 'NONE', ( #43935 ), #64213, .T. ) ;
#18695=ORIENTED_EDGE ( 'NONE', *, *, #60555, .F. ) ;
#18702=DIRECTION ( 'NONE',  ( 0.000000000000000000, 0.000000000000000000, 1.000000000000000000 ) ) ;
#18704=EDGE_CURVE ( 'NONE', #10069, #62776, #24491, .T. ) ;
#18708=CYLINDRICAL_SURFACE ( 'NONE', #38359, 6.936499999999988120 ) ;
#18714=CARTESIAN_POINT ( 'NONE',  ( -26.74023318801843629, 1.425982498898183071, 3.035730054944064005 ) ) ;
#18717=CYLINDRICAL_SURFACE ( 'NONE', #21465, 6.936499999999988120 ) ;
#18718=CARTESIAN_POINT ( 'NONE',  ( -22.27709082389155171, -3.569727173833824985, 0.8996430462092213087 ) ) ;
#18722=ORIENTED_EDGE ( 'NONE', *, *, #45207, .T. ) ;
#18733=LINE ( 'NONE', #54641, #186 ) ;
#18736=CARTESIAN_POINT ( 'NONE',  ( 2.000000000000001776, 0.000000000000000000, 0.000000000000000000 ) ) ;
#18738=CARTESIAN_POINT ( 'NONE',  ( -35.04709527796842394, 0.005220632201000108275, 0.01120703303051501232 ) ) ;
#18742=CARTESIAN_POINT ( 'NONE',  ( 0.000000000000000000, -6.812627895098285258, -0.04423456934733380197 ) ) ;
#18746=DIRECTION ( 'NONE',  ( -1.000000000000000000, 0.000000000000000000, 0.000000000000000000 ) ) ;
#18756=CARTESIAN_POINT ( 'NONE',  ( -22.27706485742869091, 0.9221835209182547288, 3.563814065926663499 ) ) ;
#18769=EDGE_CURVE ( 'NONE', #5130, #33557, #7812, .T. ) ;
#18772=VERTEX_POINT ( 'NONE', #14088 ) ;
#18774=DIRECTION ( 'NONE',  ( 1.000000000000000000, 0.000000000000000000, 0.000000000000000000 ) ) ;
#18778=DIRECTION ( 'NONE',  ( -1.000000000000000000, 0.000000000000000000, 0.000000000000000000 ) ) ;
#18786=CARTESIAN_POINT ( 'NONE',  ( -27.15511094194037511, -1.124668417986064650, 2.237231637349069935 ) ) ;
#18788=EDGE_LOOP ( 'NONE', ( #5100, #23454, #52299, #31255 ) ) ;
#18789=AXIS2_PLACEMENT_3D ( 'NONE', #1570, #21844, #32444 ) ;
#18790=CARTESIAN_POINT ( 'NONE',  ( -35.04834644901396956, 0.01358669851861657799, 0.002604658385688424921 ) ) ;
#18795=CARTESIAN_POINT ( 'NONE',  ( -28.66013792860432119, -1.673433383655446249, -0.7552004871165390876 ) ) ;
#18800=DIRECTION ( 'NONE',  ( 0.9582930651793755139, -0.01979360193296142434, -0.2851010602429191465 ) ) ;
#18802=CARTESIAN_POINT ( 'NONE',  ( -22.27715526084302056, 2.228953214080639622, 2.930376837866810025 ) ) ;
#18803=ORIENTED_EDGE ( 'NONE', *, *, #3539, .F. ) ;
#18817=CARTESIAN_POINT ( 'NONE',  ( 0.000000000000000000, 0.000000000000000000, 0.000000000000000000 ) ) ;
#18823=CARTESIAN_POINT ( 'NONE',  ( -27.15525204139121840, -2.394850816831292306, 0.7327319213109850793 ) ) ;
#18828=ORIENTED_EDGE ( 'NONE', *, *, #51864, .T. ) ;
#18834=DIRECTION ( 'NONE',  ( 0.000000000000000000, 0.2149704402110178270, 0.9766205557100881007 ) ) ;
#18844=EDGE_CURVE ( 'NONE', #52522, #39065, #14409, .T. ) ;
#18847=CARTESIAN_POINT ( 'NONE',  ( -22.29195009621226475, -2.585382421603431347, 2.682867222693514186 ) ) ;
#18864=AXIS2_PLACEMENT_3D ( 'NONE', #63277, #39313, #17746 ) ;
#18865=CARTESIAN_POINT ( 'NONE',  ( 2.000000000000001776, 0.000000000000000000, 0.000000000000000000 ) ) ;
#18868=ORIENTED_EDGE ( 'NONE', *, *, #20961, .F. ) ;
#18872=CARTESIAN_POINT ( 'NONE',  ( 2.000000000000001776, 3.786546189469266466, -5.663561025469129540 ) ) ;
#18876=EDGE_CURVE ( 'NONE', #37616, #18330, #45016, .T. ) ;
#18882=EDGE_LOOP ( 'NONE', ( #24019, #62398, #52487, #38402 ) ) ;
#18884=CARTESIAN_POINT ( 'NONE',  ( -22.29382655386184808, 2.586160974799843970, -2.689927793811009771 ) ) ;
#18891=DIRECTION ( 'NONE',  ( 0.000000000000000000, 0.000000000000000000, 1.000000000000000000 ) ) ;
#18894=CYLINDRICAL_SURFACE ( 'NONE', #57615, 6.936499999999988120 ) ;
#18899=LINE ( 'NONE', #49810, #58139 ) ;
#18901=CARTESIAN_POINT ( 'NONE',  ( -27.09150307427448112, -2.306459590995638020, 0.1754204729056251799 ) ) ;
#18907=DIRECTION ( 'NONE',  ( -1.000000000000000000, 0.000000000000000000, 0.000000000000000000 ) ) ;
#18911=CARTESIAN_POINT ( 'NONE',  ( -22.71097035706202760, 2.846599994298365743, -4.089776368546553798 ) ) ;
#18912=CARTESIAN_POINT ( 'NONE',  ( -27.08430792439084556, 1.625846845508333027, -1.614882584890335870 ) ) ;
#18918=DIRECTION ( 'NONE',  ( -1.000000000000000000, 0.000000000000000000, 0.000000000000000000 ) ) ;
#18927=ORIENTED_EDGE ( 'NONE', *, *, #35390, .F. ) ;
#18930=CARTESIAN_POINT ( 'NONE',  ( 1.000000000000000888, 7.203928197742101247, 2.086484728383167564 ) ) ;
#18931=VECTOR ( 'NONE', #31339, 1000.000000000000000 ) ;
#18932=CARTESIAN_POINT ( 'NONE',  ( -22.28546858134833286, 2.654201075783140684, 2.587024666338633594 ) ) ;
#18941=DIRECTION ( 'NONE',  ( -1.000000000000000000, 0.000000000000000000, 0.000000000000000000 ) ) ;
#18949=FACE_OUTER_BOUND ( 'NONE', #62966, .T. ) ;
#18952=EDGE_CURVE ( 'NONE', #32989, #666, #57288, .T. ) ;
#18960=ORIENTED_EDGE ( 'NONE', *, *, #1276, .T. ) ;
#18962=CARTESIAN_POINT ( 'NONE',  ( 2.000000000000001776, -7.248432822490255667, 1.926193556692974429 ) ) ;
#18965=ORIENTED_EDGE ( 'NONE', *, *, #49925, .F. ) ;
#18969=CARTESIAN_POINT ( 'NONE',  ( 0.000000000000000000, 7.203928197742132333, -2.086484728383096510 ) ) ;
#18971=ORIENTED_EDGE ( 'NONE', *, *, #47994, .T. ) ;
#18974=ORIENTED_EDGE ( 'NONE', *, *, #63333, .F. ) ;
#18976=EDGE_LOOP ( 'NONE', ( #28836, #63931, #23395, #10746 ) ) ;
#18979=ORIENTED_EDGE ( 'NONE', *, *, #6916, .F. ) ;
#18981=CARTESIAN_POINT ( 'NONE',  ( -35.04660725145885891, 0.004999447127077803754, -0.01123650152081124946 ) ) ;
#18990=CARTESIAN_POINT ( 'NONE',  ( 2.000000000000001776, 0.000000000000000000, 0.000000000000000000 ) ) ;
#18991=EDGE_LOOP ( 'NONE', ( #63351, #9501, #61537, #54838 ) ) ;
#18992=CYLINDRICAL_SURFACE ( 'NONE', #59404, 2.899999999999994582 ) ;
#19002=CARTESIAN_POINT ( 'NONE',  ( -27.08417568107323348, 2.142502990753195835, 0.8117865859100116266 ) ) ;
#19007=CARTESIAN_POINT ( 'NONE',  ( -35.05012975565874456, -0.01089417657934746084, 0.008684292310210053531 ) ) ;
#19010=VECTOR ( 'NONE', #29559, 1000.000000000000000 ) ;
#19013=CARTESIAN_POINT ( 'NONE',  ( -22.46509356695202086, 4.154553862421376920, 0.8809186187925714950 ) ) ;
#19016=DIRECTION ( 'NONE',  ( 0.000000000000000000, 0.000000000000000000, 1.000000000000000000 ) ) ;
#19017=CARTESIAN_POINT ( 'NONE',  ( 0.000000000000000000, -5.997115278587647147, 3.485633455389469226 ) ) ;
#19022=CARTESIAN_POINT ( 'NONE',  ( -27.08579483061203064, -1.318128465624909706, -1.879952013015660395 ) ) ;
#19029=ORIENTED_EDGE ( 'NONE', *, *, #49913, .T. ) ;
#19030=VERTEX_POINT ( 'NONE', #26361 ) ;
#19035=EDGE_LOOP ( 'NONE', ( #46060, #59290, #11440, #64615, #49859, #8574, #8058, #18447, #63575, #62591, #28379, #23221, #30486, #41460, #2053, #6220, #32265, #32891, #58995, #53096, #399, #43487, #21628, #37754, #806, #4926, #19109, #22277, #29362, #23776, #2910, #26204, #21217, #55242 ) ) ;
#19036=CARTESIAN_POINT ( 'NONE',  ( -22.27722015946438816, -2.356370737780152602, -2.828901469906482724 ) ) ;
#19042=AXIS2_PLACEMENT_3D ( 'NONE', #16020, #31000, #36312 ) ;
#19043=DIRECTION ( 'NONE',  ( 1.000000000000000000, 0.000000000000000000, 0.000000000000000000 ) ) ;
#19044=DIRECTION ( 'NONE',  ( -0.9582930651793755139, -0.06744057189511995509, 0.2777159889015688998 ) ) ;
#19045=ORIENTED_EDGE ( 'NONE', *, *, #5565, .F. ) ;
#19049=CYLINDRICAL_SURFACE ( 'NONE', #52869, 2.899999999999994582 ) ;
#19058=CARTESIAN_POINT ( 'NONE',  ( -27.10719052120871098, -1.962717903527672059, 1.310802520592011966 ) ) ;
#19059=ORIENTED_EDGE ( 'NONE', *, *, #3309, .T. ) ;
#19071=CARTESIAN_POINT ( 'NONE',  ( -22.31328051695926007, 2.109671368890633669, 3.148362328073145200 ) ) ;
#19072=CARTESIAN_POINT ( 'NONE',  ( -22.30078715814471479, 1.645949880549432365, -3.372109767220907273 ) ) ;
#19077=VERTEX_POINT ( 'NONE', #34296 ) ;
#19079=DIRECTION ( 'NONE',  ( -1.000000000000000000, 0.000000000000000000, 0.000000000000000000 ) ) ;
#19080=CARTESIAN_POINT ( 'NONE',  ( -22.30625920655495165, 2.110841417170918000, 3.150098859949304941 ) ) ;
#19081=ADVANCED_FACE ( 'NONE', ( #7729 ), #42965, .T. ) ;
#19082=ADVANCED_BREP_SHAPE_REPRESENTATION ( '', ( #6945, #24966 ), #29232 ) ;
#19084=CIRCLE ( 'NONE', #9508, 7.499999999999988454 ) ;
#19087=FACE_OUTER_BOUND ( 'NONE', #21833, .T. ) ;
#19090=CARTESIAN_POINT ( 'NONE',  ( 1.000000000000000888, -6.586971819220299729, -3.586335490831473738 ) ) ;
#19099=CARTESIAN_POINT ( 'NONE',  ( -22.27384469013076185, -2.625926801827875412, 2.581192766446261722 ) ) ;
#19109=ORIENTED_EDGE ( 'NONE', *, *, #35072, .T. ) ;
#19114=CARTESIAN_POINT ( 'NONE',  ( -35.04643116707788408, 0.01204777744935082995, -0.001845126042314057524 ) ) ;
#19119=CARTESIAN_POINT ( 'NONE',  ( -22.51237073810381162, -4.319597983500831795, -0.9543406717316693655 ) ) ;
#19129=ORIENTED_EDGE ( 'NONE', *, *, #62885, .F. ) ;
#19130=EDGE_CURVE ( 'NONE', #52731, #4816, #40487, .T. ) ;
#19131=ORIENTED_EDGE ( 'NONE', *, *, #30198, .T. ) ;
#19132=ADVANCED_FACE ( 'NONE', ( #59257 ), #18708, .T. ) ;
#19145=ORIENTED_EDGE ( 'NONE', *, *, #18844, .F. ) ;
#19147=ORIENTED_EDGE ( 'NONE', *, *, #45329, .T. ) ;
#19148=DIRECTION ( 'NONE',  ( -1.000000000000000000, 0.000000000000000000, 0.000000000000000000 ) ) ;
#19157=DIRECTION ( 'NONE',  ( 0.000000000000000000, 0.5155538571770230671, -0.8568571761675883858 ) ) ;
#19165=CIRCLE ( 'NONE', #27655, 2.899999999999997691 ) ;
#19167=AXIS2_PLACEMENT_3D ( 'NONE', #41170, #31217, #638 ) ;
#19181=EDGE_CURVE ( 'NONE', #30137, #2564, #17142, .T. ) ;
#19186=VECTOR ( 'NONE', #37618, 1000.000000000000114 ) ;
#19187=CARTESIAN_POINT ( 'NONE',  ( 1.000000000000000888, 6.997684042076945055, -2.698595569414161677 ) ) ;
#19189=CARTESIAN_POINT ( 'NONE',  ( 2.000000000000001776, 0.000000000000000000, 0.000000000000000000 ) ) ;
#19190=FACE_OUTER_BOUND ( 'NONE', #10067, .T. ) ;
#19219=CIRCLE ( 'NONE', #13878, 7.499999999999988454 ) ;
#19220=CARTESIAN_POINT ( 'NONE',  ( 0.000000000000000000, -6.936109781200648250, -2.853135311045116307 ) ) ;
#19223=DIRECTION ( 'NONE',  ( -1.000000000000000000, 0.000000000000000000, 0.000000000000000000 ) ) ;
#19228=EDGE_CURVE ( 'NONE', #40566, #7359, #9675, .T. ) ;
#19233=DIRECTION ( 'NONE',  ( 0.000000000000000000, 0.1764146379942750087, 0.9843159429275484262 ) ) ;
#19236=CARTESIAN_POINT ( 'NONE',  ( 1.000000000000000888, -5.217815162096861137, 5.387430271863535403 ) ) ;
#19238=ADVANCED_FACE ( 'NONE', ( #64869 ), #3899, .F. ) ;
#19258=CARTESIAN_POINT ( 'NONE',  ( -27.08430418657510685, 2.086666645150422994, 0.9470735946412616180 ) ) ;
#19280=LINE ( 'NONE', #49866, #56154 ) ;
#19282=VERTEX_POINT ( 'NONE', #27270 ) ;
#19290=EDGE_LOOP ( 'NONE', ( #45139, #39332, #17759, #63534 ) ) ;
#19318=CARTESIAN_POINT ( 'NONE',  ( 0.000000000000000000, -6.164400007374799095, 2.900694413976478536 ) ) ;
#19320=CIRCLE ( 'NONE', #16123, 7.499999999999988454 ) ;
#19327=CIRCLE ( 'NONE', #37337, 6.936499999999993449 ) ;
#19329=VECTOR ( 'NONE', #5791, 1000.000000000000000 ) ;
#19340=VERTEX_POINT ( 'NONE', #704 ) ;
#19343=AXIS2_PLACEMENT_3D ( 'NONE', #39324, #9722, #34656 ) ;
#19348=CARTESIAN_POINT ( 'NONE',  ( -22.59969328935894239, 4.594269189967342015, 0.7214993884004420321 ) ) ;
#19349=CARTESIAN_POINT ( 'NONE',  ( -22.27384469013076185, 1.508555848190777926, -3.358914544760239540 ) ) ;
#19352=ADVANCED_FACE ( 'NONE', ( #20962, #56902 ), #26952, .F. ) ;
#19355=CARTESIAN_POINT ( 'NONE',  ( -27.08430418657512107, -1.333569526608691991, -1.863523114788429691 ) ) ;
#19371=B_SPLINE_CURVE_WITH_KNOTS ( 'NONE', 3,
 ( #24900, #15237, #40848, #293, #41149, #30211 ),
 .UNSPECIFIED., .F., .F.,
 ( 4, 2, 4 ),
 ( 0.000000000000000000, 0.0004528561986909433257, 0.0009057123973818866514 ),
 .UNSPECIFIED. ) ;
#19372=ORIENTED_EDGE ( 'NONE', *, *, #30564, .T. ) ;
#19385=ORIENTED_EDGE ( 'NONE', *, *, #28077, .F. ) ;
#19393=DIRECTION ( 'NONE',  ( 0.000000000000000000, -0.3193015301359872216, 0.9476531711827999027 ) ) ;
#19404=EDGE_LOOP ( 'NONE', ( #9423, #62304, #59205, #58321 ) ) ;
#19407=DIRECTION ( 'NONE',  ( 0.000000000000000000, 0.000000000000000000, -1.000000000000000000 ) ) ;
#19415=ORIENTED_EDGE ( 'NONE', *, *, #64656, .F. ) ;
#19429=CARTESIAN_POINT ( 'NONE',  ( 0.000000000000000000, 5.107597897712416568, -4.693343793638371508 ) ) ;
#19431=AXIS2_PLACEMENT_3D ( 'NONE', #62020, #28987, #32705 ) ;
#19433=CARTESIAN_POINT ( 'NONE',  ( -27.35552965826137140, 1.773915698030573473, -2.548625910254528559 ) ) ;
#19444=EDGE_LOOP ( 'NONE', ( #32542, #16242, #47709, #3931 ) ) ;
#19450=CARTESIAN_POINT ( 'NONE',  ( 2.000000000000001776, -6.664893814313753495, 3.439359016433473748 ) ) ;
#19478=CIRCLE ( 'NONE', #61948, 2.899999999999996358 ) ;
#19480=CARTESIAN_POINT ( 'NONE',  ( -22.28284753389937478, 0.9231250029035257265, -3.581493264753382810 ) ) ;
#19482=CARTESIAN_POINT ( 'NONE',  ( -22.27715526084302056, 1.423304177213893684, -3.395518526174213569 ) ) ;
#19484=FACE_OUTER_BOUND ( 'NONE', #25991, .T. ) ;
#19494=VECTOR ( 'NONE', #30558, 1000.000000000000000 ) ;
#19500=ORIENTED_EDGE ( 'NONE', *, *, #9979, .F. ) ;
#19505=CIRCLE ( 'NONE', #384, 2.999999999999996447 ) ;
#19511=EDGE_CURVE ( 'NONE', #38245, #45593, #33134, .T. ) ;
#19513=VERTEX_POINT ( 'NONE', #50189 ) ;
#19522=CARTESIAN_POINT ( 'NONE',  ( -22.38932658256918984, 4.011828264158244117, -0.2254938976656405414 ) ) ;
#19523=CARTESIAN_POINT ( 'NONE',  ( -22.28169757117798966, -0.9841724999439904753, -3.561623073126556793 ) ) ;
#19525=CARTESIAN_POINT ( 'NONE',  ( -27.08588607604433562, 2.220764381377020147, 0.5840042213196856569 ) ) ;
#19531=CARTESIAN_POINT ( 'NONE',  ( -27.09364415740165910, 1.303410551736471801, 1.918701019213880032 ) ) ;
#19534=DIRECTION ( 'NONE',  ( 0.000000000000000000, -0.8276889981568956722, 0.5611870653623748373 ) ) ;
#19535=CARTESIAN_POINT ( 'NONE',  ( -22.51237073810381517, 4.319597983500838012, 0.9543406717316287313 ) ) ;
#19538=ORIENTED_EDGE ( 'NONE', *, *, #60290, .T. ) ;
#19546=EDGE_CURVE ( 'NONE', #49777, #29500, #59697, .T. ) ;
#19562=VECTOR ( 'NONE', #13371, 1000.000000000000227 ) ;
#19581=DIRECTION ( 'NONE',  ( -1.000000000000000000, 0.000000000000000000, 0.000000000000000000 ) ) ;
#19582=CARTESIAN_POINT ( 'NONE',  ( 2.000000000000001776, -3.795144977083660720, 6.468916029978772464 ) ) ;
#19586=LINE ( 'NONE', #14251, #65755 ) ;
#19587=B_SPLINE_CURVE_WITH_KNOTS ( 'NONE', 3,
 ( #12013, #63213, #12655, #1068, #26655, #46950 ),
 .UNSPECIFIED., .F., .F.,
 ( 4, 2, 4 ),
 ( 5.043579854804842159E-18, 0.0004528561986909453857, 0.0009057123973818857841 ),
 .UNSPECIFIED. ) ;
#19594=AXIS2_PLACEMENT_3D ( 'NONE', #23079, #29054, #63615 ) ;
#19605=DIRECTION ( 'NONE',  ( -1.000000000000000000, 0.000000000000000000, 0.000000000000000000 ) ) ;
#19606=CARTESIAN_POINT ( 'NONE',  ( 0.000000000000000000, -5.814643797626954935, 3.550179297009551149 ) ) ;
#19610=CYLINDRICAL_SURFACE ( 'NONE', #36063, 6.936499999999988120 ) ;
#19616=DIRECTION ( 'NONE',  ( 0.000000000000000000, 0.000000000000000000, -1.000000000000000000 ) ) ;
#19617=EDGE_CURVE ( 'NONE', #36553, #22075, #32037, .T. ) ;
#19629=EDGE_CURVE ( 'NONE', #18227, #16636, #55396, .T. ) ;
#19640=VERTEX_POINT ( 'NONE', #36520 ) ;
#19654=DIRECTION ( 'NONE',  ( -1.000000000000000000, 0.000000000000000000, 0.000000000000000000 ) ) ;
#19670=DIRECTION ( 'NONE',  ( 0.000000000000000000, 0.000000000000000000, -1.000000000000000000 ) ) ;
#19673=EDGE_CURVE ( 'NONE', #11283, #5130, #49066, .T. ) ;
#19675=CARTESIAN_POINT ( 'NONE',  ( 0.000000000000000000, 0.000000000000000000, 0.000000000000000000 ) ) ;
#19678=AXIS2_PLACEMENT_3D ( 'NONE', #22379, #52975, #62950 ) ;
#19683=ADVANCED_FACE ( 'NONE', ( #52150 ), #10574, .T. ) ;
#19686=DIRECTION ( 'NONE',  ( 0.000000000000000000, 0.5155538571770231782, -0.8568571761675882748 ) ) ;
#19701=EDGE_CURVE ( 'NONE', #40113, #21973, #1260, .T. ) ;
#19703=EDGE_LOOP ( 'NONE', ( #63165, #4713, #1562, #33003 ) ) ;
#19706=DIRECTION ( 'NONE',  ( 0.000000000000000000, -0.6876994588534139918, -0.7259954919231395021 ) ) ;
#19717=DIRECTION ( 'NONE',  ( 0.000000000000000000, 0.000000000000000000, 1.000000000000000000 ) ) ;
#19718=ORIENTED_EDGE ( 'NONE', *, *, #58838, .F. ) ;
#19722=CARTESIAN_POINT ( 'NONE',  ( -22.70624764888619751, 4.097886656202288869, 3.282666355490642118 ) ) ;
#19723=CIRCLE ( 'NONE', #29246, 7.499999999999988454 ) ;
#19729=CYLINDRICAL_SURFACE ( 'NONE', #6625, 6.936499999999988120 ) ;
#19738=CARTESIAN_POINT ( 'NONE',  ( -28.67667724226168602, -0.4371157725390015791, 1.840944188131422576 ) ) ;
#19744=EDGE_LOOP ( 'NONE', ( #63664, #32718, #23057, #24367 ) ) ;
#19760=ADVANCED_FACE ( 'NONE', ( #28829 ), #27508, .T. ) ;
#19762=CARTESIAN_POINT ( 'NONE',  ( 2.000000000000001776, -6.997684042076919297, 2.698595569414185658 ) ) ;
#19763=DIRECTION ( 'NONE',  ( -1.000000000000000000, 0.000000000000000000, 0.000000000000000000 ) ) ;
#19770=CARTESIAN_POINT ( 'NONE',  ( 2.000000000000001776, 6.750946897830741200, -1.593658756657007514 ) ) ;
#19788=ORIENTED_EDGE ( 'NONE', *, *, #1525, .T. ) ;
#19791=ORIENTED_EDGE ( 'NONE', *, *, #34736, .F. ) ;
#19794=CARTESIAN_POINT ( 'NONE',  ( -22.27218376572352554, -0.3046453028544371944, -3.670373711461411670 ) ) ;
#19795=CARTESIAN_POINT ( 'NONE',  ( 1.000000000000000888, -3.224464355699868889, 6.771471746881965181 ) ) ;
#19801=LINE ( 'NONE', #50057, #23144 ) ;
#19805=CARTESIAN_POINT ( 'NONE',  ( -22.29382655386184453, 0.8947172055470843377, -3.622626291186091141 ) ) ;
#19824=DIRECTION ( 'NONE',  ( -0.9606638835031802159, -0.1943236796486244866, -0.1984016392583667632 ) ) ;
#19832=CARTESIAN_POINT ( 'NONE',  ( -35.04834644901396956, -0.002604658385690415082, 0.01358669851862255064 ) ) ;
#19835=EDGE_LOOP ( 'NONE', ( #20905, #58484, #59302, #30450 ) ) ;
#19838=CYLINDRICAL_SURFACE ( 'NONE', #49300, 6.936499999999988120 ) ;
#19861=FACE_OUTER_BOUND ( 'NONE', #8959, .T. ) ;
#19870=CARTESIAN_POINT ( 'NONE',  ( -27.08702828306175547, 0.5765135930309237544, -2.226264228964716985 ) ) ;
#19871=ORIENTED_EDGE ( 'NONE', *, *, #54536, .F. ) ;
#19872=CARTESIAN_POINT ( 'NONE',  ( -27.09602251845210930, 2.320865065108510539, -0.1644056400645273475 ) ) ;
#19885=CARTESIAN_POINT ( 'NONE',  ( -27.09569413923886216, 1.607816962455218102, -1.680421072128820192 ) ) ;
#19890=EDGE_CURVE ( 'NONE', #42057, #6580, #22334, .T. ) ;
#19894=CARTESIAN_POINT ( 'NONE',  ( -22.28121537037576871, -3.680034389105489190, 0.3168735205819568357 ) ) ;
#19896=CARTESIAN_POINT ( 'NONE',  ( 0.000000000000000000, -3.937687286050851831, 6.383151168292441113 ) ) ;
#19913=CARTESIAN_POINT ( 'NONE',  ( 1.000000000000000888, 2.473437528934240515, -7.080403010454960011 ) ) ;
#19914=CARTESIAN_POINT ( 'NONE',  ( 2.000000000000001776, 1.225832621831852931, 6.827324998361547159 ) ) ;
#19918=DIRECTION ( 'NONE',  ( -1.000000000000000000, 0.000000000000000000, 0.000000000000000000 ) ) ;
#19925=CYLINDRICAL_SURFACE ( 'NONE', #31702, 6.936499999999988120 ) ;
#19927=ORIENTED_EDGE ( 'NONE', *, *, #1384, .T. ) ;
#19930=ORIENTED_EDGE ( 'NONE', *, *, #35157, .F. ) ;
#19931=FACE_OUTER_BOUND ( 'NONE', #24350, .T. ) ;
#19951=AXIS2_PLACEMENT_3D ( 'NONE', #18817, #39077, #55705 ) ;
#19959=EDGE_LOOP ( 'NONE', ( #19045, #7493, #13222, #37863 ) ) ;
#19961=EDGE_CURVE ( 'NONE', #10662, #31156, #49114, .T. ) ;
#19967=CARTESIAN_POINT ( 'NONE',  ( 1.000000000000000888, 3.795144977083636739, 6.468916029978800886 ) ) ;
#19973=EDGE_CURVE ( 'NONE', #61727, #662, #33184, .T. ) ;
#19979=ORIENTED_EDGE ( 'NONE', *, *, #23807, .F. ) ;
#19981=DIRECTION ( 'NONE',  ( 0.000000000000000000, 0.5155538571770171830, 0.8568571761675919385 ) ) ;
#19982=CARTESIAN_POINT ( 'NONE',  ( -27.20102706715912788, -1.765193291701709688, 1.966718264078082923 ) ) ;
#19986=CIRCLE ( 'NONE', #53983, 6.936499999999989008 ) ;
#19987=ADVANCED_FACE ( 'NONE', ( #31446 ), #1541, .T. ) ;
#19992=AXIS2_PLACEMENT_3D ( 'NONE', #30809, #32457, #5925 ) ;
#19994=CARTESIAN_POINT ( 'NONE',  ( -27.09048036756591671, -1.306202114107277712, -1.905306051559101377 ) ) ;
#19998=( BOUNDED_SURFACE ( )  B_SPLINE_SURFACE ( 3, 1, ( 
 ( #195, #36062 ),
 ( #16130, #4864 ),
 ( #51724, #25130 ),
 ( #15471, #35735 ) ),
 .UNSPECIFIED., .F., .F., .F. ) 
 B_SPLINE_SURFACE_WITH_KNOTS ( ( 4, 4 ),
 ( 2, 2 ),
 ( 0.000000000000000000, 1.000000000000000000 ),
 ( 0.000000000000000000, 1.000000000000000000 ),
 .UNSPECIFIED. ) 
 GEOMETRIC_REPRESENTATION_ITEM ( )  RATIONAL_B_SPLINE_SURFACE ( (
 ( 1.000000000000000000, 1.000000000000000000),
 ( 0.8716676215708681896, 0.8964445200148164483),
 ( 0.8716676215708681896, 0.8964445200148164483),
 ( 1.000000000000000000, 1.000000000000000000) ) ) 
 REPRESENTATION_ITEM ( '' )  SURFACE ( )  );
#20002=CARTESIAN_POINT ( 'NONE',  ( 0.000000000000000000, -3.786546189469129686, -5.663561025469209476 ) ) ;
#20009=CARTESIAN_POINT ( 'NONE',  ( -22.27709082389155171, 0.8996430462092437352, 3.569727173833806333 ) ) ;
#20013=CARTESIAN_POINT ( 'NONE',  ( 2.000000000000001776, 7.414200355365259121, 1.131208685655164414 ) ) ;
#20025=ORIENTED_EDGE ( 'NONE', *, *, #62017, .T. ) ;
#20027=DIRECTION ( 'NONE',  ( 0.000000000000000000, 0.000000000000000000, 1.000000000000000000 ) ) ;
#20031=CARTESIAN_POINT ( 'NONE',  ( -27.05748184469818440, 3.214204530190199804, 0.2721081511922631146 ) ) ;
#20036=CARTESIAN_POINT ( 'NONE',  ( -27.08418322526030764, 2.265123059255413462, -0.3452258100746935510 ) ) ;
#20045=EDGE_CURVE ( 'NONE', #48006, #49701, #37399, .T. ) ;
#20046=ORIENTED_EDGE ( 'NONE', *, *, #63652, .T. ) ;
#20049=CARTESIAN_POINT ( 'NONE',  ( -27.15525204139122550, -0.7327319213109896312, -2.394850816831294527 ) ) ;
#20054=CIRCLE ( 'NONE', #57222, 6.936499999999989008 ) ;
#20056=EDGE_CURVE ( 'NONE', #38732, #26571, #7711, .T. ) ;
#20060=EDGE_CURVE ( 'NONE', #43097, #15504, #10877, .T. ) ;
#20068=DIRECTION ( 'NONE',  ( 0.000000000000000000, -0.6876994588534294239, 0.7259954919231249582 ) ) ;
#20077=AXIS2_PLACEMENT_3D ( 'NONE', #1983, #22251, #62172 ) ;
#20078=CARTESIAN_POINT ( 'NONE',  ( 0.000000000000000000, 0.3246585432986198727, 6.805031400696091914 ) ) ;
#20084=EDGE_LOOP ( 'NONE', ( #41561, #13032, #49398, #51287 ) ) ;
#20088=EDGE_CURVE ( 'NONE', #52731, #54109, #17247, .T. ) ;
#20092=AXIS2_PLACEMENT_3D ( 'NONE', #7468, #17470, #27760 ) ;
#20101=CARTESIAN_POINT ( 'NONE',  ( 2.000000000000001776, 0.000000000000000000, 0.000000000000000000 ) ) ;
#20102=ORIENTED_EDGE ( 'NONE', *, *, #23807, .T. ) ;
#20106=CARTESIAN_POINT ( 'NONE',  ( -22.27878402819507997, -0.9457981527432397506, 3.562981801125739700 ) ) ;
#20114=CARTESIAN_POINT ( 'NONE',  ( -26.74023318801844340, -2.752802096869876536, -1.916028097164421906 ) ) ;
#20118=ORIENTED_EDGE ( 'NONE', *, *, #29727, .F. ) ;
#20120=DIRECTION ( 'NONE',  ( -1.000000000000000000, 0.000000000000000000, 0.000000000000000000 ) ) ;
#20121=CARTESIAN_POINT ( 'NONE',  ( -22.28546858134833641, 0.9133285433746859416, -3.592117891549496900 ) ) ;
#20130=DIRECTION ( 'NONE',  ( -1.000000000000000000, 0.000000000000000000, 0.000000000000000000 ) ) ;
#20133=ADVANCED_FACE ( 'NONE', ( #33972 ), #18717, .T. ) ;
#20136=CARTESIAN_POINT ( 'NONE',  ( -22.31328051695926007, 2.109671368890633669, 3.148362328073145200 ) ) ;
#20137=EDGE_CURVE ( 'NONE', #7394, #51465, #28919, .T. ) ;
#20141=CARTESIAN_POINT ( 'NONE',  ( -27.08418322526030764, -2.134267017050454296, -0.8335872080609635359 ) ) ;
#20149=VERTEX_POINT ( 'NONE', #44591 ) ;
#20154=CARTESIAN_POINT ( 'NONE',  ( 1.000000000000000888, 5.769711778877386621, -4.791703871138487614 ) ) ;
#20156=CARTESIAN_POINT ( 'NONE',  ( -22.29382655386184453, -1.036465316386235180, -3.584644999358109985 ) ) ;
#20157=CARTESIAN_POINT ( 'NONE',  ( 0.000000000000000000, -3.786546189469212731, 5.663561025469122434 ) ) ;
#20164=ORIENTED_EDGE ( 'NONE', *, *, #38512, .F. ) ;
#20181=ORIENTED_EDGE ( 'NONE', *, *, #50536, .T. ) ;
#20183=( BOUNDED_SURFACE ( )  B_SPLINE_SURFACE ( 3, 1, ( 
 ( #12192, #41797 ),
 ( #37466, #37126 ),
 ( #11859, #52457 ),
 ( #17529, #47461 ) ),
 .UNSPECIFIED., .F., .F., .F. ) 
 B_SPLINE_SURFACE_WITH_KNOTS ( ( 4, 4 ),
 ( 2, 2 ),
 ( 0.000000000000000000, 1.000000000000000000 ),
 ( 0.000000000000000000, 1.000000000000000000 ),
 .UNSPECIFIED. ) 
 GEOMETRIC_REPRESENTATION_ITEM ( )  RATIONAL_B_SPLINE_SURFACE ( (
 ( 1.000000000000000000, 1.000000000000000000),
 ( 0.9932032654565553509, 0.8386279382598740284),
 ( 0.9932032654565553509, 0.8386279382598740284),
 ( 1.000000000000000000, 1.000000000000000000) ) ) 
 REPRESENTATION_ITEM ( '' )  SURFACE ( )  );
#20193=CARTESIAN_POINT ( 'NONE',  ( -27.08429572838383947, 2.279961732801592422, -0.2296550094122856711 ) ) ;
#20194=EDGE_CURVE ( 'NONE', #26404, #49976, #60232, .T. ) ;
#20199=ORIENTED_EDGE ( 'NONE', *, *, #53682, .T. ) ;
#20204=CARTESIAN_POINT ( 'NONE',  ( -22.71097035706203116, 4.965150228107710006, 0.4203397252017151420 ) ) ;
#20211=VERTEX_POINT ( 'NONE', #14992 ) ;
#20223=DIRECTION ( 'NONE',  ( -1.000000000000000000, 0.000000000000000000, 0.000000000000000000 ) ) ;
#20233=CARTESIAN_POINT ( 'NONE',  ( -27.35552965826136429, -2.810569013793742688, 1.320216934008381804 ) ) ;
#20244=CARTESIAN_POINT ( 'NONE',  ( -22.27720412283625961, -3.493592264983218953, -1.161733799004182721 ) ) ;
#20259=ORIENTED_EDGE ( 'NONE', *, *, #60598, .F. ) ;
#20261=ORIENTED_EDGE ( 'NONE', *, *, #50911, .F. ) ;
#20264=CIRCLE ( 'NONE', #36198, 2.899999999999995914 ) ;
#20268=ORIENTED_EDGE ( 'NONE', *, *, #6262, .T. ) ;
#20269=CARTESIAN_POINT ( 'NONE',  ( -10.00000000000000178, 0.000000000000000000, 0.000000000000000000 ) ) ;
#20270=ORIENTED_EDGE ( 'NONE', *, *, #48461, .T. ) ;
#20271=EDGE_CURVE ( 'NONE', #18208, #5331, #23667, .T. ) ;
#20276=VERTEX_POINT ( 'NONE', #20666 ) ;
#20290=CARTESIAN_POINT ( 'NONE',  ( -27.08850691366480490, 0.6228349286848202659, 2.218359546717751041 ) ) ;
#20294=DIRECTION ( 'NONE',  ( 0.000000000000000000, 0.000000000000000000, 1.000000000000000000 ) ) ;
#20305=ORIENTED_EDGE ( 'NONE', *, *, #8531, .T. ) ;
#20310=EDGE_CURVE ( 'NONE', #47259, #32332, #21522, .T. ) ;
#20320=EDGE_CURVE ( 'NONE', #12415, #59008, #390, .T. ) ;
#20329=ORIENTED_EDGE ( 'NONE', *, *, #57427, .F. ) ;
#20337=VERTEX_POINT ( 'NONE', #1373 ) ;
#20338=CARTESIAN_POINT ( 'NONE',  ( -27.08429572838383947, -0.2296550094122856711, -2.279961732801603080 ) ) ;
#20355=AXIS2_PLACEMENT_3D ( 'NONE', #52066, #226, #16158 ) ;
#20356=CIRCLE ( 'NONE', #29941, 7.499999999999988454 ) ;
#20378=VERTEX_POINT ( 'NONE', #62850 ) ;
#20383=CIRCLE ( 'NONE', #51210, 7.499999999999988454 ) ;
#20389=EDGE_CURVE ( 'NONE', #42450, #43097, #33238, .T. ) ;
#20400=AXIS2_PLACEMENT_3D ( 'NONE', #64744, #31164, #45797 ) ;
#20402=EDGE_CURVE ( 'NONE', #51541, #3030, #13620, .T. ) ;
#20403=CARTESIAN_POINT ( 'NONE',  ( 2.000000000000001776, 1.145812388885215194, -6.715725538143608730 ) ) ;
#20405=VERTEX_POINT ( 'NONE', #2360 ) ;
#20409=CARTESIAN_POINT ( 'NONE',  ( -22.29195009621226831, 3.580440466953064949, -1.030739959031443886 ) ) ;
#20410=ORIENTED_EDGE ( 'NONE', *, *, #56976, .F. ) ;
#20419=ORIENTED_EDGE ( 'NONE', *, *, #35390, .T. ) ;
#20421=DIRECTION ( 'NONE',  ( 0.000000000000000000, -0.6051742151937556935, -0.7960930657056508597 ) ) ;
#20437=VERTEX_POINT ( 'NONE', #27945 ) ;
#20446=VERTEX_POINT ( 'NONE', #3348 ) ;
#20455=LINE ( 'NONE', #64122, #54358 ) ;
#20457=B_SPLINE_CURVE_WITH_KNOTS ( 'NONE', 3,
 ( #42006, #32026, #17066, #52345, #12393, #7409 ),
 .UNSPECIFIED., .F., .F.,
 ( 4, 2, 4 ),
 ( 0.0002637379172192473305, 0.0009975831966643154951, 0.001731428476109383822 ),
 .UNSPECIFIED. ) ;
#20459=CARTESIAN_POINT ( 'NONE',  ( 2.000000000000001776, 3.230174184210159893, -5.998318953995314118 ) ) ;
#20467=CARTESIAN_POINT ( 'NONE',  ( 2.000000000000001776, 6.935703035393448346, -0.1051458740707923722 ) ) ;
#20469=ADVANCED_FACE ( 'NONE', ( #18307 ), #7662, .T. ) ;
#20477=APPLICATION_CONTEXT ( 'automotive_design' ) ;
#20479=DIRECTION ( 'NONE',  ( -1.000000000000000000, 0.000000000000000000, 0.000000000000000000 ) ) ;
#20492=CARTESIAN_POINT ( 'NONE',  ( -22.27706089016750113, -0.9256273512588407693, -3.562910635974996243 ) ) ;
#20494=VECTOR ( 'NONE', #15826, 1000.000000000000000 ) ;
#20496=ORIENTED_EDGE ( 'NONE', *, *, #33081, .F. ) ;
#20532=CARTESIAN_POINT ( 'NONE',  ( -27.10719052120871098, -2.261993590776032459, 0.6736837626858792616 ) ) ;
#20537=CIRCLE ( 'NONE', #26895, 2.899999999999995026 ) ;
#20549=DIRECTION ( 'NONE',  ( 0.000000000000000000, -0.5155538571770109657, -0.8568571761675956022 ) ) ;
#20575=VECTOR ( 'NONE', #10881, 1000.000000000000000 ) ;
#20577=EDGE_LOOP ( 'NONE', ( #2544, #45392, #64805, #64566 ) ) ;
#20581=CARTESIAN_POINT ( 'NONE',  ( -22.28506771379528573, -3.575989816848462510, 1.050362426369334079 ) ) ;
#20596=DIRECTION ( 'NONE',  ( -1.000000000000000000, 0.000000000000000000, 0.000000000000000000 ) ) ;
#20604=ADVANCED_FACE ( 'NONE', ( #4971 ), #5292, .T. ) ;
#20605=CARTESIAN_POINT ( 'NONE',  ( -22.27719412087655471, 3.642699606241628807, -0.5341638063191783692 ) ) ;
#20610=CARTESIAN_POINT ( 'NONE',  ( -27.08850691366480490, -2.232573186527710529, -0.5697889027535691930 ) ) ;
#20626=CARTESIAN_POINT ( 'NONE',  ( 2.000000000000001776, -5.888698556700776798, 3.665823448873372747 ) ) ;
#20632=VECTOR ( 'NONE', #54924, 1000.000000000000000 ) ;
#20639=ORIENTED_EDGE ( 'NONE', *, *, #31984, .T. ) ;
#20642=ORIENTED_EDGE ( 'NONE', *, *, #21061, .F. ) ;
#20664=ORIENTED_EDGE ( 'NONE', *, *, #35946, .T. ) ;
#20666=CARTESIAN_POINT ( 'NONE',  ( 2.000000000000001776, 0.8935325819929771374, -7.446583077151355923 ) ) ;
#20679=ORIENTED_EDGE ( 'NONE', *, *, #27620, .F. ) ;
#20680=CARTESIAN_POINT ( 'NONE',  ( 2.000000000000001776, -0.3246585432985730213, -6.805031400696120336 ) ) ;
#20690=CARTESIAN_POINT ( 'NONE',  ( 2.000000000000001776, 0.000000000000000000, 0.000000000000000000 ) ) ;
#20695=CARTESIAN_POINT ( 'NONE',  ( -27.08417473062937120, 2.249064769433619659, -0.4370481938669387723 ) ) ;
#20711=CARTESIAN_POINT ( 'NONE',  ( -22.51237073810381517, 2.986282257334773149, -3.263711251981915140 ) ) ;
#20722=CARTESIAN_POINT ( 'NONE',  ( -27.08871896697694481, -0.9878677378266937925, 2.082324523415888695 ) ) ;
#20723=AXIS2_PLACEMENT_3D ( 'NONE', #63303, #12113, #5255 ) ;
#20732=CARTESIAN_POINT ( 'NONE',  ( 2.000000000000001776, 0.000000000000000000, 0.000000000000000000 ) ) ;
#20733=CARTESIAN_POINT ( 'NONE',  ( -22.94572469358971034, -2.792384151940651371, 4.011883207821675512 ) ) ;
#20736=CARTESIAN_POINT ( 'NONE',  ( 2.000000000000001776, 6.750946897830712778, 1.593658756657066355 ) ) ;
#20743=ORIENTED_EDGE ( 'NONE', *, *, #52465, .F. ) ;
#20745=CARTESIAN_POINT ( 'NONE',  ( 2.000000000000001776, 5.396716205731433291, 4.158041573745082431 ) ) ;
#20752=CARTESIAN_POINT ( 'NONE',  ( -22.27719381268171261, -3.561499689648247369, 0.9326100520993009235 ) ) ;
#20758=CARTESIAN_POINT ( 'NONE',  ( 2.000000000000001776, 1.779948802829910193, -6.576141558201243242 ) ) ;
#20765=CARTESIAN_POINT ( 'NONE',  ( -27.10719052120871098, 1.714424047991082389, 1.622102031466668093 ) ) ;
#20781=CARTESIAN_POINT ( 'NONE',  ( 0.000000000000000000, 2.664846396702580833, -6.404188155572981600 ) ) ;
#20782=CARTESIAN_POINT ( 'NONE',  ( -22.27721688985630522, 1.293557211780076432, -3.446999288411542128 ) ) ;
#20784=EDGE_CURVE ( 'NONE', #22075, #13308, #48112, .T. ) ;
#20788=ADVANCED_FACE ( 'NONE', ( #41496 ), #44646, .F. ) ;
#20806=EDGE_CURVE ( 'NONE', #35321, #24723, #2499, .T. ) ;
#20815=CARTESIAN_POINT ( 'NONE',  ( 2.000000000000001776, 7.248432822490259220, 1.926193556693033271 ) ) ;
#20822=VECTOR ( 'NONE', #35951, 1000.000000000000000 ) ;
#20825=CARTESIAN_POINT ( 'NONE',  ( -22.70624764888619751, 4.891815784104551312, -1.907540768355076688 ) ) ;
#20832=ORIENTED_EDGE ( 'NONE', *, *, #51117, .F. ) ;
#20834=ORIENTED_EDGE ( 'NONE', *, *, #46163, .T. ) ;
#20835=DIRECTION ( 'NONE',  ( -1.000000000000000000, 0.000000000000000000, 0.000000000000000000 ) ) ;
#20836=DIRECTION ( 'NONE',  ( -1.000000000000000000, 0.000000000000000000, 0.000000000000000000 ) ) ;
#20840=VERTEX_POINT ( 'NONE', #46503 ) ;
#20849=CARTESIAN_POINT ( 'NONE',  ( 2.000000000000001776, 0.000000000000000000, 0.000000000000000000 ) ) ;
#20850=CARTESIAN_POINT ( 'NONE',  ( -27.09569413923794556, 0.5521997980586342836, -2.259195818742698592 ) ) ;
#20851=CARTESIAN_POINT ( 'NONE',  ( -27.08704841010922593, 2.291653842312379563, -0.1930432016059793476 ) ) ;
#20853=CARTESIAN_POINT ( 'NONE',  ( 1.000000000000000888, 7.493043167941616289, 0.3229614270519615693 ) ) ;
#20860=EDGE_CURVE ( 'NONE', #13608, #60024, #37501, .T. ) ;
#20870=ORIENTED_EDGE ( 'NONE', *, *, #3879, .T. ) ;
#20882=EDGE_CURVE ( 'NONE', #50607, #22014, #26874, .T. ) ;
#20884=DIRECTION ( 'NONE',  ( -1.000000000000000000, 0.000000000000000000, 0.000000000000000000 ) ) ;
#20885=EDGE_LOOP ( 'NONE', ( #53232, #1283, #64009, #30516 ) ) ;
#20888=ORIENTED_EDGE ( 'NONE', *, *, #59713, .F. ) ;
#20891=CARTESIAN_POINT ( 'NONE',  ( 2.000000000000001776, 0.000000000000000000, 0.000000000000000000 ) ) ;
#20892=ORIENTED_EDGE ( 'NONE', *, *, #52355, .F. ) ;
#20898=CARTESIAN_POINT ( 'NONE',  ( -22.27711653538342773, -3.377206745424988554, -1.465933162149073210 ) ) ;
#20905=ORIENTED_EDGE ( 'NONE', *, *, #33081, .T. ) ;
#20912=DIRECTION ( 'NONE',  ( -1.000000000000000000, 0.000000000000000000, 0.000000000000000000 ) ) ;
#20913=ORIENTED_EDGE ( 'NONE', *, *, #46453, .T. ) ;
#20929=DIRECTION ( 'NONE',  ( 0.000000000000000000, 0.000000000000000000, 1.000000000000000000 ) ) ;
#20935=CARTESIAN_POINT ( 'NONE',  ( 0.000000000000000000, 0.000000000000000000, 0.000000000000000000 ) ) ;
#20936=CARTESIAN_POINT ( 'NONE',  ( -27.09125059358652265, 0.6356863790372305756, 2.223272438024522124 ) ) ;
#20950=CARTESIAN_POINT ( 'NONE',  ( -22.66110217412718342, -1.880032915665386106, -4.573370147466340185 ) ) ;
#20951=ORIENTED_EDGE ( 'NONE', *, *, #28130, .T. ) ;
#20956=ADVANCED_FACE ( 'NONE', ( #65381 ), #29805, .T. ) ;
#20958=DIRECTION ( 'NONE',  ( -1.000000000000000000, 0.000000000000000000, 0.000000000000000000 ) ) ;
#20961=EDGE_CURVE ( 'NONE', #50893, #45822, #23708, .T. ) ;
#20962=FACE_BOUND ( 'NONE', #23125, .T. ) ;
#20980=CYLINDRICAL_SURFACE ( 'NONE', #65023, 2.899999999999994582 ) ;
#20984=CYLINDRICAL_SURFACE ( 'NONE', #2470, 2.899999999999994582 ) ;
#21000=CARTESIAN_POINT ( 'NONE',  ( -27.08871896697731785, -0.1856437051692902407, -2.297279805116104967 ) ) ;
#21003=ORIENTED_EDGE ( 'NONE', *, *, #13063, .F. ) ;
#21004=LINE ( 'NONE', #35318, #9879 ) ;
#21013=CARTESIAN_POINT ( 'NONE',  ( -27.10113028276028402, -2.245923868550884439, 0.6639289823109628674 ) ) ;
#21026=CARTESIAN_POINT ( 'NONE',  ( -27.08954555554372945, -0.9924303381770539501, 2.082904663687279889 ) ) ;
#21038=CIRCLE ( 'NONE', #17880, 2.899999999999995914 ) ;
#21041=CARTESIAN_POINT ( 'NONE',  ( -27.35552965826137140, 0.2619431035392177365, -3.094132632038957276 ) ) ;
#21042=DIRECTION ( 'NONE',  ( 0.000000000000000000, -0.9289767198167871998, -0.3701381553399246682 ) ) ;
#21047=VERTEX_POINT ( 'NONE', #10504 ) ;
#21054=CARTESIAN_POINT ( 'NONE',  ( -27.08418322526030764, -1.789041206975751086, 1.431535851194446485 ) ) ;
#21061=EDGE_CURVE ( 'NONE', #40629, #43273, #29405, .T. ) ;
#21071=CARTESIAN_POINT ( 'NONE',  ( -22.71097035706202405, 4.089776368546564456, 2.846599994298306679 ) ) ;
#21073=EDGE_LOOP ( 'NONE', ( #50866, #64765, #27390, #11539 ) ) ;
#21075=DIRECTION ( 'NONE',  ( -1.000000000000000000, 0.000000000000000000, 0.000000000000000000 ) ) ;
#21079=ADVANCED_FACE ( 'NONE', ( #42074 ), #62054, .T. ) ;
#21082=B_SPLINE_CURVE_WITH_KNOTS ( 'NONE', 3,
 ( #40474, #51134, #60772, #24874, #15530, #35798 ),
 .UNSPECIFIED., .F., .F.,
 ( 4, 2, 4 ),
 ( 0.0002637379172192671714, 0.0009975831966643365287, 0.001731428476109405940 ),
 .UNSPECIFIED. ) ;
#21087=ORIENTED_EDGE ( 'NONE', *, *, #41952, .F. ) ;
#21088=CARTESIAN_POINT ( 'NONE',  ( -25.42680463514452427, -3.188632951113941516, -2.219378695194090145 ) ) ;
#21097=CARTESIAN_POINT ( 'NONE',  ( 0.000000000000000000, 5.814643797626930954, 3.550179297009575574 ) ) ;
#21104=( NAMED_UNIT ( * ) PLANE_ANGLE_UNIT ( ) SI_UNIT ( $, .RADIAN. ) );
#21117=VECTOR ( 'NONE', #1505, 1000.000000000000000 ) ;
#21125=DIRECTION ( 'NONE',  ( 0.000000000000000000, 0.000000000000000000, 1.000000000000000000 ) ) ;
#21127=ORIENTED_EDGE ( 'NONE', *, *, #24164, .T. ) ;
#21128=LINE ( 'NONE', #6846, #39760 ) ;
#21133=ORIENTED_EDGE ( 'NONE', *, *, #42215, .F. ) ;
#21134=DIRECTION ( 'NONE',  ( -1.000000000000000000, 0.000000000000000000, 0.000000000000000000 ) ) ;
#21137=ORIENTED_EDGE ( 'NONE', *, *, #7443, .F. ) ;
#21142=FACE_OUTER_BOUND ( 'NONE', #11019, .T. ) ;
#21143=EDGE_CURVE ( 'NONE', #26098, #15301, #47061, .T. ) ;
#21145=EDGE_CURVE ( 'NONE', #4330, #35715, #54519, .T. ) ;
#21150=ORIENTED_EDGE ( 'NONE', *, *, #40905, .T. ) ;
#21156=VECTOR ( 'NONE', #19581, 1000.000000000000000 ) ;
#21163=AXIS2_PLACEMENT_3D ( 'NONE', #12346, #42589, #36648 ) ;
#21165=ADVANCED_FACE ( 'NONE', ( #22806 ), #27439, .T. ) ;
#21169=VERTEX_POINT ( 'NONE', #2536 ) ;
#21171=CARTESIAN_POINT ( 'NONE',  ( -27.10512513516277977, 0.5469390009826167187, -2.289566223068213890 ) ) ;
#21172=CYLINDRICAL_SURFACE ( 'NONE', #11833, 7.499999999999988454 ) ;
#21174=CARTESIAN_POINT ( 'NONE',  ( 2.000000000000001776, 2.480520636974283821, -6.345145617221223944 ) ) ;
#21189=ORIENTED_EDGE ( 'NONE', *, *, #64229, .T. ) ;
#21197=ORIENTED_EDGE ( 'NONE', *, *, #3426, .F. ) ;
#21215=AXIS2_PLACEMENT_3D ( 'NONE', #10267, #45513, #5298 ) ;
#21217=ORIENTED_EDGE ( 'NONE', *, *, #5842, .T. ) ;
#21224=CARTESIAN_POINT ( 'NONE',  ( -22.27718112499583469, -3.412978993569796504, -1.380338971069148712 ) ) ;
#21227=EDGE_CURVE ( 'NONE', #49976, #8685, #25888, .T. ) ;
#21232=DIRECTION ( 'NONE',  ( 0.000000000000000000, 0.000000000000000000, 1.000000000000000000 ) ) ;
#21233=AXIS2_PLACEMENT_3D ( 'NONE', #53892, #3366, #23634 ) ;
#21234=EDGE_LOOP ( 'NONE', ( #58962, #33196, #18803, #12638 ) ) ;
#21237=ORIENTED_EDGE ( 'NONE', *, *, #11498, .F. ) ;
#21238=DIRECTION ( 'NONE',  ( -1.000000000000000000, 0.000000000000000000, 0.000000000000000000 ) ) ;
#21249=ORIENTED_EDGE ( 'NONE', *, *, #12055, .T. ) ;
#21258=CARTESIAN_POINT ( 'NONE',  ( 2.000000000000001776, -3.805198749487401777, -5.799611601383285020 ) ) ;
#21266=DIRECTION ( 'NONE',  ( 0.000000000000000000, 0.2149704402110246548, -0.9766205557100865464 ) ) ;
#21267=CARTESIAN_POINT ( 'NONE',  ( -27.10113028276028757, 0.6639289823109749689, 2.245923868550868896 ) ) ;
#21275=DIRECTION ( 'NONE',  ( -1.000000000000000000, 0.000000000000000000, 0.000000000000000000 ) ) ;
#21281=CARTESIAN_POINT ( 'NONE',  ( -27.08485414902839494, -0.5952588087544560258, -2.214586389210155382 ) ) ;
#21282=CARTESIAN_POINT ( 'NONE',  ( -35.05012975565874456, -0.01377677982613203199, 0.002073729464861247002 ) ) ;
#21289=DIRECTION ( 'NONE',  ( 0.000000000000000000, 0.2149704402110178825, 0.9766205557100882118 ) ) ;
#21304=ORIENTED_EDGE ( 'NONE', *, *, #48457, .F. ) ;
#21311=EDGE_LOOP ( 'NONE', ( #48155, #63133, #34438, #52631 ) ) ;
#21312=ORIENTED_EDGE ( 'NONE', *, *, #42910, .T. ) ;
#21342=FACE_OUTER_BOUND ( 'NONE', #14330, .T. ) ;
#21344=ORIENTED_EDGE ( 'NONE', *, *, #53183, .T. ) ;
#21347=EDGE_CURVE ( 'NONE', #24059, #12311, #26929, .T. ) ;
#21349=VERTEX_POINT ( 'NONE', #49407 ) ;
#21353=CARTESIAN_POINT ( 'NONE',  ( -35.04643116707788408, 0.008094444324494021181, 0.009112266603801891240 ) ) ;
#21363=CYLINDRICAL_SURFACE ( 'NONE', #46228, 7.499999999999988454 ) ;
#21368=AXIS2_PLACEMENT_3D ( 'NONE', #29621, #45264, #65213 ) ;
#21385=CIRCLE ( 'NONE', #17165, 7.499999999999988454 ) ;
#21388=CARTESIAN_POINT ( 'NONE',  ( -22.27721688985630522, 3.446999288411551898, 1.293557211780032246 ) ) ;
#21393=CARTESIAN_POINT ( 'NONE',  ( -35.05175862995318425, -0.01253051761586874979, 0.001087818442104329653 ) ) ;
#21396=EDGE_CURVE ( 'NONE', #36553, #14035, #26077, .T. ) ;
#21399=ORIENTED_EDGE ( 'NONE', *, *, #48292, .T. ) ;
#21401=VECTOR ( 'NONE', #55494, 1000.000000000000000 ) ;
#21402=CARTESIAN_POINT ( 'NONE',  ( -27.08423805673873375, -1.665498649074237836, 1.573803011992709111 ) ) ;
#21403=AXIS2_PLACEMENT_3D ( 'NONE', #44414, #2916, #18550 ) ;
#21409=EDGE_LOOP ( 'NONE', ( #18974, #45679, #47843, #15253 ) ) ;
#21412=CARTESIAN_POINT ( 'NONE',  ( -10.00000000000000178, 0.000000000000000000, 0.000000000000000000 ) ) ;
#21425=VERTEX_POINT ( 'NONE', #32019 ) ;
#21426=CARTESIAN_POINT ( 'NONE',  ( -22.27706485742869091, 3.662257305743817692, -0.3729136217355926153 ) ) ;
#21430=ORIENTED_EDGE ( 'NONE', *, *, #22766, .T. ) ;
#21433=DIRECTION ( 'NONE',  ( 0.9582930651793755139, -0.2370079598497639439, 0.1596922922278021517 ) ) ;
#21434=EDGE_LOOP ( 'NONE', ( #27670, #37765, #46661, #25464 ) ) ;
#21442=DIRECTION ( 'NONE',  ( -1.000000000000000000, 0.000000000000000000, 0.000000000000000000 ) ) ;
#21453=AXIS2_PLACEMENT_3D ( 'NONE', #60633, #15075, #35355 ) ;
#21454=DIRECTION ( 'NONE',  ( 0.000000000000000000, 0.8276889981568920085, -0.5611870653623801664 ) ) ;
#21458=CARTESIAN_POINT ( 'NONE',  ( -35.04582288351658548, -0.006479247284611515389, -0.01092946910274314974 ) ) ;
#21459=ORIENTED_EDGE ( 'NONE', *, *, #49992, .T. ) ;
#21460=CARTESIAN_POINT ( 'NONE',  ( -27.08421723179412410, 0.5069555058557477789, 2.234476190936493190 ) ) ;
#21463=CARTESIAN_POINT ( 'NONE',  ( 2.000000000000001776, 6.664893814313725962, 3.439359016433505278 ) ) ;
#21465=AXIS2_PLACEMENT_3D ( 'NONE', #59267, #54284, #8723 ) ;
#21468=FACE_OUTER_BOUND ( 'NONE', #34234, .T. ) ;
#21471=CARTESIAN_POINT ( 'NONE',  ( -27.35552965826137140, -2.548625910254533888, -1.773915698030580357 ) ) ;
#21473=CIRCLE ( 'NONE', #15096, 2.899999999999995026 ) ;
#21492=DIRECTION ( 'NONE',  ( -1.000000000000000000, 0.000000000000000000, 0.000000000000000000 ) ) ;
#21494=CARTESIAN_POINT ( 'NONE',  ( 2.000000000000001776, -0.08317740279935835479, 7.499538753794344537 ) ) ;
#21499=ORIENTED_EDGE ( 'NONE', *, *, #11622, .F. ) ;
#21500=AXIS2_PLACEMENT_3D ( 'NONE', #12634, #62860, #27606 ) ;
#21502=CYLINDRICAL_SURFACE ( 'NONE', #62337, 2.899999999999994582 ) ;
#21511=CARTESIAN_POINT ( 'NONE',  ( -22.27719443589224113, -1.139586749255966147, 3.500848524682618645 ) ) ;
#21517=CARTESIAN_POINT ( 'NONE',  ( -22.38932658256919339, 3.361598243548654441, -2.201197575855948330 ) ) ;
#21522=CIRCLE ( 'NONE', #52333, 2.899999999999995470 ) ;
#21523=CARTESIAN_POINT ( 'NONE',  ( 2.000000000000001776, -0.2704997240205401221, 6.931223712253438585 ) ) ;
#21524=CARTESIAN_POINT ( 'NONE',  ( -28.67667724226168602, -0.5419187306520707459, -1.812862320140639749 ) ) ;
#21532=CARTESIAN_POINT ( 'NONE',  ( -22.70624764888619751, 4.501516772829880608, 2.702761586319117892 ) ) ;
#21537=VERTEX_POINT ( 'NONE', #10428 ) ;
#21541=EDGE_CURVE ( 'NONE', #25715, #9803, #21668, .T. ) ;
#21549=CARTESIAN_POINT ( 'NONE',  ( 0.000000000000000000, -4.976357229393876480, 4.652926418895529714 ) ) ;
#21558=CARTESIAN_POINT ( 'NONE',  ( -27.10719052120871098, 1.622102031466687189, -1.714424047991080613 ) ) ;
#21562=ORIENTED_EDGE ( 'NONE', *, *, #28431, .F. ) ;
#21567=AXIS2_PLACEMENT_3D ( 'NONE', #22423, #42689, #21454 ) ;
#21570=DIRECTION ( 'NONE',  ( 0.000000000000000000, 0.000000000000000000, 1.000000000000000000 ) ) ;
#21576=ORIENTED_EDGE ( 'NONE', *, *, #23195, .T. ) ;
#21592=CYLINDRICAL_SURFACE ( 'NONE', #41790, 2.899999999999994582 ) ;
#21593=CARTESIAN_POINT ( 'NONE',  ( -22.46225619532222950, 1.978788174090817309, -3.746472695305357981 ) ) ;
#21602=VERTEX_POINT ( 'NONE', #7402 ) ;
#21604=CARTESIAN_POINT ( 'NONE',  ( -22.27718150314433387, -2.721613812022967593, 2.479231311682832395 ) ) ;
#21616=CIRCLE ( 'NONE', #6708, 2.899999999999994582 ) ;
#21618=LINE ( 'NONE', #41883, #42722 ) ;
#21619=CYLINDRICAL_SURFACE ( 'NONE', #8405, 7.499999999999988454 ) ;
#21626=DIRECTION ( 'NONE',  ( 0.000000000000000000, 0.000000000000000000, -1.000000000000000000 ) ) ;
#21628=ORIENTED_EDGE ( 'NONE', *, *, #32180, .T. ) ;
#21631=CIRCLE ( 'NONE', #58811, 7.499999999999988454 ) ;
#21633=CARTESIAN_POINT ( 'NONE',  ( -27.08850691366480135, -0.6228349286848144928, -2.218359546717751041 ) ) ;
#21635=CARTESIAN_POINT ( 'NONE',  ( -27.10719052120871098, 1.962717903527675611, -1.310802520592017295 ) ) ;
#21639=DIRECTION ( 'NONE',  ( -1.000000000000000000, 0.000000000000000000, 0.000000000000000000 ) ) ;
#21649=AXIS2_PLACEMENT_3D ( 'NONE', #19675, #34918, #10011 ) ;
#21654=ADVANCED_FACE ( 'NONE', ( #22373 ), #17737, .T. ) ;
#21655=ORIENTED_EDGE ( 'NONE', *, *, #455, .T. ) ;
#21663=VERTEX_POINT ( 'NONE', #3108 ) ;
#21668=CIRCLE ( 'NONE', #58859, 2.899999999999995026 ) ;
#21681=CARTESIAN_POINT ( 'NONE',  ( 2.000000000000001776, 0.000000000000000000, 0.000000000000000000 ) ) ;
#21690=ORIENTED_EDGE ( 'NONE', *, *, #27468, .F. ) ;
#21705=ADVANCED_FACE ( 'NONE', ( #37682 ), #2791, .T. ) ;
#21717=AXIS2_PLACEMENT_3D ( 'NONE', #11466, #1526, #42051 ) ;
#21727=LINE ( 'NONE', #61947, #60896 ) ;
#21747=B_SPLINE_CURVE_WITH_KNOTS ( 'NONE', 3,
 ( #5181, #50417, #61036, #56032, #194, #30436 ),
 .UNSPECIFIED., .F., .F.,
 ( 4, 2, 4 ),
 ( 0.0001654224980408314249, 0.0006219428995476478528, 0.001078463301054464335 ),
 .UNSPECIFIED. ) ;
#21753=AXIS2_PLACEMENT_3D ( 'NONE', #52041, #51722, #43031 ) ;
#21756=CARTESIAN_POINT ( 'NONE',  ( 0.000000000000000000, -1.956810415765224187, 6.654767106875530303 ) ) ;
#21761=CIRCLE ( 'NONE', #14329, 2.899999999999995026 ) ;
#21765=CARTESIAN_POINT ( 'NONE',  ( 2.000000000000001776, 5.769711778877384845, -4.791703871138491166 ) ) ;
#21768=ORIENTED_EDGE ( 'NONE', *, *, #29050, .T. ) ;
#21773=ORIENTED_EDGE ( 'NONE', *, *, #27620, .T. ) ;
#21776=ORIENTED_EDGE ( 'NONE', *, *, #20806, .T. ) ;
#21780=ADVANCED_FACE ( 'NONE', ( #16910 ), #21910, .T. ) ;
#21786=DIRECTION ( 'NONE',  ( 0.000000000000000000, 0.8835120444460240474, -0.4684084406997878758 ) ) ;
#21789=DIRECTION ( 'NONE',  ( -1.000000000000000000, 0.000000000000000000, 0.000000000000000000 ) ) ;
#21802=CARTESIAN_POINT ( 'NONE',  ( -27.08416974970326763, 0.4041872645907068629, 2.255186831366090772 ) ) ;
#21817=CARTESIAN_POINT ( 'NONE',  ( 0.000000000000000000, -6.606214214351039615, -2.114938770769998477 ) ) ;
#21828=CARTESIAN_POINT ( 'NONE',  ( -27.35552965826137140, -3.094132632038958608, -0.2619431035392160156 ) ) ;
#21829=CARTESIAN_POINT ( 'NONE',  ( -10.00000000000000178, 0.000000000000000000, 0.000000000000000000 ) ) ;
#21830=CARTESIAN_POINT ( 'NONE',  ( 2.000000000000001776, 0.000000000000000000, 0.000000000000000000 ) ) ;
#21833=EDGE_LOOP ( 'NONE', ( #7746, #24938, #25253, #54471 ) ) ;
#21834=VERTEX_POINT ( 'NONE', #57827 ) ;
#21838=CARTESIAN_POINT ( 'NONE',  ( 0.000000000000000000, 0.000000000000000000, 0.000000000000000000 ) ) ;
#21842=EDGE_CURVE ( 'NONE', #13989, #61330, #37602, .T. ) ;
#21843=AXIS2_PLACEMENT_3D ( 'NONE', #49454, #13200, #39772 ) ;
#21844=DIRECTION ( 'NONE',  ( -1.000000000000000000, 0.000000000000000000, 0.000000000000000000 ) ) ;
#21851=CARTESIAN_POINT ( 'NONE',  ( 2.000000000000001776, -1.754183803416586196, 6.711026108862235162 ) ) ;
#21853=AXIS2_PLACEMENT_3D ( 'NONE', #49251, #4004, #13957 ) ;
#21863=CARTESIAN_POINT ( 'NONE',  ( -22.30625920655495165, 2.750410778797888867, 2.610366806364660341 ) ) ;
#21870=ORIENTED_EDGE ( 'NONE', *, *, #35415, .F. ) ;
#21872=ORIENTED_EDGE ( 'NONE', *, *, #11135, .T. ) ;
#21883=AXIS2_PLACEMENT_3D ( 'NONE', #65563, #45620, #51298 ) ;
#21891=CARTESIAN_POINT ( 'NONE',  ( 0.000000000000000000, 0.000000000000000000, 0.000000000000000000 ) ) ;
#21894=CIRCLE ( 'NONE', #14414, 2.899999999999995470 ) ;
#21906=CARTESIAN_POINT ( 'NONE',  ( 2.000000000000001776, 5.814643797626930954, 3.550179297009575574 ) ) ;
#21907=ORIENTED_EDGE ( 'NONE', *, *, #17762, .T. ) ;
#21909=ORIENTED_EDGE ( 'NONE', *, *, #49416, .F. ) ;
#21910=CYLINDRICAL_SURFACE ( 'NONE', #32271, 2.899999999999994582 ) ;
#21913=VERTEX_POINT ( 'NONE', #59133 ) ;
#21918=VERTEX_POINT ( 'NONE', #12902 ) ;
#21921=EDGE_CURVE ( 'NONE', #20840, #18772, #15023, .T. ) ;
#21923=EDGE_LOOP ( 'NONE', ( #60312, #55174, #27426, #36836 ) ) ;
#21931=EDGE_LOOP ( 'NONE', ( #64519, #41363, #21870, #5337 ) ) ;
#21932=CIRCLE ( 'NONE', #59100, 2.899999999999995026 ) ;
#21935=ORIENTED_EDGE ( 'NONE', *, *, #14250, .F. ) ;
#21937=CARTESIAN_POINT ( 'NONE',  ( -22.27719412087655471, 2.887588494201237310, -2.283949229175413098 ) ) ;
#21947=VERTEX_POINT ( 'NONE', #58471 ) ;
#21951=CARTESIAN_POINT ( 'NONE',  ( -27.09342121492584710, -0.6436068655225301027, -2.227768580955221012 ) ) ;
#21961=DIRECTION ( 'NONE',  ( 1.000000000000000000, 0.000000000000000000, 0.000000000000000000 ) ) ;
#21964=AXIS2_PLACEMENT_3D ( 'NONE', #7676, #3361, #58559 ) ;
#21973=VERTEX_POINT ( 'NONE', #8564 ) ;
#21979=CARTESIAN_POINT ( 'NONE',  ( 2.000000000000001776, 6.777474576704075382, -0.6925993764990371337 ) ) ;
#21986=DIRECTION ( 'NONE',  ( -1.000000000000000000, 0.000000000000000000, 0.000000000000000000 ) ) ;
#22001=AXIS2_PLACEMENT_3D ( 'NONE', #34664, #55637, #49662 ) ;
#22010=VERTEX_POINT ( 'NONE', #62025 ) ;
#22014=VERTEX_POINT ( 'NONE', #57704 ) ;
#22017=CARTESIAN_POINT ( 'NONE',  ( 2.000000000000001776, -2.664846396702537312, 6.404188155572974495 ) ) ;
#22020=DIRECTION ( 'NONE',  ( 0.000000000000000000, 0.000000000000000000, 1.000000000000000000 ) ) ;
#22038=LINE ( 'NONE', #37328, #17282 ) ;
#22039=ORIENTED_EDGE ( 'NONE', *, *, #60621, .F. ) ;
#22040=CARTESIAN_POINT ( 'NONE',  ( -22.30625920655495165, -1.672644928563074451, 3.403091720605004866 ) ) ;
#22042=EDGE_CURVE ( 'NONE', #63998, #15877, #16575, .T. ) ;
#22053=CARTESIAN_POINT ( 'NONE',  ( 2.000000000000001776, 4.915517050588409376, 4.717154614762108622 ) ) ;
#22054=FACE_OUTER_BOUND ( 'NONE', #7721, .T. ) ;
#22059=ORIENTED_EDGE ( 'NONE', *, *, #60555, .T. ) ;
#22075=VERTEX_POINT ( 'NONE', #22431 ) ;
#22077=ADVANCED_FACE ( 'NONE', ( #57041 ), #1181, .T. ) ;
#22078=VERTEX_POINT ( 'NONE', #58026 ) ;
#22080=DIRECTION ( 'NONE',  ( -0.9606638835031803270, 0.06908842350339206018, 0.2689826995745341343 ) ) ;
#22084=CARTESIAN_POINT ( 'NONE',  ( 2.000000000000001776, 0.000000000000000000, 0.000000000000000000 ) ) ;
#22088=CARTESIAN_POINT ( 'NONE',  ( -22.27711351828769892, -0.8770428151440446962, -3.575417021793779515 ) ) ;
#22090=AXIS2_PLACEMENT_3D ( 'NONE', #58414, #38447, #37461 ) ;
#22094=AXIS2_PLACEMENT_3D ( 'NONE', #3802, #7781, #29361 ) ;
#22096=AXIS2_PLACEMENT_3D ( 'NONE', #22084, #42342, #62316 ) ;
#22101=DIRECTION ( 'NONE',  ( -1.000000000000000000, 0.000000000000000000, 0.000000000000000000 ) ) ;
#22102=VERTEX_POINT ( 'NONE', #47501 ) ;
#22103=CARTESIAN_POINT ( 'NONE',  ( -27.08423805673873375, 0.5302040644010427295, 2.229265646063304018 ) ) ;
#22110=ORIENTED_EDGE ( 'NONE', *, *, #16641, .F. ) ;
#22120=CARTESIAN_POINT ( 'NONE',  ( 0.000000000000000000, 5.997115278587632936, 3.485633455389514523 ) ) ;
#22123=CIRCLE ( 'NONE', #30609, 7.499999999999988454 ) ;
#22132=( BOUNDED_SURFACE ( )  B_SPLINE_SURFACE ( 3, 1, ( 
 ( #3278, #7942 ),
 ( #53498, #24191 ),
 ( #8251, #35781 ),
 ( #55771, #61390 ) ),
 .UNSPECIFIED., .F., .F., .F. ) 
 B_SPLINE_SURFACE_WITH_KNOTS ( ( 4, 4 ),
 ( 2, 2 ),
 ( 0.000000000000000000, 1.000000000000000000 ),
 ( 0.000000000000000000, 1.000000000000000000 ),
 .UNSPECIFIED. ) 
 GEOMETRIC_REPRESENTATION_ITEM ( )  RATIONAL_B_SPLINE_SURFACE ( (
 ( 1.000000000000000000, 1.000000000000000000),
 ( 0.9932032654565553509, 0.8386279382598740284),
 ( 0.9932032654565553509, 0.8386279382598740284),
 ( 1.000000000000000000, 1.000000000000000000) ) ) 
 REPRESENTATION_ITEM ( '' )  SURFACE ( )  );
#22133=DIRECTION ( 'NONE',  ( -1.000000000000000000, 0.000000000000000000, 0.000000000000000000 ) ) ;
#22146=CARTESIAN_POINT ( 'NONE',  ( -27.08426571771018487, 0.9198084705429482311, -2.098821047392056549 ) ) ;
#22154=CARTESIAN_POINT ( 'NONE',  ( 2.000000000000001776, 3.230174184210159893, -5.998318953995314118 ) ) ;
#22162=EDGE_CURVE ( 'NONE', #29549, #40046, #57805, .T. ) ;
#22175=CARTESIAN_POINT ( 'NONE',  ( -27.08579483061202708, 0.2015567301747612228, 2.287150433979697528 ) ) ;
#22183=ORIENTED_EDGE ( 'NONE', *, *, #14390, .F. ) ;
#22189=CARTESIAN_POINT ( 'NONE',  ( 0.000000000000000000, 6.883677378339475794, 0.8544109087186002593 ) ) ;
#22195=CARTESIAN_POINT ( 'NONE',  ( -35.04643116707788408, -0.01156612771643569793, -0.003844232202723438241 ) ) ;
#22200=DIRECTION ( 'NONE',  ( 0.000000000000000000, 0.1764146379942750364, 0.9843159429275484262 ) ) ;
#22202=ORIENTED_EDGE ( 'NONE', *, *, #4217, .T. ) ;
#22203=ORIENTED_EDGE ( 'NONE', *, *, #21347, .T. ) ;
#22204=ORIENTED_EDGE ( 'NONE', *, *, #53553, .T. ) ;
#22206=CARTESIAN_POINT ( 'NONE',  ( -22.27834755396594346, 3.434702243602638205, 1.338300169228680003 ) ) ;
#22208=DIRECTION ( 'NONE',  ( -1.000000000000000000, 0.000000000000000000, 0.000000000000000000 ) ) ;
#22225=CIRCLE ( 'NONE', #10536, 2.899999999999996803 ) ;
#22229=CARTESIAN_POINT ( 'NONE',  ( 0.000000000000000000, 0.08317740279931498670, 7.499538753794337431 ) ) ;
#22230=VERTEX_POINT ( 'NONE', #65061 ) ;
#22234=EDGE_LOOP ( 'NONE', ( #48998, #4158, #7796, #46896, #42266, #3532, #62419, #60872, #8308, #41330, #23198, #16091, #13478, #63003, #56055, #9018, #57189, #20834, #13446, #54650, #32030, #59606, #65526, #27816, #14108, #13671, #45142, #53374, #40057, #45363, #16993, #36125, #55153, #45366, #60924, #2226, #51592, #28340, #14821, #28565, #46595, #22059, #27874, #34223, #41008, #14061, #52135, #17158, #20888, #43231, #17144, #16529, #59209, #57243, #14465, #56479, #14317, #40834, #60989, #2358, #20913, #14478, #39348, #22203, #21249, #39234, #45015, #63845, #20181, #28827, #19131, #33835, #46792, #18014, #13064, #44013, #49887, #33977, #41359, #17779, #36718, #56453, #16421, #42167, #50137, #37921, #43053, #40605, #29819, #24945, #47945, #28476, #1676, #58144, #17852, #2619, #42979, #52219, #50250, #55135, #24862, #57472, #50195, #7947, #65616, #15730, #52335, #35292, #25648, #65270, #61019, #7503, #55525, #2131, #62274, #847, #28419, #63288, #61476, #20639, #18665, #48481, #17311, #34800, #23993, #3062, #63679, #13452, #35162, #12559, #52784, #5659, #55332, #58432, #49429, #26622, #44206, #55917, #5287, #56775, #43104, #28705, #55985, #48643, #55884, #63126, #15425, #51239, #29327, #3737, #8453, #26790, #64561, #44886, #27079, #35226, #14722, #38543, #31497, #52331, #42141, #15450, #37340, #29401, #37905, #61813, #39406, #11843, #14456, #26560, #59442, #29321, #56860, #18579, #1180, #7258, #33531, #12642, #52215, #36499, #18333, #11120, #58600, #42521, #49869, #15287, #59514, #5219, #59933, #22039, #36713, #31832, #65301, #55872, #1195, #41869, #23976, #52320, #7671, #12175, #2737, #14385, #52884, #47558, #22721, #65803, #49582, #13276, #57821, #23880, #4512, #12189, #62858, #53243, #38892, #49900, #54922, #5984, #39327, #20259, #3759, #4834, #27601, #41200, #39757, #24484, #15562, #54440, #27959, #10381, #49320, #29187, #16525, #40459, #31298, #63608, #4937 ) ) ;
#22243=CARTESIAN_POINT ( 'NONE',  ( -27.32343372485685862, 1.625341394141133655, -2.534722478175129190 ) ) ;
#22251=DIRECTION ( 'NONE',  ( 1.000000000000000000, 0.000000000000000000, 0.000000000000000000 ) ) ;
#22261=CARTESIAN_POINT ( 'NONE',  ( -27.08429572838383947, -0.5764601019425836803, -2.217805374070540125 ) ) ;
#22264=LINE ( 'NONE', #17631, #54739 ) ;
#22271=FACE_OUTER_BOUND ( 'NONE', #64211, .T. ) ;
#22277=ORIENTED_EDGE ( 'NONE', *, *, #33206, .T. ) ;
#22278=ORIENTED_EDGE ( 'NONE', *, *, #41891, .F. ) ;
#22284=VERTEX_POINT ( 'NONE', #21494 ) ;
#22300=ORIENTED_EDGE ( 'NONE', *, *, #37222, .F. ) ;
#22315=DIRECTION ( 'NONE',  ( 0.000000000000000000, 0.000000000000000000, 1.000000000000000000 ) ) ;
#22318=CYLINDRICAL_SURFACE ( 'NONE', #21163, 2.899999999999994582 ) ;
#22326=ORIENTED_EDGE ( 'NONE', *, *, #8923, .F. ) ;
#22328=CARTESIAN_POINT ( 'NONE',  ( -27.08421860617808008, 2.116856729767824685, 0.8768262158915500759 ) ) ;
#22330=CIRCLE ( 'NONE', #40408, 2.899999999999996358 ) ;
#22334=B_SPLINE_CURVE_WITH_KNOTS ( 'NONE', 3,
 ( #45418, #54446, #19522, #44123, #34769, #50105, #40426, #10176 ),
 .UNSPECIFIED., .F., .F.,
 ( 4, 2, 2, 4 ),
 ( 0.000000000000000000, 0.0003639104015149874404, 0.0007278208030299748808, 0.001455641606059947593 ),
 .UNSPECIFIED. ) ;
#22337=STYLED_ITEM ( 'NONE', ( #43769 ), #6945 ) ;
#22344=CARTESIAN_POINT ( 'NONE',  ( 2.000000000000001776, 1.754183803416655474, -6.711026108862266248 ) ) ;
#22351=VERTEX_POINT ( 'NONE', #6204 ) ;
#22353=DIRECTION ( 'NONE',  ( -1.000000000000000000, 0.000000000000000000, 0.000000000000000000 ) ) ;
#22357=CARTESIAN_POINT ( 'NONE',  ( -22.28350523959500862, 3.687952016964566759, -0.3047406164877188850 ) ) ;
#22360=EDGE_LOOP ( 'NONE', ( #29297, #40058, #45678, #17475 ) ) ;
#22368=CARTESIAN_POINT ( 'NONE',  ( -27.08416813689867908, -1.759517419957075113, 1.467601568343269491 ) ) ;
#22369=VERTEX_POINT ( 'NONE', #51762 ) ;
#22373=FACE_OUTER_BOUND ( 'NONE', #776, .T. ) ;
#22379=CARTESIAN_POINT ( 'NONE',  ( -27.05874794189610455, 1.734723475976807094E-15, -8.673617379884035472E-15 ) ) ;
#22381=ORIENTED_EDGE ( 'NONE', *, *, #60536, .T. ) ;
#22392=AXIS2_PLACEMENT_3D ( 'NONE', #14553, #23925, #39186 ) ;
#22393=CARTESIAN_POINT ( 'NONE',  ( 1.000000000000000888, 3.073484823194335025, 6.841322316745041654 ) ) ;
#22406=CARTESIAN_POINT ( 'NONE',  ( -22.29770266787582500, 1.047554374660461418, 3.593535545924332109 ) ) ;
#22407=DIRECTION ( 'NONE',  ( -1.000000000000000000, 0.000000000000000000, 0.000000000000000000 ) ) ;
#22408=AXIS2_PLACEMENT_3D ( 'NONE', #55612, #21238, #6948 ) ;
#22412=DIRECTION ( 'NONE',  ( -1.000000000000000000, 0.000000000000000000, 0.000000000000000000 ) ) ;
#22414=ORIENTED_EDGE ( 'NONE', *, *, #16980, .T. ) ;
#22419=B_SPLINE_CURVE_WITH_KNOTS ( 'NONE', 3,
 ( #64243, #18718, #8389, #38973, #32336, #52649, #7074, #27347, #29008, #40, #64551, #49315, #30311, #59268, #8724, #39952, #13690, #54285, #9043, #65531, #44944, #59926 ),
 .UNSPECIFIED., .F., .F.,
 ( 4, 3, 3, 3, 3, 3, 3, 4 ),
 ( 6.732537572691704696E-18, 6.990956068646403821E-05, 0.0001398191187764042775, 0.0002097286751720212191, 0.0002796382307041356675, 0.0003495477861619808576, 0.0004194573423310286289, 0.0005586102576333144961 ),
 .UNSPECIFIED. ) ;
#22420=CARTESIAN_POINT ( 'NONE',  ( -35.04643116707788408, 0.003844232202716499347, -0.01156612771644957571 ) ) ;
#22423=CARTESIAN_POINT ( 'NONE',  ( 0.000000000000000000, 0.000000000000000000, 0.000000000000000000 ) ) ;
#22424=CIRCLE ( 'NONE', #57475, 7.499999999999988454 ) ;
#22431=CARTESIAN_POINT ( 'NONE',  ( 2.000000000000001776, 2.469490258309515518, -6.482025155313297482 ) ) ;
#22439=DIRECTION ( 'NONE',  ( 0.000000000000000000, 0.9868265225415265851, -0.1617819965527618475 ) ) ;
#22446=CARTESIAN_POINT ( 'NONE',  ( -35.04834644901396956, 0.01383120537647295270, -0.0002835132723611888264 ) ) ;
#22448=CARTESIAN_POINT ( 'NONE',  ( 1.000000000000000888, 5.097042323172538580, -5.501832381651401427 ) ) ;
#22450=ORIENTED_EDGE ( 'NONE', *, *, #10956, .T. ) ;
#22457=LINE ( 'NONE', #7156, #63696 ) ;
#22463=CARTESIAN_POINT ( 'NONE',  ( 0.000000000000000000, 3.152010634611773110, -6.039758645301250617 ) ) ;
#22464=DIRECTION ( 'NONE',  ( -1.000000000000000000, 0.000000000000000000, 0.000000000000000000 ) ) ;
#22469=DIRECTION ( 'NONE',  ( -1.000000000000000000, 0.000000000000000000, 0.000000000000000000 ) ) ;
#22478=DIRECTION ( 'NONE',  ( 0.000000000000000000, 0.000000000000000000, 1.000000000000000000 ) ) ;
#22482=CARTESIAN_POINT ( 'NONE',  ( -27.08419797710328680, 0.8552720754637080924, -2.125717714519615331 ) ) ;
#22489=CYLINDRICAL_SURFACE ( 'NONE', #15197, 7.499999999999988454 ) ;
#22492=CYLINDRICAL_SURFACE ( 'NONE', #43365, 6.936499999999988120 ) ;
#22493=CARTESIAN_POINT ( 'NONE',  ( 2.000000000000001776, -6.777474576704058506, 0.6925993764990423518 ) ) ;
#22494=DIRECTION ( 'NONE',  ( -1.000000000000000000, 0.000000000000000000, 0.000000000000000000 ) ) ;
#22502=AXIS2_PLACEMENT_3D ( 'NONE', #17044, #47975, #63565 ) ;
#22503=B_SPLINE_CURVE_WITH_KNOTS ( 'NONE', 3,
 ( #39245, #17678, #64510, #38255, #13003, #27627, #43574, #47930, #18341, #37939, #13645, #58232, #3048, #33287, #48926, #28957, #3381, #12652, #32935, #59223, #18677, #58920 ),
 .UNSPECIFIED., .F., .F.,
 ( 4, 3, 3, 3, 3, 3, 3, 4 ),
 ( 0.000000000000000000, 4.455945684386718414E-05, 6.636307477203950002E-05, 8.816671873158800788E-05, 0.0001099660380492623735, 0.0001317545563165321062, 0.0001762613022895059660, 0.0001867992666138413812 ),
 .UNSPECIFIED. ) ;
#22505=ORIENTED_EDGE ( 'NONE', *, *, #44469, .F. ) ;
#22510=CARTESIAN_POINT ( 'NONE',  ( -35.04834644901396956, 0.006670072992069154237, -0.01211993185718438990 ) ) ;
#22513=LINE ( 'NONE', #23491, #27668 ) ;
#22521=DIRECTION ( 'NONE',  ( 0.000000000000000000, 0.000000000000000000, -1.000000000000000000 ) ) ;
#22522=CYLINDRICAL_SURFACE ( 'NONE', #45069, 2.899999999999994582 ) ;
#22526=ADVANCED_FACE ( 'NONE', ( #44061 ), #63662, .T. ) ;
#22529=CARTESIAN_POINT ( 'NONE',  ( -22.30398854582848145, -2.594196582746997493, 2.724439933030915473 ) ) ;
#22534=AXIS2_PLACEMENT_3D ( 'NONE', #44086, #49100, #54410 ) ;
#22552=EDGE_CURVE ( 'NONE', #16346, #2801, #53619, .T. ) ;
#22554=CARTESIAN_POINT ( 'NONE',  ( -27.08426571771018487, -2.277536580310468128, 0.2528330215897273692 ) ) ;
#22564=CARTESIAN_POINT ( 'NONE',  ( 0.000000000000000000, 0.4804830611970945520, -6.919838746524566986 ) ) ;
#22565=ORIENTED_EDGE ( 'NONE', *, *, #58482, .F. ) ;
#22569=CARTESIAN_POINT ( 'NONE',  ( -22.28482751661422867, -1.587261331312489032, 3.347211412506312822 ) ) ;
#22582=VERTEX_POINT ( 'NONE', #54039 ) ;
#22589=DIRECTION ( 'NONE',  ( -1.000000000000000000, 0.000000000000000000, 0.000000000000000000 ) ) ;
#22593=CARTESIAN_POINT ( 'NONE',  ( -22.27720412283625961, 2.752887114864236207, -2.444672752438185270 ) ) ;
#22595=AXIS2_PLACEMENT_3D ( 'NONE', #3165, #33069, #43046 ) ;
#22599=ADVANCED_FACE ( 'NONE', ( #54383 ), #16696, .F. ) ;
#22603=VECTOR ( 'NONE', #25728, 1000.000000000000000 ) ;
#22610=DIRECTION ( 'NONE',  ( -1.000000000000000000, 0.000000000000000000, 0.000000000000000000 ) ) ;
#22626=EDGE_CURVE ( 'NONE', #27004, #7169, #51536, .T. ) ;
#22630=VERTEX_POINT ( 'NONE', #45044 ) ;
#22636=CARTESIAN_POINT ( 'NONE',  ( -22.31328051695926007, -2.109671368890623455, -3.148362328073181615 ) ) ;
#22637=ORIENTED_EDGE ( 'NONE', *, *, #29417, .F. ) ;
#22652=CARTESIAN_POINT ( 'NONE',  ( 2.000000000000001776, 0.000000000000000000, 0.000000000000000000 ) ) ;
#22660=ORIENTED_EDGE ( 'NONE', *, *, #53545, .T. ) ;
#22665=FACE_OUTER_BOUND ( 'NONE', #34212, .T. ) ;
#22667=DIRECTION ( 'NONE',  ( 0.000000000000000000, -0.6876994588534296460, 0.7259954919231248471 ) ) ;
#22678=EDGE_LOOP ( 'NONE', ( #19791, #10787, #31536, #5723 ) ) ;
#22684=VECTOR ( 'NONE', #14691, 1000.000000000000000 ) ;
#22694=AXIS2_PLACEMENT_3D ( 'NONE', #23090, #2834, #18103 ) ;
#22702=DIRECTION ( 'NONE',  ( 0.000000000000000000, 0.6876994588534245390, -0.7259954919231297321 ) ) ;
#22704=CARTESIAN_POINT ( 'NONE',  ( -22.28856623400852044, -2.668530796663827420, -2.585606290939622021 ) ) ;
#22705=AXIS2_PLACEMENT_3D ( 'NONE', #43039, #17783, #38045 ) ;
#22708=VERTEX_POINT ( 'NONE', #61309 ) ;
#22709=CARTESIAN_POINT ( 'NONE',  ( -24.42101984568203932, 1.824625598916893798, 3.884389025764499515 ) ) ;
#22714=CARTESIAN_POINT ( 'NONE',  ( -22.39032720737627713, 2.936932155721193816, 2.746561316202127401 ) ) ;
#22719=DIRECTION ( 'NONE',  ( 0.000000000000000000, 0.000000000000000000, 1.000000000000000000 ) ) ;
#22721=ORIENTED_EDGE ( 'NONE', *, *, #37533, .T. ) ;
#22725=CARTESIAN_POINT ( 'NONE',  ( -10.00000000000000178, 0.000000000000000000, 0.000000000000000000 ) ) ;
#22728=CYLINDRICAL_SURFACE ( 'NONE', #25843, 2.899999999999994582 ) ;
#22740=VECTOR ( 'NONE', #50633, 1000.000000000000000 ) ;
#22744=DIRECTION ( 'NONE',  ( -1.000000000000000000, 0.000000000000000000, 0.000000000000000000 ) ) ;
#22749=CARTESIAN_POINT ( 'NONE',  ( -22.28856623400852044, -3.603818606161813598, -0.9049353338066584707 ) ) ;
#22754=LINE ( 'NONE', #62306, #15711 ) ;
#22760=CARTESIAN_POINT ( 'NONE',  ( -22.28629837673888048, 3.348758206500249468, 1.594277649056495827 ) ) ;
#22761=CARTESIAN_POINT ( 'NONE',  ( -27.28573687977896967, 2.702109387930250239, -1.043905432732882277 ) ) ;
#22762=CARTESIAN_POINT ( 'NONE',  ( -22.31213670151049300, 2.108126385153810567, 3.145266995071653859 ) ) ;
#22766=EDGE_CURVE ( 'NONE', #65266, #59, #55783, .T. ) ;
#22769=CIRCLE ( 'NONE', #27025, 7.499999999999988454 ) ;
#22776=AXIS2_PLACEMENT_3D ( 'NONE', #45316, #29367, #19407 ) ;
#22782=AXIS2_PLACEMENT_3D ( 'NONE', #22725, #7085, #42987 ) ;
#22784=CARTESIAN_POINT ( 'NONE',  ( -22.27834755396594346, -0.7418417409069250068, -3.610802913011852411 ) ) ;
#22786=CARTESIAN_POINT ( 'NONE',  ( 0.000000000000000000, -6.997684042076912192, 2.698595569414189210 ) ) ;
#22788=DIRECTION ( 'NONE',  ( -1.000000000000000000, 0.000000000000000000, 0.000000000000000000 ) ) ;
#22792=DIRECTION ( 'NONE',  ( 0.000000000000000000, 0.000000000000000000, 1.000000000000000000 ) ) ;
#22793=CARTESIAN_POINT ( 'NONE',  ( 2.000000000000001776, 0.000000000000000000, 0.000000000000000000 ) ) ;
#22794=ORIENTED_EDGE ( 'NONE', *, *, #13501, .F. ) ;
#22795=CYLINDRICAL_SURFACE ( 'NONE', #6414, 7.499999999999988454 ) ;
#22798=VERTEX_POINT ( 'NONE', #52004 ) ;
#22801=EDGE_CURVE ( 'NONE', #30460, #22630, #3750, .T. ) ;
#22802=CARTESIAN_POINT ( 'NONE',  ( 2.000000000000001776, -1.865193240757140991, 6.552473556515165498 ) ) ;
#22806=FACE_OUTER_BOUND ( 'NONE', #23075, .T. ) ;
#22811=EDGE_LOOP ( 'NONE', ( #13020, #16264, #23672, #30713 ) ) ;
#22815=VERTEX_POINT ( 'NONE', #21756 ) ;
#22820=DIRECTION ( 'NONE',  ( -1.000000000000000000, 0.000000000000000000, 0.000000000000000000 ) ) ;
#22821=EDGE_CURVE ( 'NONE', #4778, #11936, #62286, .T. ) ;
#22824=VERTEX_POINT ( 'NONE', #1477 ) ;
#22825=CARTESIAN_POINT ( 'NONE',  ( -22.27720387087365239, 0.5572161790460056219, 3.639274226782802657 ) ) ;
#22832=EDGE_CURVE ( 'NONE', #13076, #51860, #20457, .T. ) ;
#22834=DIRECTION ( 'NONE',  ( -1.000000000000000000, 0.000000000000000000, 0.000000000000000000 ) ) ;
#22837=CARTESIAN_POINT ( 'NONE',  ( -22.27786964138239867, 3.004507515156379593, -2.131221155130656353 ) ) ;
#22845=ADVANCED_FACE ( 'NONE', ( #46676 ), #1131, .T. ) ;
#22853=ORIENTED_EDGE ( 'NONE', *, *, #47994, .F. ) ;
#22855=CARTESIAN_POINT ( 'NONE',  ( -27.09861164373156583, 0.1603819633258403432, 2.328930759213672541 ) ) ;
#22857=VERTEX_POINT ( 'NONE', #2797 ) ;
#22869=CARTESIAN_POINT ( 'NONE',  ( -27.08416974970326407, -0.4151546250413312156, -2.253221199357866134 ) ) ;
#22872=DIRECTION ( 'NONE',  ( -1.000000000000000000, 0.000000000000000000, 0.000000000000000000 ) ) ;
#22882=ORIENTED_EDGE ( 'NONE', *, *, #50969, .T. ) ;
#22888=DIRECTION ( 'NONE',  ( -1.000000000000000000, 0.000000000000000000, 0.000000000000000000 ) ) ;
#22899=CARTESIAN_POINT ( 'NONE',  ( -22.27719381268171617, 2.618044180756139205, -2.588413841766857182 ) ) ;
#22909=CARTESIAN_POINT ( 'NONE',  ( 2.000000000000001776, -7.387287142779332960, -1.295372019972250710 ) ) ;
#22915=CARTESIAN_POINT ( 'NONE',  ( -22.27720387087365239, -2.873095842208885031, 2.302200479844923375 ) ) ;
#22924=DIRECTION ( 'NONE',  ( 0.000000000000000000, 0.1764146379942750642, 0.9843159429275485373 ) ) ;
#22926=DIRECTION ( 'NONE',  ( -1.000000000000000000, 0.000000000000000000, 0.000000000000000000 ) ) ;
#22929=LINE ( 'NONE', #5765, #18931 ) ;
#22932=CARTESIAN_POINT ( 'NONE',  ( -27.08423923533013422, 1.376387618994802997, 1.832018136655343188 ) ) ;
#22936=VERTEX_POINT ( 'NONE', #18065 ) ;
#22939=AXIS2_PLACEMENT_3D ( 'NONE', #56118, #30208, #1271 ) ;
#22942=CARTESIAN_POINT ( 'NONE',  ( 0.000000000000000000, -6.253963800348222968, -4.139799123621093813 ) ) ;
#22957=LINE ( 'NONE', #18296, #62385 ) ;
#22967=CARTESIAN_POINT ( 'NONE',  ( -22.28776923226071105, -2.100802264239985284, -3.061913732988077452 ) ) ;
#22977=CARTESIAN_POINT ( 'NONE',  ( -22.28482751661422867, -0.2989970708918257558, -3.692400780723914089 ) ) ;
#22980=CARTESIAN_POINT ( 'NONE',  ( -27.08416974970326407, -0.3922151116844065921, -2.257332547928110777 ) ) ;
#22982=DIRECTION ( 'NONE',  ( -1.000000000000000000, 0.000000000000000000, 0.000000000000000000 ) ) ;
#23002=FACE_OUTER_BOUND ( 'NONE', #19035, .T. ) ;
#23004=CARTESIAN_POINT ( 'NONE',  ( -22.27384469013076185, 2.581192766446265274, 2.625926801827853208 ) ) ;
#23005=EDGE_CURVE ( 'NONE', #7169, #46362, #30328, .T. ) ;
#23006=ORIENTED_EDGE ( 'NONE', *, *, #24960, .F. ) ;
#23008=CARTESIAN_POINT ( 'NONE',  ( 2.000000000000001776, -0.4804830611970390408, 6.919838746524553663 ) ) ;
#23014=CARTESIAN_POINT ( 'NONE',  ( -27.08416813689867553, 2.150738950797704607, 0.7899859999124249077 ) ) ;
#23024=CARTESIAN_POINT ( 'NONE',  ( 0.000000000000000000, -6.470132594555817462, 2.133363481234057168 ) ) ;
#23028=CARTESIAN_POINT ( 'NONE',  ( -22.28073302975500880, -2.626377654649347804, -2.595086548180010055 ) ) ;
#23031=EDGE_LOOP ( 'NONE', ( #42337, #38622, #17403, #63380 ) ) ;
#23032=CARTESIAN_POINT ( 'NONE',  ( -27.35552965826137140, 1.320216934008397569, 2.810569013793730697 ) ) ;
#23034=VERTEX_POINT ( 'NONE', #4417 ) ;
#23037=CYLINDRICAL_SURFACE ( 'NONE', #49143, 6.936499999999988120 ) ;
#23045=DIRECTION ( 'NONE',  ( -1.000000000000000000, 0.000000000000000000, 0.000000000000000000 ) ) ;
#23046=CARTESIAN_POINT ( 'NONE',  ( -22.27704833740210333, -3.351945466913909932, -1.521679877253181878 ) ) ;
#23050=DIRECTION ( 'NONE',  ( -1.000000000000000000, 0.000000000000000000, 0.000000000000000000 ) ) ;
#23054=DIRECTION ( 'NONE',  ( 0.000000000000000000, 0.000000000000000000, -1.000000000000000000 ) ) ;
#23057=ORIENTED_EDGE ( 'NONE', *, *, #19890, .F. ) ;
#23075=EDGE_LOOP ( 'NONE', ( #7975, #37058, #27594, #55858 ) ) ;
#23077=CARTESIAN_POINT ( 'NONE',  ( 2.000000000000001776, 5.396716205731493687, -4.158041573745044239 ) ) ;
#23078=CARTESIAN_POINT ( 'NONE',  ( -22.29677679919927868, 3.364642266483124811, 1.633785040807670175 ) ) ;
#23079=CARTESIAN_POINT ( 'NONE',  ( -10.00000000000000178, 0.000000000000000000, 0.000000000000000000 ) ) ;
#23080=CARTESIAN_POINT ( 'NONE',  ( -22.28482751661422867, 2.105139449411431052, 3.048214341614463585 ) ) ;
#23081=CARTESIAN_POINT ( 'NONE',  ( 2.000000000000001776, 4.570217215903371155, 5.218059682435623792 ) ) ;
#23083=CARTESIAN_POINT ( 'NONE',  ( 2.000000000000001776, 2.562706407243636075, 6.312399813420339179 ) ) ;
#23087=CARTESIAN_POINT ( 'NONE',  ( -27.08426571771018487, -1.357728109767519564, -1.845988025802334231 ) ) ;
#23090=CARTESIAN_POINT ( 'NONE',  ( 0.000000000000000000, 0.000000000000000000, 0.000000000000000000 ) ) ;
#23094=DIRECTION ( 'NONE',  ( 1.000000000000000000, -0.000000000000000000, -0.000000000000000000 ) ) ;
#23096=CARTESIAN_POINT ( 'NONE',  ( -27.04788180060268843, -1.373100113388784349, -2.923150379392654319 ) ) ;
#23097=VECTOR ( 'NONE', #53080, 1000.000000000000000 ) ;
#23100=DIRECTION ( 'NONE',  ( -1.000000000000000000, 0.000000000000000000, 0.000000000000000000 ) ) ;
#23102=( BOUNDED_SURFACE ( )  B_SPLINE_SURFACE ( 3, 1, ( 
 ( #55577, #64232 ),
 ( #29963, #50268 ),
 ( #28992, #34614 ),
 ( #10017, #60544 ) ),
 .UNSPECIFIED., .F., .F., .F. ) 
 B_SPLINE_SURFACE_WITH_KNOTS ( ( 4, 4 ),
 ( 2, 2 ),
 ( 0.000000000000000000, 1.000000000000000000 ),
 ( 0.000000000000000000, 1.000000000000000000 ),
 .UNSPECIFIED. ) 
 GEOMETRIC_REPRESENTATION_ITEM ( )  RATIONAL_B_SPLINE_SURFACE ( (
 ( 1.000000000000000000, 1.000000000000000000),
 ( 0.9932032654565553509, 0.8386279382598740284),
 ( 0.9932032654565553509, 0.8386279382598740284),
 ( 1.000000000000000000, 1.000000000000000000) ) ) 
 REPRESENTATION_ITEM ( '' )  SURFACE ( )  );
#23106=LINE ( 'NONE', #13761, #30750 ) ;
#23117=CARTESIAN_POINT ( 'NONE',  ( -10.00000000000000178, 0.000000000000000000, 0.000000000000000000 ) ) ;
#23121=DIRECTION ( 'NONE',  ( 1.000000000000000000, -0.000000000000000000, -0.000000000000000000 ) ) ;
#23123=DIRECTION ( 'NONE',  ( -1.000000000000000000, 0.000000000000000000, 0.000000000000000000 ) ) ;
#23125=EDGE_LOOP ( 'NONE', ( #8097, #1654 ) ) ;
#23128=ORIENTED_EDGE ( 'NONE', *, *, #59532, .T. ) ;
#23139=CARTESIAN_POINT ( 'NONE',  ( -22.27722015946438816, 0.6262261846986705294, 3.628085906632207092 ) ) ;
#23140=CARTESIAN_POINT ( 'NONE',  ( -22.65999102136915866, -4.450325798697170043, 1.886119913916104229 ) ) ;
#23143=CARTESIAN_POINT ( 'NONE',  ( 2.000000000000001776, 1.754183803416544452, 6.711026108862249373 ) ) ;
#23144=VECTOR ( 'NONE', #509, 1000.000000000000000 ) ;
#23150=CARTESIAN_POINT ( 'NONE',  ( 0.000000000000000000, 5.450255447309745982, 4.087611905901426645 ) ) ;
#23152=CARTESIAN_POINT ( 'NONE',  ( -27.10128162969864007, -1.945744751331068167, 1.304299867635182242 ) ) ;
#23158=DIRECTION ( 'NONE',  ( 0.000000000000000000, 0.1081190184239352453, 0.9941379571543603744 ) ) ;
#23160=FILL_AREA_STYLE ('',( #9163 ) ) ;
#23166=CARTESIAN_POINT ( 'NONE',  ( 2.000000000000001776, 6.812627895098307462, -0.04423456934727655609 ) ) ;
#23172=CARTESIAN_POINT ( 'NONE',  ( -22.29570301036918423, -2.586939527522297055, 2.696988360630612203 ) ) ;
#23174=B_SPLINE_CURVE_WITH_KNOTS ( 'NONE', 3,
 ( #64360, #18823, #12835, #2568, #43412, #14139 ),
 .UNSPECIFIED., .F., .F.,
 ( 4, 2, 4 ),
 ( 0.000000000000000000, 0.0004528561986909391515, 0.0009057123973818783031 ),
 .UNSPECIFIED. ) ;
#23188=EDGE_CURVE ( 'NONE', #12876, #10229, #42920, .T. ) ;
#23189=LINE ( 'NONE', #48800, #6836 ) ;
#23195=EDGE_CURVE ( 'NONE', #21663, #25020, #63199, .T. ) ;
#23198=ORIENTED_EDGE ( 'NONE', *, *, #43658, .T. ) ;
#23205=B_SPLINE_CURVE_WITH_KNOTS ( 'NONE', 3,
 ( #59999, #14420, #34694, #54993, #4478, #45344, #40342, #40688, #1111, #56978, #15415, #15080, #5796, #10103, #21388, #55665, #26371, #56658, #41010, #26063, #31675, #16412 ),
 .UNSPECIFIED., .F., .F.,
 ( 4, 3, 3, 3, 3, 3, 3, 4 ),
 ( 1.167721476617577340E-18, 6.990956068646398400E-05, 0.0001398191187764044130, 0.0002097286751720215715, 0.0002796382307041361554, 0.0003495477861619811829, 0.0004194573423310285747, 0.0005586102576333138456 ),
 .UNSPECIFIED. ) ;
#23207=CARTESIAN_POINT ( 'NONE',  ( 2.000000000000001776, -5.450255447309769963, 4.087611905901399112 ) ) ;
#23209=ORIENTED_EDGE ( 'NONE', *, *, #53098, .T. ) ;
#23211=CARTESIAN_POINT ( 'NONE',  ( -22.28284753389937123, 2.590196335759734847, -2.640101649307530884 ) ) ;
#23214=EDGE_CURVE ( 'NONE', #65319, #12565, #19723, .T. ) ;
#23221=ORIENTED_EDGE ( 'NONE', *, *, #36269, .T. ) ;
#23226=ORIENTED_EDGE ( 'NONE', *, *, #47591, .F. ) ;
#23227=ORIENTED_EDGE ( 'NONE', *, *, #65406, .F. ) ;
#23229=CARTESIAN_POINT ( 'NONE',  ( -27.08588607604449194, -1.616144682268085608, 1.631236259433588742 ) ) ;
#23236=ORIENTED_EDGE ( 'NONE', *, *, #27535, .F. ) ;
#23238=CARTESIAN_POINT ( 'NONE',  ( -22.27721056931765631, 2.768264578996979974, -2.427163553894355452 ) ) ;
#23248=DIRECTION ( 'NONE',  ( 0.000000000000000000, 0.000000000000000000, 1.000000000000000000 ) ) ;
#23253=CARTESIAN_POINT ( 'NONE',  ( -27.10719052120871098, -1.044362304621479165, 2.116547233941197703 ) ) ;
#23257=CARTESIAN_POINT ( 'NONE',  ( -35.04582288351658548, -0.01270482153516100908, 0.0001464581944993508693 ) ) ;
#23260=B_SPLINE_CURVE_WITH_KNOTS ( 'NONE', 3,
 ( #17392, #48975, #37979, #58282, #7742, #57964, #37667, #22357, #42974, #3432, #27672, #43624, #12701, #33657, #53634, #32984, #52955, #12374, #38306, #47979, #32644, #53295 ),
 .UNSPECIFIED., .F., .F.,
 ( 4, 3, 3, 3, 3, 3, 3, 4 ),
 ( 0.000000000000000000, 4.447697177976369992E-05, 6.624143997791436314E-05, 8.800576886944573996E-05, 0.0001097699864780930454, 0.0001315341395364416101, 0.0001760120188223352595, 0.0001867971373174796466 ),
 .UNSPECIFIED. ) ;
#23262=EDGE_CURVE ( 'NONE', #48402, #51469, #37735, .T. ) ;
#23269=CARTESIAN_POINT ( 'NONE',  ( -35.04643116707788408, 0.009112266603805360687, -0.008094444324502694799 ) ) ;
#23272=VERTEX_POINT ( 'NONE', #18969 ) ;
#23278=CARTESIAN_POINT ( 'NONE',  ( -27.08430792439081003, -1.614882584889912431, -1.625846845508604144 ) ) ;
#23280=EDGE_CURVE ( 'NONE', #32989, #35536, #65351, .T. ) ;
#23281=DIRECTION ( 'NONE',  ( 1.000000000000000000, 0.000000000000000000, 0.000000000000000000 ) ) ;
#23282=VERTEX_POINT ( 'NONE', #28604 ) ;
#23288=EDGE_CURVE ( 'NONE', #54975, #40566, #55829, .T. ) ;
#23294=CARTESIAN_POINT ( 'NONE',  ( -22.27706485742869091, -0.3729136217355977778, -3.662257305743823022 ) ) ;
#23298=FACE_OUTER_BOUND ( 'NONE', #34258, .T. ) ;
#23300=VERTEX_POINT ( 'NONE', #43235 ) ;
#23302=EDGE_CURVE ( 'NONE', #21425, #8645, #63513, .T. ) ;
#23308=DIRECTION ( 'NONE',  ( -1.000000000000000000, 0.000000000000000000, 0.000000000000000000 ) ) ;
#23317=AXIS2_PLACEMENT_3D ( 'NONE', #13016, #9011, #43259 ) ;
#23319=DIRECTION ( 'NONE',  ( -1.000000000000000000, 0.000000000000000000, 0.000000000000000000 ) ) ;
#23324=VECTOR ( 'NONE', #34558, 1000.000000000000000 ) ;
#23340=EDGE_CURVE ( 'NONE', #57752, #52961, #64309, .T. ) ;
#23344=EDGE_CURVE ( 'NONE', #46695, #40629, #24322, .T. ) ;
#23346=DIRECTION ( 'NONE',  ( 0.000000000000000000, 0.000000000000000000, 1.000000000000000000 ) ) ;
#23347=DIRECTION ( 'NONE',  ( -1.000000000000000000, 0.000000000000000000, 0.000000000000000000 ) ) ;
#23348=AXIS2_PLACEMENT_3D ( 'NONE', #64463, #64158, #49534 ) ;
#23356=EDGE_LOOP ( 'NONE', ( #33241, #57932, #47937, #32363 ) ) ;
#23359=ORIENTED_EDGE ( 'NONE', *, *, #30278, .T. ) ;
#23365=CARTESIAN_POINT ( 'NONE',  ( -22.27706485742869091, -3.358064672837095976, -1.508175983031630585 ) ) ;
#23368=CARTESIAN_POINT ( 'NONE',  ( -22.27721056931765631, -2.427163553894363890, -2.768264578996979974 ) ) ;
#23370=AXIS2_PLACEMENT_3D ( 'NONE', #22802, #11488, #1856 ) ;
#23379=EDGE_CURVE ( 'NONE', #57516, #13558, #60839, .T. ) ;
#23383=AXIS2_PLACEMENT_3D ( 'NONE', #42166, #56163, #61166 ) ;
#23386=FACE_OUTER_BOUND ( 'NONE', #37016, .T. ) ;
#23395=ORIENTED_EDGE ( 'NONE', *, *, #10956, .F. ) ;
#23403=CIRCLE ( 'NONE', #56332, 2.899999999999994582 ) ;
#23411=CARTESIAN_POINT ( 'NONE',  ( -27.08423923533013422, -1.376387618994799000, -1.832018136655361396 ) ) ;
#23416=AXIS2_PLACEMENT_3D ( 'NONE', #10394, #6097, #26354 ) ;
#23420=ORIENTED_EDGE ( 'NONE', *, *, #52586, .F. ) ;
#23422=DIRECTION ( 'NONE',  ( -1.000000000000000000, 0.000000000000000000, 0.000000000000000000 ) ) ;
#23423=FACE_OUTER_BOUND ( 'NONE', #49061, .T. ) ;
#23425=EDGE_CURVE ( 'NONE', #65358, #61028, #54747, .T. ) ;
#23426=CARTESIAN_POINT ( 'NONE',  ( -27.20164183316781248, 0.1019800881472613385, 2.642567708136680960 ) ) ;
#23427=DIRECTION ( 'NONE',  ( 0.000000000000000000, 0.000000000000000000, 1.000000000000000000 ) ) ;
#23429=EDGE_LOOP ( 'NONE', ( #46509, #50555, #51267, #4094 ) ) ;
#23430=CARTESIAN_POINT ( 'NONE',  ( 0.000000000000000000, 0.000000000000000000, 0.000000000000000000 ) ) ;
#23432=CARTESIAN_POINT ( 'NONE',  ( -22.27834755396593991, -2.756126180273653414, 2.447855249718975390 ) ) ;
#23435=VECTOR ( 'NONE', #52737, 1000.000000000000000 ) ;
#23438=ORIENTED_EDGE ( 'NONE', *, *, #33397, .T. ) ;
#23443=VERTEX_POINT ( 'NONE', #28443 ) ;
#23453=CARTESIAN_POINT ( 'NONE',  ( -22.27719412087655471, 2.283949229175435303, 2.887588494201198230 ) ) ;
#23454=ORIENTED_EDGE ( 'NONE', *, *, #55642, .F. ) ;
#23455=CARTESIAN_POINT ( 'NONE',  ( -22.66110217412718342, -4.900671186447923766, -0.6585288088160191622 ) ) ;
#23462=AXIS2_PLACEMENT_3D ( 'NONE', #19318, #19654, #50242 ) ;
#23463=CYLINDRICAL_SURFACE ( 'NONE', #45557, 2.899999999999994582 ) ;
#23466=CARTESIAN_POINT ( 'NONE',  ( -27.08417568107323703, 0.8117865859100341641, -2.142502990753190506 ) ) ;
#23467=EDGE_LOOP ( 'NONE', ( #31856, #24239, #6184, #8680 ) ) ;
#23474=CARTESIAN_POINT ( 'NONE',  ( 0.000000000000000000, 6.796153407501448029, 1.388283512725836388 ) ) ;
#23479=DIRECTION ( 'NONE',  ( -1.000000000000000000, 0.000000000000000000, 0.000000000000000000 ) ) ;
#23480=CARTESIAN_POINT ( 'NONE',  ( -22.28121537037577227, 3.028566507474732550, -2.114437713163330290 ) ) ;
#23490=SURFACE_STYLE_USAGE ( .BOTH. , #4188 ) ;
#23491=CARTESIAN_POINT ( 'NONE',  ( 2.000000000000001776, -6.250523986464001425, 3.007653927006548766 ) ) ;
#23492=AXIS2_PLACEMENT_3D ( 'NONE', #42810, #48804, #22200 ) ;
#23501=DIRECTION ( 'NONE',  ( 0.000000000000000000, 0.000000000000000000, 1.000000000000000000 ) ) ;
#23502=CARTESIAN_POINT ( 'NONE',  ( -27.09364415740217424, -2.088137158972232843, -1.009938549039995692 ) ) ;
#23506=DIRECTION ( 'NONE',  ( -1.000000000000000000, 0.000000000000000000, 0.000000000000000000 ) ) ;
#23509=CARTESIAN_POINT ( 'NONE',  ( -22.23402523511428086, -0.6266381416564568152, -3.496364702451518092 ) ) ;
#23511=ADVANCED_FACE ( 'NONE', ( #8171 ), #65331, .T. ) ;
#23512=VECTOR ( 'NONE', #36337, 1000.000000000000227 ) ;
#23516=ORIENTED_EDGE ( 'NONE', *, *, #10306, .F. ) ;
#23530=DIRECTION ( 'NONE',  ( -1.000000000000000000, 0.000000000000000000, 0.000000000000000000 ) ) ;
#23533=CIRCLE ( 'NONE', #3386, 7.499999999999988454 ) ;
#23543=VECTOR ( 'NONE', #56839, 1000.000000000000000 ) ;
#23548=AXIS2_PLACEMENT_3D ( 'NONE', #20891, #26873, #21570 ) ;
#23552=LINE ( 'NONE', #7250, #40432 ) ;
#23562=ORIENTED_EDGE ( 'NONE', *, *, #43943, .T. ) ;
#23564=DIRECTION ( 'NONE',  ( 0.000000000000000000, -0.6051742151937717917, 0.7960930657056387583 ) ) ;
#23566=AXIS2_PLACEMENT_3D ( 'NONE', #36166, #46493, #56473 ) ;
#23567=CARTESIAN_POINT ( 'NONE',  ( -27.10422407540562517, -2.346206748218703009, 0.1544383239736372149 ) ) ;
#23569=DIRECTION ( 'NONE',  ( -1.000000000000000000, 0.000000000000000000, 0.000000000000000000 ) ) ;
#23586=ORIENTED_EDGE ( 'NONE', *, *, #23280, .F. ) ;
#23592=LINE ( 'NONE', #37569, #1146 ) ;
#23600=VECTOR ( 'NONE', #22133, 1000.000000000000000 ) ;
#23615=ORIENTED_EDGE ( 'NONE', *, *, #28956, .T. ) ;
#23622=ORIENTED_EDGE ( 'NONE', *, *, #43573, .T. ) ;
#23631=CARTESIAN_POINT ( 'NONE',  ( -22.30986928587821794, -0.2539257557460598003, -3.771068405887407771 ) ) ;
#23632=ORIENTED_EDGE ( 'NONE', *, *, #26352, .T. ) ;
#23634=DIRECTION ( 'NONE',  ( 0.000000000000000000, 0.000000000000000000, -1.000000000000000000 ) ) ;
#23637=VERTEX_POINT ( 'NONE', #11128 ) ;
#23648=CIRCLE ( 'NONE', #25719, 7.499999999999988454 ) ;
#23649=DIRECTION ( 'NONE',  ( -1.000000000000000000, 0.000000000000000000, 0.000000000000000000 ) ) ;
#23650=CIRCLE ( 'NONE', #51276, 7.499999999999988454 ) ;
#23651=ADVANCED_FACE ( 'NONE', ( #25762 ), #15111, .T. ) ;
#23661=ORIENTED_EDGE ( 'NONE', *, *, #45275, .T. ) ;
#23662=CARTESIAN_POINT ( 'NONE',  ( 0.000000000000000000, 0.000000000000000000, 0.000000000000000000 ) ) ;
#23665=B_SPLINE_CURVE_WITH_KNOTS ( 'NONE', 3,
 ( #40056, #5163, #35718, #15451, #56343, #21088, #61653, #20114, #35396, #25113 ),
 .UNSPECIFIED., .F., .F.,
 ( 4, 3, 3, 4 ),
 ( 5.401523115762575937E-05, 0.0008136511341527827203, 0.004068255670953102761, 0.005063778443040927411 ),
 .UNSPECIFIED. ) ;
#23667=CIRCLE ( 'NONE', #59773, 2.899999999999995026 ) ;
#23668=ORIENTED_EDGE ( 'NONE', *, *, #42291, .T. ) ;
#23672=ORIENTED_EDGE ( 'NONE', *, *, #51033, .T. ) ;
#23677=VECTOR ( 'NONE', #28862, 1000.000000000000000 ) ;
#23681=VERTEX_POINT ( 'NONE', #31071 ) ;
#23689=CARTESIAN_POINT ( 'NONE',  ( 2.000000000000001776, -6.883677378339447372, -0.8544109087186817497 ) ) ;
#23690=CARTESIAN_POINT ( 'NONE',  ( -10.00000000000000178, 0.000000000000000000, 0.000000000000000000 ) ) ;
#23693=AXIS2_PLACEMENT_3D ( 'NONE', #42442, #32153, #15869 ) ;
#23697=( BOUNDED_SURFACE ( )  B_SPLINE_SURFACE ( 3, 1, ( 
 ( #60878, #1017 ),
 ( #25966, #15951 ),
 ( #21282, #20950 ),
 ( #41560, #61851 ) ),
 .UNSPECIFIED., .F., .F., .F. ) 
 B_SPLINE_SURFACE_WITH_KNOTS ( ( 4, 4 ),
 ( 2, 2 ),
 ( 0.000000000000000000, 1.000000000000000000 ),
 ( 0.000000000000000000, 1.000000000000000000 ),
 .UNSPECIFIED. ) 
 GEOMETRIC_REPRESENTATION_ITEM ( )  RATIONAL_B_SPLINE_SURFACE ( (
 ( 1.000000000000000000, 1.000000000000000000),
 ( 0.8716676215708681896, 0.8964445200148164483),
 ( 0.8716676215708681896, 0.8964445200148164483),
 ( 1.000000000000000000, 1.000000000000000000) ) ) 
 REPRESENTATION_ITEM ( '' )  SURFACE ( )  );
#23700=CARTESIAN_POINT ( 'NONE',  ( 0.000000000000000000, 0.000000000000000000, 0.000000000000000000 ) ) ;
#23708=CIRCLE ( 'NONE', #62987, 2.899999999999994582 ) ;
#23710=ADVANCED_FACE ( 'NONE', ( #25107 ), #64641, .F. ) ;
#23713=CARTESIAN_POINT ( 'NONE',  ( -22.27711351828769892, -2.547249869018253676, -2.657880562424696613 ) ) ;
#23715=DIRECTION ( 'NONE',  ( -1.000000000000000000, 0.000000000000000000, 0.000000000000000000 ) ) ;
#23726=CARTESIAN_POINT ( 'NONE',  ( -35.04683013664716640, 0.006266879427285388868, 0.01065093278704546884 ) ) ;
#23738=FACE_OUTER_BOUND ( 'NONE', #340, .T. ) ;
#23744=ORIENTED_EDGE ( 'NONE', *, *, #53288, .F. ) ;
#23745=FACE_OUTER_BOUND ( 'NONE', #19703, .T. ) ;
#23747=CARTESIAN_POINT ( 'NONE',  ( -27.20102706715913854, 2.512061365242613142, -0.8206313329275921609 ) ) ;
#23748=CARTESIAN_POINT ( 'NONE',  ( -22.28350523959500862, 2.107889123925603680, 3.041489826385490591 ) ) ;
#23764=EDGE_CURVE ( 'NONE', #55569, #36553, #21894, .T. ) ;
#23770=CARTESIAN_POINT ( 'NONE',  ( 1.000000000000000888, 2.473437528934141483, 7.080403010454977775 ) ) ;
#23776=ORIENTED_EDGE ( 'NONE', *, *, #32758, .T. ) ;
#23777=CYLINDRICAL_SURFACE ( 'NONE', #22595, 2.899999999999994582 ) ;
#23779=CARTESIAN_POINT ( 'NONE',  ( -22.27706485742869091, 2.154081322712221969, 2.985151051101477382 ) ) ;
#23782=CARTESIAN_POINT ( 'NONE',  ( 2.000000000000001776, 0.000000000000000000, 0.000000000000000000 ) ) ;
#23796=B_SPLINE_CURVE_WITH_KNOTS ( 'NONE', 3,
 ( #9960, #45869, #45520, #30553, #30879, #45209, #50857, #56155, #15272, #51198, #40538, #55846, #50212, #36190, #10274, #5305, #25574, #5983, #24935 ),
 .UNSPECIFIED., .F., .F.,
 ( 4, 3, 3, 3, 3, 3, 4 ),
 ( 0.000000000000000000, 2.836829843012877734E-05, 4.224792512550914851E-05, 5.612066614913206291E-05, 6.998859278354786935E-05, 9.832141288087123897E-05, 0.0001178161482478541221 ),
 .UNSPECIFIED. ) ;
#23799=DIRECTION ( 'NONE',  ( -1.000000000000000000, 0.000000000000000000, 0.000000000000000000 ) ) ;
#23801=PRODUCT_DEFINITION_SHAPE ( 'NONE', 'NONE',  #64445 ) ;
#23803=EDGE_LOOP ( 'NONE', ( #42168, #27464, #64969, #29049 ) ) ;
#23806=ORIENTED_EDGE ( 'NONE', *, *, #45390, .F. ) ;
#23807=EDGE_CURVE ( 'NONE', #40945, #41782, #53750, .T. ) ;
#23812=CARTESIAN_POINT ( 'NONE',  ( 2.000000000000001776, 0.000000000000000000, 0.000000000000000000 ) ) ;
#23813=CARTESIAN_POINT ( 'NONE',  ( 0.000000000000000000, -2.480520636974139936, -6.345145617221269241 ) ) ;
#23818=ORIENTED_EDGE ( 'NONE', *, *, #14342, .T. ) ;
#23820=DIRECTION ( 'NONE',  ( -1.000000000000000000, 0.000000000000000000, 0.000000000000000000 ) ) ;
#23824=FACE_OUTER_BOUND ( 'NONE', #49964, .T. ) ;
#23827=CARTESIAN_POINT ( 'NONE',  ( -22.31213670151049300, 3.145266995071685834, -2.108126385153777704 ) ) ;
#23829=VECTOR ( 'NONE', #27314, 1000.000000000000000 ) ;
#23836=AXIS2_PLACEMENT_3D ( 'NONE', #23862, #44122, #64389 ) ;
#23838=EDGE_CURVE ( 'NONE', #39026, #24684, #31423, .T. ) ;
#23840=CYLINDRICAL_SURFACE ( 'NONE', #43867, 6.936499999999988120 ) ;
#23841=ADVANCED_FACE ( 'NONE', ( #13405 ), #43661, .T. ) ;
#23854=CARTESIAN_POINT ( 'NONE',  ( -27.08429572838383947, 1.338867938658203860, 1.859677275556406384 ) ) ;
#23862=CARTESIAN_POINT ( 'NONE',  ( -10.00000000000000178, 0.000000000000000000, 0.000000000000000000 ) ) ;
#23880=ORIENTED_EDGE ( 'NONE', *, *, #61619, .T. ) ;
#23884=CARTESIAN_POINT ( 'NONE',  ( -22.29570301036918778, 2.586939527522315707, -2.696988360630598880 ) ) ;
#23886=CARTESIAN_POINT ( 'NONE',  ( -22.29479313954897890, -1.627767898183747119, 3.360948587163227863 ) ) ;
#23915=DIRECTION ( 'NONE',  ( 0.000000000000000000, 0.000000000000000000, 1.000000000000000000 ) ) ;
#23916=CARTESIAN_POINT ( 'NONE',  ( -22.71097035706202405, -4.510116093748277599, 2.118550233809401107 ) ) ;
#23925=DIRECTION ( 'NONE',  ( 1.000000000000000000, 0.000000000000000000, 0.000000000000000000 ) ) ;
#23931=CARTESIAN_POINT ( 'NONE',  ( -22.27834755396594346, 3.610802913011834203, -0.7418417409069075763 ) ) ;
#23932=DIRECTION ( 'NONE',  ( 0.000000000000000000, 0.000000000000000000, -1.000000000000000000 ) ) ;
#23933=CARTESIAN_POINT ( 'NONE',  ( -22.28694879868232803, 2.661377239830763131, 2.586016167700781576 ) ) ;
#23939=ORIENTED_EDGE ( 'NONE', *, *, #43030, .F. ) ;
#23943=DIRECTION ( 'NONE',  ( 1.000000000000000000, 0.000000000000000000, 0.000000000000000000 ) ) ;
#23947=CARTESIAN_POINT ( 'NONE',  ( -27.10719052120871098, 2.261993590776037788, -0.6736837626858775963 ) ) ;
#23948=EDGE_CURVE ( 'NONE', #21913, #6336, #47386, .T. ) ;
#23961=ORIENTED_EDGE ( 'NONE', *, *, #10244, .T. ) ;
#23969=ORIENTED_EDGE ( 'NONE', *, *, #20310, .F. ) ;
#23976=ORIENTED_EDGE ( 'NONE', *, *, #61719, .T. ) ;
#23978=DIRECTION ( 'NONE',  ( 0.000000000000000000, 0.000000000000000000, 1.000000000000000000 ) ) ;
#23984=DIRECTION ( 'NONE',  ( 0.000000000000000000, 0.000000000000000000, 1.000000000000000000 ) ) ;
#23991=CARTESIAN_POINT ( 'NONE',  ( -35.04643116707788408, -0.002453861112623398344, -0.01193867652721398998 ) ) ;
#23993=ORIENTED_EDGE ( 'NONE', *, *, #32550, .T. ) ;
#24004=EDGE_CURVE ( 'NONE', #19340, #36463, #10776, .T. ) ;
#24008=B_SPLINE_CURVE_WITH_KNOTS ( 'NONE', 3,
 ( #32760, #23140, #48433, #8176, #17167, #37107 ),
 .UNSPECIFIED., .F., .F.,
 ( 4, 2, 4 ),
 ( 0.0002637379172149909154, 0.0009975831966603271490, 0.001731428476105663708 ),
 .UNSPECIFIED. ) ;
#24012=DIRECTION ( 'NONE',  ( -1.000000000000000000, 0.000000000000000000, 0.000000000000000000 ) ) ;
#24016=CARTESIAN_POINT ( 'NONE',  ( -27.08429572838383947, -1.338867938658200307, -1.859677275556420151 ) ) ;
#24017=AXIS2_PLACEMENT_3D ( 'NONE', #117, #45338, #14724 ) ;
#24018=EDGE_CURVE ( 'NONE', #39168, #59008, #39918, .T. ) ;
#24019=ORIENTED_EDGE ( 'NONE', *, *, #37458, .F. ) ;
#24020=CARTESIAN_POINT ( 'NONE',  ( 2.000000000000001776, 4.915517050588478654, -4.717154614762057108 ) ) ;
#24026=VERTEX_POINT ( 'NONE', #60268 ) ;
#24027=ORIENTED_EDGE ( 'NONE', *, *, #44272, .T. ) ;
#24031=ORIENTED_EDGE ( 'NONE', *, *, #6802, .F. ) ;
#24032=CARTESIAN_POINT ( 'NONE',  ( -22.27721038036499834, -2.320305412324239036, -2.858424446490937854 ) ) ;
#24039=CARTESIAN_POINT ( 'NONE',  ( 0.000000000000000000, -6.662861565602071323, 1.421313227905616650 ) ) ;
#24054=CARTESIAN_POINT ( 'NONE',  ( -27.15511094194037156, -2.092607239484530091, 1.375165223101502576 ) ) ;
#24057=ORIENTED_EDGE ( 'NONE', *, *, #32225, .T. ) ;
#24059=VERTEX_POINT ( 'NONE', #46301 ) ;
#24061=DIRECTION ( 'NONE',  ( 0.000000000000000000, 0.000000000000000000, 1.000000000000000000 ) ) ;
#24071=CARTESIAN_POINT ( 'NONE',  ( -27.08421723179412410, -1.556274442127719704, -1.681635392574643673 ) ) ;
#24073=ORIENTED_EDGE ( 'NONE', *, *, #49049, .F. ) ;
#24082=EDGE_CURVE ( 'NONE', #58016, #28622, #19587, .T. ) ;
#24086=VERTEX_POINT ( 'NONE', #41943 ) ;
#24107=CARTESIAN_POINT ( 'NONE',  ( 0.000000000000000000, 0.000000000000000000, 0.000000000000000000 ) ) ;
#24112=CARTESIAN_POINT ( 'NONE',  ( -35.05012975565874456, -0.005092487515925959649, 0.01296790604420273996 ) ) ;
#24126=CARTESIAN_POINT ( 'NONE',  ( 2.000000000000001776, 6.250523986463984549, 3.007653927006597172 ) ) ;
#24132=CARTESIAN_POINT ( 'NONE',  ( 0.000000000000000000, 4.962980376314141573, -4.846014654777754060 ) ) ;
#24140=DIRECTION ( 'NONE',  ( -1.000000000000000000, 0.000000000000000000, 0.000000000000000000 ) ) ;
#24150=ORIENTED_EDGE ( 'NONE', *, *, #27678, .T. ) ;
#24152=LINE ( 'NONE', #61046, #294 ) ;
#24162=DIRECTION ( 'NONE',  ( 0.000000000000000000, 0.9289767198167898643, 0.3701381553399183955 ) ) ;
#24164=EDGE_CURVE ( 'NONE', #49356, #13076, #8497, .T. ) ;
#24174=CARTESIAN_POINT ( 'NONE',  ( 0.000000000000000000, 0.000000000000000000, 0.000000000000000000 ) ) ;
#24178=CARTESIAN_POINT ( 'NONE',  ( 2.000000000000001776, -2.664846396702436948, -6.404188155573047325 ) ) ;
#24180=EDGE_LOOP ( 'NONE', ( #38207, #38278, #58455, #60550 ) ) ;
#24191=CARTESIAN_POINT ( 'NONE',  ( -22.27218376572352554, -0.9173404081777536412, 3.566922835983782569 ) ) ;
#24204=CARTESIAN_POINT ( 'NONE',  ( 2.000000000000001776, 6.812627895098307462, 2.855765430652722259 ) ) ;
#24209=DIRECTION ( 'NONE',  ( -1.000000000000000000, 0.000000000000000000, 0.000000000000000000 ) ) ;
#24213=DIRECTION ( 'NONE',  ( -1.000000000000000000, -1.685093406416449860E-16, 1.011030131491573426E-17 ) ) ;
#24214=CARTESIAN_POINT ( 'NONE',  ( -27.10307689719147817, 1.615391801699798791, -1.703783570823888871 ) ) ;
#24215=CARTESIAN_POINT ( 'NONE',  ( -27.15525204139121840, 2.440367606305298587, 0.5628609503965231742 ) ) ;
#24220=ORIENTED_EDGE ( 'NONE', *, *, #10142, .F. ) ;
#24223=ORIENTED_EDGE ( 'NONE', *, *, #54746, .T. ) ;
#24228=LINE ( 'NONE', #30836, #39244 ) ;
#24232=EDGE_CURVE ( 'NONE', #36610, #29381, #44189, .T. ) ;
#24239=ORIENTED_EDGE ( 'NONE', *, *, #41382, .T. ) ;
#24240=CARTESIAN_POINT ( 'NONE',  ( -35.04582288351658548, 0.002280196168869179450, -0.01249938581188446245 ) ) ;
#24254=DIRECTION ( 'NONE',  ( 0.000000000000000000, 0.000000000000000000, 1.000000000000000000 ) ) ;
#24259=CARTESIAN_POINT ( 'NONE',  ( -22.30625920655495165, 3.635849356906417640, -1.076742202099146839 ) ) ;
#24261=AXIS2_PLACEMENT_3D ( 'NONE', #3294, #23569, #17920 ) ;
#24263=VERTEX_POINT ( 'NONE', #15931 ) ;
#24264=DIRECTION ( 'NONE',  ( 0.000000000000000000, -0.1081190184239489566, 0.9941379571543588201 ) ) ;
#24266=CARTESIAN_POINT ( 'NONE',  ( -22.51237073810381517, 0.2145858836692361438, 4.418556976583610130 ) ) ;
#24273=CARTESIAN_POINT ( 'NONE',  ( -27.09229696323320979, -2.247106967994379811, -0.5586335684093849396 ) ) ;
#24275=ORIENTED_EDGE ( 'NONE', *, *, #61695, .F. ) ;
#24279=DIRECTION ( 'NONE',  ( -1.000000000000000000, 0.000000000000000000, 0.000000000000000000 ) ) ;
#24281=ORIENTED_EDGE ( 'NONE', *, *, #4672, .F. ) ;
#24282=AXIS2_PLACEMENT_3D ( 'NONE', #38785, #44097, #54742 ) ;
#24287=CARTESIAN_POINT ( 'NONE',  ( -22.46225619532221529, -0.1595555201818088242, -4.233934615764606946 ) ) ;
#24288=ORIENTED_EDGE ( 'NONE', *, *, #9458, .T. ) ;
#24292=DIRECTION ( 'NONE',  ( 0.000000000000000000, 0.000000000000000000, 1.000000000000000000 ) ) ;
#24301=EDGE_CURVE ( 'NONE', #60499, #16108, #21761, .T. ) ;
#24305=CARTESIAN_POINT ( 'NONE',  ( 0.000000000000000000, -6.935703035393425253, 0.1051458740707039013 ) ) ;
#24314=VECTOR ( 'NONE', #10736, 1000.000000000000114 ) ;
#24322=B_SPLINE_CURVE_WITH_KNOTS ( 'NONE', 3,
 ( #8330, #45217, #15280, #4334, #44538, #40888, #34570, #20610, #59867, #49883, #331, #24273, #61167, #55186, #14929, #60176, #55524, #10283, #30889 ),
 .UNSPECIFIED., .F., .F.,
 ( 4, 3, 3, 3, 3, 3, 4 ),
 ( 0.000000000000000000, 2.832085443540737559E-05, 4.217789847394784225E-05, 5.603488375046119081E-05, 6.989180858579295227E-05, 9.821094829918946873E-05, 0.0001178165571465047653 ),
 .UNSPECIFIED. ) ;
#24327=CARTESIAN_POINT ( 'NONE',  ( 2.000000000000001776, 0.000000000000000000, 0.000000000000000000 ) ) ;
#24328=CARTESIAN_POINT ( 'NONE',  ( 0.000000000000000000, 1.754183803416544452, 6.711026108862249373 ) ) ;
#24333=CARTESIAN_POINT ( 'NONE',  ( -27.20164183316780182, 2.642567708136682736, -0.1019800881472440052 ) ) ;
#24342=VERTEX_POINT ( 'NONE', #60857 ) ;
#24344=CIRCLE ( 'NONE', #19042, 2.899999999999995470 ) ;
#24350=EDGE_LOOP ( 'NONE', ( #5221, #59453, #46739, #17273 ) ) ;
#24352=ORIENTED_EDGE ( 'NONE', *, *, #3815, .T. ) ;
#24353=FACE_OUTER_BOUND ( 'NONE', #13464, .T. ) ;
#24367=ORIENTED_EDGE ( 'NONE', *, *, #296, .F. ) ;
#24368=ORIENTED_EDGE ( 'NONE', *, *, #17934, .F. ) ;
#24372=CARTESIAN_POINT ( 'NONE',  ( -27.08429572838383947, -2.217805374070538349, 0.5764601019425888984 ) ) ;
#24374=CARTESIAN_POINT ( 'NONE',  ( -22.29290468048228036, 1.621390503294497742, -3.357740900108092674 ) ) ;
#24378=EDGE_CURVE ( 'NONE', #29292, #5936, #48918, .T. ) ;
#24379=EDGE_LOOP ( 'NONE', ( #56344, #4084, #63610, #3458 ) ) ;
#24381=CYLINDRICAL_SURFACE ( 'NONE', #15399, 7.499999999999988454 ) ;
#24382=ADVANCED_FACE ( 'NONE', ( #9631 ), #51082, .F. ) ;
#24390=FACE_OUTER_BOUND ( 'NONE', #36518, .T. ) ;
#24393=EDGE_CURVE ( 'NONE', #20149, #34412, #348, .T. ) ;
#24394=CARTESIAN_POINT ( 'NONE',  ( 2.000000000000001776, -3.979254915827401540, 5.681598592373737766 ) ) ;
#24401=EDGE_LOOP ( 'NONE', ( #57891, #24944, #55469, #23006 ) ) ;
#24415=DIRECTION ( 'NONE',  ( 1.000000000000000000, -0.000000000000000000, -0.000000000000000000 ) ) ;
#24417=CARTESIAN_POINT ( 'NONE',  ( -22.46225619532223305, -2.255146441673796964, -3.586917175123550017 ) ) ;
#24419=CARTESIAN_POINT ( 'NONE',  ( 2.000000000000001776, -6.812627895098285258, 0.04423456934719675882 ) ) ;
#24422=CARTESIAN_POINT ( 'NONE',  ( -22.27711653538342773, 2.191780254295688568, 2.958138731383619380 ) ) ;
#24438=CARTESIAN_POINT ( 'NONE',  ( 2.000000000000001776, -4.444115772890149252, 5.163689623839303522 ) ) ;
#24450=VECTOR ( 'NONE', #64713, 1000.000000000000000 ) ;
#24452=( BOUNDED_SURFACE ( )  B_SPLINE_SURFACE ( 3, 1, ( 
 ( #33286, #53589 ),
 ( #18981, #3047 ),
 ( #39243, #49263 ),
 ( #44548, #64830 ) ),
 .UNSPECIFIED., .F., .F., .F. ) 
 B_SPLINE_SURFACE_WITH_KNOTS ( ( 4, 4 ),
 ( 2, 2 ),
 ( 0.000000000000000000, 1.000000000000000000 ),
 ( 0.000000000000000000, 1.000000000000000000 ),
 .UNSPECIFIED. ) 
 GEOMETRIC_REPRESENTATION_ITEM ( )  RATIONAL_B_SPLINE_SURFACE ( (
 ( 1.000000000000000000, 1.000000000000000000),
 ( 0.9932032654565553509, 0.8386279382598740284),
 ( 0.9932032654565553509, 0.8386279382598740284),
 ( 1.000000000000000000, 1.000000000000000000) ) ) 
 REPRESENTATION_ITEM ( '' )  SURFACE ( )  );
#24457=DIRECTION ( 'NONE',  ( 1.000000000000000000, -0.000000000000000000, -0.000000000000000000 ) ) ;
#24459=CARTESIAN_POINT ( 'NONE',  ( 2.000000000000001776, 6.883677378339481123, -0.8544109087185395301 ) ) ;
#24467=AXIS2_PLACEMENT_3D ( 'NONE', #26154, #21492, #6860 ) ;
#24475=AXIS2_PLACEMENT_3D ( 'NONE', #38056, #33415, #43050 ) ;
#24484=ORIENTED_EDGE ( 'NONE', *, *, #53760, .T. ) ;
#24486=CARTESIAN_POINT ( 'NONE',  ( 2.000000000000001776, 0.000000000000000000, 0.000000000000000000 ) ) ;
#24487=CARTESIAN_POINT ( 'NONE',  ( -22.29195009621226475, -1.030739959031446107, -3.580440466953083156 ) ) ;
#24489=CARTESIAN_POINT ( 'NONE',  ( -27.08485414902839494, 2.215517476308469291, 0.5917839443972277014 ) ) ;
#24491=CIRCLE ( 'NONE', #25598, 7.499999999999988454 ) ;
#24496=CIRCLE ( 'NONE', #36159, 6.936499999999989008 ) ;
#24499=LINE ( 'NONE', #29479, #56471 ) ;
#24508=VECTOR ( 'NONE', #49896, 1000.000000000000000 ) ;
#24514=ORIENTED_EDGE ( 'NONE', *, *, #19629, .F. ) ;
#24518=ORIENTED_EDGE ( 'NONE', *, *, #57008, .T. ) ;
#24520=DIRECTION ( 'NONE',  ( -1.000000000000000000, 0.000000000000000000, 0.000000000000000000 ) ) ;
#24525=EDGE_LOOP ( 'NONE', ( #4967, #62507, #28292, #40915 ) ) ;
#24527=DIRECTION ( 'NONE',  ( -1.000000000000000000, 0.000000000000000000, 0.000000000000000000 ) ) ;
#24528=CIRCLE ( 'NONE', #7533, 6.936499999999991672 ) ;
#24530=CARTESIAN_POINT ( 'NONE',  ( 1.000000000000000888, -6.586971819220345026, 3.586335490831356054 ) ) ;
#24567=CYLINDRICAL_SURFACE ( 'NONE', #48901, 6.936499999999988120 ) ;
#24571=EDGE_LOOP ( 'NONE', ( #59119, #51281, #2574, #12081 ) ) ;
#24578=CIRCLE ( 'NONE', #138, 2.899999999999995914 ) ;
#24582=CARTESIAN_POINT ( 'NONE',  ( 2.000000000000001776, 5.396716205731493687, -4.158041573745044239 ) ) ;
#24592=VERTEX_POINT ( 'NONE', #48207 ) ;
#24602=ADVANCED_FACE ( 'NONE', ( #63450 ), #28873, .F. ) ;
#24612=ORIENTED_EDGE ( 'NONE', *, *, #27123, .F. ) ;
#24615=B_SPLINE_CURVE_WITH_KNOTS ( 'NONE', 3,
 ( #25435, #39749, #45384, #514, #45071, #41052, #19805, #14775, #55712, #61333, #25775, #20121, #15122, #19480, #36048, #50405, #65007, #55037, #14459, #56348, #34734, #10146 ),
 .UNSPECIFIED., .F., .F.,
 ( 4, 3, 3, 3, 3, 3, 3, 4 ),
 ( 0.000000000000000000, 4.455945684386757038E-05, 6.636307477204008278E-05, 8.816671873158727604E-05, 0.0001099660380492610995, 0.0001317545563165303715, 0.0001762613022895040686, 0.0001867992666138395923 ),
 .UNSPECIFIED. ) ;
#24627=CIRCLE ( 'NONE', #27805, 6.936499999999989896 ) ;
#24629=ORIENTED_EDGE ( 'NONE', *, *, #63792, .F. ) ;
#24632=DIRECTION ( 'NONE',  ( -1.000000000000000000, 0.000000000000000000, 0.000000000000000000 ) ) ;
#24633=ADVANCED_FACE ( 'NONE', ( #59458 ), #39164, .T. ) ;
#24634=ORIENTED_EDGE ( 'NONE', *, *, #4285, .F. ) ;
#24635=AXIS2_PLACEMENT_3D ( 'NONE', #4564, #24833, #29793 ) ;
#24636=AXIS2_PLACEMENT_3D ( 'NONE', #58491, #47528, #17918 ) ;
#24652=AXIS2_PLACEMENT_3D ( 'NONE', #5110, #8787, #29383 ) ;
#24653=EDGE_CURVE ( 'NONE', #18772, #52659, #53831, .T. ) ;
#24654=( BOUNDED_SURFACE ( )  B_SPLINE_SURFACE ( 3, 1, ( 
 ( #13591, #63805 ),
 ( #13912, #3667 ),
 ( #23257, #23931 ),
 ( #34204, #53856 ) ),
 .UNSPECIFIED., .F., .F., .F. ) 
 B_SPLINE_SURFACE_WITH_KNOTS ( ( 4, 4 ),
 ( 2, 2 ),
 ( 0.000000000000000000, 1.000000000000000000 ),
 ( 0.000000000000000000, 1.000000000000000000 ),
 .UNSPECIFIED. ) 
 GEOMETRIC_REPRESENTATION_ITEM ( )  RATIONAL_B_SPLINE_SURFACE ( (
 ( 1.000000000000000000, 1.000000000000000000),
 ( 0.9257577194822556033, 0.9980522942447415113),
 ( 0.9257577194822556033, 0.9980522942447415113),
 ( 1.000000000000000000, 1.000000000000000000) ) ) 
 REPRESENTATION_ITEM ( '' )  SURFACE ( )  );
#24657=CARTESIAN_POINT ( 'NONE',  ( 2.000000000000001776, -4.570217215903314312, -5.218059682435693958 ) ) ;
#24664=ORIENTED_EDGE ( 'NONE', *, *, #29765, .T. ) ;
#24666=( BOUNDED_SURFACE ( )  B_SPLINE_SURFACE ( 3, 1, ( 
 ( #8696, #28976 ),
 ( #34280, #54592 ),
 ( #29299, #49593 ),
 ( #44566, #10312 ) ),
 .UNSPECIFIED., .F., .F., .F. ) 
 B_SPLINE_SURFACE_WITH_KNOTS ( ( 4, 4 ),
 ( 2, 2 ),
 ( 0.000000000000000000, 1.000000000000000000 ),
 ( 0.000000000000000000, 1.000000000000000000 ),
 .UNSPECIFIED. ) 
 GEOMETRIC_REPRESENTATION_ITEM ( )  RATIONAL_B_SPLINE_SURFACE ( (
 ( 1.000000000000000000, 1.000000000000000000),
 ( 0.9932032654565553509, 0.8386279382598736953),
 ( 0.9932032654565553509, 0.8386279382598736953),
 ( 1.000000000000000000, 1.000000000000000000) ) ) 
 REPRESENTATION_ITEM ( '' )  SURFACE ( )  );
#24678=ORIENTED_EDGE ( 'NONE', *, *, #36857, .F. ) ;
#24684=VERTEX_POINT ( 'NONE', #35795 ) ;
#24699=AXIS2_PLACEMENT_3D ( 'NONE', #24020, #64880, #44280 ) ;
#24702=CARTESIAN_POINT ( 'NONE',  ( -27.09252613521642772, -0.1722886739160256198, -2.309775830546441533 ) ) ;
#24710=VECTOR ( 'NONE', #17909, 1000.000000000000000 ) ;
#24718=CARTESIAN_POINT ( 'NONE',  ( 2.000000000000001776, -6.750946897830710114, 1.593658756657014397 ) ) ;
#24722=CIRCLE ( 'NONE', #13035, 6.936499999999990784 ) ;
#24723=VERTEX_POINT ( 'NONE', #25857 ) ;
#24725=LINE ( 'NONE', #15395, #44073 ) ;
#24730=VECTOR ( 'NONE', #12862, 1000.000000000000000 ) ;
#24734=B_SPLINE_CURVE_WITH_KNOTS ( 'NONE', 3,
 ( #32645, #27673, #47980, #2437, #22714, #42975 ),
 .UNSPECIFIED., .F., .F.,
 ( 4, 2, 4 ),
 ( 0.0002637379172189280329, 0.0009975831966640225437, 0.001731428476109116892 ),
 .UNSPECIFIED. ) ;
#24753=CARTESIAN_POINT ( 'NONE',  ( 1.000000000000000888, -3.795144977083577675, -6.468916029978841742 ) ) ;
#24756=ORIENTED_EDGE ( 'NONE', *, *, #64493, .F. ) ;
#24765=CARTESIAN_POINT ( 'NONE',  ( -27.08429572838383947, 1.608131779585724619, 1.632445743623414325 ) ) ;
#24775=CARTESIAN_POINT ( 'NONE',  ( -27.15525204139121840, 1.831989866434750480, 1.707635684994303515 ) ) ;
#24780=ADVANCED_FACE ( 'NONE', ( #10216 ), #4262, .T. ) ;
#24785=VERTEX_POINT ( 'NONE', #60433 ) ;
#24799=CIRCLE ( 'NONE', #33293, 7.499999999999988454 ) ;
#24811=CARTESIAN_POINT ( 'NONE',  ( -22.31328051695926007, 2.748895659348141507, 2.608921479762082551 ) ) ;
#24815=CARTESIAN_POINT ( 'NONE',  ( -28.66013792860432119, 1.289369452666815796, 1.306994062650322919 ) ) ;
#24818=CIRCLE ( 'NONE', #48203, 6.936499999999989896 ) ;
#24822=ORIENTED_EDGE ( 'NONE', *, *, #38913, .T. ) ;
#24825=AXIS2_PLACEMENT_3D ( 'NONE', #64448, #18918, #39183 ) ;
#24833=DIRECTION ( 'NONE',  ( -1.000000000000000000, 0.000000000000000000, 0.000000000000000000 ) ) ;
#24839=CARTESIAN_POINT ( 'NONE',  ( 2.000000000000001776, -5.997115278587605403, -3.485633455389573587 ) ) ;
#24843=ADVANCED_FACE ( 'NONE', ( #263 ), #40136, .T. ) ;
#24848=EDGE_CURVE ( 'NONE', #21602, #25841, #48686, .T. ) ;
#24849=EDGE_LOOP ( 'NONE', ( #64332, #54812, #17068, #42956 ) ) ;
#24851=VERTEX_POINT ( 'NONE', #57100 ) ;
#24854=EDGE_CURVE ( 'NONE', #58967, #60906, #22123, .T. ) ;
#24862=ORIENTED_EDGE ( 'NONE', *, *, #52120, .T. ) ;
#24865=CARTESIAN_POINT ( 'NONE',  ( 2.000000000000001776, -6.201547234536999298, -2.820401998297984214 ) ) ;
#24871=CARTESIAN_POINT ( 'NONE',  ( -27.09150307427401216, 1.001311209615680209, -2.085162835056712627 ) ) ;
#24874=CARTESIAN_POINT ( 'NONE',  ( -22.46509356695199600, -1.314379028669519833, -4.038408495643935225 ) ) ;
#24891=CARTESIAN_POINT ( 'NONE',  ( 0.000000000000000000, -7.414200355365264450, 1.131208685655129775 ) ) ;
#24900=CARTESIAN_POINT ( 'NONE',  ( -27.10719052120871098, -0.5475695427849570640, 2.295785794152556125 ) ) ;
#24912=CARTESIAN_POINT ( 'NONE',  ( 0.000000000000000000, -3.073484823194281290, -6.841322316745092280 ) ) ;
#24917=B_SPLINE_CURVE_WITH_KNOTS ( 'NONE', 3,
 ( #32687, #12417, #33377, #8114, #17765, #8432, #48025, #2482, #18436, #22760, #43019, #64287, #63293, #38019, #7787, #23078, #43337, #63613, #38354, #13412, #39011, #28385 ),
 .UNSPECIFIED., .F., .F.,
 ( 4, 3, 3, 3, 3, 3, 3, 4 ),
 ( 0.000000000000000000, 4.447697177976197875E-05, 6.624143997791211342E-05, 8.800576886944256867E-05, 0.0001097699864780881122, 0.0001315341395364362433, 0.0001760120188223267756, 0.0001867971373174692653 ),
 .UNSPECIFIED. ) ;
#24918=DIRECTION ( 'NONE',  ( -1.000000000000000000, 0.000000000000000000, 0.000000000000000000 ) ) ;
#24927=CARTESIAN_POINT ( 'NONE',  ( -27.08416974970326052, -0.4041872645907051420, -2.255186831366117417 ) ) ;
#24935=CARTESIAN_POINT ( 'NONE',  ( -27.08429572838383947, 1.859677275556428810, -1.338867938658195200 ) ) ;
#24937=CARTESIAN_POINT ( 'NONE',  ( -22.30625920655495165, 0.2529928606556913206, 3.783486345733959588 ) ) ;
#24938=ORIENTED_EDGE ( 'NONE', *, *, #1517, .F. ) ;
#24941=CARTESIAN_POINT ( 'NONE',  ( 0.000000000000000000, 0.000000000000000000, 0.000000000000000000 ) ) ;
#24944=ORIENTED_EDGE ( 'NONE', *, *, #62315, .T. ) ;
#24945=ORIENTED_EDGE ( 'NONE', *, *, #59532, .F. ) ;
#24947=EDGE_CURVE ( 'NONE', #62360, #57516, #50856, .T. ) ;
#24952=ORIENTED_EDGE ( 'NONE', *, *, #61841, .F. ) ;
#24957=CARTESIAN_POINT ( 'NONE',  ( -22.39032720737626647, -2.746561316202153602, 2.936932155721176496 ) ) ;
#24960=EDGE_CURVE ( 'NONE', #4743, #45642, #26493, .T. ) ;
#24965=EDGE_CURVE ( 'NONE', #39372, #37744, #29788, .T. ) ;
#24966=AXIS2_PLACEMENT_3D ( 'NONE', #10040, #15352, #14667 ) ;
#24974=CIRCLE ( 'NONE', #62130, 6.936499999999987232 ) ;
#24989=DIRECTION ( 'NONE',  ( 0.000000000000000000, 0.000000000000000000, 1.000000000000000000 ) ) ;
#24997=CARTESIAN_POINT ( 'NONE',  ( -27.08871896697732140, -1.309412067287333059, -1.896680818246855305 ) ) ;
#25015=CIRCLE ( 'NONE', #57962, 6.936499999999991672 ) ;
#25020=VERTEX_POINT ( 'NONE', #7874 ) ;
#25021=CARTESIAN_POINT ( 'NONE',  ( 2.000000000000001776, -4.376687952327356079, 5.220963330856582374 ) ) ;
#25026=LINE ( 'NONE', #15670, #62699 ) ;
#25031=CARTESIAN_POINT ( 'NONE',  ( -22.27720387087365239, -0.5572161790459744246, -3.639274226782821753 ) ) ;
#25036=DIRECTION ( 'NONE',  ( -1.000000000000000000, 0.000000000000000000, 0.000000000000000000 ) ) ;
#25044=EDGE_LOOP ( 'NONE', ( #21576, #14783, #32728, #1935 ) ) ;
#25047=DIRECTION ( 'NONE',  ( 0.000000000000000000, -0.8835120444460178302, -0.4684084406997996441 ) ) ;
#25050=EDGE_CURVE ( 'NONE', #59201, #24026, #15792, .T. ) ;
#25060=CIRCLE ( 'NONE', #58015, 2.899999999999994582 ) ;
#25063=DIRECTION ( 'NONE',  ( -1.000000000000000000, 0.000000000000000000, 0.000000000000000000 ) ) ;
#25066=DIRECTION ( 'NONE',  ( -1.000000000000000000, 0.000000000000000000, 0.000000000000000000 ) ) ;
#25068=CARTESIAN_POINT ( 'NONE',  ( 2.000000000000001776, 4.444115772890187444, -5.163689623839299081 ) ) ;
#25071=B_SPLINE_CURVE_WITH_KNOTS ( 'NONE', 3,
 ( #21471, #46099, #16487, #65680, #5539, #40421 ),
 .UNSPECIFIED., .F., .F.,
 ( 4, 2, 4 ),
 ( 0.0001654224980408457906, 0.0006219428995476565265, 0.001078463301054467154 ),
 .UNSPECIFIED. ) ;
#25075=CARTESIAN_POINT ( 'NONE',  ( -35.04660725145885891, -0.007231372203124366085, -0.009947898977309622276 ) ) ;
#25078=ORIENTED_EDGE ( 'NONE', *, *, #32758, .F. ) ;
#25080=CARTESIAN_POINT ( 'NONE',  ( 2.000000000000001776, 3.805198749487436416, 5.799611601383225512 ) ) ;
#25081=EDGE_LOOP ( 'NONE', ( #20892, #11927, #47545, #21655 ) ) ;
#25082=EDGE_CURVE ( 'NONE', #30859, #42091, #33844, .T. ) ;
#25088=DIRECTION ( 'NONE',  ( 0.000000000000000000, 0.000000000000000000, 1.000000000000000000 ) ) ;
#25090=CARTESIAN_POINT ( 'NONE',  ( 0.000000000000000000, 6.164400007374793766, -2.900694413976553143 ) ) ;
#25099=ORIENTED_EDGE ( 'NONE', *, *, #38369, .T. ) ;
#25100=ORIENTED_EDGE ( 'NONE', *, *, #44272, .F. ) ;
#25105=LINE ( 'NONE', #5495, #8945 ) ;
#25107=FACE_OUTER_BOUND ( 'NONE', #64573, .T. ) ;
#25113=CARTESIAN_POINT ( 'NONE',  ( -27.35552965826137140, -2.548625910254533888, -1.773915698030580357 ) ) ;
#25114=ORIENTED_EDGE ( 'NONE', *, *, #35099, .T. ) ;
#25126=LINE ( 'NONE', #60358, #45538 ) ;
#25130=CARTESIAN_POINT ( 'NONE',  ( -22.66110217412718342, -4.573370147466322422, 1.880032915665391879 ) ) ;
#25154=CARTESIAN_POINT ( 'NONE',  ( -27.09030469827879628, 2.239626370111425846, 0.5638997280369931753 ) ) ;
#25155=CARTESIAN_POINT ( 'NONE',  ( -22.71097035706202405, -4.965150228107763297, -0.4203397252017324615 ) ) ;
#25161=FACE_OUTER_BOUND ( 'NONE', #25670, .T. ) ;
#25175=VERTEX_POINT ( 'NONE', #42631 ) ;
#25181=CARTESIAN_POINT ( 'NONE',  ( 2.000000000000001776, -6.606214214351077807, 2.114938770769887455 ) ) ;
#25197=LINE ( 'NONE', #45470, #6661 ) ;
#25200=DIRECTION ( 'NONE',  ( -1.000000000000000000, 0.000000000000000000, 0.000000000000000000 ) ) ;
#25206=CARTESIAN_POINT ( 'NONE',  ( 2.000000000000001776, 1.779948802829816490, 6.576141558201244131 ) ) ;
#25208=DIRECTION ( 'NONE',  ( 0.000000000000000000, -0.9868265225415244757, -0.1617819965527746984 ) ) ;
#25210=DIRECTION ( 'NONE',  ( -1.000000000000000000, 0.000000000000000000, 0.000000000000000000 ) ) ;
#25215=ADVANCED_FACE ( 'NONE', ( #4316 ), #19925, .T. ) ;
#25220=CARTESIAN_POINT ( 'NONE',  ( -27.08935880048797529, -0.5666837974560299251, 2.235999130319374029 ) ) ;
#25222=DIRECTION ( 'NONE',  ( 0.9606638835031803270, -0.1133241553124307438, 0.2535400141108146710 ) ) ;
#25226=CARTESIAN_POINT ( 'NONE',  ( 1.000000000000000888, 7.484036900328563391, 0.4890722589969403455 ) ) ;
#25229=ORIENTED_EDGE ( 'NONE', *, *, #40260, .F. ) ;
#25230=CARTESIAN_POINT ( 'NONE',  ( -27.10113028276028757, 2.245923868550873781, -0.6639289823109628674 ) ) ;
#25232=EDGE_LOOP ( 'NONE', ( #59032, #7750, #33294, #38915 ) ) ;
#25234=( BOUNDED_SURFACE ( )  B_SPLINE_SURFACE ( 3, 1, ( 
 ( #30943, #60888 ),
 ( #703, #31592 ),
 ( #41238, #15329 ),
 ( #55896, #41572 ) ),
 .UNSPECIFIED., .F., .F., .F. ) 
 B_SPLINE_SURFACE_WITH_KNOTS ( ( 4, 4 ),
 ( 2, 2 ),
 ( 0.000000000000000000, 1.000000000000000000 ),
 ( 0.000000000000000000, 1.000000000000000000 ),
 .UNSPECIFIED. ) 
 GEOMETRIC_REPRESENTATION_ITEM ( )  RATIONAL_B_SPLINE_SURFACE ( (
 ( 1.000000000000000000, 1.000000000000000000),
 ( 0.9932032654565553509, 0.8386279382598736953),
 ( 0.9932032654565553509, 0.8386279382598736953),
 ( 1.000000000000000000, 1.000000000000000000) ) ) 
 REPRESENTATION_ITEM ( '' )  SURFACE ( )  );
#25236=CARTESIAN_POINT ( 'NONE',  ( -22.27721056931765631, -3.486117586310729433, -1.183805672860834379 ) ) ;
#25243=ORIENTED_EDGE ( 'NONE', *, *, #38369, .F. ) ;
#25245=DIRECTION ( 'NONE',  ( 1.977578355587678392E-17, -0.1764146379942750364, -0.9843159429275484262 ) ) ;
#25247=CARTESIAN_POINT ( 'NONE',  ( -22.70624764888619751, -0.7939291279022604453, 5.190207123845781645 ) ) ;
#25253=ORIENTED_EDGE ( 'NONE', *, *, #65521, .T. ) ;
#25260=ORIENTED_EDGE ( 'NONE', *, *, #21842, .F. ) ;
#25267=CARTESIAN_POINT ( 'NONE',  ( -35.04643116707788408, -0.001845126042319261694, -0.01204777744935776884 ) ) ;
#25277=B_SPLINE_CURVE_WITH_KNOTS ( 'NONE', 3,
 ( #28652, #8063, #58950, #58617, #42613, #3082, #53624, #37656, #27659, #62915, #8377, #37968, #58269, #12690, #32632, #48317 ),
 .UNSPECIFIED., .F., .F.,
 ( 4, 3, 3, 3, 3, 4 ),
 ( 1.843143693225351375E-18, 6.991367980366411871E-05, 0.0001398269368981365046, 0.0002097400188389092002, 0.0002811534801551363234, 0.0003526297678872491494 ),
 .UNSPECIFIED. ) ;
#25279=CIRCLE ( 'NONE', #7227, 7.499999999999988454 ) ;
#25280=ADVANCED_FACE ( 'NONE', ( #38312 ), #63256, .T. ) ;
#25284=EDGE_CURVE ( 'NONE', #9839, #42155, #25360, .T. ) ;
#25289=EDGE_CURVE ( 'NONE', #33280, #19513, #54541, .T. ) ;
#25290=FACE_OUTER_BOUND ( 'NONE', #54695, .T. ) ;
#25296=EDGE_CURVE ( 'NONE', #33192, #50535, #60481, .T. ) ;
#25299=EDGE_CURVE ( 'NONE', #6060, #49356, #19280, .T. ) ;
#25304=B_SPLINE_CURVE_WITH_KNOTS ( 'NONE', 3,
 ( #65579, #20049, #440, #49663, #60607, #4103 ),
 .UNSPECIFIED., .F., .F.,
 ( 4, 2, 4 ),
 ( 0.000000000000000000, 0.0004528561986909385552, 0.0009057123973818773273 ),
 .UNSPECIFIED. ) ;
#25310=AXIS2_PLACEMENT_3D ( 'NONE', #50041, #65322, #5486 ) ;
#25312=CARTESIAN_POINT ( 'NONE',  ( 2.000000000000001776, 4.376687952327335651, 5.220963330856624118 ) ) ;
#25327=ORIENTED_EDGE ( 'NONE', *, *, #14563, .T. ) ;
#25334=CARTESIAN_POINT ( 'NONE',  ( 2.000000000000001776, 0.000000000000000000, 0.000000000000000000 ) ) ;
#25335=VERTEX_POINT ( 'NONE', #46836 ) ;
#25338=CARTESIAN_POINT ( 'NONE',  ( -22.71097035706202405, -4.965150228107763297, -0.4203397252017324615 ) ) ;
#25340=CARTESIAN_POINT ( 'NONE',  ( -22.71097035706202405, -4.089776368546547580, -2.846599994298351977 ) ) ;
#25345=CARTESIAN_POINT ( 'NONE',  ( -27.08416813689867908, 2.257587568255730037, -0.3912215308406206127 ) ) ;
#25349=CARTESIAN_POINT ( 'NONE',  ( -22.70624764888619751, -5.190207123845783421, -0.7939291279022795411 ) ) ;
#25350=VERTEX_POINT ( 'NONE', #11266 ) ;
#25360=CIRCLE ( 'NONE', #7306, 7.499999999999988454 ) ;
#25364=CIRCLE ( 'NONE', #40201, 2.899999999999995026 ) ;
#25365=VECTOR ( 'NONE', #56594, 1000.000000000000000 ) ;
#25369=CIRCLE ( 'NONE', #59355, 2.899999999999994582 ) ;
#25379=CARTESIAN_POINT ( 'NONE',  ( 2.000000000000001776, 3.341639490130761114, 6.078525953551427996 ) ) ;
#25386=DIRECTION ( 'NONE',  ( 0.000000000000000000, 0.4198891015602657650, -0.9075754196709565624 ) ) ;
#25398=EDGE_LOOP ( 'NONE', ( #54489, #60214, #35357, #29461 ) ) ;
#25404=AXIS2_PLACEMENT_3D ( 'NONE', #3674, #13920, #64160 ) ;
#25406=DIRECTION ( 'NONE',  ( 0.000000000000000000, 0.000000000000000000, 1.000000000000000000 ) ) ;
#25411=ORIENTED_EDGE ( 'NONE', *, *, #48608, .T. ) ;
#25416=AXIS2_PLACEMENT_3D ( 'NONE', #54974, #14401, #15702 ) ;
#25430=VERTEX_POINT ( 'NONE', #16252 ) ;
#25432=ADVANCED_FACE ( 'NONE', ( #56147 ), #37874, .F. ) ;
#25434=CARTESIAN_POINT ( 'NONE',  ( -27.08704841010922948, -2.291653842312380895, 0.1930432016059762668 ) ) ;
#25435=CARTESIAN_POINT ( 'NONE',  ( -22.31328051695926007, 0.8849444482788259014, -3.685074213229314388 ) ) ;
#25440=ORIENTED_EDGE ( 'NONE', *, *, #29727, .T. ) ;
#25450=FACE_OUTER_BOUND ( 'NONE', #39455, .T. ) ;
#25454=CARTESIAN_POINT ( 'NONE',  ( -27.08423923533013777, -2.107995711831556651, -0.8983804370399715022 ) ) ;
#25461=ADVANCED_FACE ( 'NONE', ( #52153 ), #12800, .F. ) ;
#25464=ORIENTED_EDGE ( 'NONE', *, *, #25296, .T. ) ;
#25469=CARTESIAN_POINT ( 'NONE',  ( 0.000000000000000000, 6.936109781200720192, -2.853135311044974198 ) ) ;
#25470=DIRECTION ( 'NONE',  ( 0.000000000000000000, 0.000000000000000000, -1.000000000000000000 ) ) ;
#25471=CARTESIAN_POINT ( 'NONE',  ( -22.27878402819508352, -0.9624056734348174214, -3.558531829368164257 ) ) ;
#25477=CARTESIAN_POINT ( 'NONE',  ( -27.04788180060269198, -3.218072544330550677, -0.2724356095623453045 ) ) ;
#25486=ORIENTED_EDGE ( 'NONE', *, *, #57420, .F. ) ;
#25495=DIRECTION ( 'NONE',  ( -1.000000000000000000, 0.000000000000000000, 0.000000000000000000 ) ) ;
#25504=CARTESIAN_POINT ( 'NONE',  ( 2.000000000000001776, 3.230174184210066191, 5.998318953995321223 ) ) ;
#25508=CARTESIAN_POINT ( 'NONE',  ( 0.000000000000000000, 0.000000000000000000, 0.000000000000000000 ) ) ;
#25520=CYLINDRICAL_SURFACE ( 'NONE', #64989, 6.936499999999988120 ) ;
#25524=VECTOR ( 'NONE', #46177, 999.9999999999998863 ) ;
#25525=AXIS2_PLACEMENT_3D ( 'NONE', #38270, #58594, #17011 ) ;
#25527=AXIS2_PLACEMENT_3D ( 'NONE', #17965, #64796, #28269 ) ;
#25537=DIRECTION ( 'NONE',  ( -1.000000000000000000, 0.000000000000000000, 0.000000000000000000 ) ) ;
#25540=CIRCLE ( 'NONE', #47865, 7.499999999999988454 ) ;
#25542=AXIS2_PLACEMENT_3D ( 'NONE', #56962, #57281, #5437 ) ;
#25544=VECTOR ( 'NONE', #67, 1000.000000000000000 ) ;
#25547=CIRCLE ( 'NONE', #10837, 2.899999999999994582 ) ;
#25548=CARTESIAN_POINT ( 'NONE',  ( -27.09342121492660738, -0.5565043948835766141, 2.251107617623969936 ) ) ;
#25551=DIRECTION ( 'NONE',  ( -1.000000000000000000, 0.000000000000000000, 0.000000000000000000 ) ) ;
#25552=B_SPLINE_CURVE_WITH_KNOTS ( 'NONE', 3,
 ( #5584, #56090, #50477, #14850, #25853, #19872, #258, #9541, #16194, #10529, #46144, #45145, #589, #20851, #35138, #61401, #45456, #65721, #20193 ),
 .UNSPECIFIED., .F., .F.,
 ( 4, 3, 3, 3, 3, 3, 4 ),
 ( 0.000000000000000000, 2.836829842860372840E-05, 4.224792512343171551E-05, 5.612066614707813677E-05, 6.998859278151645395E-05, 9.832141287888645782E-05, 0.0001178161482480164814 ),
 .UNSPECIFIED. ) ;
#25554=CARTESIAN_POINT ( 'NONE',  ( -35.04709527796842394, -0.007095259204982495849, 0.01012471662512753889 ) ) ;
#25557=ORIENTED_EDGE ( 'NONE', *, *, #24301, .T. ) ;
#25568=EDGE_LOOP ( 'NONE', ( #52422, #9738, #47384, #35748 ) ) ;
#25571=VERTEX_POINT ( 'NONE', #17560 ) ;
#25572=CARTESIAN_POINT ( 'NONE',  ( -35.05012975565874456, -0.002073729464865227325, -0.01377677982612606281 ) ) ;
#25573=CIRCLE ( 'NONE', #60610, 2.899999999999995026 ) ;
#25574=CARTESIAN_POINT ( 'NONE',  ( -27.08456565417846207, 1.867985369021581299, -1.328664661356733445 ) ) ;
#25595=AXIS2_PLACEMENT_3D ( 'NONE', #33186, #27880, #2641 ) ;
#25598=AXIS2_PLACEMENT_3D ( 'NONE', #8682, #13652, #3730 ) ;
#25607=CARTESIAN_POINT ( 'NONE',  ( -27.09569413923794912, 0.6513788562879481159, 2.232620870184064188 ) ) ;
#25612=DIRECTION ( 'NONE',  ( 1.000000000000000000, -0.000000000000000000, -0.000000000000000000 ) ) ;
#25617=VECTOR ( 'NONE', #61177, 1000.000000000000000 ) ;
#25640=ORIENTED_EDGE ( 'NONE', *, *, #63652, .F. ) ;
#25641=CIRCLE ( 'NONE', #59645, 2.899999999999996358 ) ;
#25645=CARTESIAN_POINT ( 'NONE',  ( 2.000000000000001776, -6.470132594555817462, 2.133363481234057168 ) ) ;
#25648=ORIENTED_EDGE ( 'NONE', *, *, #49925, .T. ) ;
#25649=AXIS2_PLACEMENT_3D ( 'NONE', #61025, #6479, #36405 ) ;
#25650=ORIENTED_EDGE ( 'NONE', *, *, #41966, .F. ) ;
#25661=DIRECTION ( 'NONE',  ( 0.000000000000000000, 0.000000000000000000, 1.000000000000000000 ) ) ;
#25669=LINE ( 'NONE', #65251, #28397 ) ;
#25670=EDGE_LOOP ( 'NONE', ( #22450, #9281, #53950, #13285 ) ) ;
#25675=CIRCLE ( 'NONE', #24635, 6.936499999999989008 ) ;
#25694=CARTESIAN_POINT ( 'NONE',  ( -22.31328051695926007, 1.671726071983979711, -3.401210163132561082 ) ) ;
#25695=CIRCLE ( 'NONE', #14004, 7.499999999999988454 ) ;
#25703=CARTESIAN_POINT ( 'NONE',  ( 0.000000000000000000, 5.097042323172538580, -5.501832381651401427 ) ) ;
#25707=CARTESIAN_POINT ( 'NONE',  ( 0.000000000000000000, -6.906413915731192787, 0.6453518998147164121 ) ) ;
#25710=CARTESIAN_POINT ( 'NONE',  ( -27.09048036756547972, -0.9969423855787317157, 2.083857239072904211 ) ) ;
#25711=CIRCLE ( 'NONE', #9748, 7.499999999999988454 ) ;
#25715=VERTEX_POINT ( 'NONE', #30142 ) ;
#25719=AXIS2_PLACEMENT_3D ( 'NONE', #1754, #54516, #28567 ) ;
#25722=AXIS2_PLACEMENT_3D ( 'NONE', #60443, #4935, #35154 ) ;
#25724=DIRECTION ( 'NONE',  ( 0.000000000000000000, -0.9635499925192253512, 0.2675283385292120397 ) ) ;
#25726=ORIENTED_EDGE ( 'NONE', *, *, #46394, .F. ) ;
#25728=DIRECTION ( 'NONE',  ( -1.000000000000000000, 0.000000000000000000, 0.000000000000000000 ) ) ;
#25735=ORIENTED_EDGE ( 'NONE', *, *, #36346, .T. ) ;
#25745=CIRCLE ( 'NONE', #38505, 7.499999999999988454 ) ;
#25747=AXIS2_PLACEMENT_3D ( 'NONE', #24865, #24520, #9536 ) ;
#25755=DIRECTION ( 'NONE',  ( -1.000000000000000000, 0.000000000000000000, 0.000000000000000000 ) ) ;
#25758=CARTESIAN_POINT ( 'NONE',  ( -22.27710395300133328, -0.9764373854729024860, 3.549456197028676208 ) ) ;
#25762=FACE_OUTER_BOUND ( 'NONE', #40715, .T. ) ;
#25768=ORIENTED_EDGE ( 'NONE', *, *, #50269, .T. ) ;
#25775=CARTESIAN_POINT ( 'NONE',  ( -22.28694879868232803, 0.9088670759108249397, -3.597828382597549446 ) ) ;
#25777=EDGE_CURVE ( 'NONE', #35536, #39745, #554, .T. ) ;
#25783=ORIENTED_EDGE ( 'NONE', *, *, #61056, .F. ) ;
#25785=DIRECTION ( 'NONE',  ( -1.000000000000000000, 0.000000000000000000, 0.000000000000000000 ) ) ;
#25795=CARTESIAN_POINT ( 'NONE',  ( -35.04643116707788408, -0.002453861112623398344, -0.01193867652721398998 ) ) ;
#25800=EDGE_CURVE ( 'NONE', #30228, #5306, #45756, .T. ) ;
#25812=AXIS2_PLACEMENT_3D ( 'NONE', #7579, #32501, #1630 ) ;
#25817=DIRECTION ( 'NONE',  ( 1.000000000000000000, -0.000000000000000000, -0.000000000000000000 ) ) ;
#25818=CIRCLE ( 'NONE', #26914, 6.936499999999990784 ) ;
#25819=AXIS2_PLACEMENT_3D ( 'NONE', #5974, #46198, #19616 ) ;
#25824=CARTESIAN_POINT ( 'NONE',  ( -27.28573687977896611, -2.862048090118451071, -0.4470060700698573197 ) ) ;
#25826=DIRECTION ( 'NONE',  ( 0.000000000000000000, 0.1081190184239417817, -0.9941379571543595972 ) ) ;
#25836=EDGE_CURVE ( 'NONE', #34412, #30073, #33893, .T. ) ;
#25838=AXIS2_PLACEMENT_3D ( 'NONE', #3521, #62680, #42724 ) ;
#25841=VERTEX_POINT ( 'NONE', #15165 ) ;
#25842=CARTESIAN_POINT ( 'NONE',  ( 0.000000000000000000, 0.000000000000000000, 0.000000000000000000 ) ) ;
#25843=AXIS2_PLACEMENT_3D ( 'NONE', #43311, #54302, #58645 ) ;
#25845=CARTESIAN_POINT ( 'NONE',  ( -22.27709082389155171, -1.005749854561698298, 3.541295940224338246 ) ) ;
#25847=AXIS2_PLACEMENT_3D ( 'NONE', #28304, #28962, #23984 ) ;
#25850=VERTEX_POINT ( 'NONE', #10497 ) ;
#25853=CARTESIAN_POINT ( 'NONE',  ( -27.09729107899853062, 2.324833743198347236, -0.1622107421537140326 ) ) ;
#25857=CARTESIAN_POINT ( 'NONE',  ( 2.000000000000001776, -0.4804830611969332366, -6.919838746524582085 ) ) ;
#25858=AXIS2_PLACEMENT_3D ( 'NONE', #5185, #61674, #30752 ) ;
#25866=AXIS2_PLACEMENT_3D ( 'NONE', #45257, #60881, #19981 ) ;
#25877=CARTESIAN_POINT ( 'NONE',  ( -22.28629837673887693, -3.697248502489102417, 0.2936941584814368733 ) ) ;
#25882=VERTEX_POINT ( 'NONE', #22120 ) ;
#25884=DIRECTION ( 'NONE',  ( 0.000000000000000000, 0.000000000000000000, -1.000000000000000000 ) ) ;
#25885=CARTESIAN_POINT ( 'NONE',  ( 2.000000000000001776, -0.3246585432985730213, -6.805031400696120336 ) ) ;
#25887=CARTESIAN_POINT ( 'NONE',  ( -22.49803948133828513, 3.817825231362860450, 2.073427785788346522 ) ) ;
#25888=CIRCLE ( 'NONE', #37562, 7.499999999999988454 ) ;
#25891=CARTESIAN_POINT ( 'NONE',  ( 2.000000000000001776, 6.253963800348250501, 4.139799123621038746 ) ) ;
#25907=CARTESIAN_POINT ( 'NONE',  ( -22.27715526084302056, -3.395518526174221563, -1.423304177213884580 ) ) ;
#25908=LINE ( 'NONE', #15898, #57678 ) ;
#25916=EDGE_LOOP ( 'NONE', ( #27561, #58260, #65644, #3529 ) ) ;
#25931=FACE_OUTER_BOUND ( 'NONE', #18976, .T. ) ;
#25934=ORIENTED_EDGE ( 'NONE', *, *, #5578, .F. ) ;
#25936=ORIENTED_EDGE ( 'NONE', *, *, #54218, .T. ) ;
#25949=VECTOR ( 'NONE', #32370, 1000.000000000000000 ) ;
#25955=CARTESIAN_POINT ( 'NONE',  ( -28.66013792860432119, 1.490739498621024284, -1.071635578228289587 ) ) ;
#25958=VECTOR ( 'NONE', #15308, 1000.000000000000000 ) ;
#25961=VERTEX_POINT ( 'NONE', #44283 ) ;
#25966=CARTESIAN_POINT ( 'NONE',  ( -35.04834644901396956, -0.01183641858481921869, 0.007161132384413747970 ) ) ;
#25989=EDGE_LOOP ( 'NONE', ( #11723, #57394, #27063, #24288 ) ) ;
#25991=EDGE_LOOP ( 'NONE', ( #11051, #28611, #31300, #58088 ) ) ;
#25999=CARTESIAN_POINT ( 'NONE',  ( 0.000000000000000000, 3.937687286050817193, 6.383151168292468647 ) ) ;
#26000=ORIENTED_EDGE ( 'NONE', *, *, #40687, .F. ) ;
#26005=DIRECTION ( 'NONE',  ( 0.000000000000000000, 0.4198891015602590482, 0.9075754196709594490 ) ) ;
#26006=VERTEX_POINT ( 'NONE', #9685 ) ;
#26007=CARTESIAN_POINT ( 'NONE',  ( 2.000000000000001776, 6.883677378339475794, 0.8544109087186002593 ) ) ;
#26011=DIRECTION ( 'NONE',  ( -1.000000000000000000, 0.000000000000000000, 0.000000000000000000 ) ) ;
#26013=CARTESIAN_POINT ( 'NONE',  ( -22.65999102136919419, -3.858590659383846155, -2.911035239830930710 ) ) ;
#26016=CARTESIAN_POINT ( 'NONE',  ( -27.08418179957658367, 2.244544746853584627, -0.4604195552868197705 ) ) ;
#26020=CARTESIAN_POINT ( 'NONE',  ( -35.05175862995318425, -0.007207337213509246165, -0.01030783735685852909 ) ) ;
#26021=AXIS2_PLACEMENT_3D ( 'NONE', #15470, #45731, #50080 ) ;
#26026=EDGE_CURVE ( 'NONE', #10792, #57938, #45616, .T. ) ;
#26031=FACE_OUTER_BOUND ( 'NONE', #53821, .T. ) ;
#26037=ORIENTED_EDGE ( 'NONE', *, *, #51308, .F. ) ;
#26046=FACE_OUTER_BOUND ( 'NONE', #65307, .T. ) ;
#26048=EDGE_CURVE ( 'NONE', #56404, #28290, #9478, .T. ) ;
#26055=CARTESIAN_POINT ( 'NONE',  ( -26.74023318801843629, -1.916028097164416133, 2.752802096869872983 ) ) ;
#26063=CARTESIAN_POINT ( 'NONE',  ( -22.27715526084302056, 3.395518526174225560, 1.423304177213846167 ) ) ;
#26075=CARTESIAN_POINT ( 'NONE',  ( 2.000000000000001776, -6.164400007374799095, 2.900694413976478536 ) ) ;
#26077=LINE ( 'NONE', #56314, #34371 ) ;
#26078=CARTESIAN_POINT ( 'NONE',  ( 2.000000000000001776, 5.860254403322073813, -3.474373880649762381 ) ) ;
#26079=ORIENTED_EDGE ( 'NONE', *, *, #33263, .T. ) ;
#26088=ORIENTED_EDGE ( 'NONE', *, *, #34947, .F. ) ;
#26098=VERTEX_POINT ( 'NONE', #10032 ) ;
#26100=ORIENTED_EDGE ( 'NONE', *, *, #13728, .T. ) ;
#26103=ORIENTED_EDGE ( 'NONE', *, *, #3331, .F. ) ;
#26104=DIRECTION ( 'NONE',  ( 0.000000000000000000, 0.6051742151937661296, -0.7960930657056429771 ) ) ;
#26127=DIRECTION ( 'NONE',  ( 0.000000000000000000, 0.3193015301359806712, -0.9476531711828022342 ) ) ;
#26142=CARTESIAN_POINT ( 'NONE',  ( 2.000000000000001776, -6.539067737394485214, -2.314222412769890713 ) ) ;
#26149=EDGE_CURVE ( 'NONE', #3825, #28939, #47569, .T. ) ;
#26150=CARTESIAN_POINT ( 'NONE',  ( -35.05012975565874456, 0.009279204628448394984, 0.01039213056761046847 ) ) ;
#26154=CARTESIAN_POINT ( 'NONE',  ( 18.00005080000000035, 0.000000000000000000, 0.000000000000000000 ) ) ;
#26156=EDGE_CURVE ( 'NONE', #56181, #634, #51918, .T. ) ;
#26161=DIRECTION ( 'NONE',  ( -1.000000000000000000, 0.000000000000000000, 0.000000000000000000 ) ) ;
#26162=ORIENTED_EDGE ( 'NONE', *, *, #50547, .F. ) ;
#26172=ORIENTED_EDGE ( 'NONE', *, *, #25050, .T. ) ;
#26176=CARTESIAN_POINT ( 'NONE',  ( -27.09030469827880339, 0.5638997280370295906, -2.239626370111434284 ) ) ;
#26178=CARTESIAN_POINT ( 'NONE',  ( -27.09252613521593744, 1.005681546875665466, -2.086468883257839746 ) ) ;
#26180=CARTESIAN_POINT ( 'NONE',  ( -35.04709527796842394, -0.01120703303052195121, 0.005220632200989699934 ) ) ;
#26181=DIRECTION ( 'NONE',  ( 0.000000000000000000, 0.000000000000000000, 1.000000000000000000 ) ) ;
#26186=CARTESIAN_POINT ( 'NONE',  ( 2.000000000000001776, -0.4804830611970390408, 6.919838746524553663 ) ) ;
#26189=CARTESIAN_POINT ( 'NONE',  ( 2.000000000000001776, 0.000000000000000000, 0.000000000000000000 ) ) ;
#26192=AXIS2_PLACEMENT_3D ( 'NONE', #61724, #27147, #26817 ) ;
#26204=ORIENTED_EDGE ( 'NONE', *, *, #16787, .T. ) ;
#26209=DIRECTION ( 'NONE',  ( -1.000000000000000000, 0.000000000000000000, 0.000000000000000000 ) ) ;
#26216=DIRECTION ( 'NONE',  ( -1.000000000000000000, 0.000000000000000000, 0.000000000000000000 ) ) ;
#26218=CARTESIAN_POINT ( 'NONE',  ( -35.04660725145885891, -0.004999447127056843958, 0.01123650152079029053 ) ) ;
#26220=EDGE_CURVE ( 'NONE', #48023, #33594, #18011, .T. ) ;
#26224=ADVANCED_FACE ( 'NONE', ( #43548 ), #59199, .T. ) ;
#26234=VERTEX_POINT ( 'NONE', #12627 ) ;
#26242=CARTESIAN_POINT ( 'NONE',  ( -27.09833916700336687, 1.689564470273831276, 1.609723001518200247 ) ) ;
#26243=DIRECTION ( 'NONE',  ( 0.000000000000000000, 0.6876994588534194319, 0.7259954919231345061 ) ) ;
#26244=ORIENTED_EDGE ( 'NONE', *, *, #38232, .F. ) ;
#26247=CARTESIAN_POINT ( 'NONE',  ( 2.000000000000001776, -6.906413915731171471, -0.6453518998148326524 ) ) ;
#26264=ADVANCED_FACE ( 'NONE', ( #32576 ), #7779, .F. ) ;
#26265=ORIENTED_EDGE ( 'NONE', *, *, #7656, .F. ) ;
#26268=CARTESIAN_POINT ( 'NONE',  ( -27.08639648637140951, 0.6092497698725228839, 2.215564006614428205 ) ) ;
#26272=DIRECTION ( 'NONE',  ( -1.000000000000000000, 0.000000000000000000, 0.000000000000000000 ) ) ;
#26273=EDGE_CURVE ( 'NONE', #51107, #10675, #3359, .T. ) ;
#26274=ORIENTED_EDGE ( 'NONE', *, *, #57127, .F. ) ;
#26287=DIRECTION ( 'NONE',  ( -1.000000000000000000, 0.000000000000000000, 0.000000000000000000 ) ) ;
#26288=AXIS2_PLACEMENT_3D ( 'NONE', #1406, #13001, #12650 ) ;
#26293=DIRECTION ( 'NONE',  ( 0.000000000000000000, 0.000000000000000000, -1.000000000000000000 ) ) ;
#26304=ORIENTED_EDGE ( 'NONE', *, *, #59950, .T. ) ;
#26308=VECTOR ( 'NONE', #38091, 1000.000000000000000 ) ;
#26310=ORIENTED_EDGE ( 'NONE', *, *, #12585, .F. ) ;
#26312=DIRECTION ( 'NONE',  ( -1.000000000000000000, 0.000000000000000000, 0.000000000000000000 ) ) ;
#26314=ORIENTED_EDGE ( 'NONE', *, *, #31188, .T. ) ;
#26315=CARTESIAN_POINT ( 'NONE',  ( -22.29115169517546136, 0.2790989024813086417, 3.712980101756706564 ) ) ;
#26318=ORIENTED_EDGE ( 'NONE', *, *, #50641, .T. ) ;
#26327=CIRCLE ( 'NONE', #39040, 2.899999999999995026 ) ;
#26336=DIRECTION ( 'NONE',  ( -1.000000000000000000, 0.000000000000000000, 0.000000000000000000 ) ) ;
#26341=CARTESIAN_POINT ( 'NONE',  ( -27.10307689719059709, -2.250862122746733807, 0.6678239540327238766 ) ) ;
#26347=VERTEX_POINT ( 'NONE', #55841 ) ;
#26348=CARTESIAN_POINT ( 'NONE',  ( -35.04660725145885891, -0.009947898977292157080, 0.007231372203115632620 ) ) ;
#26350=B_SPLINE_CURVE_WITH_KNOTS ( 'NONE', 3,
 ( #55200, #45893, #40901, #29590, #61180, #39905, #64831, #5327, #14612, #34894 ),
 .UNSPECIFIED., .F., .F.,
 ( 4, 3, 3, 4 ),
 ( 5.401523115762579325E-05, 0.0008136511341527786004, 0.004068255670953081077, 0.005063778443040918738 ),
 .UNSPECIFIED. ) ;
#26352=EDGE_CURVE ( 'NONE', #33280, #44784, #49908, .T. ) ;
#26353=VERTEX_POINT ( 'NONE', #60160 ) ;
#26354=DIRECTION ( 'NONE',  ( 0.000000000000000000, -0.9635499925192254622, 0.2675283385292119842 ) ) ;
#26360=CIRCLE ( 'NONE', #39079, 7.499999999999988454 ) ;
#26361=CARTESIAN_POINT ( 'NONE',  ( -22.31328051695926007, 0.8849444482788259014, -3.685074213229314388 ) ) ;
#26364=VECTOR ( 'NONE', #44996, 1000.000000000000114 ) ;
#26369=VERTEX_POINT ( 'NONE', #24927 ) ;
#26371=CARTESIAN_POINT ( 'NONE',  ( -22.27720387087365239, 3.430312021254886989, 1.337073746937850860 ) ) ;
#26375=FACE_OUTER_BOUND ( 'NONE', #29781, .T. ) ;
#26381=EDGE_CURVE ( 'NONE', #47012, #4327, #59851, .T. ) ;
#26386=CARTESIAN_POINT ( 'NONE',  ( 2.000000000000001776, 0.000000000000000000, 0.000000000000000000 ) ) ;
#26390=DIRECTION ( 'NONE',  ( -1.000000000000000000, 0.000000000000000000, 0.000000000000000000 ) ) ;
#26394=ORIENTED_EDGE ( 'NONE', *, *, #23838, .F. ) ;
#26396=ORIENTED_EDGE ( 'NONE', *, *, #32715, .T. ) ;
#26404=VERTEX_POINT ( 'NONE', #50206 ) ;
#26408=EDGE_LOOP ( 'NONE', ( #27932, #65536, #44316, #13171 ) ) ;
#26409=VECTOR ( 'NONE', #36914, 1000.000000000000000 ) ;
#26413=ADVANCED_FACE ( 'NONE', ( #44868 ), #55511, .T. ) ;
#26415=ORIENTED_EDGE ( 'NONE', *, *, #18769, .T. ) ;
#26422=FACE_OUTER_BOUND ( 'NONE', #36086, .T. ) ;
#26441=DIRECTION ( 'NONE',  ( 0.000000000000000000, 0.8835120444460210498, 0.4684084406997938155 ) ) ;
#26445=AXIS2_PLACEMENT_3D ( 'NONE', #22793, #27425, #57374 ) ;
#26457=DIRECTION ( 'NONE',  ( 0.000000000000000000, -0.9868265225415276953, 0.1617819965527551584 ) ) ;
#26463=DIRECTION ( 'NONE',  ( -1.000000000000000000, 0.000000000000000000, 0.000000000000000000 ) ) ;
#26475=EDGE_CURVE ( 'NONE', #50103, #10610, #9525, .T. ) ;
#26483=ORIENTED_EDGE ( 'NONE', *, *, #52025, .F. ) ;
#26493=LINE ( 'NONE', #21524, #34868 ) ;
#26507=ADVANCED_FACE ( 'NONE', ( #53486 ), #28201, .T. ) ;
#26511=EDGE_CURVE ( 'NONE', #7359, #20437, #18053, .T. ) ;
#26519=DIRECTION ( 'NONE',  ( 0.000000000000000000, 0.000000000000000000, 1.000000000000000000 ) ) ;
#26523=AXIS2_PLACEMENT_3D ( 'NONE', #58948, #3080, #18026 ) ;
#26525=LINE ( 'NONE', #1279, #2176 ) ;
#26528=DIRECTION ( 'NONE',  ( -1.000000000000000000, 0.000000000000000000, 0.000000000000000000 ) ) ;
#26532=DIRECTION ( 'NONE',  ( -1.000000000000000000, 0.000000000000000000, 0.000000000000000000 ) ) ;
#26535=AXIS2_PLACEMENT_3D ( 'NONE', #23207, #47502, #47821 ) ;
#26545=LINE ( 'NONE', #51526, #31120 ) ;
#26555=B_SPLINE_CURVE_WITH_KNOTS ( 'NONE', 3,
 ( #42617, #38643, #53941, #37659, #53286, #57957, #2427, #12050, #27340, #22704, #32328, #7067, #13364, #8381, #42967, #23028, #17385, #17714, #33651, #47325, #47634, #53628 ),
 .UNSPECIFIED., .F., .F.,
 ( 4, 3, 3, 3, 3, 3, 3, 4 ),
 ( 1.371419323662817635E-18, 4.455945684386977945E-05, 6.636307477204154645E-05, 8.816671873159025760E-05, 0.0001099660380492627801, 0.0001317545563165332175, 0.0001762613022895079989, 0.0001867992666138373426 ),
 .UNSPECIFIED. ) ;
#26559=CARTESIAN_POINT ( 'NONE',  ( -27.10719052120871098, 1.714424047991082389, 1.622102031466668093 ) ) ;
#26560=ORIENTED_EDGE ( 'NONE', *, *, #22552, .F. ) ;
#26562=CARTESIAN_POINT ( 'NONE',  ( -22.49803948133827092, 2.073427785788399813, -3.817825231362854677 ) ) ;
#26570=ORIENTED_EDGE ( 'NONE', *, *, #30968, .F. ) ;
#26571=VERTEX_POINT ( 'NONE', #62773 ) ;
#26573=CARTESIAN_POINT ( 'NONE',  ( -22.27721688985630522, -2.843753050855867937, 2.338410344701243648 ) ) ;
#26576=CIRCLE ( 'NONE', #48903, 2.899999999999994582 ) ;
#26581=CARTESIAN_POINT ( 'NONE',  ( 0.000000000000000000, 0.000000000000000000, 0.000000000000000000 ) ) ;
#26583=B_SPLINE_CURVE_WITH_KNOTS ( 'NONE', 3,
 ( #37167, #22554, #41495, #57476, #12544, #61791, #56836, #51833, #6281, #11901, #52500, #6933, #27203, #47495, #62766, #48170 ),
 .UNSPECIFIED., .F., .F.,
 ( 4, 3, 3, 3, 3, 4 ),
 ( 6.079513230985732741E-18, 6.991367980366406450E-05, 0.0001398269368981362064, 0.0002097400188389093899, 0.0002811534801551362692, 0.0003526297678872492036 ),
 .UNSPECIFIED. ) ;
#26601=CARTESIAN_POINT ( 'NONE',  ( -27.10719052120871098, -0.6736837626858844796, -2.261993590776034235 ) ) ;
#26602=FACE_OUTER_BOUND ( 'NONE', #24401, .T. ) ;
#26607=CYLINDRICAL_SURFACE ( 'NONE', #53470, 6.936499999999988120 ) ;
#26608=DIRECTION ( 'NONE',  ( -1.000000000000000000, 0.000000000000000000, 0.000000000000000000 ) ) ;
#26611=CARTESIAN_POINT ( 'NONE',  ( 1.000000000000000888, 3.073484823194434057, -6.841322316745026555 ) ) ;
#26622=ORIENTED_EDGE ( 'NONE', *, *, #12940, .T. ) ;
#26623=CARTESIAN_POINT ( 'NONE',  ( -22.31328051695926007, 3.633840107626944871, -1.076152733467184985 ) ) ;
#26627=ORIENTED_EDGE ( 'NONE', *, *, #13093, .T. ) ;
#26632=AXIS2_PLACEMENT_3D ( 'NONE', #64264, #34641, #65246 ) ;
#26633=CARTESIAN_POINT ( 'NONE',  ( -27.05874794189610455, -0.3907329275428090276, -2.180117559290211116 ) ) ;
#26636=CIRCLE ( 'NONE', #56353, 2.899999999999995026 ) ;
#26639=VERTEX_POINT ( 'NONE', #24178 ) ;
#26649=CYLINDRICAL_SURFACE ( 'NONE', #58514, 2.899999999999994582 ) ;
#26655=CARTESIAN_POINT ( 'NONE',  ( -27.32337605527166957, -2.404211887218375754, -1.812546145273364662 ) ) ;
#26656=CARTESIAN_POINT ( 'NONE',  ( -28.66013792860432119, 0.1826938850344184129, 1.826836065344823457 ) ) ;
#26658=CARTESIAN_POINT ( 'NONE',  ( -35.05012975565874456, 0.004360246756751652575, -0.01323209221895734096 ) ) ;
#26659=CIRCLE ( 'NONE', #53200, 7.499999999999988454 ) ;
#26671=CARTESIAN_POINT ( 'NONE',  ( -27.08423805673873375, 1.573803011992720435, 1.665498649074229842 ) ) ;
#26687=AXIS2_PLACEMENT_3D ( 'NONE', #54274, #28994, #22702 ) ;
#26690=DIRECTION ( 'NONE',  ( -1.000000000000000000, 0.000000000000000000, 0.000000000000000000 ) ) ;
#26710=ORIENTED_EDGE ( 'NONE', *, *, #11402, .F. ) ;
#26712=ORIENTED_EDGE ( 'NONE', *, *, #28460, .F. ) ;
#26714=AXIS2_PLACEMENT_3D ( 'NONE', #29546, #23943, #49226 ) ;
#26718=AXIS2_PLACEMENT_3D ( 'NONE', #52789, #26209, #6265 ) ;
#26721=CARTESIAN_POINT ( 'NONE',  ( -22.28284753389937478, -3.563226652211058720, 0.9912969289936491846 ) ) ;
#26729=VERTEX_POINT ( 'NONE', #16168 ) ;
#26734=CARTESIAN_POINT ( 'NONE',  ( 0.000000000000000000, 6.750946897830741200, -1.593658756657007514 ) ) ;
#26744=VERTEX_POINT ( 'NONE', #35462 ) ;
#26745=EDGE_LOOP ( 'NONE', ( #54769, #1227, #22853, #64110 ) ) ;
#26749=ORIENTED_EDGE ( 'NONE', *, *, #44204, .F. ) ;
#26752=CARTESIAN_POINT ( 'NONE',  ( -28.66013792860432119, -0.4631296695479288905, -1.776574787184034498 ) ) ;
#26754=CARTESIAN_POINT ( 'NONE',  ( -28.66013792860432119, 1.776574787184030946, -0.4631296695479306114 ) ) ;
#26760=CARTESIAN_POINT ( 'NONE',  ( -22.28776923226071105, -3.061913732988072567, 2.100802264239994610 ) ) ;
#26762=CIRCLE ( 'NONE', #28903, 2.899999999999995470 ) ;
#26766=CIRCLE ( 'NONE', #43703, 2.899999999999995914 ) ;
#26771=CARTESIAN_POINT ( 'NONE',  ( -27.08417473062937120, 0.4370481938669439903, 2.249064769433617883 ) ) ;
#26788=CARTESIAN_POINT ( 'NONE',  ( 2.000000000000001776, -6.160607635185433750, 4.277489166005560506 ) ) ;
#26790=ORIENTED_EDGE ( 'NONE', *, *, #36659, .T. ) ;
#26791=DIRECTION ( 'NONE',  ( 1.000000000000000000, 1.685093406416449860E-16, -1.011030131491573426E-17 ) ) ;
#26793=DIRECTION ( 'NONE',  ( -1.000000000000000000, 0.000000000000000000, 0.000000000000000000 ) ) ;
#26794=ORIENTED_EDGE ( 'NONE', *, *, #36296, .F. ) ;
#26799=( BOUNDED_SURFACE ( )  B_SPLINE_SURFACE ( 3, 1, ( 
 ( #44263, #34919 ),
 ( #55229, #64536 ),
 ( #19007, #39273 ),
 ( #59570, #14002 ) ),
 .UNSPECIFIED., .F., .F., .T. ) 
 B_SPLINE_SURFACE_WITH_KNOTS ( ( 4, 4 ),
 ( 2, 2 ),
 ( 0.000000000000000000, 1.000000000000000000 ),
 ( 0.000000000000000000, 1.000000000000000000 ),
 .UNSPECIFIED. ) 
 GEOMETRIC_REPRESENTATION_ITEM ( )  RATIONAL_B_SPLINE_SURFACE ( (
 ( 1.000000000000000000, 1.000000000000000000),
 ( 0.8716676215708681896, 0.8964445200148164483),
 ( 0.8716676215708681896, 0.8964445200148164483),
 ( 1.000000000000000000, 1.000000000000000000) ) ) 
 REPRESENTATION_ITEM ( '' )  SURFACE ( )  );
#26807=B_SPLINE_CURVE_WITH_KNOTS ( 'NONE', 3,
 ( #43885, #43215, #17961, #8003, #28267, #49545, #3985, #50196, #29250, #44515, #64479, #4652, #4306, #13609, #4968, #25230, #49229, #64170, #23947 ),
 .UNSPECIFIED., .F., .F.,
 ( 4, 3, 3, 3, 3, 3, 4 ),
 ( 0.000000000000000000, 2.832085443540605422E-05, 4.217789847394686647E-05, 5.603488375046026924E-05, 6.989180858579268122E-05, 9.821094829918735453E-05, 0.0001178165571465090750 ),
 .UNSPECIFIED. ) ;
#26815=ORIENTED_EDGE ( 'NONE', *, *, #32256, .F. ) ;
#26817=DIRECTION ( 'NONE',  ( 0.000000000000000000, 0.000000000000000000, 1.000000000000000000 ) ) ;
#26818=CARTESIAN_POINT ( 'NONE',  ( -22.27713295444592845, -1.050517974989007008, 3.528329525272660749 ) ) ;
#26823=DIRECTION ( 'NONE',  ( 0.000000000000000000, 0.000000000000000000, 1.000000000000000000 ) ) ;
#26824=CARTESIAN_POINT ( 'NONE',  ( -22.59983133926798970, 4.058100437359467350, -2.272383229042361119 ) ) ;
#26832=VECTOR ( 'NONE', #35935, 1000.000000000000000 ) ;
#26872=CIRCLE ( 'NONE', #64033, 2.899999999999995470 ) ;
#26873=DIRECTION ( 'NONE',  ( -1.000000000000000000, 0.000000000000000000, 0.000000000000000000 ) ) ;
#26874=CIRCLE ( 'NONE', #64039, 7.499999999999988454 ) ;
#26885=ADVANCED_FACE ( 'NONE', ( #37425 ), #47430, .T. ) ;
#26891=ORIENTED_EDGE ( 'NONE', *, *, #15545, .T. ) ;
#26895=AXIS2_PLACEMENT_3D ( 'NONE', #49750, #59730, #55730 ) ;
#26897=CARTESIAN_POINT ( 'NONE',  ( 2.000000000000001776, 4.915517050588409376, 4.717154614762108622 ) ) ;
#26899=DIRECTION ( 'NONE',  ( 0.000000000000000000, 0.000000000000000000, 1.000000000000000000 ) ) ;
#26904=EDGE_CURVE ( 'NONE', #31041, #3171, #7845, .T. ) ;
#26907=VERTEX_POINT ( 'NONE', #62685 ) ;
#26914=AXIS2_PLACEMENT_3D ( 'NONE', #1447, #51336, #6422 ) ;
#26923=AXIS2_PLACEMENT_3D ( 'NONE', #6578, #57438, #31811 ) ;
#26929=CIRCLE ( 'NONE', #12052, 2.899999999999994582 ) ;
#26932=CARTESIAN_POINT ( 'NONE',  ( 0.000000000000000000, -5.997115278587591192, -3.485633455389576696 ) ) ;
#26947=EDGE_CURVE ( 'NONE', #1614, #57966, #63343, .T. ) ;
#26950=CARTESIAN_POINT ( 'NONE',  ( 2.000000000000001776, -4.915517050588371184, -4.717154614762162801 ) ) ;
#26951=ADVANCED_FACE ( 'NONE', ( #38074 ), #27443, .T. ) ;
#26952=PLANE ( 'NONE',  #14986 ) ;
#26963=CIRCLE ( 'NONE', #26923, 2.899999999999996803 ) ;
#26966=EDGE_CURVE ( 'NONE', #21913, #36610, #28120, .T. ) ;
#26978=FACE_OUTER_BOUND ( 'NONE', #10260, .T. ) ;
#26997=ORIENTED_EDGE ( 'NONE', *, *, #53933, .F. ) ;
#26999=( BOUNDED_SURFACE ( )  B_SPLINE_SURFACE ( 3, 1, ( 
 ( #45357, #45038 ),
 ( #44687, #40701 ),
 ( #40035, #30063 ),
 ( #60993, #50374 ) ),
 .UNSPECIFIED., .F., .F., .F. ) 
 B_SPLINE_SURFACE_WITH_KNOTS ( ( 4, 4 ),
 ( 2, 2 ),
 ( 0.000000000000000000, 1.000000000000000000 ),
 ( 0.000000000000000000, 1.000000000000000000 ),
 .UNSPECIFIED. ) 
 GEOMETRIC_REPRESENTATION_ITEM ( )  RATIONAL_B_SPLINE_SURFACE ( (
 ( 1.000000000000000000, 1.000000000000000000),
 ( 0.8716676215708681896, 0.8964445200148164483),
 ( 0.8716676215708681896, 0.8964445200148164483),
 ( 1.000000000000000000, 1.000000000000000000) ) ) 
 REPRESENTATION_ITEM ( '' )  SURFACE ( )  );
#27004=VERTEX_POINT ( 'NONE', #4827 ) ;
#27006=CIRCLE ( 'NONE', #64165, 7.499999999999988454 ) ;
#27013=ORIENTED_EDGE ( 'NONE', *, *, #41177, .F. ) ;
#27020=EDGE_CURVE ( 'NONE', #38810, #39229, #25540, .T. ) ;
#27021=CARTESIAN_POINT ( 'NONE',  ( 0.000000000000000000, 3.224464355699941720, -6.771471746881976728 ) ) ;
#27023=CYLINDRICAL_SURFACE ( 'NONE', #10615, 2.899999999999994582 ) ;
#27025=AXIS2_PLACEMENT_3D ( 'NONE', #49323, #23045, #37988 ) ;
#27036=VERTEX_POINT ( 'NONE', #24765 ) ;
#27048=CARTESIAN_POINT ( 'NONE',  ( -27.15511094194037867, -1.375165223101520784, -2.092607239484544746 ) ) ;
#27052=CARTESIAN_POINT ( 'NONE',  ( -22.30398854582847790, -3.608860109585138254, 1.062335901716044750 ) ) ;
#27054=CARTESIAN_POINT ( 'NONE',  ( 2.000000000000001776, 0.000000000000000000, 0.000000000000000000 ) ) ;
#27060=ORIENTED_EDGE ( 'NONE', *, *, #37555, .F. ) ;
#27063=ORIENTED_EDGE ( 'NONE', *, *, #41373, .T. ) ;
#27074=CARTESIAN_POINT ( 'NONE',  ( -22.30861784526116054, -3.671054459752210786, -0.8834205920623630082 ) ) ;
#27078=ORIENTED_EDGE ( 'NONE', *, *, #24018, .T. ) ;
#27079=ORIENTED_EDGE ( 'NONE', *, *, #5050, .T. ) ;
#27084=DIRECTION ( 'NONE',  ( 0.000000000000000000, 0.000000000000000000, 1.000000000000000000 ) ) ;
#27100=CARTESIAN_POINT ( 'NONE',  ( -35.04643116707788408, -0.01135624435144415301, -0.004425962698870883338 ) ) ;
#27108=EDGE_CURVE ( 'NONE', #62166, #4778, #27663, .T. ) ;
#27116=CARTESIAN_POINT ( 'NONE',  ( -35.04709527796842394, 0.01120703303052542066, -0.005220632201003577721 ) ) ;
#27123=EDGE_CURVE ( 'NONE', #63127, #38516, #42515, .T. ) ;
#27124=DIRECTION ( 'NONE',  ( 0.000000000000000000, 0.9868265225415265851, -0.1617819965527619031 ) ) ;
#27135=CARTESIAN_POINT ( 'NONE',  ( -22.27713295444592845, 2.530364014314313792, 2.673940016108976803 ) ) ;
#27147=DIRECTION ( 'NONE',  ( -1.000000000000000000, 0.000000000000000000, 0.000000000000000000 ) ) ;
#27152=ORIENTED_EDGE ( 'NONE', *, *, #59747, .F. ) ;
#27156=AXIS2_PLACEMENT_3D ( 'NONE', #53235, #18328, #44228 ) ;
#27173=CARTESIAN_POINT ( 'NONE',  ( -27.09150307427447757, 0.1754204729056442480, 2.306459590995622477 ) ) ;
#27188=VECTOR ( 'NONE', #44663, 1000.000000000000000 ) ;
#27203=CARTESIAN_POINT ( 'NONE',  ( -27.08421723179412055, -2.234476190936508733, 0.5069555058557426719 ) ) ;
#27212=CARTESIAN_POINT ( 'NONE',  ( 0.000000000000000000, 6.767909380267608022, 2.119450094687897579 ) ) ;
#27222=CARTESIAN_POINT ( 'NONE',  ( -22.35190811654613441, 1.736165297231020199, -3.498661567523014604 ) ) ;
#27225=ORIENTED_EDGE ( 'NONE', *, *, #9524, .T. ) ;
#27229=EDGE_LOOP ( 'NONE', ( #52530, #15721, #1128, #29816 ) ) ;
#27232=FACE_OUTER_BOUND ( 'NONE', #44951, .T. ) ;
#27233=ADVANCED_FACE ( 'NONE', ( #38328 ), #62605, .T. ) ;
#27238=CARTESIAN_POINT ( 'NONE',  ( -22.46225619532221884, -3.746472695305363310, -1.978788174090802876 ) ) ;
#27244=CARTESIAN_POINT ( 'NONE',  ( 2.000000000000001776, 0.000000000000000000, 0.000000000000000000 ) ) ;
#27262=LINE ( 'NONE', #16958, #29093 ) ;
#27266=FACE_OUTER_BOUND ( 'NONE', #52357, .T. ) ;
#27270=CARTESIAN_POINT ( 'NONE',  ( 2.000000000000001776, 1.693411908627302509, -7.306323022404582979 ) ) ;
#27296=DIRECTION ( 'NONE',  ( 0.000000000000000000, 0.000000000000000000, 1.000000000000000000 ) ) ;
#27298=DIRECTION ( 'NONE',  ( 0.000000000000000000, 0.000000000000000000, 1.000000000000000000 ) ) ;
#27305=DIRECTION ( 'NONE',  ( -1.000000000000000000, 0.000000000000000000, 0.000000000000000000 ) ) ;
#27306=ORIENTED_EDGE ( 'NONE', *, *, #61952, .T. ) ;
#27314=DIRECTION ( 'NONE',  ( 1.000000000000000000, -0.000000000000000000, -0.000000000000000000 ) ) ;
#27315=CIRCLE ( 'NONE', #55986, 6.936499999999992561 ) ;
#27318=CIRCLE ( 'NONE', #28376, 2.899999999999995914 ) ;
#27321=ORIENTED_EDGE ( 'NONE', *, *, #20389, .T. ) ;
#27325=CARTESIAN_POINT ( 'NONE',  ( -27.08423923533013422, 2.107995711831542884, 0.8983804370399492978 ) ) ;
#27326=CARTESIAN_POINT ( 'NONE',  ( -22.27384469013076185, 3.358914544760244869, 1.508555848190732851 ) ) ;
#27327=FACE_OUTER_BOUND ( 'NONE', #37046, .T. ) ;
#27331=EDGE_CURVE ( 'NONE', #8685, #9789, #38677, .T. ) ;
#27337=DIRECTION ( 'NONE',  ( -1.000000000000000000, 0.000000000000000000, 0.000000000000000000 ) ) ;
#27340=CARTESIAN_POINT ( 'NONE',  ( -22.29018399051993526, -2.675685774027730002, -2.585196332786389384 ) ) ;
#27343=CARTESIAN_POINT ( 'NONE',  ( -22.94572469358971389, 2.078200699019463915, 4.424217216616495030 ) ) ;
#27346=ORIENTED_EDGE ( 'NONE', *, *, #206, .T. ) ;
#27347=CARTESIAN_POINT ( 'NONE',  ( -22.27719443589224113, -3.601617131804399907, 0.7635131876695111508 ) ) ;
#27353=VERTEX_POINT ( 'NONE', #44965 ) ;
#27355=EDGE_LOOP ( 'NONE', ( #45422, #25327, #53971, #43044 ) ) ;
#27358=AXIS2_PLACEMENT_3D ( 'NONE', #43322, #32671, #48354 ) ;
#27365=( BOUNDED_SURFACE ( )  B_SPLINE_SURFACE ( 3, 1, ( 
 ( #48232, #18283 ),
 ( #59817, #53191 ),
 ( #12948, #48865 ),
 ( #33565, #33876 ) ),
 .UNSPECIFIED., .F., .F., .F. ) 
 B_SPLINE_SURFACE_WITH_KNOTS ( ( 4, 4 ),
 ( 2, 2 ),
 ( 0.000000000000000000, 1.000000000000000000 ),
 ( 0.000000000000000000, 1.000000000000000000 ),
 .UNSPECIFIED. ) 
 GEOMETRIC_REPRESENTATION_ITEM ( )  RATIONAL_B_SPLINE_SURFACE ( (
 ( 1.000000000000000000, 1.000000000000000000),
 ( 0.9932032654565553509, 0.8386279382598740284),
 ( 0.9932032654565553509, 0.8386279382598740284),
 ( 1.000000000000000000, 1.000000000000000000) ) ) 
 REPRESENTATION_ITEM ( '' )  SURFACE ( )  );
#27368=DIRECTION ( 'NONE',  ( -1.000000000000000000, 0.000000000000000000, 0.000000000000000000 ) ) ;
#27372=EDGE_LOOP ( 'NONE', ( #60343, #28171, #31552, #45036 ) ) ;
#27375=ORIENTED_EDGE ( 'NONE', *, *, #58338, .T. ) ;
#27378=B_SPLINE_CURVE_WITH_KNOTS ( 'NONE', 3,
 ( #8456, #37396, #52713, #38383, #57706, #32401, #53024, #43698, #23096, #12127 ),
 .UNSPECIFIED., .F., .F.,
 ( 4, 3, 3, 4 ),
 ( 5.401523115762941855E-05, 0.0008136511341527816361, 0.004068255670953097557, 0.005063778443040919605 ),
 .UNSPECIFIED. ) ;
#27381=EDGE_CURVE ( 'NONE', #22857, #28767, #45719, .T. ) ;
#27386=ORIENTED_EDGE ( 'NONE', *, *, #27955, .F. ) ;
#27389=EDGE_CURVE ( 'NONE', #19030, #60178, #53968, .T. ) ;
#27390=ORIENTED_EDGE ( 'NONE', *, *, #60266, .F. ) ;
#27398=CARTESIAN_POINT ( 'NONE',  ( -22.27720412283625961, -0.7407051501189847453, -3.606406551442380870 ) ) ;
#27402=VECTOR ( 'NONE', #60683, 1000.000000000000114 ) ;
#27403=CARTESIAN_POINT ( 'NONE',  ( -22.31328051695926007, -3.148362328073157190, 2.109671368890621679 ) ) ;
#27406=CARTESIAN_POINT ( 'NONE',  ( -35.04582288351658548, -0.0001464581945162154444, -0.01270482153516100908 ) ) ;
#27410=EDGE_CURVE ( 'NONE', #28290, #50412, #43613, .T. ) ;
#27417=CARTESIAN_POINT ( 'NONE',  ( 0.000000000000000000, -5.769711778877344877, 4.791703871138500936 ) ) ;
#27424=DIRECTION ( 'NONE',  ( 0.000000000000000000, 0.000000000000000000, 1.000000000000000000 ) ) ;
#27425=DIRECTION ( 'NONE',  ( -1.000000000000000000, 0.000000000000000000, 0.000000000000000000 ) ) ;
#27426=ORIENTED_EDGE ( 'NONE', *, *, #57069, .F. ) ;
#27427=LINE ( 'NONE', #22448, #41461 ) ;
#27429=VERTEX_POINT ( 'NONE', #54937 ) ;
#27430=ORIENTED_EDGE ( 'NONE', *, *, #23005, .F. ) ;
#27434=VERTEX_POINT ( 'NONE', #45291 ) ;
#27435=CARTESIAN_POINT ( 'NONE',  ( 0.000000000000000000, -5.814643797626899868, -3.550179297009637747 ) ) ;
#27436=EDGE_CURVE ( 'NONE', #27036, #43191, #29538, .T. ) ;
#27438=CIRCLE ( 'NONE', #869, 2.899999999999993694 ) ;
#27439=CYLINDRICAL_SURFACE ( 'NONE', #40736, 7.499999999999988454 ) ;
#27440=CARTESIAN_POINT ( 'NONE',  ( -27.35552965826135008, 3.094132632038936404, 0.2619431035391969198 ) ) ;
#27443=CYLINDRICAL_SURFACE ( 'NONE', #46808, 7.499999999999988454 ) ;
#27445=VECTOR ( 'NONE', #31258, 1000.000000000000000 ) ;
#27446=CYLINDRICAL_SURFACE ( 'NONE', #33045, 2.899999999999994582 ) ;
#27462=DIRECTION ( 'NONE',  ( 0.000000000000000000, -0.2149704402110114709, -0.9766205557100894330 ) ) ;
#27464=ORIENTED_EDGE ( 'NONE', *, *, #32386, .T. ) ;
#27468=EDGE_CURVE ( 'NONE', #21918, #35321, #64872, .T. ) ;
#27469=CARTESIAN_POINT ( 'NONE',  ( -27.08954555554372590, 0.9924303381770641641, -2.082904663687288771 ) ) ;
#27470=CARTESIAN_POINT ( 'NONE',  ( 2.000000000000001776, -4.962980376314093611, 4.846014654777763830 ) ) ;
#27471=CARTESIAN_POINT ( 'NONE',  ( -27.08430418657511751, -1.863523114788417701, 1.333569526608693767 ) ) ;
#27474=ORIENTED_EDGE ( 'NONE', *, *, #50707, .F. ) ;
#27476=CIRCLE ( 'NONE', #31733, 7.499999999999988454 ) ;
#27483=VECTOR ( 'NONE', #54855, 1000.000000000000000 ) ;
#27486=CARTESIAN_POINT ( 'NONE',  ( -27.10719052120871098, 0.1538293304135379680, 2.355164825213503121 ) ) ;
#27498=CARTESIAN_POINT ( 'NONE',  ( -26.74023318801844340, -0.2829279580741936306, 3.342010596062582106 ) ) ;
#27503=DIRECTION ( 'NONE',  ( -1.000000000000000000, 0.000000000000000000, 0.000000000000000000 ) ) ;
#27508=CYLINDRICAL_SURFACE ( 'NONE', #16144, 2.899999999999994582 ) ;
#27509=DIRECTION ( 'NONE',  ( -1.000000000000000000, 0.000000000000000000, 0.000000000000000000 ) ) ;
#27511=FACE_OUTER_BOUND ( 'NONE', #7050, .T. ) ;
#27535=EDGE_CURVE ( 'NONE', #20211, #62601, #63789, .T. ) ;
#27541=CARTESIAN_POINT ( 'NONE',  ( -35.04643116707788408, 0.009511118309135299653, -0.007621814750509436909 ) ) ;
#27548=DIRECTION ( 'NONE',  ( 0.000000000000000000, -0.8276889981568955612, 0.5611870653623749483 ) ) ;
#27553=EDGE_CURVE ( 'NONE', #44784, #50728, #23552, .T. ) ;
#27554=DIRECTION ( 'NONE',  ( -1.000000000000000000, 0.000000000000000000, 0.000000000000000000 ) ) ;
#27559=CARTESIAN_POINT ( 'NONE',  ( -22.38932658256920050, -3.587092141214311525, -1.810630688302303559 ) ) ;
#27560=( BOUNDED_SURFACE ( )  B_SPLINE_SURFACE ( 3, 1, ( 
 ( #15414, #49392 ),
 ( #25075, #39366 ),
 ( #45343, #126 ),
 ( #59669, #65606 ) ),
 .UNSPECIFIED., .F., .F., .F. ) 
 B_SPLINE_SURFACE_WITH_KNOTS ( ( 4, 4 ),
 ( 2, 2 ),
 ( 0.000000000000000000, 1.000000000000000000 ),
 ( 0.000000000000000000, 1.000000000000000000 ),
 .UNSPECIFIED. ) 
 GEOMETRIC_REPRESENTATION_ITEM ( )  RATIONAL_B_SPLINE_SURFACE ( (
 ( 1.000000000000000000, 1.000000000000000000),
 ( 0.9932032654565553509, 0.8386279382598740284),
 ( 0.9932032654565553509, 0.8386279382598740284),
 ( 1.000000000000000000, 1.000000000000000000) ) ) 
 REPRESENTATION_ITEM ( '' )  SURFACE ( )  );
#27561=ORIENTED_EDGE ( 'NONE', *, *, #4540, .T. ) ;
#27563=CARTESIAN_POINT ( 'NONE',  ( -22.27721038036499834, 2.858424446490944959, -2.320305412324239036 ) ) ;
#27564=CYLINDRICAL_SURFACE ( 'NONE', #52309, 7.499999999999988454 ) ;
#27571=DIRECTION ( 'NONE',  ( -1.000000000000000000, 0.000000000000000000, 0.000000000000000000 ) ) ;
#27576=CARTESIAN_POINT ( 'NONE',  ( 0.000000000000000000, -1.956810415765137368, -6.654767106875573823 ) ) ;
#27586=DIRECTION ( 'NONE',  ( -1.000000000000000000, 0.000000000000000000, 0.000000000000000000 ) ) ;
#27587=EDGE_LOOP ( 'NONE', ( #4833, #15750, #37825, #42163 ) ) ;
#27593=EDGE_CURVE ( 'NONE', #59964, #34255, #17606, .T. ) ;
#27594=ORIENTED_EDGE ( 'NONE', *, *, #57543, .F. ) ;
#27599=CARTESIAN_POINT ( 'NONE',  ( -22.30078715814471479, -2.097357782488222799, -3.111489293522219146 ) ) ;
#27601=ORIENTED_EDGE ( 'NONE', *, *, #61536, .T. ) ;
#27605=VECTOR ( 'NONE', #20958, 1000.000000000000000 ) ;
#27606=DIRECTION ( 'NONE',  ( 0.000000000000000000, 0.000000000000000000, -1.000000000000000000 ) ) ;
#27608=EDGE_CURVE ( 'NONE', #14035, #62269, #41529, .T. ) ;
#27610=DIRECTION ( 'NONE',  ( 0.000000000000000000, -0.3193015301359870550, 0.9476531711828000137 ) ) ;
#27614=DIRECTION ( 'NONE',  ( -1.000000000000000000, 0.000000000000000000, 0.000000000000000000 ) ) ;
#27617=ORIENTED_EDGE ( 'NONE', *, *, #49473, .F. ) ;
#27620=EDGE_CURVE ( 'NONE', #46658, #65174, #63834, .T. ) ;
#27627=CARTESIAN_POINT ( 'NONE',  ( -22.29570301036918778, 3.629130197778204003, 0.8918611685730862826 ) ) ;
#27628=FACE_OUTER_BOUND ( 'NONE', #59354, .T. ) ;
#27633=CARTESIAN_POINT ( 'NONE',  ( -35.05175862995318425, -0.001087818442123411611, -0.01253051761585834145 ) ) ;
#27635=CARTESIAN_POINT ( 'NONE',  ( -22.31328051695926007, 3.685074213229321494, 0.8849444482787824917 ) ) ;
#27640=AXIS2_PLACEMENT_3D ( 'NONE', #43404, #33108, #53418 ) ;
#27648=CARTESIAN_POINT ( 'NONE',  ( -27.08423805673873375, 2.195702713475279122, 0.6554626340705826948 ) ) ;
#27655=AXIS2_PLACEMENT_3D ( 'NONE', #17866, #27503, #47802 ) ;
#27659=CARTESIAN_POINT ( 'NONE',  ( -27.08416781016246588, -0.7680651426971742968, 2.158663327075677429 ) ) ;
#27663=CIRCLE ( 'NONE', #64828, 6.936499999999992561 ) ;
#27668=VECTOR ( 'NONE', #42774, 1000.000000000000000 ) ;
#27670=ORIENTED_EDGE ( 'NONE', *, *, #51752, .F. ) ;
#27671=EDGE_CURVE ( 'NONE', #35989, #34255, #18585, .T. ) ;
#27672=CARTESIAN_POINT ( 'NONE',  ( -22.28776923226071460, 3.702096209084097644, -0.2883912626656479072 ) ) ;
#27673=CARTESIAN_POINT ( 'NONE',  ( -22.65999102136916221, 3.858590659383648092, 2.911035239830945365 ) ) ;
#27678=EDGE_CURVE ( 'NONE', #49980, #4847, #1203, .T. ) ;
#27706=CARTESIAN_POINT ( 'NONE',  ( 0.000000000000000000, -6.250523986464001425, 3.007653927006548766 ) ) ;
#27713=VERTEX_POINT ( 'NONE', #55436 ) ;
#27719=LINE ( 'NONE', #57680, #11579 ) ;
#27723=CARTESIAN_POINT ( 'NONE',  ( -22.28236030719477512, 2.111163412226061631, 3.035028179399193782 ) ) ;
#27737=CARTESIAN_POINT ( 'NONE',  ( -22.27834755396594346, 0.5583491773602499153, 3.643689482009640379 ) ) ;
#27741=CARTESIAN_POINT ( 'NONE',  ( 1.000000000000000888, -3.795144977083660720, 6.468916029978762694 ) ) ;
#27746=DIRECTION ( 'NONE',  ( 0.000000000000000000, -0.4198891015602528864, -0.9075754196709624466 ) ) ;
#27750=VECTOR ( 'NONE', #38037, 1000.000000000000000 ) ;
#27753=DIRECTION ( 'NONE',  ( -0.9606638835031803270, 0.1943236796486226547, 0.1984016392583679012 ) ) ;
#27756=ORIENTED_EDGE ( 'NONE', *, *, #1525, .F. ) ;
#27760=DIRECTION ( 'NONE',  ( 0.000000000000000000, 0.000000000000000000, 1.000000000000000000 ) ) ;
#27763=DIRECTION ( 'NONE',  ( 0.000000000000000000, 0.000000000000000000, 1.000000000000000000 ) ) ;
#27769=CYLINDRICAL_SURFACE ( 'NONE', #23370, 2.899999999999994582 ) ;
#27783=ORIENTED_EDGE ( 'NONE', *, *, #8643, .F. ) ;
#27787=VERTEX_POINT ( 'NONE', #14837 ) ;
#27795=CARTESIAN_POINT ( 'NONE',  ( -27.08416781016246588, 0.7680651426971888407, -2.158663327075699634 ) ) ;
#27796=ORIENTED_EDGE ( 'NONE', *, *, #59303, .F. ) ;
#27805=AXIS2_PLACEMENT_3D ( 'NONE', #19189, #18571, #3609 ) ;
#27810=CARTESIAN_POINT ( 'NONE',  ( -22.30986928587821794, 3.138878161034337921, -2.105440358094949449 ) ) ;
#27816=ORIENTED_EDGE ( 'NONE', *, *, #17726, .F. ) ;
#27829=ORIENTED_EDGE ( 'NONE', *, *, #36346, .F. ) ;
#27830=DIRECTION ( 'NONE',  ( 0.000000000000000000, -0.9635499925192201331, -0.2675283385292311911 ) ) ;
#27831=CARTESIAN_POINT ( 'NONE',  ( 2.000000000000001776, -5.107597897712365054, 4.693343793638375061 ) ) ;
#27833=CARTESIAN_POINT ( 'NONE',  ( -27.09861164373156228, -2.097104182796950322, -1.025570525057856619 ) ) ;
#27842=CARTESIAN_POINT ( 'NONE',  ( -27.08426504710140392, -0.5533780324190645805, -2.223709847896218061 ) ) ;
#27846=CARTESIAN_POINT ( 'NONE',  ( -35.04643116707788408, 0.009511118309135299653, -0.007621814750509436909 ) ) ;
#27858=VECTOR ( 'NONE', #25537, 1000.000000000000000 ) ;
#27859=CIRCLE ( 'NONE', #7695, 7.499999999999988454 ) ;
#27863=VERTEX_POINT ( 'NONE', #247 ) ;
#27874=ORIENTED_EDGE ( 'NONE', *, *, #53933, .T. ) ;
#27880=DIRECTION ( 'NONE',  ( -1.000000000000000000, 0.000000000000000000, 0.000000000000000000 ) ) ;
#27881=ORIENTED_EDGE ( 'NONE', *, *, #49913, .F. ) ;
#27884=FACE_OUTER_BOUND ( 'NONE', #33631, .T. ) ;
#27898=CARTESIAN_POINT ( 'NONE',  ( -22.71097035706202405, -4.510116093748277599, 2.118550233809401107 ) ) ;
#27903=CARTESIAN_POINT ( 'NONE',  ( 2.000000000000001776, 0.000000000000000000, 0.000000000000000000 ) ) ;
#27904=FACE_OUTER_BOUND ( 'NONE', #60759, .T. ) ;
#27909=LINE ( 'NONE', #62479, #29160 ) ;
#27912=CIRCLE ( 'NONE', #21500, 2.899999999999994582 ) ;
#27917=CARTESIAN_POINT ( 'NONE',  ( 1.000000000000000888, 0.8935325819929771374, -7.446583077151355923 ) ) ;
#27924=CARTESIAN_POINT ( 'NONE',  ( 2.000000000000001776, -3.341639490130703827, -6.078525953551491057 ) ) ;
#27926=CIRCLE ( 'NONE', #3551, 2.899999999999995914 ) ;
#27930=AXIS2_PLACEMENT_3D ( 'NONE', #39545, #54850, #313 ) ;
#27931=DIRECTION ( 'NONE',  ( 0.000000000000000000, 0.000000000000000000, 1.000000000000000000 ) ) ;
#27932=ORIENTED_EDGE ( 'NONE', *, *, #46187, .T. ) ;
#27937=ADVANCED_FACE ( 'NONE', ( #5908 ), #40803, .T. ) ;
#27939=EDGE_CURVE ( 'NONE', #24263, #49961, #61751, .T. ) ;
#27941=ORIENTED_EDGE ( 'NONE', *, *, #5734, .F. ) ;
#27945=CARTESIAN_POINT ( 'NONE',  ( 2.000000000000001776, -3.341639490130797530, 6.078525953551414673 ) ) ;
#27948=CARTESIAN_POINT ( 'NONE',  ( -35.04683013664716640, 0.01216443238273415967, 0.002177781393181293674 ) ) ;
#27949=ORIENTED_EDGE ( 'NONE', *, *, #7253, .F. ) ;
#27951=VECTOR ( 'NONE', #64102, 1000.000000000000000 ) ;
#27955=EDGE_CURVE ( 'NONE', #4690, #28947, #61721, .T. ) ;
#27956=AXIS2_PLACEMENT_3D ( 'NONE', #46724, #41735, #36749 ) ;
#27959=ORIENTED_EDGE ( 'NONE', *, *, #62847, .T. ) ;
#27961=CARTESIAN_POINT ( 'NONE',  ( -22.29290468048227680, -0.2747050847461753875, -3.718584170466891603 ) ) ;
#27986=ORIENTED_EDGE ( 'NONE', *, *, #43492, .T. ) ;
#28006=ORIENTED_EDGE ( 'NONE', *, *, #47419, .F. ) ;
#28007=CIRCLE ( 'NONE', #6743, 6.936499999999986343 ) ;
#28013=VECTOR ( 'NONE', #22872, 1000.000000000000000 ) ;
#28023=ORIENTED_EDGE ( 'NONE', *, *, #54244, .T. ) ;
#28027=CARTESIAN_POINT ( 'NONE',  ( 1.000000000000000888, 3.937687286050817193, 6.383151168292468647 ) ) ;
#28028=FACE_OUTER_BOUND ( 'NONE', #10548, .T. ) ;
#28030=ORIENTED_EDGE ( 'NONE', *, *, #44096, .F. ) ;
#28032=ORIENTED_EDGE ( 'NONE', *, *, #31437, .F. ) ;
#28039=CARTESIAN_POINT ( 'NONE',  ( -22.27711653538342773, -2.191780254295667696, -2.958138731383664233 ) ) ;
#28048=ORIENTED_EDGE ( 'NONE', *, *, #14804, .F. ) ;
#28067=ORIENTED_EDGE ( 'NONE', *, *, #23005, .T. ) ;
#28069=CIRCLE ( 'NONE', #59921, 7.499999999999988454 ) ;
#28070=CYLINDRICAL_SURFACE ( 'NONE', #34908, 2.899999999999994582 ) ;
#28077=EDGE_CURVE ( 'NONE', #34425, #26744, #37433, .T. ) ;
#28078=CYLINDRICAL_SURFACE ( 'NONE', #6849, 7.499999999999988454 ) ;
#28084=LINE ( 'NONE', #33047, #64236 ) ;
#28087=DIRECTION ( 'NONE',  ( 0.000000000000000000, 0.000000000000000000, 1.000000000000000000 ) ) ;
#28101=CYLINDRICAL_SURFACE ( 'NONE', #6562, 7.499999999999988454 ) ;
#28120=LINE ( 'NONE', #43386, #9627 ) ;
#28121=VERTEX_POINT ( 'NONE', #34725 ) ;
#28124=CARTESIAN_POINT ( 'NONE',  ( -35.04834644901396956, 0.0002835132723552184503, 0.01383120537647892362 ) ) ;
#28130=EDGE_CURVE ( 'NONE', #40566, #36018, #13792, .T. ) ;
#28137=CARTESIAN_POINT ( 'NONE',  ( -22.27706485742869091, -0.3729136217355977778, -3.662257305743823022 ) ) ;
#28139=CARTESIAN_POINT ( 'NONE',  ( 0.000000000000000000, -5.769711778877296027, -4.791703871138604853 ) ) ;
#28141=CARTESIAN_POINT ( 'NONE',  ( 0.000000000000000000, 5.396716205731493687, -4.158041573745044239 ) ) ;
#28152=VERTEX_POINT ( 'NONE', #55700 ) ;
#28157=CARTESIAN_POINT ( 'NONE',  ( -27.15511094194037867, 1.375165223101532108, 2.092607239484509662 ) ) ;
#28171=ORIENTED_EDGE ( 'NONE', *, *, #3231, .F. ) ;
#28178=EDGE_CURVE ( 'NONE', #23034, #42911, #3357, .T. ) ;
#28180=CARTESIAN_POINT ( 'NONE',  ( 1.000000000000000888, 4.472310526050767621, 6.020667617347370104 ) ) ;
#28189=DIRECTION ( 'NONE',  ( -0.9606638835031803270, -0.06908842350339414184, -0.2689826995745334681 ) ) ;
#28201=CYLINDRICAL_SURFACE ( 'NONE', #49945, 7.499999999999988454 ) ;
#28209=CARTESIAN_POINT ( 'NONE',  ( -22.28236030719477512, -1.572829798448329486, 3.345835236227606924 ) ) ;
#28223=CARTESIAN_POINT ( 'NONE',  ( -27.10113028276155589, -1.613062633976931837, 1.697941299269279281 ) ) ;
#28227=DIRECTION ( 'NONE',  ( -1.000000000000000000, 0.000000000000000000, 0.000000000000000000 ) ) ;
#28230=VERTEX_POINT ( 'NONE', #30727 ) ;
#28235=CARTESIAN_POINT ( 'NONE',  ( -35.05175862995318425, -0.003331684148545621671, -0.01212835938695783211 ) ) ;
#28236=CARTESIAN_POINT ( 'NONE',  ( -22.46509356695211679, 2.840174833751863304, -3.157489876851686805 ) ) ;
#28248=CARTESIAN_POINT ( 'NONE',  ( 2.000000000000001776, 5.457833520448724940, -4.281014542496488495 ) ) ;
#28251=DIRECTION ( 'NONE',  ( -1.000000000000000000, 0.000000000000000000, 0.000000000000000000 ) ) ;
#28253=CARTESIAN_POINT ( 'NONE',  ( -27.10719052120871098, 2.116547233941204809, 1.044362304621460069 ) ) ;
#28255=ADVANCED_FACE ( 'NONE', ( #164 ), #1150, .T. ) ;
#28265=VERTEX_POINT ( 'NONE', #36039 ) ;
#28267=CARTESIAN_POINT ( 'NONE',  ( -27.08639648637141661, 2.215564006614429982, -0.6092497698725152233 ) ) ;
#28269=DIRECTION ( 'NONE',  ( 0.000000000000000000, 0.000000000000000000, 1.000000000000000000 ) ) ;
#28271=CARTESIAN_POINT ( 'NONE',  ( -27.09833916700227618, -1.689564470270175534, -1.609723001517283203 ) ) ;
#28278=EDGE_CURVE ( 'NONE', #29418, #18668, #61324, .T. ) ;
#28280=AXIS2_PLACEMENT_3D ( 'NONE', #54706, #30705, #39380 ) ;
#28285=VECTOR ( 'NONE', #49047, 1000.000000000000000 ) ;
#28286=DIRECTION ( 'NONE',  ( -1.000000000000000000, 0.000000000000000000, 0.000000000000000000 ) ) ;
#28288=DIRECTION ( 'NONE',  ( 0.000000000000000000, -0.3193015301359872216, 0.9476531711827999027 ) ) ;
#28290=VERTEX_POINT ( 'NONE', #41362 ) ;
#28292=ORIENTED_EDGE ( 'NONE', *, *, #32203, .T. ) ;
#28303=ORIENTED_EDGE ( 'NONE', *, *, #32895, .F. ) ;
#28304=CARTESIAN_POINT ( 'NONE',  ( 2.000000000000001776, 0.000000000000000000, 0.000000000000000000 ) ) ;
#28334=DIRECTION ( 'NONE',  ( 1.000000000000000000, -0.000000000000000000, -0.000000000000000000 ) ) ;
#28335=CYLINDRICAL_SURFACE ( 'NONE', #37487, 7.499999999999988454 ) ;
#28340=ORIENTED_EDGE ( 'NONE', *, *, #56706, .T. ) ;
#28348=ORIENTED_EDGE ( 'NONE', *, *, #40477, .T. ) ;
#28351=CARTESIAN_POINT ( 'NONE',  ( -22.30986928587821794, -3.392803916780404716, -1.665628047792451216 ) ) ;
#28355=DIRECTION ( 'NONE',  ( 0.000000000000000000, 0.000000000000000000, 1.000000000000000000 ) ) ;
#28374=EDGE_CURVE ( 'NONE', #51860, #36273, #14341, .T. ) ;
#28376=AXIS2_PLACEMENT_3D ( 'NONE', #49246, #36102, #24264 ) ;
#28379=ORIENTED_EDGE ( 'NONE', *, *, #2236, .T. ) ;
#28385=CARTESIAN_POINT ( 'NONE',  ( -22.31328051695926007, 3.401210163132566411, 1.671726071983929307 ) ) ;
#28390=DIRECTION ( 'NONE',  ( 0.000000000000000000, 0.7621620551276377942, -0.6473862847818260269 ) ) ;
#28394=CARTESIAN_POINT ( 'NONE',  ( -27.08429572838383947, -1.338867938658200307, -1.859677275556420151 ) ) ;
#28397=VECTOR ( 'NONE', #45962, 1000.000000000000000 ) ;
#28405=CARTESIAN_POINT ( 'NONE',  ( -35.04582288351658548, 0.0001464581944843601751, 0.01270482153514039536 ) ) ;
#28408=CARTESIAN_POINT ( 'NONE',  ( -27.32343372485685506, -0.1402256980610406267, 3.007804754713657047 ) ) ;
#28419=ORIENTED_EDGE ( 'NONE', *, *, #64471, .T. ) ;
#28427=CYLINDRICAL_SURFACE ( 'NONE', #14024, 2.899999999999994582 ) ;
#28428=DIRECTION ( 'NONE',  ( 0.000000000000000000, 0.000000000000000000, 1.000000000000000000 ) ) ;
#28431=EDGE_CURVE ( 'NONE', #5947, #34267, #33690, .T. ) ;
#28439=AXIS2_PLACEMENT_3D ( 'NONE', #44543, #64823, #35564 ) ;
#28441=ADVANCED_FACE ( 'NONE', ( #23738 ), #19729, .T. ) ;
#28443=CARTESIAN_POINT ( 'NONE',  ( 2.000000000000001776, 5.888698556700773246, 3.665823448873418045 ) ) ;
#28444=CARTESIAN_POINT ( 'NONE',  ( -27.08418322526030764, 0.8335872080609603163, -2.134267017050449855 ) ) ;
#28450=VERTEX_POINT ( 'NONE', #58994 ) ;
#28451=CYLINDRICAL_SURFACE ( 'NONE', #48121, 7.499999999999988454 ) ;
#28459=CARTESIAN_POINT ( 'NONE',  ( -27.09150307427447757, -1.909742362151675810, 1.305148381377976730 ) ) ;
#28460=EDGE_CURVE ( 'NONE', #29500, #39372, #2484, .T. ) ;
#28461=DIRECTION ( 'NONE',  ( 0.000000000000000000, -0.2149704402110318713, 0.9766205557100849921 ) ) ;
#28466=LINE ( 'NONE', #50076, #53112 ) ;
#28470=EDGE_LOOP ( 'NONE', ( #50543, #38971, #23615, #42986 ) ) ;
#28476=ORIENTED_EDGE ( 'NONE', *, *, #43699, .T. ) ;
#28479=CARTESIAN_POINT ( 'NONE',  ( -23.18047892478189098, 0.4043282704081693768, -4.776019214182026573 ) ) ;
#28481=AXIS2_PLACEMENT_3D ( 'NONE', #3642, #28227, #48518 ) ;
#28483=CARTESIAN_POINT ( 'NONE',  ( -27.08417142187571613, -0.4261087887162083865, -2.251180450989576531 ) ) ;
#28488=CARTESIAN_POINT ( 'NONE',  ( 2.000000000000001776, -1.225832621831797420, -6.827324998361596009 ) ) ;
#28491=EDGE_LOOP ( 'NONE', ( #25440, #64786, #8507, #57146 ) ) ;
#28504=DIRECTION ( 'NONE',  ( 0.000000000000000000, -0.5155538571770110767, -0.8568571761675956022 ) ) ;
#28509=CARTESIAN_POINT ( 'NONE',  ( -26.43258404273187523, 2.854888342447774896, 1.987083010659142612 ) ) ;
#28515=ORIENTED_EDGE ( 'NONE', *, *, #5829, .F. ) ;
#28516=CARTESIAN_POINT ( 'NONE',  ( -22.29978294495153790, 2.590262069787980348, -2.710748743830168284 ) ) ;
#28519=EDGE_CURVE ( 'NONE', #15374, #63832, #55447, .T. ) ;
#28521=VERTEX_POINT ( 'NONE', #44314 ) ;
#28524=AXIS2_PLACEMENT_3D ( 'NONE', #55367, #5167, #51394 ) ;
#28547=DIRECTION ( 'NONE',  ( -1.000000000000000000, 0.000000000000000000, 0.000000000000000000 ) ) ;
#28550=DIRECTION ( 'NONE',  ( 0.000000000000000000, 0.7621620551276333533, 0.6473862847818313560 ) ) ;
#28552=CARTESIAN_POINT ( 'NONE',  ( 2.000000000000001776, 3.341639490130849488, -6.078525953551423555 ) ) ;
#28555=AXIS2_PLACEMENT_3D ( 'NONE', #14787, #5178, #65659 ) ;
#28559=ORIENTED_EDGE ( 'NONE', *, *, #42118, .T. ) ;
#28563=DIRECTION ( 'NONE',  ( -1.000000000000000000, 0.000000000000000000, 0.000000000000000000 ) ) ;
#28565=ORIENTED_EDGE ( 'NONE', *, *, #18332, .F. ) ;
#28567=DIRECTION ( 'NONE',  ( 0.000000000000000000, 0.000000000000000000, 1.000000000000000000 ) ) ;
#28569=CARTESIAN_POINT ( 'NONE',  ( -22.31328051695926007, 2.748895659348141507, 2.608921479762082551 ) ) ;
#28571=EDGE_CURVE ( 'NONE', #24263, #25850, #35956, .T. ) ;
#28582=ORIENTED_EDGE ( 'NONE', *, *, #64340, .T. ) ;
#28584=AXIS2_PLACEMENT_3D ( 'NONE', #46179, #45840, #36163 ) ;
#28586=CARTESIAN_POINT ( 'NONE',  ( 0.000000000000000000, 6.936109781200682889, 2.853135311045038591 ) ) ;
#28589=CARTESIAN_POINT ( 'NONE',  ( -35.04660725145885891, 0.01184012236748180000, 0.003326400506015331823 ) ) ;
#28595=CYLINDRICAL_SURFACE ( 'NONE', #12874, 7.499999999999988454 ) ;
#28597=EDGE_LOOP ( 'NONE', ( #23420, #54682, #21776, #52400 ) ) ;
#28599=CARTESIAN_POINT ( 'NONE',  ( -22.31213670151049300, -0.2530575063955998738, -3.777944311993719051 ) ) ;
#28604=CARTESIAN_POINT ( 'NONE',  ( 0.000000000000000000, 0.000000000000000000, 7.500000000000000000 ) ) ;
#28611=ORIENTED_EDGE ( 'NONE', *, *, #13202, .T. ) ;
#28620=CARTESIAN_POINT ( 'NONE',  ( 2.000000000000001776, -0.2704997240204360387, -6.931223712253490987 ) ) ;
#28622=VERTEX_POINT ( 'NONE', #15373 ) ;
#28638=AXIS2_PLACEMENT_3D ( 'NONE', #3685, #24918, #14899 ) ;
#28639=ORIENTED_EDGE ( 'NONE', *, *, #29765, .F. ) ;
#28646=VECTOR ( 'NONE', #10602, 1000.000000000000000 ) ;
#28649=ADVANCED_FACE ( 'NONE', ( #59499 ), #29244, .T. ) ;
#28652=CARTESIAN_POINT ( 'NONE',  ( -27.08429572838383947, -0.9410937941433956677, 2.089332284968712816 ) ) ;
#28658=CIRCLE ( 'NONE', #5326, 6.936499999999990784 ) ;
#28668=EDGE_LOOP ( 'NONE', ( #27986, #12696, #10523, #18722 ) ) ;
#28673=LINE ( 'NONE', #32654, #59265 ) ;
#28677=CIRCLE ( 'NONE', #4350, 2.899999999999994582 ) ;
#28680=ORIENTED_EDGE ( 'NONE', *, *, #38674, .T. ) ;
#28684=CARTESIAN_POINT ( 'NONE',  ( -28.67667724226168602, 0.4371157725390067972, -1.840944188131425907 ) ) ;
#28693=EDGE_CURVE ( 'NONE', #59877, #54376, #53328, .T. ) ;
#28696=CYLINDRICAL_SURFACE ( 'NONE', #12316, 2.899999999999994582 ) ;
#28702=DIRECTION ( 'NONE',  ( 0.000000000000000000, -0.8835120444460272671, 0.4684084406997819916 ) ) ;
#28705=ORIENTED_EDGE ( 'NONE', *, *, #16306, .F. ) ;
#28706=DIRECTION ( 'NONE',  ( -1.000000000000000000, 0.000000000000000000, 0.000000000000000000 ) ) ;
#28711=CARTESIAN_POINT ( 'NONE',  ( 2.000000000000001776, 6.643843315911800218, 1.507714007300793968 ) ) ;
#28719=CARTESIAN_POINT ( 'NONE',  ( -27.08418179957658367, -1.521007404704310950, -1.713622993062714928 ) ) ;
#28727=( BOUNDED_SURFACE ( )  B_SPLINE_SURFACE ( 3, 1, ( 
 ( #52115, #21863 ),
 ( #22510, #57428 ),
 ( #57108, #38109 ),
 ( #16543, #21532 ) ),
 .UNSPECIFIED., .F., .F., .F. ) 
 B_SPLINE_SURFACE_WITH_KNOTS ( ( 4, 4 ),
 ( 2, 2 ),
 ( 0.000000000000000000, 1.000000000000000000 ),
 ( 0.000000000000000000, 1.000000000000000000 ),
 .UNSPECIFIED. ) 
 GEOMETRIC_REPRESENTATION_ITEM ( )  RATIONAL_B_SPLINE_SURFACE ( (
 ( 1.000000000000000000, 1.000000000000000000),
 ( 0.8716676215708681896, 0.8964445200148164483),
 ( 0.8716676215708681896, 0.8964445200148164483),
 ( 1.000000000000000000, 1.000000000000000000) ) ) 
 REPRESENTATION_ITEM ( '' )  SURFACE ( )  );
#28740=DIRECTION ( 'NONE',  ( 0.000000000000000000, 0.5155538571770171830, 0.8568571761675919385 ) ) ;
#28741=CARTESIAN_POINT ( 'NONE',  ( 2.000000000000001776, -7.414200355365264450, 1.131208685655129775 ) ) ;
#28742=CARTESIAN_POINT ( 'NONE',  ( -22.27834755396593991, -2.876353066242412382, 2.305389312780939726 ) ) ;
#28745=VECTOR ( 'NONE', #39057, 1000.000000000000000 ) ;
#28748=EDGE_CURVE ( 'NONE', #13308, #28265, #54843, .T. ) ;
#28756=LINE ( 'NONE', #33425, #31277 ) ;
#28760=CONICAL_SURFACE ( 'NONE', #37247, 5.135612550275435062, 1.249045772030607848 ) ;
#28763=VERTEX_POINT ( 'NONE', #39205 ) ;
#28767=VERTEX_POINT ( 'NONE', #13926 ) ;
#28772=DIRECTION ( 'NONE',  ( -1.000000000000000000, 0.000000000000000000, 0.000000000000000000 ) ) ;
#28773=DIRECTION ( 'NONE',  ( -1.000000000000000000, 0.000000000000000000, 0.000000000000000000 ) ) ;
#28776=ORIENTED_EDGE ( 'NONE', *, *, #44511, .T. ) ;
#28778=CARTESIAN_POINT ( 'NONE',  ( -28.67667724226168602, 1.812862320140632866, -0.5419187306520724112 ) ) ;
#28783=DIRECTION ( 'NONE',  ( -1.000000000000000000, 0.000000000000000000, 0.000000000000000000 ) ) ;
#28791=DIRECTION ( 'NONE',  ( 0.000000000000000000, 0.000000000000000000, 1.000000000000000000 ) ) ;
#28794=CIRCLE ( 'NONE', #30862, 7.499999999999988454 ) ;
#28798=CARTESIAN_POINT ( 'NONE',  ( 0.000000000000000000, 6.606214214351110670, -2.114938770769863030 ) ) ;
#28801=AXIS2_PLACEMENT_3D ( 'NONE', #60469, #54191, #61442 ) ;
#28807=CARTESIAN_POINT ( 'NONE',  ( -27.35552965826136429, -1.320216934008378473, -2.810569013793753346 ) ) ;
#28809=LINE ( 'NONE', #32795, #14990 ) ;
#28810=EDGE_CURVE ( 'NONE', #634, #29257, #25695, .T. ) ;
#28814=CARTESIAN_POINT ( 'NONE',  ( 0.000000000000000000, 7.484036900328569608, -0.4890722589968761191 ) ) ;
#28816=VECTOR ( 'NONE', #11196, 1000.000000000000000 ) ;
#28818=B_SPLINE_CURVE_WITH_KNOTS ( 'NONE', 3,
 ( #34709, #5138, #50376, #24417, #45359, #55993, #15094, #35373 ),
 .UNSPECIFIED., .F., .F.,
 ( 4, 2, 2, 4 ),
 ( 0.000000000000000000, 0.0003639104015150019687, 0.0007278208030300039374, 0.001455641606060010477 ),
 .UNSPECIFIED. ) ;
#28821=CARTESIAN_POINT ( 'NONE',  ( -27.08419642509983305, -0.4837273216074956528, -2.239682169453958149 ) ) ;
#28827=ORIENTED_EDGE ( 'NONE', *, *, #11762, .F. ) ;
#28829=FACE_OUTER_BOUND ( 'NONE', #18991, .T. ) ;
#28836=ORIENTED_EDGE ( 'NONE', *, *, #41962, .F. ) ;
#28844=CARTESIAN_POINT ( 'NONE',  ( -23.41523303002442091, 3.856096202952873142, 2.683951991546253524 ) ) ;
#28854=AXIS2_PLACEMENT_3D ( 'NONE', #17787, #53026, #58353 ) ;
#28855=CARTESIAN_POINT ( 'NONE',  ( -22.28350523959500862, -1.580062893038977068, 3.346230442873244559 ) ) ;
#28860=VERTEX_POINT ( 'NONE', #320 ) ;
#28862=DIRECTION ( 'NONE',  ( 1.000000000000000000, -0.000000000000000000, -0.000000000000000000 ) ) ;
#28868=CARTESIAN_POINT ( 'NONE',  ( -27.08639648637162267, -1.614109828501627097, 1.635407781268140237 ) ) ;
#28871=CARTESIAN_POINT ( 'NONE',  ( -27.08456565417852246, -2.282055114149002417, 0.2166646653333839379 ) ) ;
#28872=DIRECTION ( 'NONE',  ( 0.000000000000000000, 0.4198891015602656540, -0.9075754196709564514 ) ) ;
#28873=CYLINDRICAL_SURFACE ( 'NONE', #24261, 1.499999999999997780 ) ;
#28875=CARTESIAN_POINT ( 'NONE',  ( 1.000000000000000888, 3.224464355699941720, -6.771471746881976728 ) ) ;
#28880=CARTESIAN_POINT ( 'NONE',  ( 2.000000000000001776, -2.469490258309361419, -6.482025155313371201 ) ) ;
#28883=CARTESIAN_POINT ( 'NONE',  ( -27.09229696323388481, 1.607344345646389172, -1.666734935102333948 ) ) ;
#28884=AXIS2_PLACEMENT_3D ( 'NONE', #8504, #15127, #28791 ) ;
#28885=CARTESIAN_POINT ( 'NONE',  ( -27.08426504710140392, 1.591094357919273117, 1.649100202714188779 ) ) ;
#28891=AXIS2_PLACEMENT_3D ( 'NONE', #13414, #7789, #8435 ) ;
#28897=DIRECTION ( 'NONE',  ( 0.000000000000000000, 0.6051742151937661296, -0.7960930657056429771 ) ) ;
#28903=AXIS2_PLACEMENT_3D ( 'NONE', #8892, #49478, #38494 ) ;
#28905=CARTESIAN_POINT ( 'NONE',  ( -22.28856623400852399, 2.668530796663842963, 2.585606290939587382 ) ) ;
#28906=AXIS2_PLACEMENT_3D ( 'NONE', #33235, #18628, #38209 ) ;
#28911=VERTEX_POINT ( 'NONE', #47826 ) ;
#28919=CIRCLE ( 'NONE', #24699, 2.899999999999995026 ) ;
#28926=CARTESIAN_POINT ( 'NONE',  ( 2.000000000000001776, -4.976357229393876480, 4.652926418895529714 ) ) ;
#28931=ORIENTED_EDGE ( 'NONE', *, *, #9556, .F. ) ;
#28932=EDGE_LOOP ( 'NONE', ( #37353, #2453, #7264, #49177 ) ) ;
#28938=CARTESIAN_POINT ( 'NONE',  ( -35.04709527796842394, -0.01016988845958625987, -0.007030359780627049027 ) ) ;
#28939=VERTEX_POINT ( 'NONE', #22564 ) ;
#28942=DIRECTION ( 'NONE',  ( 0.000000000000000000, 0.000000000000000000, 1.000000000000000000 ) ) ;
#28947=VERTEX_POINT ( 'NONE', #27212 ) ;
#28956=EDGE_CURVE ( 'NONE', #13767, #3623, #2403, .T. ) ;
#28957=CARTESIAN_POINT ( 'NONE',  ( -22.28073302975501235, 3.572053042948136969, 0.9342220484184516893 ) ) ;
#28960=CARTESIAN_POINT ( 'NONE',  ( -22.65996813707689128, 0.2230532344361583763, -4.828298130757411322 ) ) ;
#28961=ORIENTED_EDGE ( 'NONE', *, *, #28571, .T. ) ;
#28962=DIRECTION ( 'NONE',  ( -1.000000000000000000, 0.000000000000000000, 0.000000000000000000 ) ) ;
#28976=CARTESIAN_POINT ( 'NONE',  ( -22.30625920655495165, 1.672644928563083333, -3.403091720605004866 ) ) ;
#28984=EDGE_CURVE ( 'NONE', #4941, #33111, #40484, .T. ) ;
#28987=DIRECTION ( 'NONE',  ( -1.000000000000000000, 0.000000000000000000, 0.000000000000000000 ) ) ;
#28992=CARTESIAN_POINT ( 'NONE',  ( -35.04683013664716640, -0.01235741808121416756, 0.0001018103929289144923 ) ) ;
#28994=DIRECTION ( 'NONE',  ( -1.000000000000000000, 0.000000000000000000, 0.000000000000000000 ) ) ;
#28996=DIRECTION ( 'NONE',  ( 0.000000000000000000, 0.9635499925192219095, 0.2675283385292247518 ) ) ;
#28998=AXIS2_PLACEMENT_3D ( 'NONE', #3274, #58822, #33185 ) ;
#29004=CARTESIAN_POINT ( 'NONE',  ( -27.09483304420799143, -1.303111346475732679, -1.923212037696920840 ) ) ;
#29005=EDGE_CURVE ( 'NONE', #28290, #61436, #64407, .T. ) ;
#29008=CARTESIAN_POINT ( 'NONE',  ( -22.27720412283625961, -3.606406551442359998, 0.7407051501189869658 ) ) ;
#29015=ORIENTED_EDGE ( 'NONE', *, *, #60204, .T. ) ;
#29017=AXIS2_PLACEMENT_3D ( 'NONE', #22463, #13454, #7483 ) ;
#29019=CARTESIAN_POINT ( 'NONE',  ( 0.000000000000000000, -4.444115772890066651, -5.163689623839394116 ) ) ;
#29026=CARTESIAN_POINT ( 'NONE',  ( 2.000000000000001776, 3.937687286050910895, -6.383151168292449107 ) ) ;
#29030=FACE_OUTER_BOUND ( 'NONE', #35033, .T. ) ;
#29049=ORIENTED_EDGE ( 'NONE', *, *, #37238, .F. ) ;
#29050=EDGE_CURVE ( 'NONE', #10275, #57905, #13234, .T. ) ;
#29053=CARTESIAN_POINT ( 'NONE',  ( -27.08421860617808008, 0.2990745872176441833, 2.271664812096779951 ) ) ;
#29054=DIRECTION ( 'NONE',  ( -1.000000000000000000, 0.000000000000000000, 0.000000000000000000 ) ) ;
#29055=CARTESIAN_POINT ( 'NONE',  ( -22.27706089016750113, 0.9256273512588665264, 3.562910635974977147 ) ) ;
#29058=B_SPLINE_CURVE_WITH_KNOTS ( 'NONE', 3,
 ( #58434, #64061, #59401, #2248, #48466, #49126, #44109, #27498, #32799, #48785 ),
 .UNSPECIFIED., .F., .F.,
 ( 4, 3, 3, 4 ),
 ( 5.401523115762557641E-05, 0.0008136511341527791425, 0.004068255670953093220, 0.005063778443040927411 ),
 .UNSPECIFIED. ) ;
#29064=CIRCLE ( 'NONE', #393, 2.899999999999995026 ) ;
#29068=ORIENTED_EDGE ( 'NONE', *, *, #20056, .T. ) ;
#29070=VECTOR ( 'NONE', #7089, 1000.000000000000000 ) ;
#29084=ORIENTED_EDGE ( 'NONE', *, *, #59756, .F. ) ;
#29093=VECTOR ( 'NONE', #36245, 1000.000000000000000 ) ;
#29094=CIRCLE ( 'NONE', #48248, 2.899999999999994582 ) ;
#29098=ORIENTED_EDGE ( 'NONE', *, *, #57655, .T. ) ;
#29101=DIRECTION ( 'NONE',  ( 0.000000000000000000, 0.000000000000000000, -1.000000000000000000 ) ) ;
#29105=CARTESIAN_POINT ( 'NONE',  ( -35.04683013664716640, 0.01162359816267300762, -0.004196202180977571042 ) ) ;
#29112=ORIENTED_EDGE ( 'NONE', *, *, #38872, .T. ) ;
#29113=VERTEX_POINT ( 'NONE', #61382 ) ;
#29124=CYLINDRICAL_SURFACE ( 'NONE', #45425, 2.899999999999994582 ) ;
#29127=ORIENTED_EDGE ( 'NONE', *, *, #14390, .T. ) ;
#29131=FACE_OUTER_BOUND ( 'NONE', #47525, .T. ) ;
#29142=CIRCLE ( 'NONE', #40811, 7.499999999999988454 ) ;
#29145=DIRECTION ( 'NONE',  ( -1.000000000000000000, 0.000000000000000000, 0.000000000000000000 ) ) ;
#29148=DIRECTION ( 'NONE',  ( 0.000000000000000000, 0.000000000000000000, 1.000000000000000000 ) ) ;
#29150=LINE ( 'NONE', #14795, #55575 ) ;
#29160=VECTOR ( 'NONE', #18271, 1000.000000000000000 ) ;
#29165=DIRECTION ( 'NONE',  ( 1.000000000000000000, -0.000000000000000000, -0.000000000000000000 ) ) ;
#29180=LINE ( 'NONE', #49476, #45738 ) ;
#29187=ORIENTED_EDGE ( 'NONE', *, *, #37745, .F. ) ;
#29201=EDGE_LOOP ( 'NONE', ( #40082, #12457 ) ) ;
#29203=EDGE_LOOP ( 'NONE', ( #37860, #39714, #31411, #46993, #59890, #5114, #3439, #7886, #52885, #12628, #36360, #18960, #15038, #14281, #57674, #10750, #31406, #35966, #39633, #11930, #38806, #58465, #37634, #46234, #44796, #50214, #43369, #32806, #18314, #29541, #39238, #28348, #5104, #32205 ) ) ;
#29204=CARTESIAN_POINT ( 'NONE',  ( 0.000000000000000000, 0.000000000000000000, 0.000000000000000000 ) ) ;
#29211=ORIENTED_EDGE ( 'NONE', *, *, #34, .F. ) ;
#29218=CARTESIAN_POINT ( 'NONE',  ( -22.49803948133826026, -3.704553751086667734, 2.269619744675254847 ) ) ;
#29219=CARTESIAN_POINT ( 'NONE',  ( 2.000000000000001776, -3.795144977083580784, -6.468916029978842630 ) ) ;
#29230=DIRECTION ( 'NONE',  ( 0.000000000000000000, 0.000000000000000000, 1.000000000000000000 ) ) ;
#29232=( GEOMETRIC_REPRESENTATION_CONTEXT ( 3 ) GLOBAL_UNCERTAINTY_ASSIGNED_CONTEXT ( ( #38928 ) ) GLOBAL_UNIT_ASSIGNED_CONTEXT ( ( #44450, #59132, #13543 ) ) REPRESENTATION_CONTEXT ( 'NONE', 'WORKASPACE' ) );
#29237=EDGE_CURVE ( 'NONE', #40945, #25882, #31772, .T. ) ;
#29238=CARTESIAN_POINT ( 'NONE',  ( 2.000000000000001776, 1.018311147294260977, -6.861346417234475581 ) ) ;
#29241=CARTESIAN_POINT ( 'NONE',  ( 0.000000000000000000, -6.662861565602053560, -1.421313227905724341 ) ) ;
#29244=CYLINDRICAL_SURFACE ( 'NONE', #56495, 7.499999999999988454 ) ;
#29245=DIRECTION ( 'NONE',  ( 0.000000000000000000, 0.000000000000000000, 1.000000000000000000 ) ) ;
#29246=AXIS2_PLACEMENT_3D ( 'NONE', #54558, #3707, #64192 ) ;
#29247=EDGE_CURVE ( 'NONE', #45502, #28763, #42700, .T. ) ;
#29249=ORIENTED_EDGE ( 'NONE', *, *, #25289, .F. ) ;
#29250=CARTESIAN_POINT ( 'NONE',  ( -27.08935880048753120, 2.219773948423736432, -0.6272370006475047610 ) ) ;
#29257=VERTEX_POINT ( 'NONE', #52082 ) ;
#29258=ORIENTED_EDGE ( 'NONE', *, *, #23188, .F. ) ;
#29271=DIRECTION ( 'NONE',  ( -1.000000000000000000, 0.000000000000000000, 0.000000000000000000 ) ) ;
#29281=DIRECTION ( 'NONE',  ( -1.000000000000000000, 0.000000000000000000, 0.000000000000000000 ) ) ;
#29285=CARTESIAN_POINT ( 'NONE',  ( -22.35190811654613441, -3.898012445334715359, 0.2457675311904958526 ) ) ;
#29290=ADVANCED_FACE ( 'NONE', ( #37430 ), #50695, .F. ) ;
#29292=VERTEX_POINT ( 'NONE', #59692 ) ;
#29297=ORIENTED_EDGE ( 'NONE', *, *, #18498, .T. ) ;
#29298=ORIENTED_EDGE ( 'NONE', *, *, #3907, .T. ) ;
#29299=CARTESIAN_POINT ( 'NONE',  ( -35.04660725145885891, 0.003039313842369092532, 0.01191704700713624304 ) ) ;
#29321=ORIENTED_EDGE ( 'NONE', *, *, #54536, .T. ) ;
#29324=CARTESIAN_POINT ( 'NONE',  ( -35.04683013664716640, -0.002177781393184786973, 0.01216443238270097441 ) ) ;
#29327=ORIENTED_EDGE ( 'NONE', *, *, #3419, .T. ) ;
#29333=CARTESIAN_POINT ( 'NONE',  ( -22.27719443589224113, -2.462030382548427543, -2.737335337013111936 ) ) ;
#29344=CARTESIAN_POINT ( 'NONE',  ( -22.28506771379528573, -3.622079238249909849, -0.8783543640077282610 ) ) ;
#29348=ORIENTED_EDGE ( 'NONE', *, *, #50217, .T. ) ;
#29350=CARTESIAN_POINT ( 'NONE',  ( -35.05175862995318425, 0.001087818442111268546, 0.01253051761584966783 ) ) ;
#29351=CARTESIAN_POINT ( 'NONE',  ( 0.000000000000000000, -4.976357229393820525, -4.652926418895619420 ) ) ;
#29355=CARTESIAN_POINT ( 'NONE',  ( -27.10128162969864007, -0.1566844438592166489, -2.337214317750539561 ) ) ;
#29361=DIRECTION ( 'NONE',  ( 0.000000000000000000, 0.000000000000000000, -1.000000000000000000 ) ) ;
#29362=ORIENTED_EDGE ( 'NONE', *, *, #33769, .T. ) ;
#29367=DIRECTION ( 'NONE',  ( 1.000000000000000000, 0.000000000000000000, 0.000000000000000000 ) ) ;
#29371=CARTESIAN_POINT ( 'NONE',  ( -22.29479313954897535, 1.627767898183768658, -3.360948587163225199 ) ) ;
#29374=DIRECTION ( 'NONE',  ( -1.000000000000000000, 0.000000000000000000, 0.000000000000000000 ) ) ;
#29379=CARTESIAN_POINT ( 'NONE',  ( -27.08421860617808008, -1.394838596205207448, -1.817782142550201208 ) ) ;
#29381=VERTEX_POINT ( 'NONE', #54047 ) ;
#29383=DIRECTION ( 'NONE',  ( 0.000000000000000000, 0.000000000000000000, 1.000000000000000000 ) ) ;
#29391=CARTESIAN_POINT ( 'NONE',  ( 2.000000000000001776, 0.000000000000000000, 0.000000000000000000 ) ) ;
#29396=ORIENTED_EDGE ( 'NONE', *, *, #19546, .T. ) ;
#29400=ADVANCED_FACE ( 'NONE', ( #64988 ), #5148, .T. ) ;
#29401=ORIENTED_EDGE ( 'NONE', *, *, #13110, .T. ) ;
#29405=B_SPLINE_CURVE_WITH_KNOTS ( 'NONE', 3,
 ( #56065, #35764, #52074, #25824, #15816, #21828 ),
 .UNSPECIFIED., .F., .F.,
 ( 4, 2, 4 ),
 ( 0.000000000000000000, 0.0004528561986909412115, 0.0009057123973818824230 ),
 .UNSPECIFIED. ) ;
#29409=DIRECTION ( 'NONE',  ( -1.000000000000000000, 0.000000000000000000, 0.000000000000000000 ) ) ;
#29412=DIRECTION ( 'NONE',  ( -1.000000000000000000, 0.000000000000000000, 0.000000000000000000 ) ) ;
#29413=DIRECTION ( 'NONE',  ( 0.000000000000000000, 0.000000000000000000, -1.000000000000000000 ) ) ;
#29417=EDGE_CURVE ( 'NONE', #26404, #9789, #45476, .T. ) ;
#29418=VERTEX_POINT ( 'NONE', #60023 ) ;
#29421=ORIENTED_EDGE ( 'NONE', *, *, #55676, .F. ) ;
#29422=CARTESIAN_POINT ( 'NONE',  ( -22.28169757117798611, -0.9284931499057216264, 3.576542310004385605 ) ) ;
#29429=VERTEX_POINT ( 'NONE', #51374 ) ;
#29432=FACE_OUTER_BOUND ( 'NONE', #32010, .T. ) ;
#29439=DIRECTION ( 'NONE',  ( 1.000000000000000000, 1.685093406416449860E-16, -1.011030131491573426E-17 ) ) ;
#29455=DIRECTION ( 'NONE',  ( -1.000000000000000000, 0.000000000000000000, 0.000000000000000000 ) ) ;
#29457=EDGE_CURVE ( 'NONE', #15504, #52589, #30611, .T. ) ;
#29459=EDGE_CURVE ( 'NONE', #48402, #32375, #41247, .T. ) ;
#29460=CARTESIAN_POINT ( 'NONE',  ( -22.27706485742869091, -1.508175983031604606, 3.358064672837097753 ) ) ;
#29461=ORIENTED_EDGE ( 'NONE', *, *, #33149, .T. ) ;
#29462=CARTESIAN_POINT ( 'NONE',  ( -22.30625920655495165, 3.783486345733975131, -0.2529928606556600679 ) ) ;
#29465=ORIENTED_EDGE ( 'NONE', *, *, #39980, .T. ) ;
#29468=DIRECTION ( 'NONE',  ( -1.000000000000000000, 0.000000000000000000, 0.000000000000000000 ) ) ;
#29478=CARTESIAN_POINT ( 'NONE',  ( -10.00000000000000178, 0.000000000000000000, 0.000000000000000000 ) ) ;
#29479=CARTESIAN_POINT ( 'NONE',  ( 2.000000000000001776, -4.409940824963369366, -5.354199675985328533 ) ) ;
#29480=LINE ( 'NONE', #38825, #55581 ) ;
#29481=CARTESIAN_POINT ( 'NONE',  ( -22.70624764888619751, 5.249808673991985586, 0.08990180771013302208 ) ) ;
#29489=CIRCLE ( 'NONE', #63477, 7.499999999999988454 ) ;
#29495=FACE_OUTER_BOUND ( 'NONE', #5318, .T. ) ;
#29500=VERTEX_POINT ( 'NONE', #10773 ) ;
#29519=CARTESIAN_POINT ( 'NONE',  ( -27.09342121492660382, 1.607500752098853347, -1.671264186073224911 ) ) ;
#29532=ORIENTED_EDGE ( 'NONE', *, *, #63655, .T. ) ;
#29538=B_SPLINE_CURVE_WITH_KNOTS ( 'NONE', 3,
 ( #10048, #16914, #16262, #36867, #41855, #9703, #62783, #40285, #50622, #61806, #30329, #5986, #11916, #1953, #26242, #37181, #52517, #60578, #26559 ),
 .UNSPECIFIED., .F., .F.,
 ( 4, 3, 3, 3, 3, 3, 4 ),
 ( 0.000000000000000000, 2.832085443685330487E-05, 4.217789847592287914E-05, 5.603488375296597566E-05, 6.989180858882679389E-05, 9.821094830335311678E-05, 0.0001178165571463684675 ),
 .UNSPECIFIED. ) ;
#29540=DIRECTION ( 'NONE',  ( 0.000000000000000000, 0.000000000000000000, 1.000000000000000000 ) ) ;
#29541=ORIENTED_EDGE ( 'NONE', *, *, #8794, .T. ) ;
#29546=CARTESIAN_POINT ( 'NONE',  ( 0.000000000000000000, -6.767909380267597363, -0.7805499053121327524 ) ) ;
#29549=VERTEX_POINT ( 'NONE', #21071 ) ;
#29559=DIRECTION ( 'NONE',  ( -1.000000000000000000, 0.000000000000000000, 0.000000000000000000 ) ) ;
#29567=AXIS2_PLACEMENT_3D ( 'NONE', #6770, #47987, #36685 ) ;
#29568=LINE ( 'NONE', #43554, #63971 ) ;
#29570=CARTESIAN_POINT ( 'NONE',  ( -35.05175862995318425, -0.01030783735685159019, 0.007207337213495368378 ) ) ;
#29586=VERTEX_POINT ( 'NONE', #26734 ) ;
#29590=CARTESIAN_POINT ( 'NONE',  ( -23.41523303002442091, 4.252418708693362248, -1.997501275420724864 ) ) ;
#29605=AXIS2_PLACEMENT_3D ( 'NONE', #42031, #58327, #46699 ) ;
#29609=LINE ( 'NONE', #14966, #40937 ) ;
#29621=CARTESIAN_POINT ( 'NONE',  ( 2.000000000000001776, 0.000000000000000000, 0.000000000000000000 ) ) ;
#29639=CARTESIAN_POINT ( 'NONE',  ( -27.32343372485684796, 3.007804754713644613, 0.1402256980610539494 ) ) ;
#29646=DIRECTION ( 'NONE',  ( 0.000000000000000000, 0.000000000000000000, 1.000000000000000000 ) ) ;
#29653=ORIENTED_EDGE ( 'NONE', *, *, #56450, .F. ) ;
#29668=AXIS2_PLACEMENT_3D ( 'NONE', #56823, #26528, #1282 ) ;
#29696=CARTESIAN_POINT ( 'NONE',  ( -22.30625920655495165, 2.110841417170918000, 3.150098859949304941 ) ) ;
#29708=ORIENTED_EDGE ( 'NONE', *, *, #17706, .F. ) ;
#29712=CARTESIAN_POINT ( 'NONE',  ( -22.31328051695926007, 3.633840107626944871, -1.076152733467184985 ) ) ;
#29713=VERTEX_POINT ( 'NONE', #63939 ) ;
#29715=LINE ( 'NONE', #24753, #56368 ) ;
#29727=EDGE_CURVE ( 'NONE', #30290, #37470, #11544, .T. ) ;
#29730=EDGE_LOOP ( 'NONE', ( #27375, #45954, #11038, #9698 ) ) ;
#29732=EDGE_LOOP ( 'NONE', ( #1400, #23969, #15512, #62099 ) ) ;
#29733=DIRECTION ( 'NONE',  ( 0.000000000000000000, 0.000000000000000000, 1.000000000000000000 ) ) ;
#29738=CARTESIAN_POINT ( 'NONE',  ( -22.23402523511428086, 1.734723475976807094E-15, -8.673617379884035472E-15 ) ) ;
#29739=AXIS2_PLACEMENT_3D ( 'NONE', #63171, #27586, #63480 ) ;
#29759=DIRECTION ( 'NONE',  ( 0.000000000000000000, 0.000000000000000000, 1.000000000000000000 ) ) ;
#29763=DIRECTION ( 'NONE',  ( 0.000000000000000000, 0.000000000000000000, -1.000000000000000000 ) ) ;
#29765=EDGE_CURVE ( 'NONE', #63874, #50124, #62367, .T. ) ;
#29774=LINE ( 'NONE', #24815, #13043 ) ;
#29775=FACE_OUTER_BOUND ( 'NONE', #28491, .T. ) ;
#29776=AXIS2_PLACEMENT_3D ( 'NONE', #622, #20884, #41152 ) ;
#29781=EDGE_LOOP ( 'NONE', ( #1292, #39919, #46221, #10551 ) ) ;
#29788=B_SPLINE_CURVE_WITH_KNOTS ( 'NONE', 3,
 ( #42762, #53753, #23152, #43415, #47771, #48116, #43094, #7519, #64040, #28459, #37790, #33122, #63694, #12837, #48761, #38101, #18524, #27471, #2223 ),
 .UNSPECIFIED., .F., .F.,
 ( 4, 3, 3, 3, 3, 3, 4 ),
 ( 3.157244383155854313E-18, 2.836829842860746890E-05, 4.224792512343399911E-05, 5.612066614708121319E-05, 6.998859278151859525E-05, 9.832141287888682374E-05, 0.0001178161482480174707 ),
 .UNSPECIFIED. ) ;
#29793=DIRECTION ( 'NONE',  ( 0.000000000000000000, 0.7621620551276376831, -0.6473862847818260269 ) ) ;
#29797=CYLINDRICAL_SURFACE ( 'NONE', #33986, 6.936499999999988120 ) ;
#29798=EDGE_CURVE ( 'NONE', #28152, #46658, #20054, .T. ) ;
#29805=CYLINDRICAL_SURFACE ( 'NONE', #36460, 7.499999999999988454 ) ;
#29807=DIRECTION ( 'NONE',  ( 0.000000000000000000, 0.000000000000000000, 1.000000000000000000 ) ) ;
#29816=ORIENTED_EDGE ( 'NONE', *, *, #35415, .T. ) ;
#29819=ORIENTED_EDGE ( 'NONE', *, *, #42398, .T. ) ;
#29829=DIRECTION ( 'NONE',  ( -1.000000000000000000, 0.000000000000000000, 0.000000000000000000 ) ) ;
#29830=CARTESIAN_POINT ( 'NONE',  ( -27.10719052120871098, 1.044362304621487825, -2.116547233941206585 ) ) ;
#29831=CIRCLE ( 'NONE', #30878, 6.936499999999988120 ) ;
#29844=CARTESIAN_POINT ( 'NONE',  ( 2.000000000000001776, -5.860254403322002759, -3.474373880649873403 ) ) ;
#29845=CARTESIAN_POINT ( 'NONE',  ( -27.10719052120871098, 1.622102031466687189, -1.714424047991080613 ) ) ;
#29847=CARTESIAN_POINT ( 'NONE',  ( 0.000000000000000000, 0.2704997240206042930, -6.931223712253475000 ) ) ;
#29848=EDGE_CURVE ( 'NONE', #14064, #55770, #25669, .T. ) ;
#29850=AXIS2_PLACEMENT_3D ( 'NONE', #18736, #64570, #38990 ) ;
#29854=AXIS2_PLACEMENT_3D ( 'NONE', #12356, #32623, #52934 ) ;
#29858=CARTESIAN_POINT ( 'NONE',  ( -22.27706485742869091, -3.662257305743835012, 0.3729136217356029959 ) ) ;
#29860=CIRCLE ( 'NONE', #10734, 6.936499999999989008 ) ;
#29871=CYLINDRICAL_SURFACE ( 'NONE', #60547, 2.899999999999994582 ) ;
#29878=CARTESIAN_POINT ( 'NONE',  ( 2.000000000000001776, 0.000000000000000000, 0.000000000000000000 ) ) ;
#29887=DIRECTION ( 'NONE',  ( 0.000000000000000000, -0.2149704402110114709, -0.9766205557100894330 ) ) ;
#29893=CARTESIAN_POINT ( 'NONE',  ( -22.27719412087655471, -3.421752300520421120, -1.358750377066208825 ) ) ;
#29922=EDGE_LOOP ( 'NONE', ( #53729, #51578, #11300, #49337 ) ) ;
#29926=CYLINDRICAL_SURFACE ( 'NONE', #41494, 6.936499999999988120 ) ;
#29928=DIRECTION ( 'NONE',  ( -1.000000000000000000, 0.000000000000000000, 0.000000000000000000 ) ) ;
#29933=EDGE_CURVE ( 'NONE', #22075, #12068, #57246, .T. ) ;
#29936=CARTESIAN_POINT ( 'NONE',  ( 2.000000000000001776, -1.145812388885072863, -6.715725538143620277 ) ) ;
#29941=AXIS2_PLACEMENT_3D ( 'NONE', #40560, #55865, #20929 ) ;
#29942=AXIS2_PLACEMENT_3D ( 'NONE', #16715, #36990, #57294 ) ;
#29950=ADVANCED_FACE ( 'NONE', ( #51291 ), #47593, .T. ) ;
#29962=VECTOR ( 'NONE', #31622, 1000.000000000000000 ) ;
#29963=CARTESIAN_POINT ( 'NONE',  ( -35.04660725145885891, -0.01223081933017596858, 0.001288602543471934793 ) ) ;
#29967=EDGE_CURVE ( 'NONE', #35715, #37190, #31949, .T. ) ;
#29993=ORIENTED_EDGE ( 'NONE', *, *, #48499, .F. ) ;
#30001=CARTESIAN_POINT ( 'NONE',  ( -10.00000000000000178, 0.000000000000000000, 0.000000000000000000 ) ) ;
#30003=CARTESIAN_POINT ( 'NONE',  ( -22.27721688985630522, 0.6032462375556890688, 3.631967556481303649 ) ) ;
#30024=CARTESIAN_POINT ( 'NONE',  ( 2.000000000000001776, 5.585096664091999230, -4.113602740025892324 ) ) ;
#30030=EDGE_CURVE ( 'NONE', #44248, #30290, #60241, .T. ) ;
#30062=CARTESIAN_POINT ( 'NONE',  ( 2.000000000000001776, 0.000000000000000000, 0.000000000000000000 ) ) ;
#30063=CARTESIAN_POINT ( 'NONE',  ( -22.66110217412718342, -3.020638270782523449, 3.914841338650325131 ) ) ;
#30073=VERTEX_POINT ( 'NONE', #13637 ) ;
#30076=CARTESIAN_POINT ( 'NONE',  ( 0.000000000000000000, -3.937687286050771895, -6.383151168292510391 ) ) ;
#30095=CARTESIAN_POINT ( 'NONE',  ( 2.000000000000001776, 6.160607635185406217, 4.277489166005578269 ) ) ;
#30096=CARTESIAN_POINT ( 'NONE',  ( -27.09048036756592381, -2.303144499688043911, 0.1785511875142930804 ) ) ;
#30107=EDGE_CURVE ( 'NONE', #4916, #57516, #57080, .T. ) ;
#30112=DIRECTION ( 'NONE',  ( -1.000000000000000000, 0.000000000000000000, 0.000000000000000000 ) ) ;
#30120=CARTESIAN_POINT ( 'NONE',  ( -27.08429572838383947, -2.089332284968714593, -0.9410937941434025511 ) ) ;
#30134=B_SPLINE_CURVE_WITH_KNOTS ( 'NONE', 3,
 ( #60911, #20009, #51275, #721, #15656, #45597, #11022, #10038, #35932, #61885, #40272, #30319, #36276 ),
 .UNSPECIFIED., .F., .F.,
 ( 4, 3, 3, 3, 4 ),
 ( 2.424349759030287857E-18, 6.990956068646416019E-05, 0.0001398191187764045215, 0.0002097286751720215173, 0.0002792983885906414167 ),
 .UNSPECIFIED. ) ;
#30137=VERTEX_POINT ( 'NONE', #60844 ) ;
#30142=CARTESIAN_POINT ( 'NONE',  ( 2.000000000000001776, 6.936109781200720192, -2.853135311044974198 ) ) ;
#30145=EDGE_CURVE ( 'NONE', #10633, #14359, #15705, .T. ) ;
#30158=VERTEX_POINT ( 'NONE', #15286 ) ;
#30166=CARTESIAN_POINT ( 'NONE',  ( 2.000000000000001776, 4.976357229393855164, 4.652926418895560801 ) ) ;
#30167=VERTEX_POINT ( 'NONE', #59534 ) ;
#30168=EDGE_LOOP ( 'NONE', ( #63505, #24368, #55171, #20870 ) ) ;
#30191=CARTESIAN_POINT ( 'NONE',  ( 0.000000000000000000, 0.000000000000000000, 0.000000000000000000 ) ) ;
#30198=EDGE_CURVE ( 'NONE', #18188, #29586, #5107, .T. ) ;
#30208=DIRECTION ( 'NONE',  ( -1.000000000000000000, 0.000000000000000000, 0.000000000000000000 ) ) ;
#30211=CARTESIAN_POINT ( 'NONE',  ( -27.35552965826137140, -0.2619431035391951434, 3.094132632038943065 ) ) ;
#30215=CARTESIAN_POINT ( 'NONE',  ( 0.000000000000000000, 6.470132594555847660, -2.133363481234036296 ) ) ;
#30228=VERTEX_POINT ( 'NONE', #64503 ) ;
#30246=ORIENTED_EDGE ( 'NONE', *, *, #59107, .F. ) ;
#30247=FACE_OUTER_BOUND ( 'NONE', #39682, .T. ) ;
#30259=ORIENTED_EDGE ( 'NONE', *, *, #35072, .F. ) ;
#30267=CARTESIAN_POINT ( 'NONE',  ( 2.000000000000001776, -3.230174184210094168, 5.998318953995296354 ) ) ;
#30272=FACE_OUTER_BOUND ( 'NONE', #47081, .T. ) ;
#30278=EDGE_CURVE ( 'NONE', #9709, #1625, #663, .T. ) ;
#30283=ORIENTED_EDGE ( 'NONE', *, *, #1531, .T. ) ;
#30284=CARTESIAN_POINT ( 'NONE',  ( 0.000000000000000000, -3.341639490130797530, 6.078525953551414673 ) ) ;
#30290=VERTEX_POINT ( 'NONE', #7863 ) ;
#30298=CARTESIAN_POINT ( 'NONE',  ( 2.000000000000001776, 5.860254403322016969, 3.474373880649828550 ) ) ;
#30306=CARTESIAN_POINT ( 'NONE',  ( -27.08954555554413801, -1.307633183325040749, -1.900922216193322134 ) ) ;
#30311=CARTESIAN_POINT ( 'NONE',  ( -22.27722019094931127, -3.623977093944207084, 0.6491642780571700300 ) ) ;
#30312=CARTESIAN_POINT ( 'NONE',  ( 1.000000000000000888, 4.604744433234674972, 5.919993978425482695 ) ) ;
#30319=CARTESIAN_POINT ( 'NONE',  ( -22.27722019117889829, 0.6723250025933701357, 3.619826115298641511 ) ) ;
#30323=CARTESIAN_POINT ( 'NONE',  ( 2.000000000000001776, 6.539067737394503865, 2.314222412769824544 ) ) ;
#30326=CARTESIAN_POINT ( 'NONE',  ( -22.31213670151049300, 0.2530575063956244097, 3.777944311993711057 ) ) ;
#30328=LINE ( 'NONE', #10356, #63177 ) ;
#30329=CARTESIAN_POINT ( 'NONE',  ( -27.09125059358712306, 1.662156772100933377, 1.607567221344176067 ) ) ;
#30338=EDGE_CURVE ( 'NONE', #2871, #30167, #32761, .T. ) ;
#30353=ORIENTED_EDGE ( 'NONE', *, *, #41690, .T. ) ;
#30356=CARTESIAN_POINT ( 'NONE',  ( -27.09125059358653331, -2.223272438024535003, 0.6356863790372223599 ) ) ;
#30361=CARTESIAN_POINT ( 'NONE',  ( 2.000000000000001776, 4.472310526050855550, -6.020667617347345235 ) ) ;
#30373=ORIENTED_EDGE ( 'NONE', *, *, #4807, .F. ) ;
#30383=CARTESIAN_POINT ( 'NONE',  ( 2.000000000000001776, 0.000000000000000000, 0.000000000000000000 ) ) ;
#30384=CARTESIAN_POINT ( 'NONE',  ( 2.000000000000001776, -1.530946385938319443, -7.342084388195388556 ) ) ;
#30396=CYLINDRICAL_SURFACE ( 'NONE', #36466, 6.936499999999988120 ) ;
#30401=VERTEX_POINT ( 'NONE', #28139 ) ;
#30403=EDGE_CURVE ( 'NONE', #38732, #55770, #4052, .T. ) ;
#30405=CARTESIAN_POINT ( 'NONE',  ( 2.000000000000001776, 0.000000000000000000, 0.000000000000000000 ) ) ;
#30411=CARTESIAN_POINT ( 'NONE',  ( -22.30625920655495165, -0.2529928606556531290, -3.783486345733990674 ) ) ;
#30421=ORIENTED_EDGE ( 'NONE', *, *, #28748, .T. ) ;
#30423=CARTESIAN_POINT ( 'NONE',  ( -27.09729107899852352, -2.324833743198345015, 0.1622107421537080929 ) ) ;
#30427=ADVANCED_FACE ( 'NONE', ( #63684 ), #29124, .T. ) ;
#30433=( LENGTH_UNIT ( ) NAMED_UNIT ( * ) SI_UNIT ( .MILLI., .METRE. ) );
#30436=CARTESIAN_POINT ( 'NONE',  ( -27.10719052120871098, -2.355164825213512003, 0.1538293304135223694 ) ) ;
#30439=FACE_OUTER_BOUND ( 'NONE', #12187, .T. ) ;
#30446=AXIS2_PLACEMENT_3D ( 'NONE', #52890, #7324, #27610 ) ;
#30450=ORIENTED_EDGE ( 'NONE', *, *, #10794, .F. ) ;
#30458=CARTESIAN_POINT ( 'NONE',  ( -22.29570301036918423, -1.042190670255880969, -3.588849529203750777 ) ) ;
#30460=VERTEX_POINT ( 'NONE', #3867 ) ;
#30461=CARTESIAN_POINT ( 'NONE',  ( -27.08702828306175903, 2.226264228964708103, 0.5765135930308941115 ) ) ;
#30462=EDGE_CURVE ( 'NONE', #5331, #59201, #9150, .T. ) ;
#30463=CARTESIAN_POINT ( 'NONE',  ( -26.43258404273186812, -3.465947334857392370, -0.2934201954354464514 ) ) ;
#30467=( BOUNDED_SURFACE ( )  B_SPLINE_SURFACE ( 3, 1, ( 
 ( #26020, #25349 ),
 ( #40305, #65570 ),
 ( #61253, #40974 ),
 ( #15037, #78 ) ),
 .UNSPECIFIED., .F., .F., .F. ) 
 B_SPLINE_SURFACE_WITH_KNOTS ( ( 4, 4 ),
 ( 2, 2 ),
 ( 0.000000000000000000, 1.000000000000000000 ),
 ( 0.000000000000000000, 1.000000000000000000 ),
 .UNSPECIFIED. ) 
 GEOMETRIC_REPRESENTATION_ITEM ( )  RATIONAL_B_SPLINE_SURFACE ( (
 ( 1.000000000000000000, 1.000000000000000000),
 ( 0.8716676215708681896, 0.8964445200148167814),
 ( 0.8716676215708681896, 0.8964445200148167814),
 ( 1.000000000000000000, 1.000000000000000000) ) ) 
 REPRESENTATION_ITEM ( '' )  SURFACE ( )  );
#30475=ORIENTED_EDGE ( 'NONE', *, *, #35946, .F. ) ;
#30477=CARTESIAN_POINT ( 'NONE',  ( 2.000000000000001776, 0.3246585432987117992, -6.805031400696120336 ) ) ;
#30480=ORIENTED_EDGE ( 'NONE', *, *, #17954, .F. ) ;
#30481=DIRECTION ( 'NONE',  ( -1.000000000000000000, 0.000000000000000000, 0.000000000000000000 ) ) ;
#30484=CARTESIAN_POINT ( 'NONE',  ( -22.27719412087655471, -1.358750377066196835, 3.421752300520410905 ) ) ;
#30486=ORIENTED_EDGE ( 'NONE', *, *, #36412, .T. ) ;
#30487=CARTESIAN_POINT ( 'NONE',  ( 2.000000000000001776, -3.152010634611648321, -6.039758645301327000 ) ) ;
#30489=CARTESIAN_POINT ( 'NONE',  ( 0.000000000000000000, 1.956810415765184219, 6.654767106875543625 ) ) ;
#30494=DIRECTION ( 'NONE',  ( -1.000000000000000000, 0.000000000000000000, 0.000000000000000000 ) ) ;
#30516=ORIENTED_EDGE ( 'NONE', *, *, #32550, .F. ) ;
#30529=EDGE_CURVE ( 'NONE', #50166, #9014, #40101, .T. ) ;
#30531=CARTESIAN_POINT ( 'NONE',  ( -26.74023318801843274, -3.035730054944082212, 1.425982498898165751 ) ) ;
#30532=AXIS2_PLACEMENT_3D ( 'NONE', #20459, #40735, #61024 ) ;
#30533=CARTESIAN_POINT ( 'NONE',  ( -22.27218376572352554, -0.9890213205919480277, -3.547715993389686240 ) ) ;
#30536=CIRCLE ( 'NONE', #42209, 2.899999999999997247 ) ;
#30539=CYLINDRICAL_SURFACE ( 'NONE', #5345, 2.899999999999994582 ) ;
#30543=CARTESIAN_POINT ( 'NONE',  ( -22.27706485742869091, -3.547445275915918295, -0.9832726768967802178 ) ) ;
#30546=EDGE_CURVE ( 'NONE', #48610, #18591, #41046, .T. ) ;
#30549=ORIENTED_EDGE ( 'NONE', *, *, #35495, .T. ) ;
#30553=CARTESIAN_POINT ( 'NONE',  ( -27.09861164373112530, 1.936722219469636963, -1.303360234155686026 ) ) ;
#30554=ORIENTED_EDGE ( 'NONE', *, *, #25284, .T. ) ;
#30558=DIRECTION ( 'NONE',  ( -1.000000000000000000, 0.000000000000000000, 0.000000000000000000 ) ) ;
#30564=EDGE_CURVE ( 'NONE', #39365, #28622, #23665, .T. ) ;
#30571=CARTESIAN_POINT ( 'NONE',  ( 2.000000000000001776, 6.750946897830712778, 1.593658756657066355 ) ) ;
#30577=CARTESIAN_POINT ( 'NONE',  ( 0.000000000000000000, 0.4129979343797385294, 6.800241778083691457 ) ) ;
#30579=CYLINDRICAL_SURFACE ( 'NONE', #47631, 6.936499999999988120 ) ;
#30585=DIRECTION ( 'NONE',  ( 0.000000000000000000, 0.000000000000000000, 1.000000000000000000 ) ) ;
#30590=FACE_OUTER_BOUND ( 'NONE', #57972, .T. ) ;
#30596=EDGE_LOOP ( 'NONE', ( #52146, #16984, #19927, #5756 ) ) ;
#30597=EDGE_CURVE ( 'NONE', #65063, #32207, #30731, .T. ) ;
#30605=EDGE_CURVE ( 'NONE', #21169, #20211, #19801, .T. ) ;
#30609=AXIS2_PLACEMENT_3D ( 'NONE', #901, #6888, #1892 ) ;
#30611=CIRCLE ( 'NONE', #52941, 7.499999999999988454 ) ;
#30613=DIRECTION ( 'NONE',  ( -1.000000000000000000, 0.000000000000000000, 0.000000000000000000 ) ) ;
#30637=ORIENTED_EDGE ( 'NONE', *, *, #61719, .F. ) ;
#30640=DIRECTION ( 'NONE',  ( 0.000000000000000000, -0.6051742151937717917, 0.7960930657056387583 ) ) ;
#30641=DIRECTION ( 'NONE',  ( 0.000000000000000000, 0.000000000000000000, 1.000000000000000000 ) ) ;
#30642=CARTESIAN_POINT ( 'NONE',  ( -22.46509356695213455, -3.157489876851681032, -2.840174833751851313 ) ) ;
#30646=CARTESIAN_POINT ( 'NONE',  ( -27.08423805673873375, 2.229265646063317341, -0.5302040644010300730 ) ) ;
#30649=ORIENTED_EDGE ( 'NONE', *, *, #38897, .T. ) ;
#30650=DIRECTION ( 'NONE',  ( 0.9606638835031803270, 0.1629100154396158073, 0.2249116044183853413 ) ) ;
#30652=VECTOR ( 'NONE', #28706, 1000.000000000000000 ) ;
#30654=ORIENTED_EDGE ( 'NONE', *, *, #63208, .F. ) ;
#30657=EDGE_LOOP ( 'NONE', ( #49228, #59485 ) ) ;
#30660=CARTESIAN_POINT ( 'NONE',  ( -27.08430792439081003, -2.215465963318195008, 0.5856059198894537632 ) ) ;
#30662=CYLINDRICAL_SURFACE ( 'NONE', #32987, 2.899999999999994582 ) ;
#30666=EDGE_CURVE ( 'NONE', #13558, #1201, #44385, .T. ) ;
#30670=CARTESIAN_POINT ( 'NONE',  ( 0.000000000000000000, 6.201547234537035713, 2.820401998297911383 ) ) ;
#30671=CARTESIAN_POINT ( 'NONE',  ( 2.000000000000001776, -6.470132594555779271, -2.133363481234176628 ) ) ;
#30673=CARTESIAN_POINT ( 'NONE',  ( 1.000000000000000888, 0.8935325819928834346, 7.446583077151348817 ) ) ;
#30684=CARTESIAN_POINT ( 'NONE',  ( -27.04788180060269198, -1.844972430941754782, 2.650714769830304185 ) ) ;
#30699=AXIS2_PLACEMENT_3D ( 'NONE', #11445, #37039, #16113 ) ;
#30703=EDGE_CURVE ( 'NONE', #38516, #18227, #22754, .T. ) ;
#30704=DIRECTION ( 'NONE',  ( 0.9582930651793754029, 0.2370079598497654427, -0.1596922922278005419 ) ) ;
#30705=DIRECTION ( 'NONE',  ( -1.000000000000000000, 0.000000000000000000, 0.000000000000000000 ) ) ;
#30707=DIRECTION ( 'NONE',  ( -1.000000000000000000, 0.000000000000000000, 0.000000000000000000 ) ) ;
#30713=ORIENTED_EDGE ( 'NONE', *, *, #56288, .T. ) ;
#30727=CARTESIAN_POINT ( 'NONE',  ( -27.08429572838383947, 1.859677275556428810, -1.338867938658195200 ) ) ;
#30730=ORIENTED_EDGE ( 'NONE', *, *, #42693, .T. ) ;
#30731=LINE ( 'NONE', #9802, #27402 ) ;
#30738=DIRECTION ( 'NONE',  ( -1.000000000000000000, 0.000000000000000000, 0.000000000000000000 ) ) ;
#30750=VECTOR ( 'NONE', #3835, 1000.000000000000000 ) ;
#30752=DIRECTION ( 'NONE',  ( 0.000000000000000000, 0.000000000000000000, 1.000000000000000000 ) ) ;
#30760=EDGE_CURVE ( 'NONE', #39372, #47492, #52023, .T. ) ;
#30761=CARTESIAN_POINT ( 'NONE',  ( 2.000000000000001776, 6.935703035393450122, 0.1051458740707594125 ) ) ;
#30767=ORIENTED_EDGE ( 'NONE', *, *, #4760, .T. ) ;
#30768=CYLINDRICAL_SURFACE ( 'NONE', #53603, 6.936499999999988120 ) ;
#30769=CARTESIAN_POINT ( 'NONE',  ( 0.000000000000000000, -1.145812388885151023, 6.715725538143585638 ) ) ;
#30773=FACE_OUTER_BOUND ( 'NONE', #64887, .T. ) ;
#30775=AXIS2_PLACEMENT_3D ( 'NONE', #13290, #7649, #27931 ) ;
#30776=CARTESIAN_POINT ( 'NONE',  ( 2.000000000000001776, -5.457833520448623688, -4.281014542496604847 ) ) ;
#30782=LINE ( 'NONE', #9862, #34205 ) ;
#30787=VERTEX_POINT ( 'NONE', #38694 ) ;
#30804=FACE_OUTER_BOUND ( 'NONE', #1687, .T. ) ;
#30807=CARTESIAN_POINT ( 'NONE',  ( -27.09729107899804745, 1.021938248125928261, -2.094470452260987159 ) ) ;
#30809=CARTESIAN_POINT ( 'NONE',  ( -10.00000000000000178, 0.000000000000000000, 0.000000000000000000 ) ) ;
#30812=EDGE_CURVE ( 'NONE', #3623, #51096, #38030, .T. ) ;
#30819=CARTESIAN_POINT ( 'NONE',  ( 2.000000000000001776, 0.000000000000000000, 0.000000000000000000 ) ) ;
#30823=B_SPLINE_CURVE_WITH_KNOTS ( 'NONE', 3,
 ( #24372, #30660, #39675, #45639, #40654, #59972, #40314, #15044, #55638, #10075, #30356, #89, #35969, #752, #56268, #21013, #26341, #6398, #10712 ),
 .UNSPECIFIED., .F., .F.,
 ( 4, 3, 3, 3, 3, 3, 4 ),
 ( 0.000000000000000000, 2.832085443540696562E-05, 4.217789847394769317E-05, 5.603488375046152285E-05, 6.989180858579407713E-05, 9.821094829918835742E-05, 0.0001178165571465097797 ),
 .UNSPECIFIED. ) ;
#30824=LINE ( 'NONE', #915, #60570 ) ;
#30830=CIRCLE ( 'NONE', #24475, 2.899999999999994582 ) ;
#30833=CARTESIAN_POINT ( 'NONE',  ( -22.29290468048228036, -3.718584170466873839, 0.2747050847461821599 ) ) ;
#30836=CARTESIAN_POINT ( 'NONE',  ( 1.000000000000000888, -5.217815162096798076, -5.387430271863655307 ) ) ;
#30837=EDGE_CURVE ( 'NONE', #2509, #4485, #16773, .T. ) ;
#30841=DIRECTION ( 'NONE',  ( -1.000000000000000000, 0.000000000000000000, 0.000000000000000000 ) ) ;
#30842=CARTESIAN_POINT ( 'NONE',  ( -22.46225619532221529, 3.746472695305362421, 1.978788174090766017 ) ) ;
#30846=CIRCLE ( 'NONE', #51055, 2.899999999999994582 ) ;
#30849=EDGE_LOOP ( 'NONE', ( #12725, #2105, #3675, #39157 ) ) ;
#30852=ORIENTED_EDGE ( 'NONE', *, *, #241, .F. ) ;
#30859=VERTEX_POINT ( 'NONE', #64922 ) ;
#30862=AXIS2_PLACEMENT_3D ( 'NONE', #54230, #29281, #55195 ) ;
#30865=CARTESIAN_POINT ( 'NONE',  ( -22.27722015946438816, -3.455127654605128829, -1.271715168852078026 ) ) ;
#30870=ORIENTED_EDGE ( 'NONE', *, *, #50707, .T. ) ;
#30871=CIRCLE ( 'NONE', #43649, 2.899999999999996358 ) ;
#30872=EDGE_CURVE ( 'NONE', #55446, #14676, #61379, .T. ) ;
#30877=EDGE_CURVE ( 'NONE', #53881, #25961, #64553, .T. ) ;
#30878=AXIS2_PLACEMENT_3D ( 'NONE', #29391, #39043, #18468 ) ;
#30879=CARTESIAN_POINT ( 'NONE',  ( -27.09729107899804390, 1.932259710106502215, -1.302895495070934162 ) ) ;
#30880=AXIS2_PLACEMENT_3D ( 'NONE', #18190, #13194, #27830 ) ;
#30884=ORIENTED_EDGE ( 'NONE', *, *, #15172, .F. ) ;
#30889=CARTESIAN_POINT ( 'NONE',  ( -27.10719052120871098, -2.295785794152564563, -0.5475695427849640584 ) ) ;
#30892=DIRECTION ( 'NONE',  ( -1.000000000000000000, 0.000000000000000000, 0.000000000000000000 ) ) ;
#30902=CARTESIAN_POINT ( 'NONE',  ( -27.35552965826137140, 1.773915698030573473, -2.548625910254528559 ) ) ;
#30918=CIRCLE ( 'NONE', #2265, 2.899999999999995026 ) ;
#30922=CARTESIAN_POINT ( 'NONE',  ( 2.000000000000001776, 0.000000000000000000, 0.000000000000000000 ) ) ;
#30923=AXIS2_PLACEMENT_3D ( 'NONE', #36946, #58229, #53246 ) ;
#30932=ORIENTED_EDGE ( 'NONE', *, *, #55778, .F. ) ;
#30935=B_SPLINE_CURVE_WITH_KNOTS ( 'NONE', 3,
 ( #35727, #60353, #14778, #50065, #55040, #55714, #50722, #40063, #4179, #65654, #61335, #35405, #35061, #4524, #20782, #5172, #65009, #56021, #15772, #19482, #50407, #36050 ),
 .UNSPECIFIED., .F., .F.,
 ( 4, 3, 3, 3, 3, 3, 3, 4 ),
 ( 0.000000000000000000, 6.990956068646445834E-05, 0.0001398191187764044672, 0.0002097286751720215444, 0.0002796382307041364807, 0.0003495477861619816708, 0.0004194573423310295505, 0.0005586102576333146046 ),
 .UNSPECIFIED. ) ;
#30943=CARTESIAN_POINT ( 'NONE',  ( -35.04709527796842394, -0.01016988845958625987, -0.007030359780627049027 ) ) ;
#30946=DIRECTION ( 'NONE',  ( -1.000000000000000000, 0.000000000000000000, 0.000000000000000000 ) ) ;
#30962=ORIENTED_EDGE ( 'NONE', *, *, #61930, .T. ) ;
#30964=AXIS2_PLACEMENT_3D ( 'NONE', #44161, #14219, #23564 ) ;
#30968=EDGE_CURVE ( 'NONE', #44673, #54109, #26360, .T. ) ;
#30979=ORIENTED_EDGE ( 'NONE', *, *, #39635, .F. ) ;
#30983=CARTESIAN_POINT ( 'NONE',  ( -22.31328051695926007, -2.748895659348118858, -2.608921479762132734 ) ) ;
#30993=DIRECTION ( 'NONE',  ( 0.000000000000000000, -0.8276889981568841259, -0.5611870653623918237 ) ) ;
#31000=DIRECTION ( 'NONE',  ( -1.000000000000000000, 0.000000000000000000, 0.000000000000000000 ) ) ;
#31021=CARTESIAN_POINT ( 'NONE',  ( -22.66110217412718697, -2.319520136975679492, -4.366928509133845004 ) ) ;
#31031=LINE ( 'NONE', #20736, #19329 ) ;
#31032=DIRECTION ( 'NONE',  ( 0.000000000000000000, -0.7621620551276289124, -0.6473862847818364630 ) ) ;
#31034=CARTESIAN_POINT ( 'NONE',  ( 1.000000000000000888, -5.769711778877296027, -4.791703871138604853 ) ) ;
#31036=CARTESIAN_POINT ( 'NONE',  ( -22.27706089016750113, 3.562910635974989582, -0.9256273512588409913 ) ) ;
#31041=VERTEX_POINT ( 'NONE', #27635 ) ;
#31042=VERTEX_POINT ( 'NONE', #12018 ) ;
#31044=AXIS2_PLACEMENT_3D ( 'NONE', #30769, #16155, #25470 ) ;
#31049=CARTESIAN_POINT ( 'NONE',  ( -22.29382655386184453, -3.584644999358097550, 1.036465316386247393 ) ) ;
#31055=CIRCLE ( 'NONE', #17257, 6.936499999999988120 ) ;
#31063=ORIENTED_EDGE ( 'NONE', *, *, #35605, .F. ) ;
#31071=CARTESIAN_POINT ( 'NONE',  ( 2.000000000000001776, 7.484036900328571384, -0.4890722589968761191 ) ) ;
#31079=ADVANCED_FACE ( 'NONE', ( #12343 ), #16017, .T. ) ;
#31083=AXIS2_PLACEMENT_3D ( 'NONE', #46513, #60489, #25245 ) ;
#31095=CARTESIAN_POINT ( 'NONE',  ( -35.04683013664716640, -0.01162359816264506296, 0.004196202180946132648 ) ) ;
#31096=ADVANCED_FACE ( 'NONE', ( #52287 ), #46619, .T. ) ;
#31099=CARTESIAN_POINT ( 'NONE',  ( -22.49803948133828513, 2.269619744675257067, 3.704553751086659297 ) ) ;
#31102=CYLINDRICAL_SURFACE ( 'NONE', #25858, 6.936499999999988120 ) ;
#31118=CARTESIAN_POINT ( 'NONE',  ( 2.000000000000001776, -6.777474576704061171, -0.6925993764991672519 ) ) ;
#31120=VECTOR ( 'NONE', #46505, 999.9999999999998863 ) ;
#31137=AXIS2_PLACEMENT_3D ( 'NONE', #33633, #42595, #12673 ) ;
#31145=ADVANCED_FACE ( 'NONE', ( #39253 ), #59548, .T. ) ;
#31149=CARTESIAN_POINT ( 'NONE',  ( 0.000000000000000000, 7.484036900328563391, 0.4890722589969403455 ) ) ;
#31153=AXIS2_PLACEMENT_3D ( 'NONE', #27054, #1789, #42308 ) ;
#31156=VERTEX_POINT ( 'NONE', #43932 ) ;
#31164=DIRECTION ( 'NONE',  ( -1.000000000000000000, 0.000000000000000000, 0.000000000000000000 ) ) ;
#31168=CARTESIAN_POINT ( 'NONE',  ( 0.000000000000000000, 0.2704997240205054276, 6.931223712253452796 ) ) ;
#31179=LINE ( 'NONE', #56444, #44030 ) ;
#31188=EDGE_CURVE ( 'NONE', #47952, #57499, #58239, .T. ) ;
#31213=VERTEX_POINT ( 'NONE', #63864 ) ;
#31215=ORIENTED_EDGE ( 'NONE', *, *, #35469, .T. ) ;
#31216=EDGE_CURVE ( 'NONE', #28521, #59877, #17926, .T. ) ;
#31217=DIRECTION ( 'NONE',  ( -1.000000000000000000, 0.000000000000000000, 0.000000000000000000 ) ) ;
#31219=CARTESIAN_POINT ( 'NONE',  ( -22.27718150314433387, -3.507884203786629129, -1.117371044661094937 ) ) ;
#31227=ORIENTED_EDGE ( 'NONE', *, *, #39929, .T. ) ;
#31233=CARTESIAN_POINT ( 'NONE',  ( -22.27719443589224113, 3.601617131804403016, -0.7635131876694990494 ) ) ;
#31241=VERTEX_POINT ( 'NONE', #49271 ) ;
#31250=DIRECTION ( 'NONE',  ( -1.000000000000000000, 0.000000000000000000, 0.000000000000000000 ) ) ;
#31255=ORIENTED_EDGE ( 'NONE', *, *, #61041, .F. ) ;
#31256=DIRECTION ( 'NONE',  ( -1.000000000000000000, 0.000000000000000000, 0.000000000000000000 ) ) ;
#31257=ORIENTED_EDGE ( 'NONE', *, *, #53553, .F. ) ;
#31258=DIRECTION ( 'NONE',  ( -1.000000000000000000, 0.000000000000000000, 0.000000000000000000 ) ) ;
#31269=( BOUNDED_SURFACE ( )  B_SPLINE_SURFACE ( 3, 1, ( 
 ( #13571, #44479 ),
 ( #49190, #14541 ),
 ( #64439, #39175 ),
 ( #34185, #55124 ) ),
 .UNSPECIFIED., .F., .F., .F. ) 
 B_SPLINE_SURFACE_WITH_KNOTS ( ( 4, 4 ),
 ( 2, 2 ),
 ( 0.000000000000000000, 1.000000000000000000 ),
 ( 0.000000000000000000, 1.000000000000000000 ),
 .UNSPECIFIED. ) 
 GEOMETRIC_REPRESENTATION_ITEM ( )  RATIONAL_B_SPLINE_SURFACE ( (
 ( 1.000000000000000000, 1.000000000000000000),
 ( 0.9932032654565553509, 0.8386279382598736953),
 ( 0.9932032654565553509, 0.8386279382598736953),
 ( 1.000000000000000000, 1.000000000000000000) ) ) 
 REPRESENTATION_ITEM ( '' )  SURFACE ( )  );
#31270=ORIENTED_EDGE ( 'NONE', *, *, #42702, .T. ) ;
#31275=LINE ( 'NONE', #693, #7342 ) ;
#31277=VECTOR ( 'NONE', #44057, 1000.000000000000000 ) ;
#31280=DIRECTION ( 'NONE',  ( 0.000000000000000000, 0.8835120444460240474, -0.4684084406997882088 ) ) ;
#31281=CARTESIAN_POINT ( 'NONE',  ( 2.000000000000001776, 3.859771122243123465, -5.613913289150012531 ) ) ;
#31282=CARTESIAN_POINT ( 'NONE',  ( 0.000000000000000000, 0.000000000000000000, 0.000000000000000000 ) ) ;
#31285=LINE ( 'NONE', #41906, #26409 ) ;
#31298=ORIENTED_EDGE ( 'NONE', *, *, #38635, .T. ) ;
#31300=ORIENTED_EDGE ( 'NONE', *, *, #40148, .F. ) ;
#31301=DIRECTION ( 'NONE',  ( 0.000000000000000000, 0.000000000000000000, 1.000000000000000000 ) ) ;
#31302=AXIS2_PLACEMENT_3D ( 'NONE', #18615, #1985, #64137 ) ;
#31303=CARTESIAN_POINT ( 'NONE',  ( -22.71097035706202760, 2.118550233809425087, 4.510116093748266053 ) ) ;
#31307=DIRECTION ( 'NONE',  ( 0.000000000000000000, 0.000000000000000000, 1.000000000000000000 ) ) ;
#31309=CARTESIAN_POINT ( 'NONE',  ( -22.28629837673888048, 0.2936941584814525275, 3.697248502489080213 ) ) ;
#31321=CARTESIAN_POINT ( 'NONE',  ( 0.000000000000000000, -5.860254403322002759, -3.474373880649873403 ) ) ;
#31331=CIRCLE ( 'NONE', #15377, 6.936499999999986343 ) ;
#31332=EDGE_LOOP ( 'NONE', ( #37898, #33938, #6077, #54226 ) ) ;
#31339=DIRECTION ( 'NONE',  ( -1.000000000000000000, 0.000000000000000000, 0.000000000000000000 ) ) ;
#31340=DIRECTION ( 'NONE',  ( -1.000000000000000000, 0.000000000000000000, 0.000000000000000000 ) ) ;
#31343=ORIENTED_EDGE ( 'NONE', *, *, #65175, .F. ) ;
#31344=DIRECTION ( 'NONE',  ( -1.000000000000000000, 0.000000000000000000, 0.000000000000000000 ) ) ;
#31345=CARTESIAN_POINT ( 'NONE',  ( -22.31328051695926007, -2.109671368890623455, -3.148362328073181615 ) ) ;
#31348=CARTESIAN_POINT ( 'NONE',  ( -27.10128162969832388, -1.032914450114644334, 2.102429195189571942 ) ) ;
#31351=CARTESIAN_POINT ( 'NONE',  ( -22.51237073810381162, -2.395115314842884757, -3.719289647955750233 ) ) ;
#31370=DIRECTION ( 'NONE',  ( -1.000000000000000000, 0.000000000000000000, 0.000000000000000000 ) ) ;
#31381=CARTESIAN_POINT ( 'NONE',  ( -22.28856623400852044, -3.573466130470485780, 1.018212315222191355 ) ) ;
#31382=DIRECTION ( 'NONE',  ( -1.000000000000000000, 0.000000000000000000, 0.000000000000000000 ) ) ;
#31392=ORIENTED_EDGE ( 'NONE', *, *, #16498, .T. ) ;
#31406=ORIENTED_EDGE ( 'NONE', *, *, #54758, .T. ) ;
#31410=ADVANCED_FACE ( 'NONE', ( #35577 ), #30579, .T. ) ;
#31411=ORIENTED_EDGE ( 'NONE', *, *, #35521, .T. ) ;
#31414=DIRECTION ( 'NONE',  ( 1.000000000000000000, 0.000000000000000000, 0.000000000000000000 ) ) ;
#31415=CARTESIAN_POINT ( 'NONE',  ( -22.29978294495153790, 1.052446240539720357, 3.598607126810713375 ) ) ;
#31423=CIRCLE ( 'NONE', #17634, 2.899999999999995026 ) ;
#31427=DIRECTION ( 'NONE',  ( 0.9606638835031803270, -0.2762341707520458711, 0.02862840969242822636 ) ) ;
#31437=EDGE_CURVE ( 'NONE', #50142, #57779, #1668, .T. ) ;
#31444=ORIENTED_EDGE ( 'NONE', *, *, #9284, .F. ) ;
#31446=FACE_OUTER_BOUND ( 'NONE', #25232, .T. ) ;
#31449=CARTESIAN_POINT ( 'NONE',  ( -22.76187086591099984, 0.9059972289356981179, 5.055065309934907880 ) ) ;
#31453=CARTESIAN_POINT ( 'NONE',  ( -26.74023318801842919, -3.342010596062586547, -0.2829279580742295463 ) ) ;
#31454=EDGE_LOOP ( 'NONE', ( #36381, #25640, #10971, #62164 ) ) ;
#31455=CARTESIAN_POINT ( 'NONE',  ( -22.51237073810381517, 3.719289647955755118, -2.395115314842871435 ) ) ;
#31469=DIRECTION ( 'NONE',  ( -1.000000000000000000, 0.000000000000000000, 0.000000000000000000 ) ) ;
#31477=CARTESIAN_POINT ( 'NONE',  ( -22.27711351828769892, -1.028167152775512516, 3.534923377568736313 ) ) ;
#31484=CARTESIAN_POINT ( 'NONE',  ( 0.000000000000000000, 6.606214214351074254, 2.114938770769925647 ) ) ;
#31497=ORIENTED_EDGE ( 'NONE', *, *, #62771, .T. ) ;
#31502=EDGE_CURVE ( 'NONE', #48023, #53160, #48733, .T. ) ;
#31504=CARTESIAN_POINT ( 'NONE',  ( 2.000000000000001776, -1.145812388885151023, 6.715725538143585638 ) ) ;
#31505=DIRECTION ( 'NONE',  ( -1.000000000000000000, 0.000000000000000000, 0.000000000000000000 ) ) ;
#31518=CARTESIAN_POINT ( 'NONE',  ( -22.28506771379528573, 3.575989816848481162, -1.050362426369340296 ) ) ;
#31519=CARTESIAN_POINT ( 'NONE',  ( 2.000000000000001776, -3.152010634611731366, 6.039758645301271933 ) ) ;
#31523=EDGE_CURVE ( 'NONE', #55926, #8645, #57227, .T. ) ;
#31531=DIRECTION ( 'NONE',  ( 0.000000000000000000, 0.000000000000000000, 1.000000000000000000 ) ) ;
#31536=ORIENTED_EDGE ( 'NONE', *, *, #30605, .F. ) ;
#31552=ORIENTED_EDGE ( 'NONE', *, *, #63706, .T. ) ;
#31561=DIRECTION ( 'NONE',  ( -1.000000000000000000, 0.000000000000000000, 0.000000000000000000 ) ) ;
#31563=CARTESIAN_POINT ( 'NONE',  ( -27.15511094194037867, 1.124668417986074864, -2.237231637349071711 ) ) ;
#31569=CYLINDRICAL_SURFACE ( 'NONE', #40509, 2.899999999999994582 ) ;
#31575=ORIENTED_EDGE ( 'NONE', *, *, #34947, .T. ) ;
#31578=ORIENTED_EDGE ( 'NONE', *, *, #38287, .T. ) ;
#31591=DIRECTION ( 'NONE',  ( -1.000000000000000000, 0.000000000000000000, 0.000000000000000000 ) ) ;
#31592=CARTESIAN_POINT ( 'NONE',  ( -22.28506771379528573, 0.2569416992704561253, 3.718191140878643441 ) ) ;
#31594=ADVANCED_FACE ( 'NONE', ( #37875 ), #42855, .T. ) ;
#31598=EDGE_CURVE ( 'NONE', #58669, #33072, #38527, .T. ) ;
#31611=DIRECTION ( 'NONE',  ( -1.000000000000000000, 0.000000000000000000, 0.000000000000000000 ) ) ;
#31622=DIRECTION ( 'NONE',  ( 1.000000000000000000, -0.000000000000000000, -0.000000000000000000 ) ) ;
#31623=ORIENTED_EDGE ( 'NONE', *, *, #4761, .T. ) ;
#31629=EDGE_CURVE ( 'NONE', #10704, #12415, #32794, .T. ) ;
#31649=LINE ( 'NONE', #1429, #39145 ) ;
#31653=B_SPLINE_CURVE_WITH_KNOTS ( 'NONE', 3,
 ( #1823, #41377, #22088, #32387, #61664, #16118, #17103, #5851, #27398, #15775, #520, #36406, #42344 ),
 .UNSPECIFIED., .F., .F.,
 ( 4, 3, 3, 3, 4 ),
 ( 2.949348774913951345E-18, 6.990956068646394335E-05, 0.0001398191187764043046, 0.0002097286751720211107, 0.0002792983885906313336 ),
 .UNSPECIFIED. ) ;
#31654=ORIENTED_EDGE ( 'NONE', *, *, #5054, .T. ) ;
#31663=CARTESIAN_POINT ( 'NONE',  ( -27.35552965826137140, 1.320216934008397569, 2.810569013793730697 ) ) ;
#31664=AXIS2_PLACEMENT_3D ( 'NONE', #18003, #17687, #8350 ) ;
#31668=CARTESIAN_POINT ( 'NONE',  ( -24.42101984568203576, -2.451666775035103552, 3.522366633939663760 ) ) ;
#31669=AXIS2_PLACEMENT_3D ( 'NONE', #9549, #2978, #28550 ) ;
#31675=CARTESIAN_POINT ( 'NONE',  ( -22.27711653538342773, 3.377206745425005874, 1.465933162149040792 ) ) ;
#31678=EDGE_LOOP ( 'NONE', ( #29532, #54958, #10359, #5235 ) ) ;
#31686=CARTESIAN_POINT ( 'NONE',  ( -22.28546858134833641, -3.567529619157803644, 1.005093225210829999 ) ) ;
#31702=AXIS2_PLACEMENT_3D ( 'NONE', #14278, #8973, #22719 ) ;
#31711=AXIS2_PLACEMENT_3D ( 'NONE', #42571, #11037, #62873 ) ;
#31715=VECTOR ( 'NONE', #8681, 999.9999999999998863 ) ;
#31719=CARTESIAN_POINT ( 'NONE',  ( 1.000000000000000888, 5.217815162096836268, 5.387430271863580700 ) ) ;
#31721=CYLINDRICAL_SURFACE ( 'NONE', #49683, 2.899999999999994582 ) ;
#31726=ORIENTED_EDGE ( 'NONE', *, *, #52938, .F. ) ;
#31733=AXIS2_PLACEMENT_3D ( 'NONE', #41050, #35401, #35722 ) ;
#31735=EDGE_CURVE ( 'NONE', #28121, #35981, #25369, .T. ) ;
#31748=CIRCLE ( 'NONE', #29668, 7.499999999999988454 ) ;
#31749=EDGE_LOOP ( 'NONE', ( #31063, #60203, #7360, #33583 ) ) ;
#31760=CARTESIAN_POINT ( 'NONE',  ( -27.09342121492585065, 2.251107617621282753, 0.5565043948849990318 ) ) ;
#31772=LINE ( 'NONE', #11504, #5583 ) ;
#31788=EDGE_CURVE ( 'NONE', #8949, #13688, #13886, .T. ) ;
#31791=CARTESIAN_POINT ( 'NONE',  ( 2.000000000000001776, -1.754183803416492493, -6.711026108862277795 ) ) ;
#31793=CARTESIAN_POINT ( 'NONE',  ( -27.08456565417846562, 0.9533904527919729865, -2.084650034356376302 ) ) ;
#31801=CARTESIAN_POINT ( 'NONE',  ( 0.000000000000000000, 1.865193240757095916, 6.552473556515182374 ) ) ;
#31806=DIRECTION ( 'NONE',  ( -1.000000000000000000, 0.000000000000000000, 0.000000000000000000 ) ) ;
#31808=CIRCLE ( 'NONE', #3173, 7.499999999999988454 ) ;
#31811=DIRECTION ( 'NONE',  ( 0.000000000000000000, 0.9868265225415254749, 0.1617819965527686754 ) ) ;
#31815=EDGE_CURVE ( 'NONE', #33072, #918, #5201, .T. ) ;
#31832=ORIENTED_EDGE ( 'NONE', *, *, #46016, .T. ) ;
#31856=ORIENTED_EDGE ( 'NONE', *, *, #27331, .T. ) ;
#31860=EDGE_CURVE ( 'NONE', #1201, #33280, #44477, .T. ) ;
#31873=B_SPLINE_CURVE_WITH_KNOTS ( 'NONE', 3,
 ( #29830, #50145, #10530, #4601, #30807, #41119, #15841, #5923, #26178, #24871, #37115, #27469, #52762, #12495, #1240, #41443, #31793, #52103, #32454 ),
 .UNSPECIFIED., .F., .F.,
 ( 4, 3, 3, 3, 3, 3, 4 ),
 ( 3.223564806431921169E-18, 2.836829843012604650E-05, 4.224792512550834891E-05, 5.612066614913120233E-05, 6.998859278354828948E-05, 9.832141288087297370E-05, 0.0001178161482478445269 ),
 .UNSPECIFIED. ) ;
#31888=DIRECTION ( 'NONE',  ( -1.000000000000000000, 0.000000000000000000, 0.000000000000000000 ) ) ;
#31895=DIRECTION ( 'NONE',  ( 1.000000000000000000, 0.000000000000000000, 0.000000000000000000 ) ) ;
#31901=CARTESIAN_POINT ( 'NONE',  ( 2.000000000000001776, -4.976357229393876480, 4.652926418895529714 ) ) ;
#31907=FACE_OUTER_BOUND ( 'NONE', #5469, .T. ) ;
#31921=ORIENTED_EDGE ( 'NONE', *, *, #15645, .F. ) ;
#31929=ORIENTED_EDGE ( 'NONE', *, *, #756, .F. ) ;
#31933=VECTOR ( 'NONE', #23319, 1000.000000000000000 ) ;
#31936=CARTESIAN_POINT ( 'NONE',  ( 1.000000000000000888, -6.160607635185357367, -4.277489166005654653 ) ) ;
#31942=CARTESIAN_POINT ( 'NONE',  ( -27.08417174366084623, -0.3802265912085517341, -2.259388872100088541 ) ) ;
#31949=LINE ( 'NONE', #26007, #25365 ) ;
#31950=AXIS2_PLACEMENT_3D ( 'NONE', #32857, #33204, #28872 ) ;
#31951=ADVANCED_FACE ( 'NONE', ( #1897 ), #32460, .T. ) ;
#31960=B_SPLINE_CURVE_WITH_KNOTS ( 'NONE', 3,
 ( #39177, #18912, #33861, #3652, #14233, #8595, #8933, #59468, #9237, #59161, #53842, #28883, #29519, #19885, #4270, #55126, #24214, #44481, #29845 ),
 .UNSPECIFIED., .F., .F.,
 ( 4, 3, 3, 3, 3, 3, 4 ),
 ( 0.000000000000000000, 2.832085443685167180E-05, 4.217789847592021607E-05, 5.603488375296165918E-05, 6.989180858882148130E-05, 9.821094830334582552E-05, 0.0001178165571463619216 ),
 .UNSPECIFIED. ) ;
#31961=LINE ( 'NONE', #41623, #50255 ) ;
#31968=ADVANCED_FACE ( 'NONE', ( #8192 ), #7524, .T. ) ;
#31973=EDGE_CURVE ( 'NONE', #3201, #57823, #51817, .T. ) ;
#31975=AXIS2_PLACEMENT_3D ( 'NONE', #47330, #22353, #1773 ) ;
#31980=CYLINDRICAL_SURFACE ( 'NONE', #47317, 6.936499999999988120 ) ;
#31984=EDGE_CURVE ( 'NONE', #10128, #16004, #5108, .T. ) ;
#31988=CARTESIAN_POINT ( 'NONE',  ( -35.05175862995318425, -0.01139565579896285874, -0.005323180402361238350 ) ) ;
#31989=CARTESIAN_POINT ( 'NONE',  ( 1.000000000000000888, 6.664893814313781029, -3.439359016433444438 ) ) ;
#31990=VECTOR ( 'NONE', #14041, 1000.000000000000000 ) ;
#31997=ORIENTED_EDGE ( 'NONE', *, *, #57090, .F. ) ;
#32002=DIRECTION ( 'NONE',  ( -1.000000000000000000, 0.000000000000000000, 0.000000000000000000 ) ) ;
#32010=EDGE_LOOP ( 'NONE', ( #21087, #36556, #10425, #21872 ) ) ;
#32014=AXIS2_PLACEMENT_3D ( 'NONE', #52198, #42501, #32215 ) ;
#32019=CARTESIAN_POINT ( 'NONE',  ( 2.000000000000001776, 5.585096664091945939, 4.113602740025928739 ) ) ;
#32023=( BOUNDED_SURFACE ( )  B_SPLINE_SURFACE ( 3, 1, ( 
 ( #27116, #47723 ),
 ( #22446, #11477 ),
 ( #47080, #6187 ),
 ( #37743, #2167 ) ),
 .UNSPECIFIED., .F., .F., .F. ) 
 B_SPLINE_SURFACE_WITH_KNOTS ( ( 4, 4 ),
 ( 2, 2 ),
 ( 0.000000000000000000, 1.000000000000000000 ),
 ( 0.000000000000000000, 1.000000000000000000 ),
 .UNSPECIFIED. ) 
 GEOMETRIC_REPRESENTATION_ITEM ( )  RATIONAL_B_SPLINE_SURFACE ( (
 ( 1.000000000000000000, 1.000000000000000000),
 ( 0.8716676215708681896, 0.8964445200148164483),
 ( 0.8716676215708681896, 0.8964445200148164483),
 ( 1.000000000000000000, 1.000000000000000000) ) ) 
 REPRESENTATION_ITEM ( '' )  SURFACE ( )  );
#32026=CARTESIAN_POINT ( 'NONE',  ( -22.65999102136915866, -4.797155153747071132, -0.5917351393135312776 ) ) ;
#32027=DIRECTION ( 'NONE',  ( 0.000000000000000000, 0.000000000000000000, 1.000000000000000000 ) ) ;
#32030=ORIENTED_EDGE ( 'NONE', *, *, #52938, .T. ) ;
#32032=ORIENTED_EDGE ( 'NONE', *, *, #47004, .F. ) ;
#32037=CIRCLE ( 'NONE', #50094, 6.936499999999989008 ) ;
#32041=CARTESIAN_POINT ( 'NONE',  ( -35.04643116707788408, 0.002453861112619928897, 0.01193867652719490802 ) ) ;
#32042=CARTESIAN_POINT ( 'NONE',  ( -22.28284753389937123, -3.581493264753385475, -0.9231250029035383831 ) ) ;
#32043=VECTOR ( 'NONE', #25063, 1000.000000000000000 ) ;
#32053=CARTESIAN_POINT ( 'NONE',  ( 2.000000000000001776, 0.000000000000000000, 0.000000000000000000 ) ) ;
#32054=CARTESIAN_POINT ( 'NONE',  ( 2.000000000000001776, 0.000000000000000000, 0.000000000000000000 ) ) ;
#32055=CARTESIAN_POINT ( 'NONE',  ( 0.000000000000000000, 1.693411908627302509, -7.306323022404582979 ) ) ;
#32059=ORIENTED_EDGE ( 'NONE', *, *, #28178, .F. ) ;
#32060=CARTESIAN_POINT ( 'NONE',  ( -22.29479313954897535, -3.090162644873540643, 2.096782908204888773 ) ) ;
#32078=EDGE_LOOP ( 'NONE', ( #35663, #55444, #16161, #37 ) ) ;
#32080=DIRECTION ( 'NONE',  ( -1.000000000000000000, 0.000000000000000000, 0.000000000000000000 ) ) ;
#32100=EDGE_CURVE ( 'NONE', #7784, #63668, #46479, .T. ) ;
#32106=CARTESIAN_POINT ( 'NONE',  ( -22.27721701579900682, 2.409654355488404676, 2.783642043008622391 ) ) ;
#32119=CARTESIAN_POINT ( 'NONE',  ( 0.000000000000000000, -2.473437528934186780, 7.080403010454960899 ) ) ;
#32126=CARTESIAN_POINT ( 'NONE',  ( -22.31328051695926007, 3.148362328073167404, -2.109671368890616350 ) ) ;
#32132=CARTESIAN_POINT ( 'NONE',  ( 1.000000000000000888, -5.769711778877330666, 4.791703871138493831 ) ) ;
#32140=DIRECTION ( 'NONE',  ( 0.000000000000000000, -0.9289767198167871998, -0.3701381553399247792 ) ) ;
#32149=CARTESIAN_POINT ( 'NONE',  ( -35.05175862995318425, 0.01216930940959280727, 0.003178856583437375538 ) ) ;
#32153=DIRECTION ( 'NONE',  ( -1.000000000000000000, 0.000000000000000000, 0.000000000000000000 ) ) ;
#32158=CIRCLE ( 'NONE', #25819, 2.899999999999994582 ) ;
#32165=CARTESIAN_POINT ( 'NONE',  ( 2.000000000000001776, -5.396716205731451943, 4.158041573745051345 ) ) ;
#32176=CARTESIAN_POINT ( 'NONE',  ( -35.04582288351658548, -0.01249938581188633595, -0.002280196168886043998 ) ) ;
#32178=CYLINDRICAL_SURFACE ( 'NONE', #25812, 2.999999999999995559 ) ;
#32180=EDGE_CURVE ( 'NONE', #37744, #55487, #53565, .T. ) ;
#32181=AXIS2_PLACEMENT_3D ( 'NONE', #32296, #6725, #42253 ) ;
#32190=DIRECTION ( 'NONE',  ( 0.000000000000000000, 0.000000000000000000, 1.000000000000000000 ) ) ;
#32195=ORIENTED_EDGE ( 'NONE', *, *, #7526, .T. ) ;
#32200=ORIENTED_EDGE ( 'NONE', *, *, #51659, .F. ) ;
#32203=EDGE_CURVE ( 'NONE', #15892, #26006, #28673, .T. ) ;
#32205=ORIENTED_EDGE ( 'NONE', *, *, #11895, .T. ) ;
#32206=AXIS2_PLACEMENT_3D ( 'NONE', #34480, #44776, #28087 ) ;
#32207=VERTEX_POINT ( 'NONE', #48985 ) ;
#32209=EDGE_CURVE ( 'NONE', #32360, #12705, #65418, .T. ) ;
#32215=DIRECTION ( 'NONE',  ( 0.000000000000000000, 0.000000000000000000, 1.000000000000000000 ) ) ;
#32220=DIRECTION ( 'NONE',  ( -1.000000000000000000, 0.000000000000000000, 0.000000000000000000 ) ) ;
#32225=EDGE_CURVE ( 'NONE', #22078, #26234, #4460, .T. ) ;
#32240=CARTESIAN_POINT ( 'NONE',  ( -27.08430792439081003, -0.5856059198894515427, -2.215465963318195897 ) ) ;
#32243=CARTESIAN_POINT ( 'NONE',  ( 0.000000000000000000, 7.387287142779368487, -1.295372019972108601 ) ) ;
#32244=CARTESIAN_POINT ( 'NONE',  ( 2.000000000000001776, 5.450255447309745982, 4.087611905901426645 ) ) ;
#32249=CARTESIAN_POINT ( 'NONE',  ( 2.000000000000001776, -1.058508696394911963, -6.730038252034928448 ) ) ;
#32250=VERTEX_POINT ( 'NONE', #63891 ) ;
#32255=AXIS2_PLACEMENT_3D ( 'NONE', #50953, #45618, #19393 ) ;
#32256=EDGE_CURVE ( 'NONE', #33557, #49753, #64548, .T. ) ;
#32257=VERTEX_POINT ( 'NONE', #3075 ) ;
#32261=CARTESIAN_POINT ( 'NONE',  ( -27.09030469827880339, -1.657623467483503754, -1.608164674722925458 ) ) ;
#32265=ORIENTED_EDGE ( 'NONE', *, *, #8526, .T. ) ;
#32271=AXIS2_PLACEMENT_3D ( 'NONE', #61802, #42158, #32190 ) ;
#32272=CARTESIAN_POINT ( 'NONE',  ( -27.35552965826137140, 2.548625910254547655, 1.773915698030531951 ) ) ;
#32275=DIRECTION ( 'NONE',  ( 0.000000000000000000, 0.000000000000000000, 1.000000000000000000 ) ) ;
#32289=VECTOR ( 'NONE', #13657, 1000.000000000000000 ) ;
#32296=CARTESIAN_POINT ( 'NONE',  ( 2.000000000000001776, 0.000000000000000000, 0.000000000000000000 ) ) ;
#32306=CARTESIAN_POINT ( 'NONE',  ( 2.000000000000001776, -6.160607635185357367, -4.277489166005654653 ) ) ;
#32313=CARTESIAN_POINT ( 'NONE',  ( -22.27218376572352554, 3.330959526935401538, 1.571356284315131413 ) ) ;
#32314=DIRECTION ( 'NONE',  ( -1.000000000000000000, 0.000000000000000000, 0.000000000000000000 ) ) ;
#32315=DIRECTION ( 'NONE',  ( -1.000000000000000000, 0.000000000000000000, 0.000000000000000000 ) ) ;
#32316=ORIENTED_EDGE ( 'NONE', *, *, #65182, .T. ) ;
#32328=CARTESIAN_POINT ( 'NONE',  ( -22.28694879868232448, -2.661377239830742258, -2.586016167700816659 ) ) ;
#32331=CIRCLE ( 'NONE', #45077, 2.899999999999995914 ) ;
#32332=VERTEX_POINT ( 'NONE', #27021 ) ;
#32336=CARTESIAN_POINT ( 'NONE',  ( -22.27715239060371744, -3.586346956688103216, 0.8317362037004271125 ) ) ;
#32337=DIRECTION ( 'NONE',  ( 0.000000000000000000, 0.000000000000000000, 1.000000000000000000 ) ) ;
#32349=FACE_OUTER_BOUND ( 'NONE', #10869, .T. ) ;
#32353=CIRCLE ( 'NONE', #3740, 6.936499999999987232 ) ;
#32360=VERTEX_POINT ( 'NONE', #57946 ) ;
#32363=ORIENTED_EDGE ( 'NONE', *, *, #26220, .T. ) ;
#32367=AXIS2_PLACEMENT_3D ( 'NONE', #63270, #27368, #47663 ) ;
#32370=DIRECTION ( 'NONE',  ( -1.000000000000000000, 0.000000000000000000, 0.000000000000000000 ) ) ;
#32371=CARTESIAN_POINT ( 'NONE',  ( -35.04582288351658548, 0.006479247284605894018, 0.01092946910272066426 ) ) ;
#32373=ORIENTED_EDGE ( 'NONE', *, *, #14107, .F. ) ;
#32375=VERTEX_POINT ( 'NONE', #14332 ) ;
#32386=EDGE_CURVE ( 'NONE', #10275, #22824, #56109, .T. ) ;
#32387=CARTESIAN_POINT ( 'NONE',  ( -22.27713295444592845, -0.8543895091636509731, -3.580881989303322577 ) ) ;
#32389=CARTESIAN_POINT ( 'NONE',  ( 2.000000000000001776, -2.480520636974139936, -6.345145617221269241 ) ) ;
#32391=CARTESIAN_POINT ( 'NONE',  ( -35.04582288351658548, -0.004274985098089345917, -0.01196488372923832158 ) ) ;
#32401=CARTESIAN_POINT ( 'NONE',  ( -25.42680463514452427, -1.651747791411766197, -3.516354806213014772 ) ) ;
#32403=VECTOR ( 'NONE', #22982, 1000.000000000000000 ) ;
#32406=CARTESIAN_POINT ( 'NONE',  ( -27.10719052120871098, 0.5475695427849553987, -2.295785794152566339 ) ) ;
#32412=CARTESIAN_POINT ( 'NONE',  ( -22.28506771379528573, 3.718191140878649659, -0.2569416992704126601 ) ) ;
#32419=CARTESIAN_POINT ( 'NONE',  ( -27.05874794189610455, 1.734723475976807094E-15, -8.673617379884035472E-15 ) ) ;
#32423=ORIENTED_EDGE ( 'NONE', *, *, #34940, .T. ) ;
#32433=CARTESIAN_POINT ( 'NONE',  ( -35.04709527796842394, 0.005220632201000108275, 0.01120703303051501232 ) ) ;
#32444=DIRECTION ( 'NONE',  ( 0.000000000000000000, -0.3193015301359870550, 0.9476531711828000137 ) ) ;
#32446=VERTEX_POINT ( 'NONE', #54905 ) ;
#32448=CARTESIAN_POINT ( 'NONE',  ( 2.000000000000001776, 0.000000000000000000, 0.000000000000000000 ) ) ;
#32454=CARTESIAN_POINT ( 'NONE',  ( -27.08429572838383947, 0.9410937941434112108, -2.089332284968719922 ) ) ;
#32457=DIRECTION ( 'NONE',  ( -1.000000000000000000, 0.000000000000000000, 0.000000000000000000 ) ) ;
#32460=CYLINDRICAL_SURFACE ( 'NONE', #52892, 7.499999999999988454 ) ;
#32468=DIRECTION ( 'NONE',  ( 0.000000000000000000, -0.9868265225415276953, 0.1617819965527552140 ) ) ;
#32471=DIRECTION ( 'NONE',  ( 0.000000000000000000, 0.000000000000000000, 1.000000000000000000 ) ) ;
#32479=CARTESIAN_POINT ( 'NONE',  ( -22.94572469358971034, 0.4123340087948583199, -4.870584850960111289 ) ) ;
#32480=FACE_OUTER_BOUND ( 'NONE', #41110, .T. ) ;
#32497=ORIENTED_EDGE ( 'NONE', *, *, #31629, .F. ) ;
#32500=LINE ( 'NONE', #46832, #23543 ) ;
#32501=DIRECTION ( 'NONE',  ( 1.000000000000000000, 0.000000000000000000, 0.000000000000000000 ) ) ;
#32512=CARTESIAN_POINT ( 'NONE',  ( -22.31328051695926007, -1.671726071983958839, 3.401210163132545539 ) ) ;
#32513=EDGE_LOOP ( 'NONE', ( #6189, #52962, #41527, #6244 ) ) ;
#32527=EDGE_CURVE ( 'NONE', #60470, #9709, #27438, .T. ) ;
#32531=AXIS2_PLACEMENT_3D ( 'NONE', #17405, #23715, #43982 ) ;
#32542=ORIENTED_EDGE ( 'NONE', *, *, #62315, .F. ) ;
#32546=CARTESIAN_POINT ( 'NONE',  ( 0.000000000000000000, 3.937687286050910895, -6.383151168292444666 ) ) ;
#32549=CARTESIAN_POINT ( 'NONE',  ( -27.09833916700227263, -0.6583442518269214672, -2.238843247505190259 ) ) ;
#32550=EDGE_CURVE ( 'NONE', #14116, #15285, #34827, .T. ) ;
#32554=DIRECTION ( 'NONE',  ( -1.000000000000000000, 0.000000000000000000, 0.000000000000000000 ) ) ;
#32555=CARTESIAN_POINT ( 'NONE',  ( 0.000000000000000000, -2.315790869867103474, 7.133520354428079635 ) ) ;
#32558=DIRECTION ( 'NONE',  ( -1.000000000000000000, 0.000000000000000000, 0.000000000000000000 ) ) ;
#32559=ORIENTED_EDGE ( 'NONE', *, *, #30030, .F. ) ;
#32576=FACE_OUTER_BOUND ( 'NONE', #42641, .T. ) ;
#32581=CARTESIAN_POINT ( 'NONE',  ( 0.000000000000000000, -2.469490258309361419, -6.482025155313371201 ) ) ;
#32583=DIRECTION ( 'NONE',  ( 0.000000000000000000, 0.000000000000000000, 1.000000000000000000 ) ) ;
#32623=DIRECTION ( 'NONE',  ( -1.000000000000000000, 0.000000000000000000, 0.000000000000000000 ) ) ;
#32629=CARTESIAN_POINT ( 'NONE',  ( 0.000000000000000000, 0.000000000000000000, 0.000000000000000000 ) ) ;
#32632=CARTESIAN_POINT ( 'NONE',  ( -27.08426504710140392, -0.6326154899769325102, 2.202478235133275231 ) ) ;
#32644=CARTESIAN_POINT ( 'NONE',  ( -22.31213670151049300, 3.777944311993714166, -0.2530575063955878279 ) ) ;
#32645=CARTESIAN_POINT ( 'NONE',  ( -22.71097035706202405, 4.089776368546564456, 2.846599994298306679 ) ) ;
#32654=CARTESIAN_POINT ( 'NONE',  ( 2.000000000000001776, 5.585096664091999230, -4.113602740025892324 ) ) ;
#32671=DIRECTION ( 'NONE',  ( -1.000000000000000000, 0.000000000000000000, 0.000000000000000000 ) ) ;
#32672=CARTESIAN_POINT ( 'NONE',  ( 0.000000000000000000, 4.915517050588478654, -4.717154614762057108 ) ) ;
#32679=EDGE_LOOP ( 'NONE', ( #479, #37264, #44613, #49543 ) ) ;
#32687=CARTESIAN_POINT ( 'NONE',  ( -22.27706485742869091, 3.358064672837120401, 1.508175983031588840 ) ) ;
#32699=CARTESIAN_POINT ( 'NONE',  ( -22.29290468048228036, -3.083035815361902188, 2.097193667172386977 ) ) ;
#32705=DIRECTION ( 'NONE',  ( 0.000000000000000000, 0.4198891015602590482, 0.9075754196709595600 ) ) ;
#32715=EDGE_CURVE ( 'NONE', #59063, #9280, #7449, .T. ) ;
#32718=ORIENTED_EDGE ( 'NONE', *, *, #45335, .T. ) ;
#32721=CARTESIAN_POINT ( 'NONE',  ( 0.000000000000000000, -6.812627895098285258, 2.855765430652664971 ) ) ;
#32728=ORIENTED_EDGE ( 'NONE', *, *, #11782, .F. ) ;
#32737=DIRECTION ( 'NONE',  ( 0.000000000000000000, 0.000000000000000000, 1.000000000000000000 ) ) ;
#32742=CARTESIAN_POINT ( 'NONE',  ( -28.67667724226168602, 1.840944188131424131, 0.4371157725389773208 ) ) ;
#32746=VERTEX_POINT ( 'NONE', #11239 ) ;
#32748=ORIENTED_EDGE ( 'NONE', *, *, #46396, .F. ) ;
#32752=CARTESIAN_POINT ( 'NONE',  ( -10.00000000000000178, 0.000000000000000000, 0.000000000000000000 ) ) ;
#32758=EDGE_CURVE ( 'NONE', #7851, #33347, #19371, .T. ) ;
#32759=CARTESIAN_POINT ( 'NONE',  ( -22.27722019117889474, -0.6494988092404023750, -3.623917154020615428 ) ) ;
#32760=CARTESIAN_POINT ( 'NONE',  ( -22.71097035706202405, -4.510116093748277599, 2.118550233809401107 ) ) ;
#32761=LINE ( 'NONE', #2559, #17819 ) ;
#32763=ORIENTED_EDGE ( 'NONE', *, *, #19890, .T. ) ;
#32774=ORIENTED_EDGE ( 'NONE', *, *, #9103, .F. ) ;
#32782=CARTESIAN_POINT ( 'NONE',  ( 0.000000000000000000, 0.000000000000000000, 0.000000000000000000 ) ) ;
#32792=FACE_OUTER_BOUND ( 'NONE', #43393, .T. ) ;
#32794=CIRCLE ( 'NONE', #56024, 2.999999999999996447 ) ;
#32795=CARTESIAN_POINT ( 'NONE',  ( -28.67667724226168602, 0.8389685652162113261, -1.695959153103727912 ) ) ;
#32799=CARTESIAN_POINT ( 'NONE',  ( -27.04788180060269909, -0.2724356095623292617, 3.218072544330532470 ) ) ;
#32800=CARTESIAN_POINT ( 'NONE',  ( -24.42101984568203932, 0.3620223918248580697, -4.276292373952003345 ) ) ;
#32806=ORIENTED_EDGE ( 'NONE', *, *, #46137, .T. ) ;
#32807=CARTESIAN_POINT ( 'NONE',  ( -22.27384469013076185, -3.564715702084494175, 0.9224151068931482067 ) ) ;
#32816=EDGE_CURVE ( 'NONE', #57499, #29549, #13008, .T. ) ;
#32831=VERTEX_POINT ( 'NONE', #41472 ) ;
#32837=CARTESIAN_POINT ( 'NONE',  ( 0.000000000000000000, 4.976357229393922665, -4.652926418895522609 ) ) ;
#32838=CIRCLE ( 'NONE', #25404, 6.936499999999992561 ) ;
#32845=VERTEX_POINT ( 'NONE', #12210 ) ;
#32846=FACE_OUTER_BOUND ( 'NONE', #5501, .T. ) ;
#32848=ORIENTED_EDGE ( 'NONE', *, *, #35965, .F. ) ;
#32850=FACE_OUTER_BOUND ( 'NONE', #28597, .T. ) ;
#32854=CARTESIAN_POINT ( 'NONE',  ( -22.27721701579900682, -2.783642043008650813, 2.409654355488387356 ) ) ;
#32857=CARTESIAN_POINT ( 'NONE',  ( 2.000000000000001776, 0.000000000000000000, 0.000000000000000000 ) ) ;
#32863=CARTESIAN_POINT ( 'NONE',  ( -22.27706485742869091, 2.985151051101503583, -2.154081322712197544 ) ) ;
#32865=ADVANCED_FACE ( 'NONE', ( #32480 ), #63087, .T. ) ;
#32870=DIRECTION ( 'NONE',  ( 0.000000000000000000, 0.000000000000000000, 1.000000000000000000 ) ) ;
#32874=VERTEX_POINT ( 'NONE', #52788 ) ;
#32876=AXIS2_PLACEMENT_3D ( 'NONE', #13105, #33388, #3147 ) ;
#32881=FACE_OUTER_BOUND ( 'NONE', #18882, .T. ) ;
#32891=ORIENTED_EDGE ( 'NONE', *, *, #42843, .T. ) ;
#32895=EDGE_CURVE ( 'NONE', #35536, #32989, #59313, .T. ) ;
#32904=CARTESIAN_POINT ( 'NONE',  ( 2.000000000000001776, 6.796153407501448029, 1.388283512725836388 ) ) ;
#32905=CARTESIAN_POINT ( 'NONE',  ( -22.27786964138239867, -2.131221155130656353, -3.004507515156384034 ) ) ;
#32910=AXIS2_PLACEMENT_3D ( 'NONE', #7992, #52566, #6995 ) ;
#32915=DIRECTION ( 'NONE',  ( -1.000000000000000000, 0.000000000000000000, 0.000000000000000000 ) ) ;
#32916=CARTESIAN_POINT ( 'NONE',  ( -22.28023996335807411, -0.3233044107360732999, -3.676538434326164673 ) ) ;
#32920=ADVANCED_FACE ( 'NONE', ( #14721 ), #40674, .T. ) ;
#32935=CARTESIAN_POINT ( 'NONE',  ( -22.27719381268171617, 3.550654232855438242, 0.9730858478813626533 ) ) ;
#32944=DIRECTION ( 'NONE',  ( -1.000000000000000000, 0.000000000000000000, 0.000000000000000000 ) ) ;
#32946=CARTESIAN_POINT ( 'NONE',  ( 0.000000000000000000, 5.217815162096925086, -5.387430271863535403 ) ) ;
#32950=AXIS2_PLACEMENT_3D ( 'NONE', #30166, #10205, #52093 ) ;
#32953=ORIENTED_EDGE ( 'NONE', *, *, #53183, .F. ) ;
#32958=DIRECTION ( 'NONE',  ( 1.000000000000000000, -0.000000000000000000, -0.000000000000000000 ) ) ;
#32961=FACE_OUTER_BOUND ( 'NONE', #21434, .T. ) ;
#32964=CIRCLE ( 'NONE', #4323, 2.899999999999995026 ) ;
#32965=MECHANICAL_DESIGN_GEOMETRIC_PRESENTATION_REPRESENTATION('',(#22337),#1096);
#32966=CIRCLE ( 'NONE', #19167, 6.936499999999989896 ) ;
#32973=CYLINDRICAL_SURFACE ( 'NONE', #345, 2.899999999999994582 ) ;
#32984=CARTESIAN_POINT ( 'NONE',  ( -22.29677679919927868, 3.730758197825081446, -0.2674217835790786979 ) ) ;
#32987=AXIS2_PLACEMENT_3D ( 'NONE', #45986, #31340, #15693 ) ;
#32989=VERTEX_POINT ( 'NONE', #23509 ) ;
#33000=DIRECTION ( 'NONE',  ( -1.000000000000000000, 0.000000000000000000, 0.000000000000000000 ) ) ;
#33003=ORIENTED_EDGE ( 'NONE', *, *, #53986, .F. ) ;
#33014=CARTESIAN_POINT ( 'NONE',  ( 2.000000000000001776, -6.767909380267597363, -0.7805499053121327524 ) ) ;
#33021=AXIS2_PLACEMENT_3D ( 'NONE', #6905, #2242, #22521 ) ;
#33023=CARTESIAN_POINT ( 'NONE',  ( -22.27834755396593991, -2.305389312780946831, -2.876353066242404388 ) ) ;
#33031=EDGE_LOOP ( 'NONE', ( #4887, #51642, #59502, #15495 ) ) ;
#33042=CIRCLE ( 'NONE', #4395, 7.499999999999988454 ) ;
#33045=AXIS2_PLACEMENT_3D ( 'NONE', #17811, #23123, #47743 ) ;
#33047=CARTESIAN_POINT ( 'NONE',  ( 2.000000000000001776, -0.4804830611969332366, -6.919838746524582085 ) ) ;
#33050=DIRECTION ( 'NONE',  ( -1.000000000000000000, 0.000000000000000000, 0.000000000000000000 ) ) ;
#33051=CARTESIAN_POINT ( 'NONE',  ( 1.000000000000000888, 6.586971819220337032, 3.586335490831404460 ) ) ;
#33054=CARTESIAN_POINT ( 'NONE',  ( 2.000000000000001776, 3.979254915827449945, -5.681598592373734213 ) ) ;
#33062=EDGE_CURVE ( 'NONE', #7394, #5728, #15403, .T. ) ;
#33064=AXIS2_PLACEMENT_3D ( 'NONE', #41649, #61942, #16400 ) ;
#33065=DIRECTION ( 'NONE',  ( -1.000000000000000000, 0.000000000000000000, 0.000000000000000000 ) ) ;
#33069=DIRECTION ( 'NONE',  ( -1.000000000000000000, 0.000000000000000000, 0.000000000000000000 ) ) ;
#33070=CYLINDRICAL_SURFACE ( 'NONE', #48041, 6.936499999999988120 ) ;
#33072=VERTEX_POINT ( 'NONE', #50988 ) ;
#33074=DIRECTION ( 'NONE',  ( -1.000000000000000000, 0.000000000000000000, 0.000000000000000000 ) ) ;
#33077=VERTEX_POINT ( 'NONE', #41000 ) ;
#33079=AXIS2_PLACEMENT_3D ( 'NONE', #36462, #11510, #46437 ) ;
#33081=EDGE_CURVE ( 'NONE', #44565, #64384, #61281, .T. ) ;
#33082=ORIENTED_EDGE ( 'NONE', *, *, #32386, .F. ) ;
#33089=CIRCLE ( 'NONE', #9740, 2.899999999999995914 ) ;
#33108=DIRECTION ( 'NONE',  ( -1.000000000000000000, 0.000000000000000000, 0.000000000000000000 ) ) ;
#33111=VERTEX_POINT ( 'NONE', #31663 ) ;
#33113=ORIENTED_EDGE ( 'NONE', *, *, #53913, .F. ) ;
#33114=CARTESIAN_POINT ( 'NONE',  ( 2.000000000000001776, 0.000000000000000000, 0.000000000000000000 ) ) ;
#33118=CARTESIAN_POINT ( 'NONE',  ( -22.27706485742869091, 2.985151051101503583, -2.154081322712197544 ) ) ;
#33122=CARTESIAN_POINT ( 'NONE',  ( -27.08954555554413446, -1.900922216193322800, 1.307633183325030313 ) ) ;
#33127=DIRECTION ( 'NONE',  ( -1.000000000000000000, 0.000000000000000000, 0.000000000000000000 ) ) ;
#33134=CIRCLE ( 'NONE', #4447, 6.936499999999989896 ) ;
#33140=CARTESIAN_POINT ( 'NONE',  ( -27.08506889328344158, -2.083363953276504255, -0.9597901767753411750 ) ) ;
#33145=CARTESIAN_POINT ( 'NONE',  ( 2.000000000000001776, 0.000000000000000000, 0.000000000000000000 ) ) ;
#33146=DIRECTION ( 'NONE',  ( 0.000000000000000000, 0.000000000000000000, 1.000000000000000000 ) ) ;
#33149=EDGE_CURVE ( 'NONE', #28911, #47012, #25364, .T. ) ;
#33152=CARTESIAN_POINT ( 'NONE',  ( -35.04582288351658548, 0.01270482153514039536, -0.0001464581945180892981 ) ) ;
#33157=DIRECTION ( 'NONE',  ( -1.000000000000000000, 0.000000000000000000, 0.000000000000000000 ) ) ;
#33166=DIRECTION ( 'NONE',  ( -1.000000000000000000, 0.000000000000000000, 0.000000000000000000 ) ) ;
#33175=EDGE_LOOP ( 'NONE', ( #56279, #9351, #29015, #24027 ) ) ;
#33181=AXIS2_PLACEMENT_3D ( 'NONE', #41850, #42825, #12244 ) ;
#33182=EDGE_CURVE ( 'NONE', #55598, #51352, #973, .T. ) ;
#33184=CIRCLE ( 'NONE', #4537, 2.899999999999996803 ) ;
#33185=DIRECTION ( 'NONE',  ( 0.000000000000000000, -0.5155538571770109657, -0.8568571761675956022 ) ) ;
#33186=CARTESIAN_POINT ( 'NONE',  ( 2.000000000000001776, 6.201547234537035713, 2.820401998297911383 ) ) ;
#33187=ORIENTED_EDGE ( 'NONE', *, *, #8169, .F. ) ;
#33192=VERTEX_POINT ( 'NONE', #22344 ) ;
#33196=ORIENTED_EDGE ( 'NONE', *, *, #17954, .T. ) ;
#33204=DIRECTION ( 'NONE',  ( -1.000000000000000000, 0.000000000000000000, 0.000000000000000000 ) ) ;
#33206=EDGE_CURVE ( 'NONE', #54252, #57333, #25277, .T. ) ;
#33216=CARTESIAN_POINT ( 'NONE',  ( -22.65999102136919063, 2.911035239830941368, -3.858590659383841714 ) ) ;
#33218=CARTESIAN_POINT ( 'NONE',  ( -27.08419797710328325, 1.413289504316736611, 1.803546201758800427 ) ) ;
#33220=VECTOR ( 'NONE', #46927, 1000.000000000000227 ) ;
#33224=ORIENTED_EDGE ( 'NONE', *, *, #24393, .F. ) ;
#33234=DIRECTION ( 'NONE',  ( -1.000000000000000000, 0.000000000000000000, 0.000000000000000000 ) ) ;
#33235=CARTESIAN_POINT ( 'NONE',  ( 0.000000000000000000, -2.480520636974233639, 6.345145617221206180 ) ) ;
#33238=CIRCLE ( 'NONE', #7752, 6.936499999999989896 ) ;
#33241=ORIENTED_EDGE ( 'NONE', *, *, #9664, .T. ) ;
#33244=CARTESIAN_POINT ( 'NONE',  ( -22.27834755396593991, -1.162947663292857037, 3.497967921180562101 ) ) ;
#33247=AXIS2_PLACEMENT_3D ( 'NONE', #64583, #59628, #34655 ) ;
#33263=EDGE_CURVE ( 'NONE', #6580, #31041, #64153, .T. ) ;
#33271=CARTESIAN_POINT ( 'NONE',  ( -23.41523303002442091, 2.683951991546301930, -3.856096202952854046 ) ) ;
#33272=DIRECTION ( 'NONE',  ( 0.000000000000000000, 0.000000000000000000, 1.000000000000000000 ) ) ;
#33280=VERTEX_POINT ( 'NONE', #24657 ) ;
#33286=CARTESIAN_POINT ( 'NONE',  ( -35.04643116707788408, 0.003844232202716499347, -0.01156612771644957571 ) ) ;
#33287=CARTESIAN_POINT ( 'NONE',  ( -22.28284753389937123, 3.581493264753388139, 0.9231250029034783200 ) ) ;
#33293=AXIS2_PLACEMENT_3D ( 'NONE', #65315, #29412, #35027 ) ;
#33294=ORIENTED_EDGE ( 'NONE', *, *, #50102, .F. ) ;
#33303=EDGE_CURVE ( 'NONE', #25961, #63874, #8713, .T. ) ;
#33308=CARTESIAN_POINT ( 'NONE',  ( 0.000000000000000000, 6.883677378339481123, -0.8544109087185395301 ) ) ;
#33316=ADVANCED_FACE ( 'NONE', ( #49608 ), #23102, .F. ) ;
#33326=FACE_OUTER_BOUND ( 'NONE', #55252, .T. ) ;
#33329=ADVANCED_FACE ( 'NONE', ( #4386 ), #38965, .T. ) ;
#33340=EDGE_CURVE ( 'NONE', #10069, #6941, #64540, .T. ) ;
#33345=CARTESIAN_POINT ( 'NONE',  ( -22.38932658256920405, 0.2254938976656722660, 4.011828264158250335 ) ) ;
#33347=VERTEX_POINT ( 'NONE', #45262 ) ;
#33353=EDGE_LOOP ( 'NONE', ( #28680, #57770, #16956, #8326 ) ) ;
#33355=DIRECTION ( 'NONE',  ( -1.000000000000000000, 0.000000000000000000, 0.000000000000000000 ) ) ;
#33358=ORIENTED_EDGE ( 'NONE', *, *, #48799, .F. ) ;
#33365=FACE_OUTER_BOUND ( 'NONE', #38432, .T. ) ;
#33370=CARTESIAN_POINT ( 'NONE',  ( -22.29978294495153435, -3.642708310327671395, -0.8878583829805674066 ) ) ;
#33374=ORIENTED_EDGE ( 'NONE', *, *, #58350, .T. ) ;
#33376=DIRECTION ( 'NONE',  ( -1.000000000000000000, 0.000000000000000000, 0.000000000000000000 ) ) ;
#33377=CARTESIAN_POINT ( 'NONE',  ( -22.27786964138239867, 3.347945419004161760, 1.536369256421326490 ) ) ;
#33379=CARTESIAN_POINT ( 'NONE',  ( -22.27945548916780183, 2.122548946923926483, 3.016427163003885248 ) ) ;
#33387=VECTOR ( 'NONE', #55023, 1000.000000000000000 ) ;
#33388=DIRECTION ( 'NONE',  ( -1.000000000000000000, 0.000000000000000000, 0.000000000000000000 ) ) ;
#33397=EDGE_CURVE ( 'NONE', #62269, #55569, #57215, .T. ) ;
#33398=CARTESIAN_POINT ( 'NONE',  ( 2.000000000000001776, 2.664846396702580833, -6.404188155572981600 ) ) ;
#33399=EDGE_CURVE ( 'NONE', #43107, #51107, #31285, .T. ) ;
#33404=CARTESIAN_POINT ( 'NONE',  ( 0.000000000000000000, -4.409940824963369366, -5.354199675985328533 ) ) ;
#33406=CARTESIAN_POINT ( 'NONE',  ( -28.66013792860432119, -1.289369452666810467, -1.306994062650345567 ) ) ;
#33413=CARTESIAN_POINT ( 'NONE',  ( -35.04582288351658548, 0.008224400713785747288, -0.009684687560357898087 ) ) ;
#33415=DIRECTION ( 'NONE',  ( 1.000000000000000000, 0.000000000000000000, 0.000000000000000000 ) ) ;
#33424=ADVANCED_FACE ( 'NONE', ( #50915 ), #25234, .F. ) ;
#33425=CARTESIAN_POINT ( 'NONE',  ( 2.000000000000001776, 5.888698556700773246, 3.665823448873418045 ) ) ;
#33431=DIRECTION ( 'NONE',  ( -1.000000000000000000, 0.000000000000000000, 0.000000000000000000 ) ) ;
#33444=DIRECTION ( 'NONE',  ( 0.000000000000000000, 0.000000000000000000, 1.000000000000000000 ) ) ;
#33448=CARTESIAN_POINT ( 'NONE',  ( -22.27718112499583469, 0.5110808820053616142, 3.645895996548640383 ) ) ;
#33452=ORIENTED_EDGE ( 'NONE', *, *, #33760, .T. ) ;
#33464=DIRECTION ( 'NONE',  ( -0.9582930651793754029, -0.2067888154783181776, -0.1972632429577070579 ) ) ;
#33483=ADVANCED_FACE ( 'NONE', ( #47888 ), #38561, .T. ) ;
#33486=CARTESIAN_POINT ( 'NONE',  ( -22.28169757117798966, -2.592369810060387803, 2.633129923220808077 ) ) ;
#33490=CARTESIAN_POINT ( 'NONE',  ( -27.08423805673873375, -0.5302040644010280745, -2.229265646063334660 ) ) ;
#33497=ORIENTED_EDGE ( 'NONE', *, *, #56558, .F. ) ;
#33500=LINE ( 'NONE', #12879, #51956 ) ;
#33512=DIRECTION ( 'NONE',  ( 0.000000000000000000, 0.6876994588534194319, 0.7259954919231345061 ) ) ;
#33519=ORIENTED_EDGE ( 'NONE', *, *, #50631, .T. ) ;
#33525=CARTESIAN_POINT ( 'NONE',  ( -22.27945548916780183, -1.551028078364841800, 3.346394890313962200 ) ) ;
#33529=CARTESIAN_POINT ( 'NONE',  ( -22.28506771379528573, -3.718191140878641221, 0.2569416992704499081 ) ) ;
#33531=ORIENTED_EDGE ( 'NONE', *, *, #13436, .T. ) ;
#33541=CARTESIAN_POINT ( 'NONE',  ( -27.09252613521643482, -2.309775830546446862, 0.1722886739160240377 ) ) ;
#33546=ORIENTED_EDGE ( 'NONE', *, *, #52155, .F. ) ;
#33552=CARTESIAN_POINT ( 'NONE',  ( -22.35190811654612375, -3.252894036332505401, 2.161847148103702931 ) ) ;
#33554=CARTESIAN_POINT ( 'NONE',  ( -22.31328051695926007, -3.633840107626937765, 1.076152733467191869 ) ) ;
#33557=VERTEX_POINT ( 'NONE', #44849 ) ;
#33560=AXIS2_PLACEMENT_3D ( 'NONE', #53023, #7455, #27746 ) ;
#33565=CARTESIAN_POINT ( 'NONE',  ( -35.04709527796842394, -0.001082316405377065083, 0.01231589140597219578 ) ) ;
#33583=ORIENTED_EDGE ( 'NONE', *, *, #31437, .T. ) ;
#33589=CARTESIAN_POINT ( 'NONE',  ( -27.08850691366480490, -1.648570643964191396, -1.609738257842918019 ) ) ;
#33592=CARTESIAN_POINT ( 'NONE',  ( -35.04643116707788408, 0.01135624435143721411, 0.004425962698848331933 ) ) ;
#33594=VERTEX_POINT ( 'NONE', #50185 ) ;
#33597=CARTESIAN_POINT ( 'NONE',  ( -27.05874794189610455, 1.734723475976807094E-15, -8.673617379884035472E-15 ) ) ;
#33598=ORIENTED_EDGE ( 'NONE', *, *, #19228, .T. ) ;
#33601=CARTESIAN_POINT ( 'NONE',  ( -22.28776923226071460, -0.2883912626656507938, -3.702096209084106082 ) ) ;
#33606=DIRECTION ( 'NONE',  ( 0.000000000000000000, 0.000000000000000000, 1.000000000000000000 ) ) ;
#33613=ORIENTED_EDGE ( 'NONE', *, *, #62847, .F. ) ;
#33619=CARTESIAN_POINT ( 'NONE',  ( -22.46225619532222950, -4.233934615764599840, 0.1595555201818281699 ) ) ;
#33631=EDGE_LOOP ( 'NONE', ( #51386, #18979, #22660, #298 ) ) ;
#33633=CARTESIAN_POINT ( 'NONE',  ( 2.000000000000001776, 0.000000000000000000, 0.000000000000000000 ) ) ;
#33640=EDGE_CURVE ( 'NONE', #27713, #6901, #63607, .T. ) ;
#33641=VERTEX_POINT ( 'NONE', #34843 ) ;
#33651=CARTESIAN_POINT ( 'NONE',  ( -22.27719381268171261, -2.588413841766858958, -2.618044180756137429 ) ) ;
#33652=EDGE_CURVE ( 'NONE', #2794, #34196, #22225, .T. ) ;
#33656=CARTESIAN_POINT ( 'NONE',  ( 0.000000000000000000, 2.480520636974191895, 6.345145617221231049 ) ) ;
#33657=CARTESIAN_POINT ( 'NONE',  ( -22.29290468048228036, 3.718584170466879613, -0.2747050847461790513 ) ) ;
#33659=ORIENTED_EDGE ( 'NONE', *, *, #19617, .F. ) ;
#33665=EDGE_CURVE ( 'NONE', #16416, #33072, #32838, .T. ) ;
#33666=CARTESIAN_POINT ( 'NONE',  ( -22.31328051695926007, -3.401210163132568187, -1.671726071983963946 ) ) ;
#33672=ORIENTED_EDGE ( 'NONE', *, *, #26156, .T. ) ;
#33690=LINE ( 'NONE', #9078, #57553 ) ;
#33700=CARTESIAN_POINT ( 'NONE',  ( -22.27719381268171617, 0.9326100520993234611, 3.561499689648252698 ) ) ;
#33707=CARTESIAN_POINT ( 'NONE',  ( -27.08418322526030764, -1.431535851194450260, -1.789041206975763076 ) ) ;
#33718=CARTESIAN_POINT ( 'NONE',  ( -22.27384469013076185, -0.3730095848193254460, -3.663183248998795882 ) ) ;
#33723=ORIENTED_EDGE ( 'NONE', *, *, #40905, .F. ) ;
#33729=CARTESIAN_POINT ( 'NONE',  ( 0.000000000000000000, -2.664846396702537312, 6.404188155572974495 ) ) ;
#33731=ORIENTED_EDGE ( 'NONE', *, *, #11895, .F. ) ;
#33735=FACE_OUTER_BOUND ( 'NONE', #55430, .T. ) ;
#33746=EDGE_LOOP ( 'NONE', ( #39530, #34313, #45818, #13309 ) ) ;
#33755=CARTESIAN_POINT ( 'NONE',  ( 2.000000000000001776, -2.315790869867103474, 7.133520354428079635 ) ) ;
#33758=CARTESIAN_POINT ( 'NONE',  ( 0.000000000000000000, 0.000000000000000000, 0.000000000000000000 ) ) ;
#33760=EDGE_CURVE ( 'NONE', #61436, #10609, #62556, .T. ) ;
#33766=CARTESIAN_POINT ( 'NONE',  ( -22.29677679919927868, 3.097220482904032401, -2.096973157017371747 ) ) ;
#33769=EDGE_CURVE ( 'NONE', #57333, #7851, #46712, .T. ) ;
#33774=EDGE_LOOP ( 'NONE', ( #48922, #11857, #63441, #26172 ) ) ;
#33792=CARTESIAN_POINT ( 'NONE',  ( -27.08417473062937120, -0.4370481938669370514, -2.249064769433628097 ) ) ;
#33813=CARTESIAN_POINT ( 'NONE',  ( -27.15525204139122195, 0.5628609503965513738, -2.440367606305306580 ) ) ;
#33814=EDGE_CURVE ( 'NONE', #21947, #10229, #31748, .T. ) ;
#33835=ORIENTED_EDGE ( 'NONE', *, *, #53294, .T. ) ;
#33843=CARTESIAN_POINT ( 'NONE',  ( -27.09833916700337397, -1.609723001518240659, 1.689564470273824837 ) ) ;
#33844=CIRCLE ( 'NONE', #29567, 2.899999999999994582 ) ;
#33856=PRODUCT ( 'motion translator_ISO - Spur gear 0.25M 58T 20PA 2FW ---S58B6H18L3.0N', 'motion translator_ISO - Spur gear 0.25M 58T 20PA 2FW ---S58B6H18L3.0N', '', ( #37769 ) ) ;
#33861=CARTESIAN_POINT ( 'NONE',  ( -27.08485414902845534, 1.620258667553448051, -1.622802444813711054 ) ) ;
#33862=CARTESIAN_POINT ( 'NONE',  ( -27.08429572838383947, 1.338867938658203860, 1.859677275556406384 ) ) ;
#33876=CARTESIAN_POINT ( 'NONE',  ( -22.30625920655495165, -2.750410778797871547, -2.610366806364701642 ) ) ;
#33881=CARTESIAN_POINT ( 'NONE',  ( -27.08506889328328171, 2.083363953276920366, 0.9597901767732474054 ) ) ;
#33882=CARTESIAN_POINT ( 'NONE',  ( -22.30398854582848145, 2.724439933030925687, 2.594196582746961965 ) ) ;
#33889=CARTESIAN_POINT ( 'NONE',  ( -35.04582288351658548, 0.006225574250530754340, -0.01107592729723687851 ) ) ;
#33891=DIRECTION ( 'NONE',  ( -1.000000000000000000, 0.000000000000000000, 0.000000000000000000 ) ) ;
#33893=CIRCLE ( 'NONE', #47714, 2.899999999999994582 ) ;
#33896=ORIENTED_EDGE ( 'NONE', *, *, #34332, .F. ) ;
#33897=DIRECTION ( 'NONE',  ( 0.000000000000000000, -0.9868265225415276953, 0.1617819965527551584 ) ) ;
#33903=ORIENTED_EDGE ( 'NONE', *, *, #59206, .F. ) ;
#33904=EDGE_CURVE ( 'NONE', #21663, #61727, #2061, .T. ) ;
#33910=ORIENTED_EDGE ( 'NONE', *, *, #29005, .T. ) ;
#33916=CARTESIAN_POINT ( 'NONE',  ( 1.000000000000000888, -4.604744433234713163, 5.919993978425451608 ) ) ;
#33923=EDGE_LOOP ( 'NONE', ( #58163, #54456, #25114, #42840 ) ) ;
#33933=CARTESIAN_POINT ( 'NONE',  ( -22.30625920655495165, -3.403091720605013748, -1.672644928563079780 ) ) ;
#33938=ORIENTED_EDGE ( 'NONE', *, *, #37912, .T. ) ;
#33939=DIRECTION ( 'NONE',  ( 0.000000000000000000, 0.6051742151937661296, -0.7960930657056429771 ) ) ;
#33942=ADVANCED_FACE ( 'NONE', ( #52399 ), #32023, .F. ) ;
#33944=ORIENTED_EDGE ( 'NONE', *, *, #16611, .T. ) ;
#33945=CARTESIAN_POINT ( 'NONE',  ( -27.08429572838383947, -2.217805374070538349, 0.5764601019425888984 ) ) ;
#33946=ADVANCED_FACE ( 'NONE', ( #16489 ), #37069, .F. ) ;
#33947=CIRCLE ( 'NONE', #11641, 6.936499999999992561 ) ;
#33956=VECTOR ( 'NONE', #40207, 1000.000000000000000 ) ;
#33961=CARTESIAN_POINT ( 'NONE',  ( -22.39032720737627002, 3.916738514147016126, 0.9101257950220676962 ) ) ;
#33965=AXIS2_PLACEMENT_3D ( 'NONE', #16042, #26690, #52310 ) ;
#33966=ADVANCED_FACE ( 'NONE', ( #7149 ), #63007, .T. ) ;
#33967=CIRCLE ( 'NONE', #36089, 2.899999999999995470 ) ;
#33968=VERTEX_POINT ( 'NONE', #23779 ) ;
#33972=FACE_OUTER_BOUND ( 'NONE', #4074, .T. ) ;
#33977=ORIENTED_EDGE ( 'NONE', *, *, #25082, .F. ) ;
#33978=ADVANCED_FACE ( 'NONE', ( #14421 ), #36697, .F. ) ;
#33983=ORIENTED_EDGE ( 'NONE', *, *, #40505, .F. ) ;
#33986=AXIS2_PLACEMENT_3D ( 'NONE', #18865, #34137, #39129 ) ;
#34000=ORIENTED_EDGE ( 'NONE', *, *, #3309, .F. ) ;
#34011=CARTESIAN_POINT ( 'NONE',  ( 2.000000000000001776, -0.3246585432986597852, 6.805031400696099020 ) ) ;
#34013=VERTEX_POINT ( 'NONE', #64626 ) ;
#34014=DIRECTION ( 'NONE',  ( -1.000000000000000000, 0.000000000000000000, 0.000000000000000000 ) ) ;
#34016=FACE_OUTER_BOUND ( 'NONE', #18576, .T. ) ;
#34017=CARTESIAN_POINT ( 'NONE',  ( -22.30527770659433173, 2.100259071719474235, 3.125767038151177513 ) ) ;
#34050=CARTESIAN_POINT ( 'NONE',  ( -22.27384469013076185, -2.985904959940905545, 2.154627400808026838 ) ) ;
#34054=CYLINDRICAL_SURFACE ( 'NONE', #40462, 7.499999999999988454 ) ;
#34065=CARTESIAN_POINT ( 'NONE',  ( 2.000000000000001776, 6.250523986464036064, -3.007653927006531447 ) ) ;
#34090=EDGE_CURVE ( 'NONE', #34196, #56385, #23106, .T. ) ;
#34093=VECTOR ( 'NONE', #13000, 1000.000000000000000 ) ;
#34100=AXIS2_PLACEMENT_3D ( 'NONE', #19606, #34848, #9587 ) ;
#34108=CYLINDRICAL_SURFACE ( 'NONE', #33965, 6.936499999999988120 ) ;
#34109=ORIENTED_EDGE ( 'NONE', *, *, #43658, .F. ) ;
#34137=DIRECTION ( 'NONE',  ( -1.000000000000000000, 0.000000000000000000, 0.000000000000000000 ) ) ;
#34150=CIRCLE ( 'NONE', #57536, 2.899999999999995914 ) ;
#34153=ORIENTED_EDGE ( 'NONE', *, *, #4890, .T. ) ;
#34154=( LENGTH_UNIT ( ) NAMED_UNIT ( * ) SI_UNIT ( .MILLI., .METRE. ) );
#34155=VECTOR ( 'NONE', #25817, 1000.000000000000000 ) ;
#34168=LINE ( 'NONE', #64111, #23677 ) ;
#34173=CARTESIAN_POINT ( 'NONE',  ( 1.000000000000000888, -7.203928197742102135, 2.086484728383119158 ) ) ;
#34181=DIRECTION ( 'NONE',  ( -1.000000000000000000, 0.000000000000000000, 0.000000000000000000 ) ) ;
#34185=CARTESIAN_POINT ( 'NONE',  ( -35.04643116707788408, 0.004425962698851801380, -0.01135624435145456135 ) ) ;
#34196=VERTEX_POINT ( 'NONE', #30384 ) ;
#34198=CARTESIAN_POINT ( 'NONE',  ( 2.000000000000001776, 6.539067737394540281, -2.314222412769769033 ) ) ;
#34204=CARTESIAN_POINT ( 'NONE',  ( -35.04643116707788408, -0.01156612771643569793, -0.003844232202723438241 ) ) ;
#34205=VECTOR ( 'NONE', #55424, 1000.000000000000000 ) ;
#34206=CARTESIAN_POINT ( 'NONE',  ( -27.08579483061179616, 2.081508743190604083, 0.9690219683526558603 ) ) ;
#34212=EDGE_LOOP ( 'NONE', ( #40068, #26162, #7523, #60535 ) ) ;
#34213=EDGE_CURVE ( 'NONE', #3030, #21349, #12535, .T. ) ;
#34217=CARTESIAN_POINT ( 'NONE',  ( -22.27384469013076185, -0.9835229356382323429, 3.548341908721027060 ) ) ;
#34223=ORIENTED_EDGE ( 'NONE', *, *, #25050, .F. ) ;
#34234=EDGE_LOOP ( 'NONE', ( #7534, #10671, #4985, #32316 ) ) ;
#34237=CARTESIAN_POINT ( 'NONE',  ( -22.71097035706202405, 4.510116093748279376, -2.118550233809386896 ) ) ;
#34244=DIRECTION ( 'NONE',  ( -1.000000000000000000, 0.000000000000000000, 0.000000000000000000 ) ) ;
#34254=CARTESIAN_POINT ( 'NONE',  ( 0.000000000000000000, 3.859771122243047081, 5.613913289150030295 ) ) ;
#34255=VERTEX_POINT ( 'NONE', #48887 ) ;
#34258=EDGE_LOOP ( 'NONE', ( #7850, #46180, #27321, #32423 ) ) ;
#34263=CARTESIAN_POINT ( 'NONE',  ( 0.000000000000000000, 3.152010634611693174, 6.039758645301271933 ) ) ;
#34264=AXIS2_PLACEMENT_3D ( 'NONE', #52326, #17721, #36995 ) ;
#34265=CARTESIAN_POINT ( 'NONE',  ( 2.000000000000001776, 0.000000000000000000, 0.000000000000000000 ) ) ;
#34266=CARTESIAN_POINT ( 'NONE',  ( -22.31328051695926007, -3.781397440874596061, 0.2528478350593901802 ) ) ;
#34267=VERTEX_POINT ( 'NONE', #3344 ) ;
#34273=DIRECTION ( 'NONE',  ( -1.000000000000000000, 0.000000000000000000, 0.000000000000000000 ) ) ;
#34278=EDGE_CURVE ( 'NONE', #37190, #1479, #33947, .T. ) ;
#34280=CARTESIAN_POINT ( 'NONE',  ( -35.04683013664716640, 0.004196202180982810774, 0.01162359816263982236 ) ) ;
#34284=CIRCLE ( 'NONE', #55563, 2.899999999999995470 ) ;
#34285=CARTESIAN_POINT ( 'NONE',  ( -27.08426504710140392, 2.202478235133278783, 0.6326154899769155238 ) ) ;
#34296=CARTESIAN_POINT ( 'NONE',  ( 0.000000000000000000, -7.203928197742085260, -2.086484728383230181 ) ) ;
#34307=CARTESIAN_POINT ( 'NONE',  ( -35.04643116707788408, -0.004425962698862209721, 0.01135624435143547939 ) ) ;
#34313=ORIENTED_EDGE ( 'NONE', *, *, #59303, .T. ) ;
#34314=ORIENTED_EDGE ( 'NONE', *, *, #11762, .T. ) ;
#34317=AXIS2_PLACEMENT_3D ( 'NONE', #47183, #51186, #5637 ) ;
#34321=EDGE_CURVE ( 'NONE', #36463, #54788, #26807, .T. ) ;
#34322=CARTESIAN_POINT ( 'NONE',  ( -22.27722022243423794, -2.391991868237149710, -2.798846704197252233 ) ) ;
#34325=CARTESIAN_POINT ( 'NONE',  ( -10.00000000000000178, 0.000000000000000000, 0.000000000000000000 ) ) ;
#34332=EDGE_CURVE ( 'NONE', #2803, #10275, #42420, .T. ) ;
#34347=ORIENTED_EDGE ( 'NONE', *, *, #47479, .F. ) ;
#34358=AXIS2_PLACEMENT_3D ( 'NONE', #59579, #14012, #19686 ) ;
#34362=EDGE_CURVE ( 'NONE', #35981, #23681, #57311, .T. ) ;
#34366=FACE_OUTER_BOUND ( 'NONE', #61652, .T. ) ;
#34370=EDGE_CURVE ( 'NONE', #33641, #25335, #50962, .T. ) ;
#34371=VECTOR ( 'NONE', #30707, 1000.000000000000000 ) ;
#34374=CIRCLE ( 'NONE', #47168, 6.936499999999989008 ) ;
#34379=LINE ( 'NONE', #24394, #27188 ) ;
#34386=CARTESIAN_POINT ( 'NONE',  ( 2.000000000000001776, 2.664846396702499121, 6.404188155572998475 ) ) ;
#34393=ORIENTED_EDGE ( 'NONE', *, *, #45870, .T. ) ;
#34406=VECTOR ( 'NONE', #29165, 1000.000000000000000 ) ;
#34412=VERTEX_POINT ( 'NONE', #54535 ) ;
#34415=ORIENTED_EDGE ( 'NONE', *, *, #50641, .F. ) ;
#34422=DIRECTION ( 'NONE',  ( 0.000000000000000000, 0.000000000000000000, -1.000000000000000000 ) ) ;
#34423=DIRECTION ( 'NONE',  ( -1.000000000000000000, 0.000000000000000000, 0.000000000000000000 ) ) ;
#34425=VERTEX_POINT ( 'NONE', #54848 ) ;
#34428=ORIENTED_EDGE ( 'NONE', *, *, #50213, .T. ) ;
#34429=DIRECTION ( 'NONE',  ( -1.000000000000000000, 0.000000000000000000, 0.000000000000000000 ) ) ;
#34430=CARTESIAN_POINT ( 'NONE',  ( 2.000000000000001776, 6.201547234537079234, -2.820401998297854096 ) ) ;
#34436=CARTESIAN_POINT ( 'NONE',  ( 0.000000000000000000, 0.000000000000000000, 0.000000000000000000 ) ) ;
#34437=ADVANCED_FACE ( 'NONE', ( #9268 ), #19610, .T. ) ;
#34438=ORIENTED_EDGE ( 'NONE', *, *, #14168, .F. ) ;
#34441=AXIS2_PLACEMENT_3D ( 'NONE', #17058, #62942, #57651 ) ;
#34446=EDGE_CURVE ( 'NONE', #3157, #35439, #47774, .T. ) ;
#34450=CARTESIAN_POINT ( 'NONE',  ( -27.08423805673873375, -2.195702713475281342, -0.6554626340706090071 ) ) ;
#34463=CARTESIAN_POINT ( 'NONE',  ( -35.05012975565874456, 0.002839961651358813028, 0.01363945138521199113 ) ) ;
#34467=DIRECTION ( 'NONE',  ( -1.000000000000000000, 0.000000000000000000, 0.000000000000000000 ) ) ;
#34469=CARTESIAN_POINT ( 'NONE',  ( -22.31328051695926007, -1.076152733467184985, -3.633840107626963967 ) ) ;
#34477=CARTESIAN_POINT ( 'NONE',  ( -27.09602251845159415, 1.302811993375597277, 1.927725285105644115 ) ) ;
#34480=CARTESIAN_POINT ( 'NONE',  ( 2.000000000000001776, -5.396716205731396876, -4.158041573745144603 ) ) ;
#34491=ORIENTED_EDGE ( 'NONE', *, *, #37923, .F. ) ;
#34494=CARTESIAN_POINT ( 'NONE',  ( 2.000000000000001776, 0.000000000000000000, 0.000000000000000000 ) ) ;
#34511=ADVANCED_FACE ( 'NONE', ( #11258 ), #30539, .T. ) ;
#34516=DIRECTION ( 'NONE',  ( -1.000000000000000000, 0.000000000000000000, 0.000000000000000000 ) ) ;
#34520=DIRECTION ( 'NONE',  ( -1.000000000000000000, 0.000000000000000000, 0.000000000000000000 ) ) ;
#34538=CARTESIAN_POINT ( 'NONE',  ( 2.000000000000001776, 0.000000000000000000, 0.000000000000000000 ) ) ;
#34539=CIRCLE ( 'NONE', #5911, 2.899999999999995470 ) ;
#34555=DIRECTION ( 'NONE',  ( -1.000000000000000000, 0.000000000000000000, 0.000000000000000000 ) ) ;
#34558=DIRECTION ( 'NONE',  ( -1.000000000000000000, 0.000000000000000000, 0.000000000000000000 ) ) ;
#34570=CARTESIAN_POINT ( 'NONE',  ( -27.08776759928964850, -2.229418711698780253, -0.5731512436792201015 ) ) ;
#34573=DIRECTION ( 'NONE',  ( 0.000000000000000000, 0.000000000000000000, 1.000000000000000000 ) ) ;
#34576=EDGE_LOOP ( 'NONE', ( #27783, #21150, #12708, #8763 ) ) ;
#34578=ORIENTED_EDGE ( 'NONE', *, *, #19546, .F. ) ;
#34582=CARTESIAN_POINT ( 'NONE',  ( 1.000000000000000888, 2.315790869867065283, 7.133520354428103616 ) ) ;
#34583=CARTESIAN_POINT ( 'NONE',  ( -22.35190811654612375, -0.2457675311904815585, -3.898012445334722909 ) ) ;
#34586=CIRCLE ( 'NONE', #45178, 7.499999999999988454 ) ;
#34592=EDGE_LOOP ( 'NONE', ( #34000, #62716, #60392, #32748 ) ) ;
#34595=CARTESIAN_POINT ( 'NONE',  ( -10.00000000000000178, 0.000000000000000000, 0.000000000000000000 ) ) ;
#34599=ADVANCED_FACE ( 'NONE', ( #47813 ), #7233, .T. ) ;
#34614=CARTESIAN_POINT ( 'NONE',  ( -22.28506771379528573, 2.571716811880577325, -2.697635452840750681 ) ) ;
#34615=CARTESIAN_POINT ( 'NONE',  ( -22.27384469013076185, 0.9835229356382479970, -3.548341908721023952 ) ) ;
#34623=CARTESIAN_POINT ( 'NONE',  ( 2.000000000000001776, -2.315790869867006219, -7.133520354428148025 ) ) ;
#34630=CARTESIAN_POINT ( 'NONE',  ( -27.10719052120871098, 2.261993590776037788, -0.6736837626858775963 ) ) ;
#34632=FACE_OUTER_BOUND ( 'NONE', #2399, .T. ) ;
#34641=DIRECTION ( 'NONE',  ( -1.000000000000000000, 0.000000000000000000, 0.000000000000000000 ) ) ;
#34643=CARTESIAN_POINT ( 'NONE',  ( -22.27384469013075829, -3.548341908721032389, -0.9835229356382479970 ) ) ;
#34644=ORIENTED_EDGE ( 'NONE', *, *, #2689, .T. ) ;
#34654=CARTESIAN_POINT ( 'NONE',  ( -27.09483304420798433, -0.1669215111592733392, -2.317106154747427649 ) ) ;
#34655=DIRECTION ( 'NONE',  ( 0.000000000000000000, 0.000000000000000000, -1.000000000000000000 ) ) ;
#34656=DIRECTION ( 'NONE',  ( 0.000000000000000000, -0.9635499925192253512, 0.2675283385292119842 ) ) ;
#34664=CARTESIAN_POINT ( 'NONE',  ( 2.000000000000001776, -4.444115772890149252, 5.163689623839303522 ) ) ;
#34671=CYLINDRICAL_SURFACE ( 'NONE', #57842, 2.899999999999994582 ) ;
#34673=ADVANCED_FACE ( 'NONE', ( #40102 ), #29797, .T. ) ;
#34674=DIRECTION ( 'NONE',  ( -1.000000000000000000, -1.685093406416449860E-16, 1.011030131491581592E-17 ) ) ;
#34675=DIRECTION ( 'NONE',  ( 1.000000000000000000, -0.000000000000000000, -0.000000000000000000 ) ) ;
#34679=EDGE_CURVE ( 'NONE', #22010, #13960, #38818, .T. ) ;
#34682=EDGE_CURVE ( 'NONE', #20446, #55528, #8884, .T. ) ;
#34694=CARTESIAN_POINT ( 'NONE',  ( -22.27711351828769892, 3.534923377568743419, 1.028167152775488535 ) ) ;
#34696=ORIENTED_EDGE ( 'NONE', *, *, #37646, .F. ) ;
#34709=CARTESIAN_POINT ( 'NONE',  ( -22.31328051695926007, -2.109671368890623455, -3.148362328073181615 ) ) ;
#34720=CARTESIAN_POINT ( 'NONE',  ( -22.31328051695926007, -0.8849444482787947042, 3.685074213229300621 ) ) ;
#34722=CARTESIAN_POINT ( 'NONE',  ( -22.27384469013076185, -0.3730095848193254460, -3.663183248998795882 ) ) ;
#34723=DIRECTION ( 'NONE',  ( -1.000000000000000000, 0.000000000000000000, 0.000000000000000000 ) ) ;
#34725=CARTESIAN_POINT ( 'NONE',  ( 2.000000000000001776, 6.935703035393448346, -0.1051458740707923722 ) ) ;
#34730=ORIENTED_EDGE ( 'NONE', *, *, #36465, .F. ) ;
#34733=CARTESIAN_POINT ( 'NONE',  ( 2.000000000000001776, 0.000000000000000000, 0.000000000000000000 ) ) ;
#34734=CARTESIAN_POINT ( 'NONE',  ( -22.27706089016750113, 0.9798385173596402264, -3.548384797797537793 ) ) ;
#34736=EDGE_CURVE ( 'NONE', #23637, #42619, #54775, .T. ) ;
#34737=DIRECTION ( 'NONE',  ( 0.000000000000000000, -0.1081190184239488317, 0.9941379571543589311 ) ) ;
#34744=VECTOR ( 'NONE', #57417, 1000.000000000000000 ) ;
#34757=DIRECTION ( 'NONE',  ( 0.000000000000000000, 0.9985334138511235968, 0.05413890858542115547 ) ) ;
#34763=ORIENTED_EDGE ( 'NONE', *, *, #33640, .F. ) ;
#34769=CARTESIAN_POINT ( 'NONE',  ( -22.49803948133826026, 4.343047530463596928, -0.1132714802761584233 ) ) ;
#34770=CARTESIAN_POINT ( 'NONE',  ( -22.27710395300133328, -0.9291085174899353927, -3.562137928983406088 ) ) ;
#34775=ORIENTED_EDGE ( 'NONE', *, *, #65354, .F. ) ;
#34780=CARTESIAN_POINT ( 'NONE',  ( 0.000000000000000000, 5.860254403322016969, 3.474373880649828550 ) ) ;
#34782=DIRECTION ( 'NONE',  ( -1.000000000000000000, 0.000000000000000000, 0.000000000000000000 ) ) ;
#34800=ORIENTED_EDGE ( 'NONE', *, *, #17934, .T. ) ;
#34801=DIRECTION ( 'NONE',  ( -1.000000000000000000, 0.000000000000000000, 0.000000000000000000 ) ) ;
#34811=DIRECTION ( 'NONE',  ( 0.000000000000000000, 0.000000000000000000, 1.000000000000000000 ) ) ;
#34813=VERTEX_POINT ( 'NONE', #30776 ) ;
#34821=CARTESIAN_POINT ( 'NONE',  ( 0.000000000000000000, 0.000000000000000000, 0.000000000000000000 ) ) ;
#34827=CIRCLE ( 'NONE', #64600, 7.499999999999988454 ) ;
#34838=CARTESIAN_POINT ( 'NONE',  ( -27.08871896697694837, 2.082324523415888695, 0.9878677378266799147 ) ) ;
#34843=CARTESIAN_POINT ( 'NONE',  ( 0.000000000000000000, -1.018311147294094443, -6.861346417234492456 ) ) ;
#34848=DIRECTION ( 'NONE',  ( -1.000000000000000000, 0.000000000000000000, 0.000000000000000000 ) ) ;
#34852=CARTESIAN_POINT ( 'NONE',  ( 0.000000000000000000, 4.376687952327412034, -5.220963330856592144 ) ) ;
#34854=EDGE_CURVE ( 'NONE', #13076, #43273, #15605, .T. ) ;
#34857=CARTESIAN_POINT ( 'NONE',  ( -22.27709082389155171, -3.541295940224330252, -1.005749854561710510 ) ) ;
#34858=DIRECTION ( 'NONE',  ( -1.000000000000000000, 0.000000000000000000, 0.000000000000000000 ) ) ;
#34864=CARTESIAN_POINT ( 'NONE',  ( -22.46225619532222950, 0.1595555201818359137, 4.233934615764590959 ) ) ;
#34866=ORIENTED_EDGE ( 'NONE', *, *, #16787, .F. ) ;
#34868=VECTOR ( 'NONE', #41789, 1000.000000000000000 ) ;
#34872=CARTESIAN_POINT ( 'NONE',  ( 2.000000000000001776, 6.767909380267608022, 2.119450094687897579 ) ) ;
#34874=ORIENTED_EDGE ( 'NONE', *, *, #53986, .T. ) ;
#34884=ORIENTED_EDGE ( 'NONE', *, *, #42693, .F. ) ;
#34894=CARTESIAN_POINT ( 'NONE',  ( -27.35552965826137140, 2.810569013793760007, -1.320216934008374920 ) ) ;
#34895=CARTESIAN_POINT ( 'NONE',  ( -22.65999102136915866, -2.911035239830966681, 3.858590659383635213 ) ) ;
#34896=ORIENTED_EDGE ( 'NONE', *, *, #57328, .F. ) ;
#34898=ORIENTED_EDGE ( 'NONE', *, *, #54595, .F. ) ;
#34908=AXIS2_PLACEMENT_3D ( 'NONE', #23077, #13411, #24061 ) ;
#34913=CARTESIAN_POINT ( 'NONE',  ( 2.000000000000001776, 6.883677378339475794, 0.8544109087186002593 ) ) ;
#34918=DIRECTION ( 'NONE',  ( -1.000000000000000000, 0.000000000000000000, 0.000000000000000000 ) ) ;
#34919=CARTESIAN_POINT ( 'NONE',  ( -22.30625920655495165, -2.750410778797871547, -2.610366806364701642 ) ) ;
#34932=ORIENTED_EDGE ( 'NONE', *, *, #5842, .F. ) ;
#34934=ADVANCED_FACE ( 'NONE', ( #47421 ), #27769, .T. ) ;
#34940=EDGE_CURVE ( 'NONE', #43097, #16340, #22457, .T. ) ;
#34947=EDGE_CURVE ( 'NONE', #62776, #1482, #28677, .T. ) ;
#34957=DIRECTION ( 'NONE',  ( 1.000000000000000000, -0.000000000000000000, -0.000000000000000000 ) ) ;
#34961=VERTEX_POINT ( 'NONE', #11810 ) ;
#34969=CARTESIAN_POINT ( 'NONE',  ( 1.000000000000000888, 5.662015959325201742, 4.918493191653995567 ) ) ;
#34970=CARTESIAN_POINT ( 'NONE',  ( -27.08429572838383947, -2.089332284968714593, -0.9410937941434025511 ) ) ;
#34986=CARTESIAN_POINT ( 'NONE',  ( -22.28236030719477867, 1.572829798448341698, -3.345835236227589604 ) ) ;
#34997=CIRCLE ( 'NONE', #50942, 7.499999999999988454 ) ;
#35000=CARTESIAN_POINT ( 'NONE',  ( -10.00000000000000178, 0.000000000000000000, 0.000000000000000000 ) ) ;
#35009=AXIS2_PLACEMENT_3D ( 'NONE', #47179, #33166, #12231 ) ;
#35014=CARTESIAN_POINT ( 'NONE',  ( -22.29770266787582500, 3.593535545924351648, -1.047554374660431442 ) ) ;
#35027=DIRECTION ( 'NONE',  ( 0.000000000000000000, 0.000000000000000000, 1.000000000000000000 ) ) ;
#35028=EDGE_CURVE ( 'NONE', #27429, #22010, #57404, .T. ) ;
#35033=EDGE_LOOP ( 'NONE', ( #42568, #41837, #31578, #55034 ) ) ;
#35036=EDGE_LOOP ( 'NONE', ( #44812, #3073, #19415, #1137 ) ) ;
#35040=CARTESIAN_POINT ( 'NONE',  ( -22.29195009621226475, -0.8975732442595466543, 3.616122380634891886 ) ) ;
#35041=ADVANCED_FACE ( 'NONE', ( #45651 ), #11384, .T. ) ;
#35061=CARTESIAN_POINT ( 'NONE',  ( -22.27722019094931483, 1.249795790945223972, -3.463038365117172557 ) ) ;
#35067=ORIENTED_EDGE ( 'NONE', *, *, #31973, .F. ) ;
#35071=CARTESIAN_POINT ( 'NONE',  ( -10.00000000000000178, 0.000000000000000000, 0.000000000000000000 ) ) ;
#35072=EDGE_CURVE ( 'NONE', #35989, #54252, #60847, .T. ) ;
#35077=DIRECTION ( 'NONE',  ( 1.000000000000000000, -0.000000000000000000, -0.000000000000000000 ) ) ;
#35079=CIRCLE ( 'NONE', #49979, 2.899999999999995026 ) ;
#35083=EDGE_CURVE ( 'NONE', #13688, #11147, #5385, .T. ) ;
#35086=AXIS2_PLACEMENT_3D ( 'NONE', #31504, #57120, #52130 ) ;
#35099=EDGE_CURVE ( 'NONE', #44602, #49587, #30824, .T. ) ;
#35109=CARTESIAN_POINT ( 'NONE',  ( -27.09861164373112885, 1.303360234155700015, 1.936722219469616091 ) ) ;
#35113=CARTESIAN_POINT ( 'NONE',  ( -22.30625920655495165, 3.687109008463850479, 0.8854385781085043483 ) ) ;
#35127=CARTESIAN_POINT ( 'NONE',  ( 2.000000000000001776, 4.376687952327412034, -5.220963330856592144 ) ) ;
#35132=ADVANCED_FACE ( 'NONE', ( #5601 ), #17193, .T. ) ;
#35133=FACE_OUTER_BOUND ( 'NONE', #25989, .T. ) ;
#35138=CARTESIAN_POINT ( 'NONE',  ( -27.08579483061202708, 2.287150433979704633, -0.2015567301747461515 ) ) ;
#35154=DIRECTION ( 'NONE',  ( 0.000000000000000000, 0.000000000000000000, -1.000000000000000000 ) ) ;
#35155=VECTOR ( 'NONE', #34423, 1000.000000000000000 ) ;
#35157=EDGE_CURVE ( 'NONE', #65319, #53863, #37468, .T. ) ;
#35158=ORIENTED_EDGE ( 'NONE', *, *, #63713, .T. ) ;
#35160=AXIS2_PLACEMENT_3D ( 'NONE', #55049, #9476, #29763 ) ;
#35162=ORIENTED_EDGE ( 'NONE', *, *, #1087, .T. ) ;
#35172=VECTOR ( 'NONE', #33464, 1000.000000000000227 ) ;
#35181=ORIENTED_EDGE ( 'NONE', *, *, #59896, .T. ) ;
#35184=CARTESIAN_POINT ( 'NONE',  ( -23.41523303002441736, -4.252418708693351590, 1.997501275420731748 ) ) ;
#35189=DIRECTION ( 'NONE',  ( 1.000000000000000000, 0.000000000000000000, 0.000000000000000000 ) ) ;
#35207=ORIENTED_EDGE ( 'NONE', *, *, #51389, .F. ) ;
#35209=CARTESIAN_POINT ( 'NONE',  ( -35.04709527796842394, -0.01012471662513968196, -0.007095259204994638913 ) ) ;
#35214=VECTOR ( 'NONE', #6907, 1000.000000000000000 ) ;
#35225=DIRECTION ( 'NONE',  ( 0.000000000000000000, 0.8276889981568877896, 0.5611870653623862726 ) ) ;
#35226=ORIENTED_EDGE ( 'NONE', *, *, #33640, .T. ) ;
#35239=VECTOR ( 'NONE', #21442, 1000.000000000000000 ) ;
#35242=CARTESIAN_POINT ( 'NONE',  ( 0.000000000000000000, -6.250523986463956128, -3.007653927006670003 ) ) ;
#35246=CARTESIAN_POINT ( 'NONE',  ( -28.66013792860432119, 1.826836065344828564, -0.1826938850344149434 ) ) ;
#35249=CIRCLE ( 'NONE', #28854, 6.936499999999989896 ) ;
#35251=FACE_OUTER_BOUND ( 'NONE', #35036, .T. ) ;
#35254=CARTESIAN_POINT ( 'NONE',  ( 2.000000000000001776, -6.606214214351046721, -2.114938770769991372 ) ) ;
#35270=CARTESIAN_POINT ( 'NONE',  ( -22.31328051695926007, 3.685074213229321494, 0.8849444482787824917 ) ) ;
#35271=CARTESIAN_POINT ( 'NONE',  ( -35.04643116707788408, -0.009112266603810564858, 0.008094444324481878117 ) ) ;
#35277=CARTESIAN_POINT ( 'NONE',  ( -27.10422407540562162, -1.306850885988421362, -1.954655484501059970 ) ) ;
#35284=VECTOR ( 'NONE', #3358, 1000.000000000000000 ) ;
#35292=ORIENTED_EDGE ( 'NONE', *, *, #6802, .T. ) ;
#35296=CARTESIAN_POINT ( 'NONE',  ( -22.31328051695926007, 0.2528478350594092761, 3.781397440874584071 ) ) ;
#35305=CARTESIAN_POINT ( 'NONE',  ( 2.000000000000001776, 4.444115772890121718, 5.163689623839328391 ) ) ;
#35309=EDGE_CURVE ( 'NONE', #38796, #918, #53440, .T. ) ;
#35311=CARTESIAN_POINT ( 'NONE',  ( -22.39032720737626292, -2.936932155721161397, -2.746561316202171810 ) ) ;
#35314=CARTESIAN_POINT ( 'NONE',  ( -27.08419642509983305, 2.239682169453941274, -0.4837273216074968185 ) ) ;
#35318=CARTESIAN_POINT ( 'NONE',  ( -28.66013792860432119, 1.071635578228296470, 1.490739498621012071 ) ) ;
#35321=VERTEX_POINT ( 'NONE', #7885 ) ;
#35326=DIRECTION ( 'NONE',  ( 1.000000000000000000, 0.000000000000000000, 0.000000000000000000 ) ) ;
#35340=AXIS2_PLACEMENT_3D ( 'NONE', #60373, #29455, #39773 ) ;
#35349=EDGE_CURVE ( 'NONE', #45593, #21947, #26636, .T. ) ;
#35355=DIRECTION ( 'NONE',  ( 0.000000000000000000, 0.000000000000000000, -1.000000000000000000 ) ) ;
#35356=DIRECTION ( 'NONE',  ( -1.000000000000000000, 0.000000000000000000, 0.000000000000000000 ) ) ;
#35357=ORIENTED_EDGE ( 'NONE', *, *, #62017, .F. ) ;
#35358=DIRECTION ( 'NONE',  ( 0.000000000000000000, 0.000000000000000000, -1.000000000000000000 ) ) ;
#35364=CARTESIAN_POINT ( 'NONE',  ( 0.000000000000000000, -7.248432822490231686, -1.926193556693109654 ) ) ;
#35365=ORIENTED_EDGE ( 'NONE', *, *, #23302, .F. ) ;
#35368=CIRCLE ( 'NONE', #33247, 2.899999999999994582 ) ;
#35373=CARTESIAN_POINT ( 'NONE',  ( -22.71097035706202760, -2.118550233809395777, -4.510116093748293586 ) ) ;
#35381=CIRCLE ( 'NONE', #22694, 7.499999999999988454 ) ;
#35390=EDGE_CURVE ( 'NONE', #44685, #41165, #22513, .T. ) ;
#35392=CARTESIAN_POINT ( 'NONE',  ( 2.000000000000001776, 0.000000000000000000, 0.000000000000000000 ) ) ;
#35396=CARTESIAN_POINT ( 'NONE',  ( -27.04788180060269553, -2.650714769830309070, -1.844972430941769215 ) ) ;
#35401=DIRECTION ( 'NONE',  ( -1.000000000000000000, 0.000000000000000000, 0.000000000000000000 ) ) ;
#35404=DIRECTION ( 'NONE',  ( 0.000000000000000000, 0.000000000000000000, 1.000000000000000000 ) ) ;
#35405=CARTESIAN_POINT ( 'NONE',  ( -22.27722022243424149, 1.227876413014602708, -3.470949075637792092 ) ) ;
#35415=EDGE_CURVE ( 'NONE', #28121, #24059, #44400, .T. ) ;
#35422=CARTESIAN_POINT ( 'NONE',  ( -22.71097035706202760, 2.118550233809425087, 4.510116093748266053 ) ) ;
#35433=CARTESIAN_POINT ( 'NONE',  ( 0.000000000000000000, 4.604744433234757572, -5.919993978425451608 ) ) ;
#35434=ADVANCED_FACE ( 'NONE', ( #45728 ), #14789, .T. ) ;
#35435=CIRCLE ( 'NONE', #15271, 7.499999999999988454 ) ;
#35439=VERTEX_POINT ( 'NONE', #50416 ) ;
#35442=AXIS2_PLACEMENT_3D ( 'NONE', #37471, #47786, #58426 ) ;
#35462=CARTESIAN_POINT ( 'NONE',  ( -27.08429572838383947, 0.6096735944848206135, -2.208905845566032866 ) ) ;
#35469=EDGE_CURVE ( 'NONE', #5947, #52522, #58513, .T. ) ;
#35475=CYLINDRICAL_SURFACE ( 'NONE', #60305, 7.499999999999988454 ) ;
#35476=CARTESIAN_POINT ( 'NONE',  ( -22.27715239060371744, -1.072868796692241888, 3.521735673127119881 ) ) ;
#35484=DIRECTION ( 'NONE',  ( 0.000000000000000000, 0.000000000000000000, 1.000000000000000000 ) ) ;
#35485=DIRECTION ( 'NONE',  ( -1.000000000000000000, 0.000000000000000000, 0.000000000000000000 ) ) ;
#35495=EDGE_CURVE ( 'NONE', #22815, #17671, #7552, .T. ) ;
#35500=LINE ( 'NONE', #55797, #59693 ) ;
#35501=DIRECTION ( 'NONE',  ( 0.000000000000000000, -0.6876994588534294239, 0.7259954919231249582 ) ) ;
#35516=FACE_OUTER_BOUND ( 'NONE', #20084, .T. ) ;
#35520=EDGE_CURVE ( 'NONE', #36018, #57723, #36218, .T. ) ;
#35521=EDGE_CURVE ( 'NONE', #22936, #63998, #60703, .T. ) ;
#35529=CARTESIAN_POINT ( 'NONE',  ( -28.66013792860432119, -0.7552004871165356459, 1.673433383655430484 ) ) ;
#35536=VERTEX_POINT ( 'NONE', #48308 ) ;
#35539=CARTESIAN_POINT ( 'NONE',  ( -22.27715239060371744, -3.521735673127123878, -1.072868796692257209 ) ) ;
#35552=ORIENTED_EDGE ( 'NONE', *, *, #2091, .T. ) ;
#35564=DIRECTION ( 'NONE',  ( 0.000000000000000000, -0.2149704402110115264, -0.9766205557100894330 ) ) ;
#35568=EDGE_LOOP ( 'NONE', ( #26304, #20329, #50858, #21773 ) ) ;
#35577=FACE_OUTER_BOUND ( 'NONE', #18390, .T. ) ;
#35584=CARTESIAN_POINT ( 'NONE',  ( 2.000000000000001776, 7.203928197742101247, 2.086484728383167564 ) ) ;
#35597=LINE ( 'NONE', #15634, #46042 ) ;
#35600=ADVANCED_FACE ( 'NONE', ( #2065 ), #16321, .F. ) ;
#35601=VECTOR ( 'NONE', #8661, 1000.000000000000000 ) ;
#35605=EDGE_CURVE ( 'NONE', #9767, #57779, #41537, .T. ) ;
#35606=CARTESIAN_POINT ( 'NONE',  ( -22.27834755396594346, 1.338300169228711090, -3.434702243602646199 ) ) ;
#35610=EDGE_CURVE ( 'NONE', #13885, #4816, #42954, .T. ) ;
#35621=CARTESIAN_POINT ( 'NONE',  ( -22.59969328935897082, 1.672297795814042143, 4.339503524536170609 ) ) ;
#35629=CARTESIAN_POINT ( 'NONE',  ( -22.27786964138239867, 0.3434379038477919366, 3.667590411551997054 ) ) ;
#35633=DIRECTION ( 'NONE',  ( 0.000000000000000000, -0.9868265225415245867, -0.1617819965527747539 ) ) ;
#35644=CARTESIAN_POINT ( 'NONE',  ( -27.08456565417852602, -0.2166646653334006467, -2.282055114149017072 ) ) ;
#35663=ORIENTED_EDGE ( 'NONE', *, *, #60632, .T. ) ;
#35668=CARTESIAN_POINT ( 'NONE',  ( -27.08430418657510330, -0.9470735946412819350, 2.086666645150418109 ) ) ;
#35670=AXIS2_PLACEMENT_3D ( 'NONE', #3159, #23422, #13751 ) ;
#35683=DIRECTION ( 'NONE',  ( 0.000000000000000000, 0.000000000000000000, 1.000000000000000000 ) ) ;
#35684=CARTESIAN_POINT ( 'NONE',  ( -22.29018399051993882, 3.576688584977253171, -1.024613686459438622 ) ) ;
#35689=ORIENTED_EDGE ( 'NONE', *, *, #30403, .F. ) ;
#35690=ORIENTED_EDGE ( 'NONE', *, *, #4155, .T. ) ;
#35697=DIRECTION ( 'NONE',  ( 0.000000000000000000, 0.9289767198167898643, 0.3701381553399182289 ) ) ;
#35708=CARTESIAN_POINT ( 'NONE',  ( -27.28573687977896611, 2.255103317860400303, 1.818142657385544148 ) ) ;
#35713=CIRCLE ( 'NONE', #10231, 2.899999999999994582 ) ;
#35715=VERTEX_POINT ( 'NONE', #34913 ) ;
#35718=CARTESIAN_POINT ( 'NONE',  ( -23.18047892478189098, -3.933989833240145728, -2.738168160732700862 ) ) ;
#35722=DIRECTION ( 'NONE',  ( 0.000000000000000000, 0.000000000000000000, 1.000000000000000000 ) ) ;
#35727=CARTESIAN_POINT ( 'NONE',  ( -22.27706485742869091, 0.9832726768967819941, -3.547445275915930285 ) ) ;
#35735=CARTESIAN_POINT ( 'NONE',  ( -22.70624764888619751, -4.591418580540049810, 2.547047087672836163 ) ) ;
#35736=CARTESIAN_POINT ( 'NONE',  ( 0.000000000000000000, 3.230174184210066191, 5.998318953995321223 ) ) ;
#35738=CARTESIAN_POINT ( 'NONE',  ( -27.08419642509983305, -2.181485315953910042, -0.7009209357102740290 ) ) ;
#35740=CARTESIAN_POINT ( 'NONE',  ( -27.10719052120871098, 2.116547233941204809, 1.044362304621460069 ) ) ;
#35748=ORIENTED_EDGE ( 'NONE', *, *, #1087, .F. ) ;
#35755=FACE_OUTER_BOUND ( 'NONE', #9937, .T. ) ;
#35764=CARTESIAN_POINT ( 'NONE',  ( -27.15525204139121840, -2.440367606305310133, -0.5628609503965597005 ) ) ;
#35766=EDGE_CURVE ( 'NONE', #1625, #13124, #18201, .T. ) ;
#35776=DIRECTION ( 'NONE',  ( -1.000000000000000000, 0.000000000000000000, 0.000000000000000000 ) ) ;
#35781=CARTESIAN_POINT ( 'NONE',  ( -22.28506771379528573, -0.8783543640076993952, 3.622079238249907629 ) ) ;
#35782=FACE_OUTER_BOUND ( 'NONE', #41366, .T. ) ;
#35783=CARTESIAN_POINT ( 'NONE',  ( -22.27721038036499834, -1.315315479297498369, 3.438655654856794364 ) ) ;
#35789=DIRECTION ( 'NONE',  ( 0.000000000000000000, 0.000000000000000000, 1.000000000000000000 ) ) ;
#35792=FACE_OUTER_BOUND ( 'NONE', #4437, .T. ) ;
#35794=DIRECTION ( 'NONE',  ( -1.000000000000000000, -0.000000000000000000, -0.000000000000000000 ) ) ;
#35795=CARTESIAN_POINT ( 'NONE',  ( 2.000000000000001776, 7.387287142779349836, 1.295372019972174549 ) ) ;
#35798=CARTESIAN_POINT ( 'NONE',  ( -22.31328051695926007, -1.076152733467184985, -3.633840107626963967 ) ) ;
#35799=EDGE_LOOP ( 'NONE', ( #3709, #60319, #3984, #4681 ) ) ;
#35809=DIRECTION ( 'NONE',  ( -1.000000000000000000, 0.000000000000000000, 0.000000000000000000 ) ) ;
#35816=DIRECTION ( 'NONE',  ( -1.000000000000000000, 0.000000000000000000, 0.000000000000000000 ) ) ;
#35819=CARTESIAN_POINT ( 'NONE',  ( -22.27719381268171617, 2.588413841766863843, 2.618044180756106343 ) ) ;
#35822=CARTESIAN_POINT ( 'NONE',  ( -27.35552965826137140, 1.773915698030573473, -2.548625910254528559 ) ) ;
#35826=CARTESIAN_POINT ( 'NONE',  ( -27.10307689719148883, -0.5470785519251840645, 2.283215755733933428 ) ) ;
#35831=CIRCLE ( 'NONE', #59237, 6.936499999999990784 ) ;
#35834=ADVANCED_FACE ( 'NONE', ( #17290 ), #6334, .T. ) ;
#35835=ORIENTED_EDGE ( 'NONE', *, *, #57035, .T. ) ;
#35849=EDGE_CURVE ( 'NONE', #64706, #45642, #17846, .T. ) ;
#35852=CARTESIAN_POINT ( 'NONE',  ( -22.27715239060371744, 2.513478159995859773, 2.689999469426664014 ) ) ;
#35856=CARTESIAN_POINT ( 'NONE',  ( 2.000000000000001776, -6.539067737394505642, 2.314222412769772586 ) ) ;
#35857=ORIENTED_EDGE ( 'NONE', *, *, #4528, .T. ) ;
#35867=ORIENTED_EDGE ( 'NONE', *, *, #53503, .T. ) ;
#35871=ORIENTED_EDGE ( 'NONE', *, *, #46187, .F. ) ;
#35881=EDGE_CURVE ( 'NONE', #42619, #21169, #33042, .T. ) ;
#35884=EDGE_LOOP ( 'NONE', ( #60794, #62635, #33546, #15173 ) ) ;
#35887=ADVANCED_FACE ( 'NONE', ( #32881 ), #27365, .F. ) ;
#35895=CYLINDRICAL_SURFACE ( 'NONE', #3593, 6.936499999999988120 ) ;
#35910=AXIS2_PLACEMENT_3D ( 'NONE', #64664, #39410, #59708 ) ;
#35912=CARTESIAN_POINT ( 'NONE',  ( -35.04643116707788408, 0.001845126042312322800, 0.01204777744935429939 ) ) ;
#35932=CARTESIAN_POINT ( 'NONE',  ( -22.27720412283625961, 0.7407051501189994003, 3.606406551442356001 ) ) ;
#35935=DIRECTION ( 'NONE',  ( 1.000000000000000000, -0.000000000000000000, -0.000000000000000000 ) ) ;
#35937=CARTESIAN_POINT ( 'NONE',  ( -22.28023996335807411, 0.3233044107360884545, 3.676538434326150906 ) ) ;
#35944=VERTEX_POINT ( 'NONE', #2681 ) ;
#35945=DIRECTION ( 'NONE',  ( -0.9582930651793754029, -0.08045274594386239708, -0.2742293873734352738 ) ) ;
#35946=EDGE_CURVE ( 'NONE', #45709, #36827, #25641, .T. ) ;
#35948=DIRECTION ( 'NONE',  ( -1.000000000000000000, 0.000000000000000000, 0.000000000000000000 ) ) ;
#35951=DIRECTION ( 'NONE',  ( -1.000000000000000000, 0.000000000000000000, 0.000000000000000000 ) ) ;
#35956=LINE ( 'NONE', #56257, #38452 ) ;
#35962=CARTESIAN_POINT ( 'NONE',  ( 0.000000000000000000, 0.000000000000000000, 0.000000000000000000 ) ) ;
#35965=EDGE_CURVE ( 'NONE', #49980, #26098, #7982, .T. ) ;
#35966=ORIENTED_EDGE ( 'NONE', *, *, #13736, .T. ) ;
#35969=CARTESIAN_POINT ( 'NONE',  ( -27.09342121492585420, -2.227768580955212574, 0.6436068655225369861 ) ) ;
#35972=DIRECTION ( 'NONE',  ( 0.000000000000000000, 0.000000000000000000, 1.000000000000000000 ) ) ;
#35973=ORIENTED_EDGE ( 'NONE', *, *, #62828, .F. ) ;
#35981=VERTEX_POINT ( 'NONE', #8947 ) ;
#35989=VERTEX_POINT ( 'NONE', #23253 ) ;
#35993=ADVANCED_FACE ( 'NONE', ( #38548 ), #8293, .T. ) ;
#35997=CIRCLE ( 'NONE', #55151, 2.899999999999996358 ) ;
#36000=CARTESIAN_POINT ( 'NONE',  ( -22.27756824490284515, 3.558840239148769236, -0.9472004376381198965 ) ) ;
#36006=EDGE_CURVE ( 'NONE', #48006, #54727, #53278, .T. ) ;
#36011=CARTESIAN_POINT ( 'NONE',  ( -27.08421723179412410, -1.681635392574622800, 1.556274442127711044 ) ) ;
#36012=ORIENTED_EDGE ( 'NONE', *, *, #25289, .T. ) ;
#36015=AXIS2_PLACEMENT_3D ( 'NONE', #29241, #49221, #18634 ) ;
#36018=VERTEX_POINT ( 'NONE', #19896 ) ;
#36036=ORIENTED_EDGE ( 'NONE', *, *, #25299, .T. ) ;
#36039=CARTESIAN_POINT ( 'NONE',  ( 0.000000000000000000, 2.473437528934240515, -7.080403010454960011 ) ) ;
#36048=CARTESIAN_POINT ( 'NONE',  ( -22.28169757117798966, 0.9284931499057414994, -3.576542310004389602 ) ) ;
#36050=CARTESIAN_POINT ( 'NONE',  ( -22.27706485742869091, 1.508175983031630585, -3.358064672837109743 ) ) ;
#36057=DIRECTION ( 'NONE',  ( 0.000000000000000000, 0.000000000000000000, 1.000000000000000000 ) ) ;
#36058=DIRECTION ( 'NONE',  ( 0.000000000000000000, 0.000000000000000000, -1.000000000000000000 ) ) ;
#36060=AXIS2_PLACEMENT_3D ( 'NONE', #21906, #20596, #56148 ) ;
#36062=CARTESIAN_POINT ( 'NONE',  ( -22.30625920655495165, -3.635849356906410534, 1.076742202099151946 ) ) ;
#36063=AXIS2_PLACEMENT_3D ( 'NONE', #39871, #60152, #14577 ) ;
#36067=ORIENTED_EDGE ( 'NONE', *, *, #59476, .T. ) ;
#36083=ADVANCED_FACE ( 'NONE', ( #9248 ), #60134, .T. ) ;
#36086=EDGE_LOOP ( 'NONE', ( #49276, #52435, #40651, #23128 ) ) ;
#36089=AXIS2_PLACEMENT_3D ( 'NONE', #6897, #31806, #32140 ) ;
#36097=CARTESIAN_POINT ( 'NONE',  ( -35.05175862995318425, 0.008837625261041981428, -0.008949502803503109338 ) ) ;
#36102=DIRECTION ( 'NONE',  ( -1.000000000000000000, 0.000000000000000000, 0.000000000000000000 ) ) ;
#36111=CARTESIAN_POINT ( 'NONE',  ( -22.27722019094931127, -1.249795790945194440, 3.463038365117186324 ) ) ;
#36122=CARTESIAN_POINT ( 'NONE',  ( -22.66110217412718342, 0.6585288088160327069, -4.900671186447929983 ) ) ;
#36125=ORIENTED_EDGE ( 'NONE', *, *, #20088, .F. ) ;
#36135=EDGE_CURVE ( 'NONE', #1460, #13960, #17145, .T. ) ;
#36136=ORIENTED_EDGE ( 'NONE', *, *, #8788, .T. ) ;
#36146=FACE_OUTER_BOUND ( 'NONE', #321, .T. ) ;
#36149=DIRECTION ( 'NONE',  ( 1.000000000000000000, -0.000000000000000000, -0.000000000000000000 ) ) ;
#36152=CARTESIAN_POINT ( 'NONE',  ( 0.000000000000000000, -0.8935325819929111901, 7.446583077151331942 ) ) ;
#36159=AXIS2_PLACEMENT_3D ( 'NONE', #44620, #40963, #30640 ) ;
#36161=ORIENTED_EDGE ( 'NONE', *, *, #28519, .F. ) ;
#36163=DIRECTION ( 'NONE',  ( 0.000000000000000000, 0.000000000000000000, -1.000000000000000000 ) ) ;
#36166=CARTESIAN_POINT ( 'NONE',  ( 0.000000000000000000, 0.000000000000000000, 0.000000000000000000 ) ) ;
#36180=DIRECTION ( 'NONE',  ( -1.000000000000000000, 0.000000000000000000, 0.000000000000000000 ) ) ;
#36190=CARTESIAN_POINT ( 'NONE',  ( -27.08704841010891684, 1.888108843317904517, -1.313007237775874136 ) ) ;
#36191=VECTOR ( 'NONE', #60790, 1000.000000000000000 ) ;
#36198=AXIS2_PLACEMENT_3D ( 'NONE', #15770, #60691, #4850 ) ;
#36208=ORIENTED_EDGE ( 'NONE', *, *, #4528, .F. ) ;
#36210=DIRECTION ( 'NONE',  ( 0.000000000000000000, 0.000000000000000000, 1.000000000000000000 ) ) ;
#36218=CIRCLE ( 'NONE', #5442, 7.499999999999988454 ) ;
#36234=ORIENTED_EDGE ( 'NONE', *, *, #46259, .T. ) ;
#36235=EDGE_CURVE ( 'NONE', #13608, #42115, #10901, .T. ) ;
#36242=CARTESIAN_POINT ( 'NONE',  ( -28.67667724226168602, -1.049259427760474983, -1.574547667005680607 ) ) ;
#36245=DIRECTION ( 'NONE',  ( 1.000000000000000000, -0.000000000000000000, -0.000000000000000000 ) ) ;
#36256=CARTESIAN_POINT ( 'NONE',  ( -27.08416813689868263, 1.759517419957079554, -1.467601568343266827 ) ) ;
#36260=VECTOR ( 'NONE', #10404, 1000.000000000000000 ) ;
#36265=CARTESIAN_POINT ( 'NONE',  ( -22.59969328935898858, 4.339503524536204360, -1.672297795814005505 ) ) ;
#36268=AXIS2_PLACEMENT_3D ( 'NONE', #7412, #52672, #42999 ) ;
#36269=EDGE_CURVE ( 'NONE', #44459, #55375, #51895, .T. ) ;
#36272=AXIS2_PLACEMENT_3D ( 'NONE', #40738, #180, #6158 ) ;
#36273=VERTEX_POINT ( 'NONE', #48135 ) ;
#36276=CARTESIAN_POINT ( 'NONE',  ( -22.27722019117890540, 0.6494988092404053726, 3.623917154020592335 ) ) ;
#36282=CARTESIAN_POINT ( 'NONE',  ( -22.27704833740210333, 0.3581593033281407767, 3.663709865074111338 ) ) ;
#36287=AXIS2_PLACEMENT_3D ( 'NONE', #24174, #54112, #33512 ) ;
#36294=CARTESIAN_POINT ( 'NONE',  ( -26.90845769821730471, 3.274239888503029938, 0.2771906250059949506 ) ) ;
#36296=EDGE_CURVE ( 'NONE', #22708, #32746, #28809, .T. ) ;
#36310=ORIENTED_EDGE ( 'NONE', *, *, #59374, .T. ) ;
#36312=DIRECTION ( 'NONE',  ( 0.000000000000000000, 0.3193015301359806712, -0.9476531711828022342 ) ) ;
#36319=ADVANCED_FACE ( 'NONE', ( #18540 ), #3887, .T. ) ;
#36326=FACE_OUTER_BOUND ( 'NONE', #17074, .T. ) ;
#36330=CARTESIAN_POINT ( 'NONE',  ( -27.08429572838383947, -0.9410937941433956677, 2.089332284968712816 ) ) ;
#36332=CARTESIAN_POINT ( 'NONE',  ( -35.04834644901396956, -0.004537648929134079599, -0.01306875526352651966 ) ) ;
#36337=DIRECTION ( 'NONE',  ( -0.3162277663656185012, -0.1673616205762862574, -0.9338040949457712125 ) ) ;
#36339=DIRECTION ( 'NONE',  ( 1.000000000000000000, -0.000000000000000000, -0.000000000000000000 ) ) ;
#36346=EDGE_CURVE ( 'NONE', #65266, #42915, #5186, .T. ) ;
#36352=DIRECTION ( 'NONE',  ( 0.000000000000000000, 0.1081190184239417679, -0.9941379571543595972 ) ) ;
#36356=FACE_OUTER_BOUND ( 'NONE', #42632, .T. ) ;
#36360=ORIENTED_EDGE ( 'NONE', *, *, #44469, .T. ) ;
#36362=CARTESIAN_POINT ( 'NONE',  ( -27.08418179957658367, -1.713622993062712707, 1.521007404704310062 ) ) ;
#36367=DIRECTION ( 'NONE',  ( 0.000000000000000000, -0.8276889981568840149, -0.5611870653623919347 ) ) ;
#36368=ORIENTED_EDGE ( 'NONE', *, *, #36690, .T. ) ;
#36369=AXIS2_PLACEMENT_3D ( 'NONE', #52593, #16986, #31307 ) ;
#36381=ORIENTED_EDGE ( 'NONE', *, *, #296, .T. ) ;
#36385=ORIENTED_EDGE ( 'NONE', *, *, #55003, .T. ) ;
#36391=AXIS2_PLACEMENT_3D ( 'NONE', #45687, #26390, #35697 ) ;
#36393=VERTEX_POINT ( 'NONE', #39430 ) ;
#36395=ORIENTED_EDGE ( 'NONE', *, *, #36988, .T. ) ;
#36405=DIRECTION ( 'NONE',  ( 0.000000000000000000, -0.3193015301359872216, 0.9476531711827999027 ) ) ;
#36406=CARTESIAN_POINT ( 'NONE',  ( -22.27722019117890895, -0.6723250025933638074, -3.619826115298663272 ) ) ;
#36408=CARTESIAN_POINT ( 'NONE',  ( -22.27786964138239867, -3.004507515156368491, 2.131221155130652356 ) ) ;
#36412=EDGE_CURVE ( 'NONE', #55375, #46695, #1947, .T. ) ;
#36414=CARTESIAN_POINT ( 'NONE',  ( 2.000000000000001776, 5.860254403322016969, 3.474373880649828550 ) ) ;
#36415=CARTESIAN_POINT ( 'NONE',  ( -22.59983133926800392, 2.272383229042392649, 4.058100437359447810 ) ) ;
#36432=VERTEX_POINT ( 'NONE', #534 ) ;
#36434=DIRECTION ( 'NONE',  ( -1.000000000000000000, 0.000000000000000000, 0.000000000000000000 ) ) ;
#36444=CARTESIAN_POINT ( 'NONE',  ( -23.18047892478188743, -4.776019214182017691, -0.4043282704081637702 ) ) ;
#36445=VERTEX_POINT ( 'NONE', #1179 ) ;
#36446=CARTESIAN_POINT ( 'NONE',  ( -22.27706485742869091, 3.547445275915927176, 0.9832726768967369191 ) ) ;
#36455=ORIENTED_EDGE ( 'NONE', *, *, #2503, .T. ) ;
#36460=AXIS2_PLACEMENT_3D ( 'NONE', #29478, #14503, #14824 ) ;
#36462=CARTESIAN_POINT ( 'NONE',  ( 2.000000000000001776, 6.812627895098307462, -0.04423456934727655609 ) ) ;
#36463=VERTEX_POINT ( 'NONE', #52047 ) ;
#36464=DIRECTION ( 'NONE',  ( -1.000000000000000000, 0.000000000000000000, 0.000000000000000000 ) ) ;
#36465=EDGE_CURVE ( 'NONE', #38516, #15834, #57556, .T. ) ;
#36466=AXIS2_PLACEMENT_3D ( 'NONE', #50694, #60014, #25406 ) ;
#36470=VECTOR ( 'NONE', #22589, 1000.000000000000000 ) ;
#36471=EDGE_LOOP ( 'NONE', ( #24223, #53607, #48227, #18828 ) ) ;
#36476=CARTESIAN_POINT ( 'NONE',  ( 2.000000000000001776, -3.155844197800055539, -6.177028383390492650 ) ) ;
#36478=CARTESIAN_POINT ( 'NONE',  ( 2.000000000000001776, 5.997115278587678233, -3.485633455389450130 ) ) ;
#36484=ADVANCED_FACE ( 'NONE', ( #41388 ), #46034, .F. ) ;
#36498=AXIS2_PLACEMENT_3D ( 'NONE', #55408, #61060, #14179 ) ;
#36499=ORIENTED_EDGE ( 'NONE', *, *, #18640, .T. ) ;
#36500=CARTESIAN_POINT ( 'NONE',  ( -22.31213670151049300, -3.777944311993720383, 0.2530575063956070347 ) ) ;
#36501=CARTESIAN_POINT ( 'NONE',  ( 0.000000000000000000, 2.469490258309423591, 6.482025155313315246 ) ) ;
#36505=AXIS2_PLACEMENT_3D ( 'NONE', #60716, #51421, #26441 ) ;
#36518=EDGE_LOOP ( 'NONE', ( #48200, #51987, #31257, #28006 ) ) ;
#36519=CARTESIAN_POINT ( 'NONE',  ( -35.04709527796842394, -0.01012471662513968196, -0.007095259204994638913 ) ) ;
#36520=CARTESIAN_POINT ( 'NONE',  ( 2.000000000000001776, 5.097042323172538580, -5.501832381651401427 ) ) ;
#36529=ORIENTED_EDGE ( 'NONE', *, *, #45870, .F. ) ;
#36533=CARTESIAN_POINT ( 'NONE',  ( -27.28563798457901513, 2.528380693767735110, -1.413023339712106141 ) ) ;
#36535=CARTESIAN_POINT ( 'NONE',  ( -35.04643116707788408, -0.003844232202718234070, 0.01156612771643049375 ) ) ;
#36538=AXIS2_PLACEMENT_3D ( 'NONE', #52832, #35948, #46607 ) ;
#36545=CARTESIAN_POINT ( 'NONE',  ( -22.27715239060371744, 3.586346956688105436, -0.8317362037004153441 ) ) ;
#36553=VERTEX_POINT ( 'NONE', #33398 ) ;
#36556=ORIENTED_EDGE ( 'NONE', *, *, #38635, .F. ) ;
#36563=DIRECTION ( 'NONE',  ( -1.000000000000000000, 0.000000000000000000, 0.000000000000000000 ) ) ;
#36571=DIRECTION ( 'NONE',  ( -1.000000000000000000, 0.000000000000000000, 0.000000000000000000 ) ) ;
#36572=AXIS2_PLACEMENT_3D ( 'NONE', #55698, #40051, #65635 ) ;
#36573=CARTESIAN_POINT ( 'NONE',  ( -27.10512513516276556, 0.6711200423626966227, 2.256292013315166489 ) ) ;
#36580=CIRCLE ( 'NONE', #31302, 7.499999999999988454 ) ;
#36587=CARTESIAN_POINT ( 'NONE',  ( -27.08935880048753120, -0.6272370006475039839, -2.219773948423735099 ) ) ;
#36591=VECTOR ( 'NONE', #63729, 1000.000000000000000 ) ;
#36595=CARTESIAN_POINT ( 'NONE',  ( 2.000000000000001776, -6.643843315911796665, -1.507714007300762660 ) ) ;
#36605=VERTEX_POINT ( 'NONE', #33054 ) ;
#36609=DIRECTION ( 'NONE',  ( -1.000000000000000000, 0.000000000000000000, 0.000000000000000000 ) ) ;
#36610=VERTEX_POINT ( 'NONE', #17778 ) ;
#36614=AXIS2_PLACEMENT_3D ( 'NONE', #30671, #50981, #55297 ) ;
#36615=CARTESIAN_POINT ( 'NONE',  ( -22.31328051695926007, 1.076152733467212741, 3.633840107626929328 ) ) ;
#36621=CARTESIAN_POINT ( 'NONE',  ( -22.29677679919927868, 0.2674217835791047326, 3.730758197825078337 ) ) ;
#36632=CARTESIAN_POINT ( 'NONE',  ( 2.000000000000001776, -1.779948802829750543, -6.576141558201276993 ) ) ;
#36641=CARTESIAN_POINT ( 'NONE',  ( -28.67667724226168602, 1.049259427760474983, 1.574547667005656404 ) ) ;
#36648=DIRECTION ( 'NONE',  ( 0.000000000000000000, 0.000000000000000000, 1.000000000000000000 ) ) ;
#36651=CARTESIAN_POINT ( 'NONE',  ( -35.04582288351658548, 0.01249938581186572396, 0.002280196168871053385 ) ) ;
#36656=ADVANCED_FACE ( 'NONE', ( #19087 ), #54350, .T. ) ;
#36659=EDGE_CURVE ( 'NONE', #24086, #4327, #5535, .T. ) ;
#36666=DIRECTION ( 'NONE',  ( -1.000000000000000000, 0.000000000000000000, 0.000000000000000000 ) ) ;
#36671=CARTESIAN_POINT ( 'NONE',  ( -23.41523303002442091, -2.683951991546276172, 3.856096202952846941 ) ) ;
#36682=CARTESIAN_POINT ( 'NONE',  ( -22.66110217412718697, -2.622110956932569348, 4.192227617777433579 ) ) ;
#36685=DIRECTION ( 'NONE',  ( 0.000000000000000000, 0.000000000000000000, -1.000000000000000000 ) ) ;
#36689=CARTESIAN_POINT ( 'NONE',  ( -27.08426504710140392, -1.649100202714204988, 1.591094357919263569 ) ) ;
#36690=EDGE_CURVE ( 'NONE', #36827, #55926, #14086, .T. ) ;
#36693=CARTESIAN_POINT ( 'NONE',  ( -22.31328051695926007, -3.633840107626937765, 1.076152733467191869 ) ) ;
#36697=( BOUNDED_SURFACE ( )  B_SPLINE_SURFACE ( 3, 1, ( 
 ( #8802, #34050 ),
 ( #33413, #28742 ),
 ( #49692, #23432 ),
 ( #38391, #19099 ) ),
 .UNSPECIFIED., .F., .F., .F. ) 
 B_SPLINE_SURFACE_WITH_KNOTS ( ( 4, 4 ),
 ( 2, 2 ),
 ( 0.000000000000000000, 1.000000000000000000 ),
 ( 0.000000000000000000, 1.000000000000000000 ),
 .UNSPECIFIED. ) 
 GEOMETRIC_REPRESENTATION_ITEM ( )  RATIONAL_B_SPLINE_SURFACE ( (
 ( 1.000000000000000000, 1.000000000000000000),
 ( 0.9257577194822556033, 0.9980522942447415113),
 ( 0.9257577194822556033, 0.9980522942447415113),
 ( 1.000000000000000000, 1.000000000000000000) ) ) 
 REPRESENTATION_ITEM ( '' )  SURFACE ( )  );
#36698=DIRECTION ( 'NONE',  ( -1.000000000000000000, 0.000000000000000000, 0.000000000000000000 ) ) ;
#36701=DIRECTION ( 'NONE',  ( -1.000000000000000000, 0.000000000000000000, 0.000000000000000000 ) ) ;
#36704=ADVANCED_FACE ( 'NONE', ( #24390 ), #41343, .F. ) ;
#36712=B_SPLINE_CURVE_WITH_KNOTS ( 'NONE', 3,
 ( #61807, #5987, #55849, #51202, #36545, #10946, #7498, #31233, #56853, #10599, #43075, #17499, #2550, #63353, #16263, #10276, #42739, #20605, #17817, #972, #56158, #61467 ),
 .UNSPECIFIED., .F., .F.,
 ( 4, 3, 3, 3, 3, 3, 3, 4 ),
 ( 0.000000000000000000, 6.990956068646414663E-05, 0.0001398191187764043317, 0.0002097286751720214631, 0.0002796382307041358844, 0.0003495477861619810203, 0.0004194573423310285747, 0.0005586102576333144961 ),
 .UNSPECIFIED. ) ;
#36713=ORIENTED_EDGE ( 'NONE', *, *, #13778, .F. ) ;
#36716=DIRECTION ( 'NONE',  ( 0.000000000000000000, 0.000000000000000000, 1.000000000000000000 ) ) ;
#36718=ORIENTED_EDGE ( 'NONE', *, *, #927, .T. ) ;
#36727=CARTESIAN_POINT ( 'NONE',  ( -22.28856623400852399, 1.018212315222208675, 3.573466130470470237 ) ) ;
#36735=AXIS2_PLACEMENT_3D ( 'NONE', #21549, #16560, #25884 ) ;
#36740=AXIS2_PLACEMENT_3D ( 'NONE', #57331, #63285, #11754 ) ;
#36749=DIRECTION ( 'NONE',  ( 0.000000000000000000, -0.6051742151937716807, 0.7960930657056387583 ) ) ;
#36762=CARTESIAN_POINT ( 'NONE',  ( 0.000000000000000000, 3.795144977083636739, 6.468916029978800886 ) ) ;
#36786=DIRECTION ( 'NONE',  ( 0.000000000000000000, -0.2149704402110317047, 0.9766205557100849921 ) ) ;
#36792=FACE_OUTER_BOUND ( 'NONE', #38092, .T. ) ;
#36797=ORIENTED_EDGE ( 'NONE', *, *, #11782, .T. ) ;
#36822=ORIENTED_EDGE ( 'NONE', *, *, #27108, .F. ) ;
#36823=CARTESIAN_POINT ( 'NONE',  ( 1.000000000000000888, -6.664893814313694875, -3.439359016433563898 ) ) ;
#36827=VERTEX_POINT ( 'NONE', #1766 ) ;
#36828=CARTESIAN_POINT ( 'NONE',  ( -35.04582288351658548, -0.008224400713808234509, 0.009684687560342908341 ) ) ;
#36835=DIRECTION ( 'NONE',  ( 0.000000000000000000, 0.000000000000000000, -1.000000000000000000 ) ) ;
#36836=ORIENTED_EDGE ( 'NONE', *, *, #9844, .F. ) ;
#36839=CARTESIAN_POINT ( 'NONE',  ( 0.000000000000000000, -0.4129979343797593461, 6.800241778083677247 ) ) ;
#36842=CARTESIAN_POINT ( 'NONE',  ( -35.04709527796842394, 0.01012471662513447779, 0.007095259204982495849 ) ) ;
#36857=EDGE_CURVE ( 'NONE', #18279, #15981, #61740, .T. ) ;
#36861=AXIS2_PLACEMENT_3D ( 'NONE', #11292, #31561, #11932 ) ;
#36863=EDGE_CURVE ( 'NONE', #26729, #2095, #52179, .T. ) ;
#36867=CARTESIAN_POINT ( 'NONE',  ( -27.08588607604449550, 1.631236259433597402, 1.616144682268070065 ) ) ;
#36869=DIRECTION ( 'NONE',  ( 1.000000000000000000, -0.000000000000000000, -0.000000000000000000 ) ) ;
#36873=B_SPLINE_CURVE_WITH_KNOTS ( 'NONE', 3,
 ( #8529, #22869, #28483, #33792, #58786, #28821, #13205, #33490, #27842, #8869 ),
 .UNSPECIFIED., .F., .F.,
 ( 4, 3, 3, 4 ),
 ( 0.0001763147164361797566, 0.0002097400188389093628, 0.0002811534801551362692, 0.0003526297678872502878 ),
 .UNSPECIFIED. ) ;
#36878=VERTEX_POINT ( 'NONE', #46984 ) ;
#36883=CARTESIAN_POINT ( 'NONE',  ( 0.000000000000000000, -2.469490258309472441, 6.482025155313308140 ) ) ;
#36892=CARTESIAN_POINT ( 'NONE',  ( -22.27722015946439171, 2.828901469906485389, -2.356370737780153046 ) ) ;
#36899=( BOUNDED_SURFACE ( )  B_SPLINE_SURFACE ( 3, 1, ( 
 ( #29570, #25247 ),
 ( #45212, #8658 ),
 ( #49247, #24266 ),
 ( #28938, #24937 ) ),
 .UNSPECIFIED., .F., .F., .T. ) 
 B_SPLINE_SURFACE_WITH_KNOTS ( ( 4, 4 ),
 ( 2, 2 ),
 ( 0.000000000000000000, 1.000000000000000000 ),
 ( 0.000000000000000000, 1.000000000000000000 ),
 .UNSPECIFIED. ) 
 GEOMETRIC_REPRESENTATION_ITEM ( )  RATIONAL_B_SPLINE_SURFACE ( (
 ( 1.000000000000000000, 1.000000000000000000),
 ( 0.8716676215708681896, 0.8964445200148167814),
 ( 0.8716676215708681896, 0.8964445200148167814),
 ( 1.000000000000000000, 1.000000000000000000) ) ) 
 REPRESENTATION_ITEM ( '' )  SURFACE ( )  );
#36900=ORIENTED_EDGE ( 'NONE', *, *, #50969, .F. ) ;
#36905=DIRECTION ( 'NONE',  ( 0.9582930651793755139, -0.1596922922278012080, -0.2370079598497647211 ) ) ;
#36906=ORIENTED_EDGE ( 'NONE', *, *, #50186, .T. ) ;
#36914=DIRECTION ( 'NONE',  ( 0.9606638835031803270, -0.1629100154396138922, -0.2249116044183865903 ) ) ;
#36921=CARTESIAN_POINT ( 'NONE',  ( -22.71097035706202405, 4.510116093748279376, -2.118550233809386896 ) ) ;
#36927=ORIENTED_EDGE ( 'NONE', *, *, #59908, .F. ) ;
#36928=EDGE_LOOP ( 'NONE', ( #15623, #6929, #50, #23209 ) ) ;
#36929=CYLINDRICAL_SURFACE ( 'NONE', #1556, 2.899999999999994582 ) ;
#36932=ORIENTED_EDGE ( 'NONE', *, *, #58654, .T. ) ;
#36933=CARTESIAN_POINT ( 'NONE',  ( 2.000000000000001776, 2.315790869867068835, 7.133520354428100951 ) ) ;
#36946=CARTESIAN_POINT ( 'NONE',  ( 0.000000000000000000, -6.812627895098285258, 0.04423456934719675882 ) ) ;
#36957=EDGE_CURVE ( 'NONE', #20446, #52831, #51133, .T. ) ;
#36962=CARTESIAN_POINT ( 'NONE',  ( 2.000000000000001776, 6.606214214351110670, -2.114938770769863030 ) ) ;
#36974=VECTOR ( 'NONE', #64124, 1000.000000000000000 ) ;
#36986=CARTESIAN_POINT ( 'NONE',  ( -27.35552965826137140, -1.773915698030568366, 2.548625910254532112 ) ) ;
#36988=EDGE_CURVE ( 'NONE', #25430, #12876, #40472, .T. ) ;
#36990=DIRECTION ( 'NONE',  ( -1.000000000000000000, 0.000000000000000000, 0.000000000000000000 ) ) ;
#36992=ORIENTED_EDGE ( 'NONE', *, *, #55787, .F. ) ;
#36995=DIRECTION ( 'NONE',  ( 0.000000000000000000, 0.000000000000000000, 1.000000000000000000 ) ) ;
#36999=DIRECTION ( 'NONE',  ( 0.000000000000000000, 0.000000000000000000, -1.000000000000000000 ) ) ;
#37014=DIRECTION ( 'NONE',  ( -1.000000000000000000, 0.000000000000000000, 0.000000000000000000 ) ) ;
#37016=EDGE_LOOP ( 'NONE', ( #48089, #56129, #26794, #5713 ) ) ;
#37020=ORIENTED_EDGE ( 'NONE', *, *, #51864, .F. ) ;
#37025=ORIENTED_EDGE ( 'NONE', *, *, #25777, .F. ) ;
#37031=AXIS2_PLACEMENT_3D ( 'NONE', #21681, #41936, #27296 ) ;
#37032=ORIENTED_EDGE ( 'NONE', *, *, #64670, .F. ) ;
#37034=ORIENTED_EDGE ( 'NONE', *, *, #26947, .F. ) ;
#37035=VECTOR ( 'NONE', #12270, 1000.000000000000000 ) ;
#37039=DIRECTION ( 'NONE',  ( -1.000000000000000000, 0.000000000000000000, 0.000000000000000000 ) ) ;
#37046=EDGE_LOOP ( 'NONE', ( #29127, #52186, #8307, #17514 ) ) ;
#37047=CARTESIAN_POINT ( 'NONE',  ( 2.000000000000001776, 4.570217215903371155, 5.218059682435623792 ) ) ;
#37058=ORIENTED_EDGE ( 'NONE', *, *, #49560, .T. ) ;
#37069=( BOUNDED_SURFACE ( )  B_SPLINE_SURFACE ( 3, 1, ( 
 ( #62663, #1538 ),
 ( #47411, #32412 ),
 ( #58036, #38054 ),
 ( #6508, #12452 ) ),
 .UNSPECIFIED., .F., .F., .F. ) 
 B_SPLINE_SURFACE_WITH_KNOTS ( ( 4, 4 ),
 ( 2, 2 ),
 ( 0.000000000000000000, 1.000000000000000000 ),
 ( 0.000000000000000000, 1.000000000000000000 ),
 .UNSPECIFIED. ) 
 GEOMETRIC_REPRESENTATION_ITEM ( )  RATIONAL_B_SPLINE_SURFACE ( (
 ( 1.000000000000000000, 1.000000000000000000),
 ( 0.9932032654565553509, 0.8386279382598736953),
 ( 0.9932032654565553509, 0.8386279382598736953),
 ( 1.000000000000000000, 1.000000000000000000) ) ) 
 REPRESENTATION_ITEM ( '' )  SURFACE ( )  );
#37072=CARTESIAN_POINT ( 'NONE',  ( 0.000000000000000000, -3.224464355699868889, 6.771471746881965181 ) ) ;
#37082=DIRECTION ( 'NONE',  ( 0.000000000000000000, 0.000000000000000000, 1.000000000000000000 ) ) ;
#37107=CARTESIAN_POINT ( 'NONE',  ( -22.31328051695926007, -3.633840107626937765, 1.076152733467191869 ) ) ;
#37111=ORIENTED_EDGE ( 'NONE', *, *, #49601, .T. ) ;
#37115=CARTESIAN_POINT ( 'NONE',  ( -27.09048036756548328, 0.9969423855787405975, -2.083857239072913092 ) ) ;
#37116=AXIS2_PLACEMENT_3D ( 'NONE', #42902, #23281, #13306 ) ;
#37126=CARTESIAN_POINT ( 'NONE',  ( -22.27218376572352554, -2.577901515391805898, 2.630375585211909506 ) ) ;
#37130=EDGE_CURVE ( 'NONE', #18591, #54727, #41569, .T. ) ;
#37136=CARTESIAN_POINT ( 'NONE',  ( -27.08429572838383947, 0.2296550094123047669, 2.279961732801582208 ) ) ;
#37138=FACE_OUTER_BOUND ( 'NONE', #135, .T. ) ;
#37148=AXIS2_PLACEMENT_3D ( 'NONE', #56900, #31591, #51903 ) ;
#37149=CARTESIAN_POINT ( 'NONE',  ( 2.000000000000001776, -7.248432822490231686, -1.926193556693109654 ) ) ;
#37153=VERTEX_POINT ( 'NONE', #37149 ) ;
#37166=VECTOR ( 'NONE', #49144, 1000.000000000000000 ) ;
#37167=CARTESIAN_POINT ( 'NONE',  ( -27.08429572838383947, -2.279961732801590646, 0.2296550094122822017 ) ) ;
#37170=CYLINDRICAL_SURFACE ( 'NONE', #38577, 6.936499999999988120 ) ;
#37181=CARTESIAN_POINT ( 'NONE',  ( -27.10113028276155234, 1.697941299269287940, 1.613062633976892091 ) ) ;
#37190=VERTEX_POINT ( 'NONE', #22189 ) ;
#37194=CARTESIAN_POINT ( 'NONE',  ( -22.27715239060371744, -2.689999469426690215, 2.513478159995840677 ) ) ;
#37207=CARTESIAN_POINT ( 'NONE',  ( -22.27713295444592845, 2.673940016109018103, -2.530364014314298249 ) ) ;
#37210=FACE_OUTER_BOUND ( 'NONE', #50259, .T. ) ;
#37211=CYLINDRICAL_SURFACE ( 'NONE', #18565, 2.899999999999994582 ) ;
#37214=ORIENTED_EDGE ( 'NONE', *, *, #61683, .T. ) ;
#37217=VERTEX_POINT ( 'NONE', #63722 ) ;
#37220=CARTESIAN_POINT ( 'NONE',  ( -27.09569413923794201, -0.6513788562879314625, -2.232620870184092610 ) ) ;
#37222=EDGE_CURVE ( 'NONE', #26369, #64706, #36873, .T. ) ;
#37226=CIRCLE ( 'NONE', #53196, 7.499999999999988454 ) ;
#37238=EDGE_CURVE ( 'NONE', #57905, #23272, #8634, .T. ) ;
#37244=EDGE_CURVE ( 'NONE', #41165, #53863, #38385, .T. ) ;
#37247=AXIS2_PLACEMENT_3D ( 'NONE', #43755, #64357, #8500 ) ;
#37253=VERTEX_POINT ( 'NONE', #23854 ) ;
#37259=EDGE_LOOP ( 'NONE', ( #34896, #14282, #4815, #25411 ) ) ;
#37264=ORIENTED_EDGE ( 'NONE', *, *, #56908, .T. ) ;
#37273=CARTESIAN_POINT ( 'NONE',  ( 2.000000000000001776, 2.469490258309515518, -6.482025155313297482 ) ) ;
#37283=DIRECTION ( 'NONE',  ( -1.000000000000000000, 0.000000000000000000, 0.000000000000000000 ) ) ;
#37286=VERTEX_POINT ( 'NONE', #5536 ) ;
#37289=CARTESIAN_POINT ( 'NONE',  ( 0.000000000000000000, -7.493043167941613625, 0.3229614270519164942 ) ) ;
#37300=CARTESIAN_POINT ( 'NONE',  ( 0.000000000000000000, 0.08317740279942427428, -7.499538753794372070 ) ) ;
#37303=DIRECTION ( 'NONE',  ( -1.000000000000000000, 0.000000000000000000, 0.000000000000000000 ) ) ;
#37307=EDGE_CURVE ( 'NONE', #28763, #56470, #44754, .T. ) ;
#37310=VECTOR ( 'NONE', #41041, 1000.000000000000000 ) ;
#37319=DIRECTION ( 'NONE',  ( -1.000000000000000000, 0.000000000000000000, 0.000000000000000000 ) ) ;
#37320=CIRCLE ( 'NONE', #14999, 7.499999999999988454 ) ;
#37328=CARTESIAN_POINT ( 'NONE',  ( 1.000000000000000888, 1.693411908627302509, -7.306323022404582979 ) ) ;
#37337=AXIS2_PLACEMENT_3D ( 'NONE', #10499, #21134, #26457 ) ;
#37340=ORIENTED_EDGE ( 'NONE', *, *, #51046, .T. ) ;
#37353=ORIENTED_EDGE ( 'NONE', *, *, #22162, .F. ) ;
#37369=ADVANCED_FACE ( 'NONE', ( #21468 ), #62655, .T. ) ;
#37377=EDGE_CURVE ( 'NONE', #54727, #26353, #6182, .T. ) ;
#37386=CARTESIAN_POINT ( 'NONE',  ( -35.04643116707788408, -0.007621814750504232738, -0.009511118309140503824 ) ) ;
#37392=DIRECTION ( 'NONE',  ( 0.000000000000000000, 0.000000000000000000, 1.000000000000000000 ) ) ;
#37394=CARTESIAN_POINT ( 'NONE',  ( -27.08417142187571613, 0.4261087887162147148, 2.251180450989566317 ) ) ;
#37396=CARTESIAN_POINT ( 'NONE',  ( -22.94572469358971034, -2.078200699019439934, -4.424217216616522563 ) ) ;
#37399=CIRCLE ( 'NONE', #4489, 6.936499999999989896 ) ;
#37402=CIRCLE ( 'NONE', #8762, 2.899999999999995026 ) ;
#37410=CARTESIAN_POINT ( 'NONE',  ( 0.000000000000000000, 0.000000000000000000, 0.000000000000000000 ) ) ;
#37414=CARTESIAN_POINT ( 'NONE',  ( 2.000000000000001776, 0.000000000000000000, 0.000000000000000000 ) ) ;
#37425=FACE_OUTER_BOUND ( 'NONE', #10962, .T. ) ;
#37430=FACE_OUTER_BOUND ( 'NONE', #46110, .T. ) ;
#37433=B_SPLINE_CURVE_WITH_KNOTS ( 'NONE', 3,
 ( #42403, #22146, #38427, #12170, #22482, #28444, #23466, #12482, #27795, #48098, #38087, #48747, #64023, #13471, #42745, #17163 ),
 .UNSPECIFIED., .F., .F.,
 ( 4, 3, 3, 3, 3, 4 ),
 ( 7.973125766754336844E-18, 6.991367980366376635E-05, 0.0001398269368981360438, 0.0002097400188389090918, 0.0002811534801551364318, 0.0003526297678872492036 ),
 .UNSPECIFIED. ) ;
#37438=EDGE_CURVE ( 'NONE', #1482, #60562, #39426, .T. ) ;
#37452=CARTESIAN_POINT ( 'NONE',  ( -22.71097035706202405, 4.510116093748279376, -2.118550233809386896 ) ) ;
#37454=LINE ( 'NONE', #12182, #23097 ) ;
#37457=CARTESIAN_POINT ( 'NONE',  ( 0.000000000000000000, -1.779948802829750543, -6.576141558201276993 ) ) ;
#37458=EDGE_CURVE ( 'NONE', #4186, #1369, #13122, .T. ) ;
#37461=DIRECTION ( 'NONE',  ( 0.000000000000000000, 0.000000000000000000, 1.000000000000000000 ) ) ;
#37464=CIRCLE ( 'NONE', #32181, 6.936499999999989896 ) ;
#37466=CARTESIAN_POINT ( 'NONE',  ( -35.04660725145885891, 0.01223081933021788817, -0.001288602543501626970 ) ) ;
#37468=LINE ( 'NONE', #52119, #42518 ) ;
#37470=VERTEX_POINT ( 'NONE', #58031 ) ;
#37471=CARTESIAN_POINT ( 'NONE',  ( 0.000000000000000000, -6.812627895098285258, -0.04423456934733380197 ) ) ;
#37472=ADVANCED_FACE ( 'NONE', ( #12446 ), #28101, .T. ) ;
#37480=ORIENTED_EDGE ( 'NONE', *, *, #16399, .F. ) ;
#37487=AXIS2_PLACEMENT_3D ( 'NONE', #3086, #23347, #63904 ) ;
#37496=DIRECTION ( 'NONE',  ( 0.000000000000000000, 0.000000000000000000, 1.000000000000000000 ) ) ;
#37501=CIRCLE ( 'NONE', #12009, 2.899999999999994582 ) ;
#37508=LINE ( 'NONE', #42816, #61684 ) ;
#37520=ORIENTED_EDGE ( 'NONE', *, *, #46770, .T. ) ;
#37523=AXIS2_PLACEMENT_3D ( 'NONE', #37926, #37608, #17331 ) ;
#37525=DIRECTION ( 'NONE',  ( -1.000000000000000000, 0.000000000000000000, 0.000000000000000000 ) ) ;
#37533=EDGE_CURVE ( 'NONE', #37217, #8268, #35249, .T. ) ;
#37534=ORIENTED_EDGE ( 'NONE', *, *, #41512, .F. ) ;
#37541=CARTESIAN_POINT ( 'NONE',  ( -22.27716857039623477, -2.705892286796401702, 2.496432241075906333 ) ) ;
#37552=CIRCLE ( 'NONE', #8874, 2.899999999999995026 ) ;
#37554=DIRECTION ( 'NONE',  ( 0.000000000000000000, 0.000000000000000000, 1.000000000000000000 ) ) ;
#37555=EDGE_CURVE ( 'NONE', #33347, #37684, #56679, .T. ) ;
#37559=CARTESIAN_POINT ( 'NONE',  ( 2.000000000000001776, 5.450255447309811707, -4.087611905901392007 ) ) ;
#37560=B_SPLINE_CURVE_WITH_KNOTS ( 'NONE', 3,
 ( #14686, #50314, #44079, #63043, #23139, #30003, #43403, #22825, #39979, #33448, #18511, #59064, #63680 ),
 .UNSPECIFIED., .F., .F.,
 ( 4, 3, 3, 3, 4 ),
 ( 0.0002792983885906414167, 0.0002796382307041358844, 0.0003495477861619811287, 0.0004194573423310287916, 0.0005586102576333146046 ),
 .UNSPECIFIED. ) ;
#37562=AXIS2_PLACEMENT_3D ( 'NONE', #47738, #17805, #32737 ) ;
#37569=CARTESIAN_POINT ( 'NONE',  ( 2.000000000000001776, 1.956810415765277922, -6.654767106875532967 ) ) ;
#37573=CARTESIAN_POINT ( 'NONE',  ( -27.09125059358653331, -0.6356863790372184742, -2.223272438024536779 ) ) ;
#37577=CARTESIAN_POINT ( 'NONE',  ( 0.000000000000000000, -6.750946897830710114, 1.593658756657014397 ) ) ;
#37586=CIRCLE ( 'NONE', #54606, 7.499999999999988454 ) ;
#37589=VERTEX_POINT ( 'NONE', #19433 ) ;
#37602=CIRCLE ( 'NONE', #38645, 2.899999999999993694 ) ;
#37608=DIRECTION ( 'NONE',  ( -1.000000000000000000, 0.000000000000000000, 0.000000000000000000 ) ) ;
#37612=ORIENTED_EDGE ( 'NONE', *, *, #54116, .F. ) ;
#37613=ORIENTED_EDGE ( 'NONE', *, *, #23425, .T. ) ;
#37616=VERTEX_POINT ( 'NONE', #19762 ) ;
#37618=DIRECTION ( 'NONE',  ( -0.9582930651793755139, 0.2067888154783164567, 0.1972632429577085844 ) ) ;
#37632=CARTESIAN_POINT ( 'NONE',  ( 1.000000000000000888, -7.414200355365264450, 1.131208685655129775 ) ) ;
#37633=AXIS2_PLACEMENT_3D ( 'NONE', #26075, #16077, #65312 ) ;
#37634=ORIENTED_EDGE ( 'NONE', *, *, #40315, .T. ) ;
#37640=ORIENTED_EDGE ( 'NONE', *, *, #42221, .F. ) ;
#37646=EDGE_CURVE ( 'NONE', #17686, #8949, #26766, .T. ) ;
#37653=CARTESIAN_POINT ( 'NONE',  ( -35.04709527796842394, 0.01232256164996302361, 0.001003525937966209813 ) ) ;
#37656=CARTESIAN_POINT ( 'NONE',  ( -27.08416813689868263, -0.7899859999124457799, 2.150738950797705940 ) ) ;
#37659=CARTESIAN_POINT ( 'NONE',  ( -22.29978294495153435, -2.710748743830170060, -2.590262069787990562 ) ) ;
#37667=CARTESIAN_POINT ( 'NONE',  ( -22.28236030719477512, 3.683993210674375351, -0.3108070568283785584 ) ) ;
#37670=B_SPLINE_CURVE_WITH_KNOTS ( 'NONE', 3,
 ( #48768, #13186, #4187, #54419, #28157, #64677 ),
 .UNSPECIFIED., .F., .F.,
 ( 4, 2, 4 ),
 ( 0.0001654224980408386077, 0.0006219428995476521897, 0.001078463301054465853 ),
 .UNSPECIFIED. ) ;
#37682=FACE_OUTER_BOUND ( 'NONE', #5838, .T. ) ;
#37684=VERTEX_POINT ( 'NONE', #65295 ) ;
#37688=CARTESIAN_POINT ( 'NONE',  ( 2.000000000000001776, -6.539067737394505642, 2.314222412769772586 ) ) ;
#37704=CARTESIAN_POINT ( 'NONE',  ( -22.27384469013076185, -2.581192766446256837, -2.625926801827886070 ) ) ;
#37706=EDGE_LOOP ( 'NONE', ( #8391, #38457, #57306, #36932 ) ) ;
#37733=CARTESIAN_POINT ( 'NONE',  ( -35.04582288351658548, 0.004274985098064986062, 0.01196488372920834035 ) ) ;
#37735=CIRCLE ( 'NONE', #21853, 6.936499999999993449 ) ;
#37741=DIRECTION ( 'NONE',  ( -1.000000000000000000, 0.000000000000000000, 0.000000000000000000 ) ) ;
#37743=CARTESIAN_POINT ( 'NONE',  ( -35.05175862995318425, 0.008949502803489231550, 0.008837625261040246705 ) ) ;
#37744=VERTEX_POINT ( 'NONE', #40337 ) ;
#37745=EDGE_CURVE ( 'NONE', #16416, #65638, #39475, .T. ) ;
#37746=DIRECTION ( 'NONE',  ( 1.000000000000000000, -0.000000000000000000, -0.000000000000000000 ) ) ;
#37748=ORIENTED_EDGE ( 'NONE', *, *, #4837, .T. ) ;
#37749=VERTEX_POINT ( 'NONE', #21041 ) ;
#37750=CYLINDRICAL_SURFACE ( 'NONE', #15071, 6.936499999999988120 ) ;
#37754=ORIENTED_EDGE ( 'NONE', *, *, #45956, .T. ) ;
#37756=CARTESIAN_POINT ( 'NONE',  ( 0.000000000000000000, 3.786546189469266466, -5.663561025469129540 ) ) ;
#37758=CYLINDRICAL_SURFACE ( 'NONE', #43598, 7.499999999999988454 ) ;
#37761=DIRECTION ( 'NONE',  ( -0.9582930651793755139, -0.2777159889015697880, -0.06744057189511687422 ) ) ;
#37764=EDGE_CURVE ( 'NONE', #13349, #48023, #31031, .T. ) ;
#37765=ORIENTED_EDGE ( 'NONE', *, *, #7322, .F. ) ;
#37768=ORIENTED_EDGE ( 'NONE', *, *, #708, .F. ) ;
#37769=PRODUCT_CONTEXT ( 'NONE', #13670, 'mechanical' ) ;
#37777=CARTESIAN_POINT ( 'NONE',  ( -22.27719412087655471, -0.5341638063191807007, -3.642699606241637245 ) ) ;
#37786=DIRECTION ( 'NONE',  ( 1.000000000000000000, 0.000000000000000000, 0.000000000000000000 ) ) ;
#37789=LINE ( 'NONE', #27470, #63852 ) ;
#37790=CARTESIAN_POINT ( 'NONE',  ( -27.09048036756592026, -1.905306051559101155, 1.306202114107285039 ) ) ;
#37803=CARTESIAN_POINT ( 'NONE',  ( -27.09483304420799143, 0.1669215111592837197, 2.317106154747420987 ) ) ;
#37804=ORIENTED_EDGE ( 'NONE', *, *, #33814, .F. ) ;
#37805=DIRECTION ( 'NONE',  ( -1.000000000000000000, 0.000000000000000000, 0.000000000000000000 ) ) ;
#37815=AXIS2_PLACEMENT_3D ( 'NONE', #34263, #38605, #43247 ) ;
#37822=CARTESIAN_POINT ( 'NONE',  ( -27.08423805673873019, 1.665498649074246496, -1.573803011992711109 ) ) ;
#37825=ORIENTED_EDGE ( 'NONE', *, *, #54188, .T. ) ;
#37827=CARTESIAN_POINT ( 'NONE',  ( 1.000000000000000888, -0.7281529553922420073, 7.464569195442772198 ) ) ;
#37833=ADVANCED_FACE ( 'NONE', ( #41983 ), #62264, .T. ) ;
#37840=FACE_OUTER_BOUND ( 'NONE', #23031, .T. ) ;
#37849=CARTESIAN_POINT ( 'NONE',  ( -22.30861784526115699, 2.600591904828422507, -2.737516124790391636 ) ) ;
#37851=EDGE_CURVE ( 'NONE', #61730, #57422, #64957, .T. ) ;
#37854=FACE_OUTER_BOUND ( 'NONE', #35884, .T. ) ;
#37856=CARTESIAN_POINT ( 'NONE',  ( -35.04660725145885891, 0.008800808525126678494, -0.008590646501141869715 ) ) ;
#37860=ORIENTED_EDGE ( 'NONE', *, *, #39939, .F. ) ;
#37863=ORIENTED_EDGE ( 'NONE', *, *, #59559, .T. ) ;
#37866=CARTESIAN_POINT ( 'NONE',  ( -22.27719443589224113, -2.737335337013107051, 2.462030382548431984 ) ) ;
#37874=( BOUNDED_SURFACE ( )  B_SPLINE_SURFACE ( 3, 1, ( 
 ( #36535, #50836 ),
 ( #26218, #30533 ),
 ( #16574, #11566 ),
 ( #25554, #45846 ) ),
 .UNSPECIFIED., .F., .F., .F. ) 
 B_SPLINE_SURFACE_WITH_KNOTS ( ( 4, 4 ),
 ( 2, 2 ),
 ( 0.000000000000000000, 1.000000000000000000 ),
 ( 0.000000000000000000, 1.000000000000000000 ),
 .UNSPECIFIED. ) 
 GEOMETRIC_REPRESENTATION_ITEM ( )  RATIONAL_B_SPLINE_SURFACE ( (
 ( 1.000000000000000000, 1.000000000000000000),
 ( 0.9932032654565553509, 0.8386279382598740284),
 ( 0.9932032654565553509, 0.8386279382598740284),
 ( 1.000000000000000000, 1.000000000000000000) ) ) 
 REPRESENTATION_ITEM ( '' )  SURFACE ( )  );
#37875=FACE_OUTER_BOUND ( 'NONE', #36928, .T. ) ;
#37876=CARTESIAN_POINT ( 'NONE',  ( 2.000000000000001776, -6.883677378339461583, 0.8544109087185534079 ) ) ;
#37888=DIRECTION ( 'NONE',  ( -1.000000000000000000, 0.000000000000000000, 0.000000000000000000 ) ) ;
#37893=DIRECTION ( 'NONE',  ( 1.000000000000000000, -0.000000000000000000, -0.000000000000000000 ) ) ;
#37898=ORIENTED_EDGE ( 'NONE', *, *, #39980, .F. ) ;
#37905=ORIENTED_EDGE ( 'NONE', *, *, #21227, .T. ) ;
#37912=EDGE_CURVE ( 'NONE', #31042, #33111, #40754, .T. ) ;
#37913=CARTESIAN_POINT ( 'NONE',  ( -22.27218376572352554, -2.099017427146257386, -3.026314224080938864 ) ) ;
#37921=ORIENTED_EDGE ( 'NONE', *, *, #43712, .F. ) ;
#37923=EDGE_CURVE ( 'NONE', #63668, #43107, #4250, .T. ) ;
#37926=CARTESIAN_POINT ( 'NONE',  ( 2.000000000000001776, 6.662861565602072211, 1.421313227905651289 ) ) ;
#37939=CARTESIAN_POINT ( 'NONE',  ( -22.28856623400852399, 3.603818606161810045, 0.9049353338066237207 ) ) ;
#37943=ORIENTED_EDGE ( 'NONE', *, *, #57878, .F. ) ;
#37944=CARTESIAN_POINT ( 'NONE',  ( -22.51237073810381162, -3.933875531624977828, -2.023441661740719155 ) ) ;
#37960=CARTESIAN_POINT ( 'NONE',  ( -27.08419642509983305, 2.181485315953908266, 0.7009209357102503812 ) ) ;
#37968=CARTESIAN_POINT ( 'NONE',  ( -27.08419642509983305, -0.7009209357102701432, 2.181485315953912707 ) ) ;
#37979=CARTESIAN_POINT ( 'NONE',  ( -22.27786964138239867, 3.667590411552012597, -0.3434379038477686774 ) ) ;
#37986=AXIS2_PLACEMENT_3D ( 'NONE', #23150, #49434, #39413 ) ;
#37988=DIRECTION ( 'NONE',  ( 0.000000000000000000, 0.000000000000000000, 1.000000000000000000 ) ) ;
#38003=CYLINDRICAL_SURFACE ( 'NONE', #36268, 7.499999999999988454 ) ;
#38012=CARTESIAN_POINT ( 'NONE',  ( -35.04582288351658548, 0.009684687560339159604, 0.008224400713780126784 ) ) ;
#38015=ORIENTED_EDGE ( 'NONE', *, *, #7520, .F. ) ;
#38018=ORIENTED_EDGE ( 'NONE', *, *, #3501, .F. ) ;
#38019=CARTESIAN_POINT ( 'NONE',  ( -22.29290468048228036, 3.357740900108103776, 1.621390503294450225 ) ) ;
#38029=CARTESIAN_POINT ( 'NONE',  ( -27.08416781016246588, -1.485424708116789061, -1.744495588874931169 ) ) ;
#38030=CIRCLE ( 'NONE', #8292, 2.899999999999995026 ) ;
#38037=DIRECTION ( 'NONE',  ( 1.000000000000000000, -0.000000000000000000, -0.000000000000000000 ) ) ;
#38045=DIRECTION ( 'NONE',  ( 0.000000000000000000, 0.000000000000000000, -1.000000000000000000 ) ) ;
#38053=DIRECTION ( 'NONE',  ( -1.000000000000000000, 0.000000000000000000, 0.000000000000000000 ) ) ;
#38054=CARTESIAN_POINT ( 'NONE',  ( -22.27218376572352554, 3.670373711461416111, -0.3046453028544185981 ) ) ;
#38056=CARTESIAN_POINT ( 'NONE',  ( 0.000000000000000000, -0.3246585432985730213, -6.805031400696120336 ) ) ;
#38059=ORIENTED_EDGE ( 'NONE', *, *, #27608, .T. ) ;
#38066=DIRECTION ( 'NONE',  ( 1.000000000000000000, 0.000000000000000000, 0.000000000000000000 ) ) ;
#38069=DIRECTION ( 'NONE',  ( -1.000000000000000000, 0.000000000000000000, 0.000000000000000000 ) ) ;
#38074=FACE_OUTER_BOUND ( 'NONE', #14298, .T. ) ;
#38087=CARTESIAN_POINT ( 'NONE',  ( -27.08418179957658367, 0.7235373421492767854, -2.174042548349540471 ) ) ;
#38091=DIRECTION ( 'NONE',  ( -1.000000000000000000, 0.000000000000000000, 0.000000000000000000 ) ) ;
#38092=EDGE_LOOP ( 'NONE', ( #53505, #46039, #31921, #62872 ) ) ;
#38094=LINE ( 'NONE', #7866, #52385 ) ;
#38099=CARTESIAN_POINT ( 'NONE',  ( 0.000000000000000000, -0.7281529553922420073, 7.464569195442772198 ) ) ;
#38101=CARTESIAN_POINT ( 'NONE',  ( -27.08506889328344158, -1.872884652028457220, 1.324351020478543806 ) ) ;
#38109=CARTESIAN_POINT ( 'NONE',  ( -22.66110217412718342, 3.914841338650350444, 3.020638270782502133 ) ) ;
#38115=CARTESIAN_POINT ( 'NONE',  ( -27.08954555554413446, 0.1819824474943435577, 2.300063521504146724 ) ) ;
#38118=CARTESIAN_POINT ( 'NONE',  ( 2.000000000000001776, 1.225832621831950187, -6.827324998361564923 ) ) ;
#38126=VECTOR ( 'NONE', #20130, 1000.000000000000000 ) ;
#38136=ORIENTED_EDGE ( 'NONE', *, *, #19617, .T. ) ;
#38138=CARTESIAN_POINT ( 'NONE',  ( 2.000000000000001776, 1.865193240757095916, 6.552473556515182374 ) ) ;
#38143=CIRCLE ( 'NONE', #55097, 6.936499999999987232 ) ;
#38151=CIRCLE ( 'NONE', #18002, 7.499999999999988454 ) ;
#38155=ORIENTED_EDGE ( 'NONE', *, *, #29457, .F. ) ;
#38169=EDGE_LOOP ( 'NONE', ( #52098, #17014, #9417, #47978 ) ) ;
#38170=CARTESIAN_POINT ( 'NONE',  ( 2.000000000000001776, 0.000000000000000000, 0.000000000000000000 ) ) ;
#38174=CIRCLE ( 'NONE', #11604, 2.899999999999995026 ) ;
#38176=CARTESIAN_POINT ( 'NONE',  ( -22.27718112499583469, -2.901898111564438221, 2.265557025479510322 ) ) ;
#38177=CARTESIAN_POINT ( 'NONE',  ( -27.10512513516319899, -1.618446180706342163, 1.709353012333651112 ) ) ;
#38178=CARTESIAN_POINT ( 'NONE',  ( 2.000000000000001776, 7.484036900328565167, 0.4890722589969472844 ) ) ;
#38186=CARTESIAN_POINT ( 'NONE',  ( -22.27721701579900682, 2.783642043008654809, -2.409654355488377586 ) ) ;
#38188=CARTESIAN_POINT ( 'NONE',  ( -10.00000000000000178, 0.000000000000000000, 0.000000000000000000 ) ) ;
#38189=CARTESIAN_POINT ( 'NONE',  ( -22.30625920655495165, 2.610366806364701642, -2.750410778797873323 ) ) ;
#38196=CIRCLE ( 'NONE', #9509, 7.499999999999988454 ) ;
#38207=ORIENTED_EDGE ( 'NONE', *, *, #20194, .F. ) ;
#38208=CYLINDRICAL_SURFACE ( 'NONE', #16473, 6.936499999999988120 ) ;
#38209=DIRECTION ( 'NONE',  ( 0.000000000000000000, 0.6876994588534192099, 0.7259954919231347281 ) ) ;
#38217=CARTESIAN_POINT ( 'NONE',  ( -22.27834755396593991, -1.338300169228702430, 3.434702243602647975 ) ) ;
#38227=CARTESIAN_POINT ( 'NONE',  ( -22.28236030719477512, -2.111163412226044311, -3.035028179399218207 ) ) ;
#38230=ORIENTED_EDGE ( 'NONE', *, *, #13316, .T. ) ;
#38232=EDGE_CURVE ( 'NONE', #53881, #42115, #43804, .T. ) ;
#38239=CARTESIAN_POINT ( 'NONE',  ( -22.28629837673888048, -0.2936941584814351525, -3.697248502489090427 ) ) ;
#38245=VERTEX_POINT ( 'NONE', #4274 ) ;
#38255=CARTESIAN_POINT ( 'NONE',  ( -22.29978294495153790, 3.642708310327678056, 0.8878583829805118954 ) ) ;
#38258=CARTESIAN_POINT ( 'NONE',  ( -22.31328051695926007, -0.2528478350593797996, -3.781397440874599614 ) ) ;
#38270=CARTESIAN_POINT ( 'NONE',  ( -10.00000000000000178, 0.000000000000000000, 0.000000000000000000 ) ) ;
#38275=EDGE_CURVE ( 'NONE', #25175, #60806, #49105, .T. ) ;
#38278=ORIENTED_EDGE ( 'NONE', *, *, #29417, .T. ) ;
#38281=DIRECTION ( 'NONE',  ( 0.000000000000000000, 0.000000000000000000, 1.000000000000000000 ) ) ;
#38287=EDGE_CURVE ( 'NONE', #51860, #40629, #25197, .T. ) ;
#38291=FACE_OUTER_BOUND ( 'NONE', #15273, .T. ) ;
#38297=CARTESIAN_POINT ( 'NONE',  ( -22.59969328935897437, -0.7214993884004085034, 4.594269189967448597 ) ) ;
#38298=AXIS2_PLACEMENT_3D ( 'NONE', #18139, #53724, #1865 ) ;
#38302=AXIS2_PLACEMENT_3D ( 'NONE', #16209, #11224, #46464 ) ;
#38303=AXIS2_PLACEMENT_3D ( 'NONE', #21891, #26532, #51822 ) ;
#38306=CARTESIAN_POINT ( 'NONE',  ( -22.30986928587821794, 3.771068405887398889, -0.2539257557460580794 ) ) ;
#38312=FACE_OUTER_BOUND ( 'NONE', #58832, .T. ) ;
#38316=CARTESIAN_POINT ( 'NONE',  ( -22.28776923226071105, -3.350304995653716755, -1.601293944844131678 ) ) ;
#38323=CARTESIAN_POINT ( 'NONE',  ( -22.27706485742869091, -2.580541389029911148, -2.625261754997698205 ) ) ;
#38328=FACE_OUTER_BOUND ( 'NONE', #62399, .T. ) ;
#38344=ADVANCED_FACE ( 'NONE', ( #7148 ), #33070, .T. ) ;
#38348=CIRCLE ( 'NONE', #60614, 2.899999999999995026 ) ;
#38353=CARTESIAN_POINT ( 'NONE',  ( 2.000000000000001776, -3.805198749487460841, 5.799611601383201531 ) ) ;
#38354=CARTESIAN_POINT ( 'NONE',  ( -22.30986928587821794, 3.392803916780413598, 1.665628047792409472 ) ) ;
#38355=CARTESIAN_POINT ( 'NONE',  ( -27.15525204139122550, 2.394850816831299856, -0.7327319213109826368 ) ) ;
#38356=CARTESIAN_POINT ( 'NONE',  ( -22.31099767395441091, 2.106713667647955202, 3.142100240805162592 ) ) ;
#38359=AXIS2_PLACEMENT_3D ( 'NONE', #17712, #13038, #43609 ) ;
#38367=CARTESIAN_POINT ( 'NONE',  ( -10.00000000000000178, 0.000000000000000000, 0.000000000000000000 ) ) ;
#38369=EDGE_CURVE ( 'NONE', #63832, #22351, #27859, .T. ) ;
#38373=DIRECTION ( 'NONE',  ( -1.000000000000000000, 0.000000000000000000, 0.000000000000000000 ) ) ;
#38383=CARTESIAN_POINT ( 'NONE',  ( -23.41523303002442091, -1.997501275420740630, -4.252418708693360472 ) ) ;
#38385=CIRCLE ( 'NONE', #9718, 2.899999999999995914 ) ;
#38388=VERTEX_POINT ( 'NONE', #28741 ) ;
#38391=CARTESIAN_POINT ( 'NONE',  ( -35.04643116707788408, 0.01193867652720184691, -0.002453861112635541408 ) ) ;
#38402=ORIENTED_EDGE ( 'NONE', *, *, #63949, .F. ) ;
#38427=CARTESIAN_POINT ( 'NONE',  ( -27.08423923533013777, 0.8983804370399791628, -2.107995711831551322 ) ) ;
#38431=DIRECTION ( 'NONE',  ( -1.000000000000000000, 0.000000000000000000, 0.000000000000000000 ) ) ;
#38432=EDGE_LOOP ( 'NONE', ( #14890, #10361, #23226, #4160 ) ) ;
#38447=DIRECTION ( 'NONE',  ( -1.000000000000000000, 0.000000000000000000, 0.000000000000000000 ) ) ;
#38448=ORIENTED_EDGE ( 'NONE', *, *, #45956, .F. ) ;
#38452=VECTOR ( 'NONE', #10063, 1000.000000000000000 ) ;
#38456=EDGE_CURVE ( 'NONE', #32332, #62269, #23650, .T. ) ;
#38457=ORIENTED_EDGE ( 'NONE', *, *, #64368, .F. ) ;
#38461=EDGE_CURVE ( 'NONE', #65063, #64384, #23205, .T. ) ;
#38462=CARTESIAN_POINT ( 'NONE',  ( -27.08704841010922948, -2.081152044925736355, -0.9786466045375251666 ) ) ;
#38466=CARTESIAN_POINT ( 'NONE',  ( -22.28284753389937478, -2.590196335759710422, 2.640101649307533105 ) ) ;
#38473=LINE ( 'NONE', #28488, #28013 ) ;
#38477=LINE ( 'NONE', #59110, #40812 ) ;
#38487=EDGE_LOOP ( 'NONE', ( #34874, #3207, #28032, #26318 ) ) ;
#38488=CARTESIAN_POINT ( 'NONE',  ( -22.65999102136916221, 0.5917351393135550364, -4.797155153747068468 ) ) ;
#38492=CARTESIAN_POINT ( 'NONE',  ( -27.32337605527165891, 0.3676050637290936285, -2.988381643048341196 ) ) ;
#38494=DIRECTION ( 'NONE',  ( 0.000000000000000000, -0.8835120444460178302, -0.4684084406997996997 ) ) ;
#38501=CARTESIAN_POINT ( 'NONE',  ( -27.28563798457901513, 0.04047623855284777222, -2.896153581097040242 ) ) ;
#38502=CARTESIAN_POINT ( 'NONE',  ( -22.28939870658739864, -1.608176106660549554, 3.352428181135941987 ) ) ;
#38505=AXIS2_PLACEMENT_3D ( 'NONE', #47030, #21075, #1489 ) ;
#38511=DIRECTION ( 'NONE',  ( -1.000000000000000000, 0.000000000000000000, 0.000000000000000000 ) ) ;
#38512=EDGE_CURVE ( 'NONE', #56181, #59691, #43857, .T. ) ;
#38514=CARTESIAN_POINT ( 'NONE',  ( 1.000000000000000888, 5.662015959325264802, -4.918493191653922736 ) ) ;
#38516=VERTEX_POINT ( 'NONE', #41325 ) ;
#38520=CARTESIAN_POINT ( 'NONE',  ( -27.10128162969864007, -2.337214317750536008, 0.1566844438592054634 ) ) ;
#38527=LINE ( 'NONE', #63453, #37035 ) ;
#38534=CARTESIAN_POINT ( 'NONE',  ( -27.08421723179412410, 1.556274442127719704, 1.681635392574617693 ) ) ;
#38536=VECTOR ( 'NONE', #49792, 1000.000000000000114 ) ;
#38538=EDGE_CURVE ( 'NONE', #44248, #49332, #51002, .T. ) ;
#38540=VECTOR ( 'NONE', #16334, 1000.000000000000000 ) ;
#38543=ORIENTED_EDGE ( 'NONE', *, *, #26026, .F. ) ;
#38548=FACE_OUTER_BOUND ( 'NONE', #18369, .T. ) ;
#38552=CARTESIAN_POINT ( 'NONE',  ( 2.000000000000001776, 1.693411908627200146, 7.306323022404582979 ) ) ;
#38561=CYLINDRICAL_SURFACE ( 'NONE', #58355, 2.899999999999994582 ) ;
#38567=DIRECTION ( 'NONE',  ( -1.000000000000000000, 0.000000000000000000, 0.000000000000000000 ) ) ;
#38577=AXIS2_PLACEMENT_3D ( 'NONE', #63108, #22208, #48487 ) ;
#38579=EDGE_LOOP ( 'NONE', ( #8533, #21237, #25100, #9117 ) ) ;
#38598=ADVANCED_FACE ( 'NONE', ( #28028 ), #23037, .T. ) ;
#38605=DIRECTION ( 'NONE',  ( 1.000000000000000000, 0.000000000000000000, 0.000000000000000000 ) ) ;
#38607=CARTESIAN_POINT ( 'NONE',  ( -22.49803948133826736, -4.343047530463636896, 0.1132714802761758260 ) ) ;
#38622=ORIENTED_EDGE ( 'NONE', *, *, #8788, .F. ) ;
#38625=DIRECTION ( 'NONE',  ( 0.000000000000000000, 0.000000000000000000, 1.000000000000000000 ) ) ;
#38635=EDGE_CURVE ( 'NONE', #918, #46346, #2431, .T. ) ;
#38637=CARTESIAN_POINT ( 'NONE',  ( -28.66013792860432119, -1.490739498621027836, 1.071635578228282482 ) ) ;
#38642=CARTESIAN_POINT ( 'NONE',  ( 0.000000000000000000, -6.586971819220345026, 3.586335490831356054 ) ) ;
#38643=CARTESIAN_POINT ( 'NONE',  ( -22.30861784526116054, -2.737516124790392080, -2.600591904828418954 ) ) ;
#38645=AXIS2_PLACEMENT_3D ( 'NONE', #46512, #7248, #41852 ) ;
#38664=CARTESIAN_POINT ( 'NONE',  ( -22.28939870658739864, -3.352428181135935326, -1.608176106660559768 ) ) ;
#38667=ORIENTED_EDGE ( 'NONE', *, *, #38876, .T. ) ;
#38671=DIRECTION ( 'NONE',  ( 0.000000000000000000, 0.000000000000000000, 1.000000000000000000 ) ) ;
#38674=EDGE_CURVE ( 'NONE', #19282, #50607, #22038, .T. ) ;
#38677=LINE ( 'NONE', #58981, #14883 ) ;
#38686=CARTESIAN_POINT ( 'NONE',  ( -35.04709527796842394, 0.005292201869334239861, 0.01117341439754379606 ) ) ;
#38694=CARTESIAN_POINT ( 'NONE',  ( -27.10719052120871098, -1.622102031466687189, 1.714424047991066846 ) ) ;
#38705=DIRECTION ( 'NONE',  ( 1.000000000000000000, -0.000000000000000000, -0.000000000000000000 ) ) ;
#38710=CARTESIAN_POINT ( 'NONE',  ( -35.04660725145885891, -0.01184012236745385360, -0.003326400506043277784 ) ) ;
#38711=EDGE_CURVE ( 'NONE', #29549, #59063, #24734, .T. ) ;
#38713=DIRECTION ( 'NONE',  ( 0.000000000000000000, 0.2149704402110178270, 0.9766205557100881007 ) ) ;
#38714=CIRCLE ( 'NONE', #10037, 6.936499999999988120 ) ;
#38732=VERTEX_POINT ( 'NONE', #24328 ) ;
#38741=ORIENTED_EDGE ( 'NONE', *, *, #4217, .F. ) ;
#38760=AXIS2_PLACEMENT_3D ( 'NONE', #59982, #40662, #5102 ) ;
#38762=DIRECTION ( 'NONE',  ( 1.000000000000000000, 0.000000000000000000, 0.000000000000000000 ) ) ;
#38772=CARTESIAN_POINT ( 'NONE',  ( -10.00000000000000178, 0.000000000000000000, 0.000000000000000000 ) ) ;
#38778=CARTESIAN_POINT ( 'NONE',  ( -22.27704833740210333, 2.993786163585794746, -2.142029987820960102 ) ) ;
#38779=DIRECTION ( 'NONE',  ( 0.000000000000000000, 0.000000000000000000, 1.000000000000000000 ) ) ;
#38785=CARTESIAN_POINT ( 'NONE',  ( 0.000000000000000000, 0.000000000000000000, 0.000000000000000000 ) ) ;
#38787=DIRECTION ( 'NONE',  ( 0.000000000000000000, 0.6051742151937610226, 0.7960930657056468629 ) ) ;
#38794=DIRECTION ( 'NONE',  ( -1.000000000000000000, 0.000000000000000000, 0.000000000000000000 ) ) ;
#38796=VERTEX_POINT ( 'NONE', #54286 ) ;
#38802=B_SPLINE_CURVE_WITH_KNOTS ( 'NONE', 3,
 ( #57548, #17637, #48242, #47885, #58529, #12293, #11967, #62498 ),
 .UNSPECIFIED., .F., .F.,
 ( 4, 2, 2, 4 ),
 ( 0.000000000000000000, 0.0003639104015149990413, 0.0007278208030299984080, 0.001455641606060001370 ),
 .UNSPECIFIED. ) ;
#38804=CARTESIAN_POINT ( 'NONE',  ( 0.000000000000000000, -4.376687952327356079, 5.220963330856582374 ) ) ;
#38805=CARTESIAN_POINT ( 'NONE',  ( 1.000000000000000888, 5.097042323172460421, 5.501832381651443171 ) ) ;
#38806=ORIENTED_EDGE ( 'NONE', *, *, #9383, .T. ) ;
#38810=VERTEX_POINT ( 'NONE', #4741 ) ;
#38818=LINE ( 'NONE', #59117, #24450 ) ;
#38823=CIRCLE ( 'NONE', #8070, 6.936499999999987232 ) ;
#38825=CARTESIAN_POINT ( 'NONE',  ( -28.67667724226168602, -1.299025457479350054, 1.375746547601627956 ) ) ;
#38829=ORIENTED_EDGE ( 'NONE', *, *, #46369, .F. ) ;
#38830=ORIENTED_EDGE ( 'NONE', *, *, #42398, .F. ) ;
#38841=CARTESIAN_POINT ( 'NONE',  ( -22.29677679919927868, -1.633785040807699707, 3.364642266483119482 ) ) ;
#38845=DIRECTION ( 'NONE',  ( -1.000000000000000000, 0.000000000000000000, 0.000000000000000000 ) ) ;
#38848=EDGE_LOOP ( 'NONE', ( #48301, #51214, #57022, #50504 ) ) ;
#38850=DIRECTION ( 'NONE',  ( 0.000000000000000000, 0.8835120444460240474, -0.4684084406997880423 ) ) ;
#38856=AXIS2_PLACEMENT_3D ( 'NONE', #10900, #31505, #23501 ) ;
#38868=LINE ( 'NONE', #53179, #50004 ) ;
#38872=EDGE_CURVE ( 'NONE', #10229, #53826, #4567, .T. ) ;
#38876=EDGE_CURVE ( 'NONE', #4358, #16416, #61875, .T. ) ;
#38883=DIRECTION ( 'NONE',  ( -1.000000000000000000, 0.000000000000000000, 0.000000000000000000 ) ) ;
#38889=CARTESIAN_POINT ( 'NONE',  ( -22.29195009621226831, 2.682867222693523956, 2.585382421603408698 ) ) ;
#38892=ORIENTED_EDGE ( 'NONE', *, *, #12685, .T. ) ;
#38897=EDGE_CURVE ( 'NONE', #60806, #28767, #10030, .T. ) ;
#38898=ADVANCED_FACE ( 'NONE', ( #56222 ), #51265, .T. ) ;
#38906=DIRECTION ( 'NONE',  ( 0.000000000000000000, 0.000000000000000000, 1.000000000000000000 ) ) ;
#38908=CARTESIAN_POINT ( 'NONE',  ( -22.28629837673887693, -2.102970853432566845, -3.055064048018814482 ) ) ;
#38913=EDGE_CURVE ( 'NONE', #20840, #48378, #60901, .T. ) ;
#38915=ORIENTED_EDGE ( 'NONE', *, *, #46453, .F. ) ;
#38926=ORIENTED_EDGE ( 'NONE', *, *, #24232, .F. ) ;
#38928=UNCERTAINTY_MEASURE_WITH_UNIT (LENGTH_MEASURE( 1.000000000000000082E-05 ), #44450, 'distance_accuracy_value', 'NONE');
#38929=EDGE_LOOP ( 'NONE', ( #49725, #58966, #56745, #38448 ) ) ;
#38937=DIRECTION ( 'NONE',  ( -1.000000000000000000, 0.000000000000000000, 0.000000000000000000 ) ) ;
#38943=DIRECTION ( 'NONE',  ( -1.000000000000000000, 0.000000000000000000, 0.000000000000000000 ) ) ;
#38953=CYLINDRICAL_SURFACE ( 'NONE', #61443, 2.899999999999994582 ) ;
#38965=CYLINDRICAL_SURFACE ( 'NONE', #59349, 2.899999999999994582 ) ;
#38966=DIRECTION ( 'NONE',  ( -1.000000000000000000, 0.000000000000000000, 0.000000000000000000 ) ) ;
#38968=CARTESIAN_POINT ( 'NONE',  ( 0.000000000000000000, 0.000000000000000000, 0.000000000000000000 ) ) ;
#38971=ORIENTED_EDGE ( 'NONE', *, *, #44921, .F. ) ;
#38973=CARTESIAN_POINT ( 'NONE',  ( -22.27713295444592845, -3.580881989303324353, 0.8543895091636493078 ) ) ;
#38981=CARTESIAN_POINT ( 'NONE',  ( -22.27721688985630522, -2.338410344701250310, -2.843753050855878151 ) ) ;
#38990=DIRECTION ( 'NONE',  ( 0.000000000000000000, -6.883382752675980017E-15, 1.000000000000000000 ) ) ;
#38997=DIRECTION ( 'NONE',  ( 1.000000000000000000, 0.000000000000000000, 0.000000000000000000 ) ) ;
#39011=CARTESIAN_POINT ( 'NONE',  ( -22.31213670151049300, 3.398324501467296699, 1.669817926839889388 ) ) ;
#39026=VERTEX_POINT ( 'NONE', #32904 ) ;
#39037=CARTESIAN_POINT ( 'NONE',  ( 2.000000000000001776, 1.530946385938479093, -7.342084388195354805 ) ) ;
#39040=AXIS2_PLACEMENT_3D ( 'NONE', #3279, #38845, #49491 ) ;
#39043=DIRECTION ( 'NONE',  ( -1.000000000000000000, 0.000000000000000000, 0.000000000000000000 ) ) ;
#39053=CARTESIAN_POINT ( 'NONE',  ( -35.04709527796842394, 0.01016988845958452514, 0.007030359780618375409 ) ) ;
#39055=CARTESIAN_POINT ( 'NONE',  ( 2.000000000000001776, 3.152010634611773110, -6.039758645301250617 ) ) ;
#39057=DIRECTION ( 'NONE',  ( -1.000000000000000000, 0.000000000000000000, 0.000000000000000000 ) ) ;
#39065=VERTEX_POINT ( 'NONE', #47902 ) ;
#39068=AXIS2_PLACEMENT_3D ( 'NONE', #34254, #24279, #40552 ) ;
#39077=DIRECTION ( 'NONE',  ( -1.000000000000000000, 0.000000000000000000, 0.000000000000000000 ) ) ;
#39079=AXIS2_PLACEMENT_3D ( 'NONE', #35962, #59967, #5757 ) ;
#39085=CARTESIAN_POINT ( 'NONE',  ( -22.28350523959501217, 3.041489826385515904, -2.107889123925570818 ) ) ;
#39104=CARTESIAN_POINT ( 'NONE',  ( -27.09483304420799143, -2.090133548856194068, -1.013994808271696746 ) ) ;
#39105=FACE_OUTER_BOUND ( 'NONE', #28470, .T. ) ;
#39126=VECTOR ( 'NONE', #10540, 1000.000000000000000 ) ;
#39129=DIRECTION ( 'NONE',  ( 0.000000000000000000, 0.000000000000000000, 1.000000000000000000 ) ) ;
#39133=DIRECTION ( 'NONE',  ( -1.000000000000000000, 0.000000000000000000, 0.000000000000000000 ) ) ;
#39142=SURFACE_SIDE_STYLE ('',( #54125 ) ) ;
#39143=CARTESIAN_POINT ( 'NONE',  ( -27.10719052120871098, -2.295785794152564563, -0.5475695427849640584 ) ) ;
#39145=VECTOR ( 'NONE', #32958, 1000.000000000000000 ) ;
#39150=AXIS2_PLACEMENT_3D ( 'NONE', #54666, #34014, #53988 ) ;
#39157=ORIENTED_EDGE ( 'NONE', *, *, #60598, .T. ) ;
#39164=CYLINDRICAL_SURFACE ( 'NONE', #28481, 2.899999999999994582 ) ;
#39168=VERTEX_POINT ( 'NONE', #61454 ) ;
#39175=CARTESIAN_POINT ( 'NONE',  ( -22.27218376572352554, -3.026314224080924209, 2.099017427146280479 ) ) ;
#39177=CARTESIAN_POINT ( 'NONE',  ( -27.08429572838383947, 1.632445743623435197, -1.608131779585709076 ) ) ;
#39183=DIRECTION ( 'NONE',  ( 0.000000000000000000, 0.000000000000000000, 1.000000000000000000 ) ) ;
#39186=DIRECTION ( 'NONE',  ( 0.000000000000000000, 0.000000000000000000, -1.000000000000000000 ) ) ;
#39205=CARTESIAN_POINT ( 'NONE',  ( 2.000000000000001776, 6.935703035393450122, 0.1051458740707594125 ) ) ;
#39224=EDGE_CURVE ( 'NONE', #42915, #61990, #32158, .T. ) ;
#39226=FACE_OUTER_BOUND ( 'NONE', #51404, .T. ) ;
#39227=DIRECTION ( 'NONE',  ( 0.000000000000000000, -0.1081190184239279872, -0.9941379571543611515 ) ) ;
#39229=VERTEX_POINT ( 'NONE', #41174 ) ;
#39234=ORIENTED_EDGE ( 'NONE', *, *, #39224, .F. ) ;
#39238=ORIENTED_EDGE ( 'NONE', *, *, #3539, .T. ) ;
#39243=CARTESIAN_POINT ( 'NONE',  ( -35.04683013664716640, 0.006090538653970694813, -0.01075274318002154145 ) ) ;
#39244=VECTOR ( 'NONE', #36149, 1000.000000000000000 ) ;
#39245=CARTESIAN_POINT ( 'NONE',  ( -22.31328051695926007, 3.685074213229321494, 0.8849444482787824917 ) ) ;
#39248=CARTESIAN_POINT ( 'NONE',  ( -22.59983133926799326, 0.06110861519533868080, -4.650609684383240960 ) ) ;
#39249=ORIENTED_EDGE ( 'NONE', *, *, #13564, .F. ) ;
#39253=FACE_OUTER_BOUND ( 'NONE', #46231, .T. ) ;
#39256=ORIENTED_EDGE ( 'NONE', *, *, #16789, .T. ) ;
#39258=FACE_OUTER_BOUND ( 'NONE', #8217, .T. ) ;
#39273=CARTESIAN_POINT ( 'NONE',  ( -22.66110217412718342, -3.914841338650320246, -3.020638270782546542 ) ) ;
#39295=VERTEX_POINT ( 'NONE', #2278 ) ;
#39299=CARTESIAN_POINT ( 'NONE',  ( -22.27715526084302056, -2.228953214080623635, -2.930376837866850437 ) ) ;
#39313=DIRECTION ( 'NONE',  ( -1.000000000000000000, 0.000000000000000000, 0.000000000000000000 ) ) ;
#39324=CARTESIAN_POINT ( 'NONE',  ( 2.000000000000001776, -4.444115772890066651, -5.163689623839394116 ) ) ;
#39325=ORIENTED_EDGE ( 'NONE', *, *, #49049, .T. ) ;
#39327=ORIENTED_EDGE ( 'NONE', *, *, #35520, .T. ) ;
#39332=ORIENTED_EDGE ( 'NONE', *, *, #16777, .F. ) ;
#39336=CARTESIAN_POINT ( 'NONE',  ( -22.27786964138239867, 2.131221155130671452, 3.004507515156356501 ) ) ;
#39337=CARTESIAN_POINT ( 'NONE',  ( -22.28629837673888048, 1.594277649056540902, -3.348758206500249468 ) ) ;
#39345=FACE_OUTER_BOUND ( 'NONE', #46828, .T. ) ;
#39347=CARTESIAN_POINT ( 'NONE',  ( -22.27384469013076185, 2.154627400808035276, 2.985904959940879344 ) ) ;
#39348=ORIENTED_EDGE ( 'NONE', *, *, #10200, .T. ) ;
#39355=CARTESIAN_POINT ( 'NONE',  ( 0.000000000000000000, -6.470132594555779271, -2.133363481234176628 ) ) ;
#39365=VERTEX_POINT ( 'NONE', #59428 ) ;
#39366=CARTESIAN_POINT ( 'NONE',  ( -22.27218376572352554, 3.566922835983793227, 0.9173404081777183361 ) ) ;
#39372=VERTEX_POINT ( 'NONE', #64093 ) ;
#39375=AXIS2_PLACEMENT_3D ( 'NONE', #5456, #19763, #31032 ) ;
#39379=CARTESIAN_POINT ( 'NONE',  ( 2.000000000000001776, 6.906413915731199005, -0.6453518998146886565 ) ) ;
#39380=DIRECTION ( 'NONE',  ( 0.000000000000000000, 0.9985334138511237079, 0.05413890858542116241 ) ) ;
#39385=CARTESIAN_POINT ( 'NONE',  ( -22.27384469013076185, -3.358914544760241316, -1.508555848190779702 ) ) ;
#39387=ORIENTED_EDGE ( 'NONE', *, *, #58082, .T. ) ;
#39398=CIRCLE ( 'NONE', #60622, 6.936499999999989896 ) ;
#39406=ORIENTED_EDGE ( 'NONE', *, *, #44096, .T. ) ;
#39408=ORIENTED_EDGE ( 'NONE', *, *, #44921, .T. ) ;
#39410=DIRECTION ( 'NONE',  ( -1.000000000000000000, 0.000000000000000000, 0.000000000000000000 ) ) ;
#39413=DIRECTION ( 'NONE',  ( 0.000000000000000000, 0.8835120444460240474, -0.4684084406997882088 ) ) ;
#39414=CYLINDRICAL_SURFACE ( 'NONE', #28884, 7.499999999999988454 ) ;
#39423=CIRCLE ( 'NONE', #12903, 6.936499999999989008 ) ;
#39424=CIRCLE ( 'NONE', #1186, 6.936499999999988120 ) ;
#39426=CIRCLE ( 'NONE', #47949, 6.936499999999987232 ) ;
#39430=CARTESIAN_POINT ( 'NONE',  ( 2.000000000000001776, -7.414200355365243134, -1.131208685655240798 ) ) ;
#39432=ORIENTED_EDGE ( 'NONE', *, *, #20320, .T. ) ;
#39433=DIRECTION ( 'NONE',  ( -1.000000000000000000, 0.000000000000000000, 0.000000000000000000 ) ) ;
#39437=EDGE_CURVE ( 'NONE', #10755, #7525, #26762, .T. ) ;
#39444=CIRCLE ( 'NONE', #1267, 7.499999999999988454 ) ;
#39450=CIRCLE ( 'NONE', #25649, 2.899999999999995914 ) ;
#39455=EDGE_LOOP ( 'NONE', ( #24073, #29396, #1739, #61419 ) ) ;
#39461=CYLINDRICAL_SURFACE ( 'NONE', #32206, 2.899999999999994582 ) ;
#39464=CARTESIAN_POINT ( 'NONE',  ( -27.04788180060269553, 2.650714769830310846, 1.844972430941732355 ) ) ;
#39469=ORIENTED_EDGE ( 'NONE', *, *, #3001, .T. ) ;
#39475=CIRCLE ( 'NONE', #21453, 2.899999999999994582 ) ;
#39479=DIRECTION ( 'NONE',  ( -1.000000000000000000, 0.000000000000000000, 0.000000000000000000 ) ) ;
#39497=DIRECTION ( 'NONE',  ( -1.000000000000000000, 0.000000000000000000, 0.000000000000000000 ) ) ;
#39503=DIRECTION ( 'NONE',  ( 0.000000000000000000, -0.5155538571770286183, 0.8568571761675850551 ) ) ;
#39505=LINE ( 'NONE', #59799, #12557 ) ;
#39508=CARTESIAN_POINT ( 'NONE',  ( -22.27706485742869091, -2.154081322712202873, -2.985151051101508468 ) ) ;
#39530=ORIENTED_EDGE ( 'NONE', *, *, #30546, .F. ) ;
#39534=CARTESIAN_POINT ( 'NONE',  ( -25.42680463514451361, -3.516354806213008111, 1.651747791411765753 ) ) ;
#39536=CARTESIAN_POINT ( 'NONE',  ( -10.00000000000000178, 0.000000000000000000, 0.000000000000000000 ) ) ;
#39545=CARTESIAN_POINT ( 'NONE',  ( 2.000000000000001776, 6.441884263200846839, -2.217201541069800275 ) ) ;
#39546=CIRCLE ( 'NONE', #36369, 7.499999999999988454 ) ;
#39552=ORIENTED_EDGE ( 'NONE', *, *, #30666, .F. ) ;
#39553=EDGE_CURVE ( 'NONE', #1479, #40758, #8728, .T. ) ;
#39591=EDGE_LOOP ( 'NONE', ( #63654, #40813, #30283, #7113 ) ) ;
#39601=DIRECTION ( 'NONE',  ( 0.000000000000000000, -0.4198891015602717602, 0.9075754196709537869 ) ) ;
#39607=CARTESIAN_POINT ( 'NONE',  ( -27.32337605527166957, -1.812546145273346010, 2.404211887218381527 ) ) ;
#39609=ADVANCED_FACE ( 'NONE', ( #25161 ), #4233, .T. ) ;
#39617=ADVANCED_FACE ( 'NONE', ( #15501 ), #9112, .F. ) ;
#39633=ORIENTED_EDGE ( 'NONE', *, *, #24004, .T. ) ;
#39635=EDGE_CURVE ( 'NONE', #15981, #63362, #30782, .T. ) ;
#39661=CARTESIAN_POINT ( 'NONE',  ( -27.09602251845210219, -0.1644056400645331761, -2.320865065108511427 ) ) ;
#39664=ORIENTED_EDGE ( 'NONE', *, *, #27593, .F. ) ;
#39675=CARTESIAN_POINT ( 'NONE',  ( -27.08485414902839139, -2.214586389210154493, 0.5952588087544555817 ) ) ;
#39682=EDGE_LOOP ( 'NONE', ( #52863, #53009, #60395, #27060 ) ) ;
#39684=VECTOR ( 'NONE', #52854, 1000.000000000000000 ) ;
#39686=CARTESIAN_POINT ( 'NONE',  ( 0.000000000000000000, 6.750946897830712778, 1.593658756657066355 ) ) ;
#39694=CARTESIAN_POINT ( 'NONE',  ( -35.05012975565874456, -0.01039213056760649075, 0.009279204628454365902 ) ) ;
#39697=DIRECTION ( 'NONE',  ( -1.000000000000000000, 0.000000000000000000, 0.000000000000000000 ) ) ;
#39703=DIRECTION ( 'NONE',  ( 0.000000000000000000, 0.000000000000000000, 1.000000000000000000 ) ) ;
#39708=ORIENTED_EDGE ( 'NONE', *, *, #5883, .F. ) ;
#39714=ORIENTED_EDGE ( 'NONE', *, *, #54665, .T. ) ;
#39717=AXIS2_PLACEMENT_3D ( 'NONE', #11719, #32002, #47333 ) ;
#39728=DIRECTION ( 'NONE',  ( -1.000000000000000000, 0.000000000000000000, 0.000000000000000000 ) ) ;
#39731=AXIS2_PLACEMENT_3D ( 'NONE', #1511, #21789, #16770 ) ;
#39745=VERTEX_POINT ( 'NONE', #1555 ) ;
#39749=CARTESIAN_POINT ( 'NONE',  ( -22.30861784526116054, 0.8834205920623713348, -3.671054459752221444 ) ) ;
#39751=CARTESIAN_POINT ( 'NONE',  ( 0.000000000000000000, 0.000000000000000000, 0.000000000000000000 ) ) ;
#39752=EDGE_CURVE ( 'NONE', #3825, #125, #40573, .T. ) ;
#39757=ORIENTED_EDGE ( 'NONE', *, *, #14911, .T. ) ;
#39758=CYLINDRICAL_SURFACE ( 'NONE', #28555, 2.899999999999994582 ) ;
#39759=CARTESIAN_POINT ( 'NONE',  ( 0.000000000000000000, 0.7281529553922073683, 7.464569195442786409 ) ) ;
#39760=VECTOR ( 'NONE', #36434, 1000.000000000000000 ) ;
#39765=CIRCLE ( 'NONE', #5816, 7.499999999999988454 ) ;
#39769=EDGE_CURVE ( 'NONE', #3146, #65336, #47428, .T. ) ;
#39772=DIRECTION ( 'NONE',  ( 0.000000000000000000, 0.000000000000000000, -1.000000000000000000 ) ) ;
#39773=DIRECTION ( 'NONE',  ( 0.000000000000000000, 0.4198891015602657650, -0.9075754196709565624 ) ) ;
#39787=CARTESIAN_POINT ( 'NONE',  ( -22.27756824490284160, -0.9472004376381237822, -3.558840239148768791 ) ) ;
#39795=DIRECTION ( 'NONE',  ( 1.000000000000000000, 0.000000000000000000, 0.000000000000000000 ) ) ;
#39796=CARTESIAN_POINT ( 'NONE',  ( -27.08430418657511396, 1.333569526609277300, 1.863523114787992041 ) ) ;
#39805=AXIS2_PLACEMENT_3D ( 'NONE', #29019, #4070, #7756 ) ;
#39808=ORIENTED_EDGE ( 'NONE', *, *, #47537, .F. ) ;
#39809=SHAPE_REPRESENTATION_RELATIONSHIP ( 'NONE' , 'NONE' ,  #13953, #19082 ) ;
#39814=CARTESIAN_POINT ( 'NONE',  ( -10.00000000000000178, 0.000000000000000000, 0.000000000000000000 ) ) ;
#39818=CYLINDRICAL_SURFACE ( 'NONE', #5594, 2.899999999999994582 ) ;
#39825=ADVANCED_FACE ( 'NONE', ( #34632 ), #28427, .T. ) ;
#39836=CARTESIAN_POINT ( 'NONE',  ( 0.000000000000000000, 0.000000000000000000, 0.000000000000000000 ) ) ;
#39855=CARTESIAN_POINT ( 'NONE',  ( -27.08954555554373300, 2.082904663687279889, 0.9924303381770370747 ) ) ;
#39868=AXIS2_PLACEMENT_3D ( 'NONE', #8024, #29271, #28288 ) ;
#39870=ORIENTED_EDGE ( 'NONE', *, *, #3544, .T. ) ;
#39871=CARTESIAN_POINT ( 'NONE',  ( 2.000000000000001776, 0.000000000000000000, 0.000000000000000000 ) ) ;
#39882=CARTESIAN_POINT ( 'NONE',  ( -22.28482751661422157, -3.347211412506306605, -1.587261331312506352 ) ) ;
#39896=CARTESIAN_POINT ( 'NONE',  ( 2.000000000000001776, -6.664893814313694875, -3.439359016433563898 ) ) ;
#39905=CARTESIAN_POINT ( 'NONE',  ( -25.42680463514451361, 3.516354806213017437, -1.651747791411759314 ) ) ;
#39908=AXIS2_PLACEMENT_3D ( 'NONE', #15369, #56253, #39981 ) ;
#39918=CIRCLE ( 'NONE', #45095, 2.999999999999995559 ) ;
#39919=ORIENTED_EDGE ( 'NONE', *, *, #60397, .F. ) ;
#39924=EDGE_CURVE ( 'NONE', #2564, #38245, #15120, .T. ) ;
#39929=EDGE_CURVE ( 'NONE', #46169, #39745, #30134, .T. ) ;
#39933=DIRECTION ( 'NONE',  ( 0.9606638835031803270, 0.1133241553124329504, -0.2535400141108139493 ) ) ;
#39934=DIRECTION ( 'NONE',  ( 0.000000000000000000, 0.000000000000000000, 1.000000000000000000 ) ) ;
#39935=CARTESIAN_POINT ( 'NONE',  ( 2.000000000000001776, 0.000000000000000000, 0.000000000000000000 ) ) ;
#39939=EDGE_CURVE ( 'NONE', #27434, #26369, #56580, .T. ) ;
#39950=ORIENTED_EDGE ( 'NONE', *, *, #11402, .T. ) ;
#39952=CARTESIAN_POINT ( 'NONE',  ( -22.27721038036499479, -3.635620891621744288, 0.5802312083658510700 ) ) ;
#39962=CARTESIAN_POINT ( 'NONE',  ( 0.000000000000000000, 6.662861565602083758, -1.421313227905602883 ) ) ;
#39975=CYLINDRICAL_SURFACE ( 'NONE', #41166, 2.899999999999994582 ) ;
#39979=CARTESIAN_POINT ( 'NONE',  ( -22.27719412087655471, 0.5341638063192103436, 3.642699606241609711 ) ) ;
#39980=EDGE_CURVE ( 'NONE', #31042, #26347, #42027, .T. ) ;
#39981=DIRECTION ( 'NONE',  ( 0.000000000000000000, 0.3193015301359742319, 0.9476531711828044546 ) ) ;
#39987=B_SPLINE_CURVE_WITH_KNOTS ( 'NONE', 3,
 ( #44015, #39995, #14392, #29053, #5093, #50650, #49982, #40312, #8768, #45315 ),
 .UNSPECIFIED., .F., .F.,
 ( 4, 3, 3, 4 ),
 ( 0.000000000000000000, 6.991367980366405095E-05, 0.0001398269368981362335, 0.0001763147164361759890 ),
 .UNSPECIFIED. ) ;
#39995=CARTESIAN_POINT ( 'NONE',  ( -27.08426571771018132, 0.2528330215897400257, 2.277536580310452141 ) ) ;
#40000=VECTOR ( 'NONE', #53719, 1000.000000000000227 ) ;
#40005=FACE_OUTER_BOUND ( 'NONE', #25398, .T. ) ;
#40006=CARTESIAN_POINT ( 'NONE',  ( -27.10719052120871098, 2.116547233941204809, 1.044362304621460069 ) ) ;
#40017=EDGE_CURVE ( 'NONE', #50103, #48840, #27912, .T. ) ;
#40035=CARTESIAN_POINT ( 'NONE',  ( -35.05012975565874456, 0.008684292310206072341, 0.01089417657933153954 ) ) ;
#40041=ORIENTED_EDGE ( 'NONE', *, *, #46576, .F. ) ;
#40045=ORIENTED_EDGE ( 'NONE', *, *, #44915, .F. ) ;
#40046=VERTEX_POINT ( 'NONE', #32272 ) ;
#40047=CARTESIAN_POINT ( 'NONE',  ( -22.29570301036918423, -0.8918611685731179239, 3.629130197778196454 ) ) ;
#40051=DIRECTION ( 'NONE',  ( -1.000000000000000000, 0.000000000000000000, 0.000000000000000000 ) ) ;
#40056=CARTESIAN_POINT ( 'NONE',  ( -22.71097035706202405, -4.089776368546547580, -2.846599994298351977 ) ) ;
#40057=ORIENTED_EDGE ( 'NONE', *, *, #60966, .T. ) ;
#40058=ORIENTED_EDGE ( 'NONE', *, *, #60686, .F. ) ;
#40063=CARTESIAN_POINT ( 'NONE',  ( -22.27719443589224113, 1.139586749255988796, -3.500848524682612872 ) ) ;
#40068=ORIENTED_EDGE ( 'NONE', *, *, #47640, .T. ) ;
#40082=ORIENTED_EDGE ( 'NONE', *, *, #61208, .F. ) ;
#40101=CIRCLE ( 'NONE', #19951, 6.936499999999990784 ) ;
#40102=FACE_OUTER_BOUND ( 'NONE', #63597, .T. ) ;
#40105=CARTESIAN_POINT ( 'NONE',  ( -27.08456565417846562, 1.328664661356744325, 1.867985369021563535 ) ) ;
#40108=CARTESIAN_POINT ( 'NONE',  ( 2.000000000000001776, -6.750946897830688798, -1.593658756657146292 ) ) ;
#40109=CARTESIAN_POINT ( 'NONE',  ( -35.04834644901396956, -0.0002835132723631789337, -0.01383120537649086199 ) ) ;
#40113=VERTEX_POINT ( 'NONE', #32581 ) ;
#40136=CYLINDRICAL_SURFACE ( 'NONE', #19992, 7.499999999999988454 ) ;
#40145=DIRECTION ( 'NONE',  ( -1.000000000000000000, 0.000000000000000000, 0.000000000000000000 ) ) ;
#40148=EDGE_CURVE ( 'NONE', #28450, #43944, #29568, .T. ) ;
#40149=EDGE_CURVE ( 'NONE', #42450, #10792, #9608, .T. ) ;
#40150=AXIS2_PLACEMENT_3D ( 'NONE', #14532, #4603, #34811 ) ;
#40156=LINE ( 'NONE', #45166, #21156 ) ;
#40180=VECTOR ( 'NONE', #6982, 1000.000000000000000 ) ;
#40192=EDGE_LOOP ( 'NONE', ( #59980, #16440, #19538, #9443 ) ) ;
#40196=CARTESIAN_POINT ( 'NONE',  ( -22.70624764888619751, 4.591418580540064021, -2.547047087672808630 ) ) ;
#40201=AXIS2_PLACEMENT_3D ( 'NONE', #57953, #27337, #12365 ) ;
#40207=DIRECTION ( 'NONE',  ( 1.000000000000000000, -0.000000000000000000, -0.000000000000000000 ) ) ;
#40210=ORIENTED_EDGE ( 'NONE', *, *, #53098, .F. ) ;
#40212=LINE ( 'NONE', #50869, #49074 ) ;
#40222=CARTESIAN_POINT ( 'NONE',  ( 0.000000000000000000, -5.457833520448679643, 4.281014542496493824 ) ) ;
#40223=LINE ( 'NONE', #34582, #24508 ) ;
#40225=CARTESIAN_POINT ( 'NONE',  ( -35.04660725145885891, -0.003039313842339400138, -0.01191704700716593457 ) ) ;
#40235=CARTESIAN_POINT ( 'NONE',  ( -22.27706485742869091, 0.3729136217356220917, 3.662257305743802149 ) ) ;
#40256=DIRECTION ( 'NONE',  ( 1.000000000000000000, -0.000000000000000000, -0.000000000000000000 ) ) ;
#40259=CARTESIAN_POINT ( 'NONE',  ( 2.000000000000001776, 0.8935325819928834346, 7.446583077151348817 ) ) ;
#40260=EDGE_CURVE ( 'NONE', #22630, #30460, #48090, .T. ) ;
#40262=CARTESIAN_POINT ( 'NONE',  ( -27.09602251845210930, -1.302811993375582844, -1.927725285107534603 ) ) ;
#40265=CARTESIAN_POINT ( 'NONE',  ( -22.28506771379528573, 3.091577134491935830, -2.081613609299053369 ) ) ;
#40268=EDGE_LOOP ( 'NONE', ( #21768, #877, #62857, #61601 ) ) ;
#40272=CARTESIAN_POINT ( 'NONE',  ( -22.27721698446158172, 0.6951119527728008007, 3.615509722105048951 ) ) ;
#40280=FACE_OUTER_BOUND ( 'NONE', #8254, .T. ) ;
#40285=CARTESIAN_POINT ( 'NONE',  ( -27.08850691366518504, 1.648570643966304594, 1.609738257842355580 ) ) ;
#40290=DIRECTION ( 'NONE',  ( -1.000000000000000000, 0.000000000000000000, 0.000000000000000000 ) ) ;
#40294=AXIS2_PLACEMENT_3D ( 'NONE', #10340, #49621, #14352 ) ;
#40297=CARTESIAN_POINT ( 'NONE',  ( -27.20650584082916978, 3.154168801321778126, 0.2670256460080390748 ) ) ;
#40301=CARTESIAN_POINT ( 'NONE',  ( -27.08416781016246588, 2.253489850813972240, -0.4141677382007631913 ) ) ;
#40305=CARTESIAN_POINT ( 'NONE',  ( -35.05012975565874456, -0.002839961651356822867, -0.01363945138521795858 ) ) ;
#40312=CARTESIAN_POINT ( 'NONE',  ( -27.08417174366084623, 0.3802265912085586175, 2.259388872100069889 ) ) ;
#40314=CARTESIAN_POINT ( 'NONE',  ( -27.08776759928964850, -2.217308861843129364, 0.6183458186125468936 ) ) ;
#40315=EDGE_CURVE ( 'NONE', #58425, #28230, #23796, .T. ) ;
#40322=ADVANCED_FACE ( 'NONE', ( #968, #60831 ), #16260, .F. ) ;
#40337=CARTESIAN_POINT ( 'NONE',  ( -27.08429572838383947, -1.859677275556421927, 1.338867938658193424 ) ) ;
#40342=CARTESIAN_POINT ( 'NONE',  ( -22.27718150314433387, 3.507884203786638011, 1.117371044661051638 ) ) ;
#40344=ORIENTED_EDGE ( 'NONE', *, *, #708, .T. ) ;
#40349=AXIS2_PLACEMENT_3D ( 'NONE', #24941, #50546, #54557 ) ;
#40364=EDGE_LOOP ( 'NONE', ( #26100, #32195, #56989, #29068 ) ) ;
#40387=DIRECTION ( 'NONE',  ( -1.000000000000000000, 0.000000000000000000, 0.000000000000000000 ) ) ;
#40389=CARTESIAN_POINT ( 'NONE',  ( 2.000000000000001776, 0.000000000000000000, 0.000000000000000000 ) ) ;
#40390=VECTOR ( 'NONE', #23121, 1000.000000000000000 ) ;
#40391=CARTESIAN_POINT ( 'NONE',  ( 2.000000000000001776, -6.935703035393425253, 0.1051458740707039013 ) ) ;
#40407=CARTESIAN_POINT ( 'NONE',  ( -27.08417568107323703, -2.142502990753192282, -0.8117865859100446002 ) ) ;
#40408=AXIS2_PLACEMENT_3D ( 'NONE', #59351, #63660, #18136 ) ;
#40420=AXIS2_PLACEMENT_3D ( 'NONE', #34430, #43410, #3870 ) ;
#40421=CARTESIAN_POINT ( 'NONE',  ( -27.10719052120871098, -2.116547233941210138, -1.044362304621491377 ) ) ;
#40425=DIRECTION ( 'NONE',  ( -1.000000000000000000, 0.000000000000000000, 0.000000000000000000 ) ) ;
#40426=CARTESIAN_POINT ( 'NONE',  ( -22.65996813707687352, 4.828298130757343820, 0.2230532344361134678 ) ) ;
#40427=CARTESIAN_POINT ( 'NONE',  ( -22.29018399051993882, -1.024613686459451944, -3.576688584977248730 ) ) ;
#40429=DIRECTION ( 'NONE',  ( 0.000000000000000000, 0.5155538571770172940, 0.8568571761675919385 ) ) ;
#40431=CARTESIAN_POINT ( 'NONE',  ( -27.10512513516274424, 2.289566223068224993, 0.5469390009825837451 ) ) ;
#40432=VECTOR ( 'NONE', #37525, 1000.000000000000000 ) ;
#40438=VECTOR ( 'NONE', #4424, 1000.000000000000000 ) ;
#40456=DIRECTION ( 'NONE',  ( 0.000000000000000000, 0.9289767198167925288, -0.3701381553399118451 ) ) ;
#40459=ORIENTED_EDGE ( 'NONE', *, *, #31815, .T. ) ;
#40462=AXIS2_PLACEMENT_3D ( 'NONE', #7472, #58713, #7828 ) ;
#40472=CIRCLE ( 'NONE', #49012, 2.899999999999994582 ) ;
#40473=EDGE_CURVE ( 'NONE', #50124, #13608, #55532, .T. ) ;
#40474=CARTESIAN_POINT ( 'NONE',  ( -22.71097035706202760, -2.118550233809395777, -4.510116093748293586 ) ) ;
#40477=EDGE_CURVE ( 'NONE', #37749, #21913, #41066, .T. ) ;
#40484=B_SPLINE_CURVE_WITH_KNOTS ( 'NONE', 3,
 ( #62777, #17895, #11585, #6622, #47193, #1636 ),
 .UNSPECIFIED., .F., .F.,
 ( 4, 2, 4 ),
 ( 0.000000000000000000, 0.0004528561986909394226, 0.0009057123973818788452 ),
 .UNSPECIFIED. ) ;
#40487=CIRCLE ( 'NONE', #26687, 6.936499999999987232 ) ;
#40494=CARTESIAN_POINT ( 'NONE',  ( -22.29115169517546136, -3.712980101756718554, 0.2790989024812929875 ) ) ;
#40497=CARTESIAN_POINT ( 'NONE',  ( 2.000000000000001776, 3.859771122243123465, -5.613913289150012531 ) ) ;
#40500=FACE_OUTER_BOUND ( 'NONE', #22360, .T. ) ;
#40501=DIRECTION ( 'NONE',  ( 0.000000000000000000, 0.9868265225415254749, 0.1617819965527686754 ) ) ;
#40503=CARTESIAN_POINT ( 'NONE',  ( -27.09048036756548683, 2.083857239072910428, 0.9969423855787087341 ) ) ;
#40505=EDGE_CURVE ( 'NONE', #65658, #18567, #53493, .T. ) ;
#40507=EDGE_LOOP ( 'NONE', ( #52843, #25099, #29993, #8139 ) ) ;
#40509=AXIS2_PLACEMENT_3D ( 'NONE', #5012, #15936, #5681 ) ;
#40513=CARTESIAN_POINT ( 'NONE',  ( 2.000000000000001776, 0.000000000000000000, 0.000000000000000000 ) ) ;
#40519=ORIENTED_EDGE ( 'NONE', *, *, #40473, .T. ) ;
#40526=CARTESIAN_POINT ( 'NONE',  ( -27.32343372485684085, 2.674948176236206621, -1.382463360572536493 ) ) ;
#40537=AXIS2_PLACEMENT_3D ( 'NONE', #57466, #51512, #11249 ) ;
#40538=CARTESIAN_POINT ( 'NONE',  ( -27.09048036756548683, 1.905306051557106084, -1.306202114107871015 ) ) ;
#40552=DIRECTION ( 'NONE',  ( 0.000000000000000000, 0.9868265225415265851, -0.1617819965527619031 ) ) ;
#40554=CIRCLE ( 'NONE', #2366, 2.899999999999995026 ) ;
#40560=CARTESIAN_POINT ( 'NONE',  ( 0.000000000000000000, 0.000000000000000000, 0.000000000000000000 ) ) ;
#40566=VERTEX_POINT ( 'NONE', #48498 ) ;
#40568=CARTESIAN_POINT ( 'NONE',  ( -27.09229696323321335, 0.6397626223479224716, 2.225368503508827978 ) ) ;
#40573=CIRCLE ( 'NONE', #43754, 6.936499999999989008 ) ;
#40574=EDGE_CURVE ( 'NONE', #10064, #8848, #13240, .T. ) ;
#40575=CIRCLE ( 'NONE', #17229, 2.899999999999996803 ) ;
#40580=( BOUNDED_SURFACE ( )  B_SPLINE_SURFACE ( 3, 1, ( 
 ( #43028, #19080 ),
 ( #53353, #13108 ),
 ( #38710, #59651 ),
 ( #58337, #39347 ) ),
 .UNSPECIFIED., .F., .F., .F. ) 
 B_SPLINE_SURFACE_WITH_KNOTS ( ( 4, 4 ),
 ( 2, 2 ),
 ( 0.000000000000000000, 1.000000000000000000 ),
 ( 0.000000000000000000, 1.000000000000000000 ),
 .UNSPECIFIED. ) 
 GEOMETRIC_REPRESENTATION_ITEM ( )  RATIONAL_B_SPLINE_SURFACE ( (
 ( 1.000000000000000000, 1.000000000000000000),
 ( 0.9932032654565553509, 0.8386279382598736953),
 ( 0.9932032654565553509, 0.8386279382598736953),
 ( 1.000000000000000000, 1.000000000000000000) ) ) 
 REPRESENTATION_ITEM ( '' )  SURFACE ( )  );
#40589=CARTESIAN_POINT ( 'NONE',  ( -27.08429572838383947, -0.5764601019425836803, -2.217805374070540125 ) ) ;
#40605=ORIENTED_EDGE ( 'NONE', *, *, #21143, .T. ) ;
#40623=ORIENTED_EDGE ( 'NONE', *, *, #2146, .F. ) ;
#40624=CARTESIAN_POINT ( 'NONE',  ( -22.28939870658739864, 0.2834927284407818271, 3.707376022556837736 ) ) ;
#40629=VERTEX_POINT ( 'NONE', #39143 ) ;
#40635=FACE_OUTER_BOUND ( 'NONE', #55964, .T. ) ;
#40648=ORIENTED_EDGE ( 'NONE', *, *, #10190, .F. ) ;
#40649=AXIS2_PLACEMENT_3D ( 'NONE', #55943, #11050, #30993 ) ;
#40651=ORIENTED_EDGE ( 'NONE', *, *, #57878, .T. ) ;
#40654=CARTESIAN_POINT ( 'NONE',  ( -27.08639648637141306, -2.215564006614440640, 0.6092497698725120037 ) ) ;
#40662=DIRECTION ( 'NONE',  ( -1.000000000000000000, 0.000000000000000000, 0.000000000000000000 ) ) ;
#40667=CARTESIAN_POINT ( 'NONE',  ( -27.09861164373112885, -1.025570525056644033, 2.097104182796081240 ) ) ;
#40674=CYLINDRICAL_SURFACE ( 'NONE', #58320, 7.499999999999988454 ) ;
#40680=CIRCLE ( 'NONE', #16238, 7.499999999999988454 ) ;
#40687=EDGE_CURVE ( 'NONE', #57207, #50893, #10515, .T. ) ;
#40688=CARTESIAN_POINT ( 'NONE',  ( -22.27719443589224113, 3.500848524682622198, 1.139586749255943054 ) ) ;
#40690=CARTESIAN_POINT ( 'NONE',  ( -22.28694879868232803, 3.570244315741564645, -1.011812214896719686 ) ) ;
#40692=CARTESIAN_POINT ( 'NONE',  ( 0.000000000000000000, 0.000000000000000000, 0.000000000000000000 ) ) ;
#40695=ORIENTED_EDGE ( 'NONE', *, *, #32816, .T. ) ;
#40697=AXIS2_PLACEMENT_3D ( 'NONE', #55940, #65567, #60594 ) ;
#40699=EDGE_CURVE ( 'NONE', #47008, #49125, #244, .T. ) ;
#40701=CARTESIAN_POINT ( 'NONE',  ( -22.51237073810381162, -2.986282257334726520, 3.263711251981911143 ) ) ;
#40713=ORIENTED_EDGE ( 'NONE', *, *, #35349, .T. ) ;
#40715=EDGE_LOOP ( 'NONE', ( #59140, #1371, #63082, #54220 ) ) ;
#40716=CARTESIAN_POINT ( 'NONE',  ( -22.27756824490284160, -0.9591204781040139071, 3.555646273932171919 ) ) ;
#40723=CARTESIAN_POINT ( 'NONE',  ( -10.00000000000000178, 0.000000000000000000, 0.000000000000000000 ) ) ;
#40735=DIRECTION ( 'NONE',  ( -1.000000000000000000, 0.000000000000000000, 0.000000000000000000 ) ) ;
#40736=AXIS2_PLACEMENT_3D ( 'NONE', #23117, #38069, #12798 ) ;
#40738=CARTESIAN_POINT ( 'NONE',  ( 0.000000000000000000, 0.000000000000000000, 0.000000000000000000 ) ) ;
#40740=ORIENTED_EDGE ( 'NONE', *, *, #49128, .F. ) ;
#40741=CIRCLE ( 'NONE', #47120, 2.899999999999995026 ) ;
#40742=DIRECTION ( 'NONE',  ( 1.000000000000000000, -0.000000000000000000, -0.000000000000000000 ) ) ;
#40754=B_SPLINE_CURVE_WITH_KNOTS ( 'NONE', 3,
 ( #58957, #27343, #64239, #42620, #22709, #2773, #62925, #18714, #17389, #23032 ),
 .UNSPECIFIED., .F., .F.,
 ( 4, 3, 3, 4 ),
 ( 5.401523115762188335E-05, 0.0008136511341527786004, 0.004068255670953086281, 0.005063778443040916136 ),
 .UNSPECIFIED. ) ;
#40755=CARTESIAN_POINT ( 'NONE',  ( -27.08416781016246588, -2.158663327075695637, -0.7680651426971915052 ) ) ;
#40756=EDGE_CURVE ( 'NONE', #29429, #32831, #16275, .T. ) ;
#40757=B_SPLINE_CURVE_WITH_KNOTS ( 'NONE', 3,
 ( #20338, #60918, #62527, #57909, #42563, #7020, #51930, #31942, #22980, #16988 ),
 .UNSPECIFIED., .F., .F.,
 ( 4, 3, 3, 4 ),
 ( 1.075835082704897855E-17, 6.991367980366405095E-05, 0.0001398269368981362064, 0.0001763147164361797566 ),
 .UNSPECIFIED. ) ;
#40758=VERTEX_POINT ( 'NONE', #31149 ) ;
#40761=VECTOR ( 'NONE', #44800, 1000.000000000000000 ) ;
#40775=DIRECTION ( 'NONE',  ( 0.000000000000000000, 0.000000000000000000, 1.000000000000000000 ) ) ;
#40776=DIRECTION ( 'NONE',  ( -1.000000000000000000, 0.000000000000000000, 0.000000000000000000 ) ) ;
#40777=CARTESIAN_POINT ( 'NONE',  ( -22.27706485742869091, -0.9221835209182183135, -3.563814065926679042 ) ) ;
#40790=DIRECTION ( 'NONE',  ( 0.000000000000000000, 0.8276889981568920085, -0.5611870653623802774 ) ) ;
#40793=CARTESIAN_POINT ( 'NONE',  ( 0.000000000000000000, 6.441884263200846839, -2.217201541069800275 ) ) ;
#40803=CYLINDRICAL_SURFACE ( 'NONE', #9732, 7.499999999999988454 ) ;
#40806=DIRECTION ( 'NONE',  ( -1.000000000000000000, 0.000000000000000000, 0.000000000000000000 ) ) ;
#40807=CARTESIAN_POINT ( 'NONE',  ( -22.27722015946438816, -1.271715168852058708, 3.455127654605140819 ) ) ;
#40811=AXIS2_PLACEMENT_3D ( 'NONE', #30062, #4492, #25088 ) ;
#40812=VECTOR ( 'NONE', #2924, 1000.000000000000000 ) ;
#40813=ORIENTED_EDGE ( 'NONE', *, *, #19973, .T. ) ;
#40815=LINE ( 'NONE', #25181, #57589 ) ;
#40816=DIRECTION ( 'NONE',  ( 0.000000000000000000, 0.000000000000000000, 1.000000000000000000 ) ) ;
#40822=DIRECTION ( 'NONE',  ( 0.000000000000000000, -0.7621620551276424571, 0.6473862847818206978 ) ) ;
#40825=FACE_OUTER_BOUND ( 'NONE', #29203, .T. ) ;
#40834=ORIENTED_EDGE ( 'NONE', *, *, #9218, .F. ) ;
#40845=CARTESIAN_POINT ( 'NONE',  ( 0.000000000000000000, 0.000000000000000000, 0.000000000000000000 ) ) ;
#40846=DIRECTION ( 'NONE',  ( 0.000000000000000000, 0.4198891015602590482, 0.9075754196709595600 ) ) ;
#40848=CARTESIAN_POINT ( 'NONE',  ( -27.20102706715913499, -0.5453431011645057946, 2.585824624629319946 ) ) ;
#40849=AXIS2_PLACEMENT_3D ( 'NONE', #34821, #45159, #65417 ) ;
#40850=B_SPLINE_CURVE_WITH_KNOTS ( 'NONE', 3,
 ( #43371, #53036, #63996, #59340, #18786, #48717 ),
 .UNSPECIFIED., .F., .F.,
 ( 4, 2, 4 ),
 ( 0.0001654224980408358430, 0.0006219428995476486118, 0.001078463301054461299 ),
 .UNSPECIFIED. ) ;
#40854=CARTESIAN_POINT ( 'NONE',  ( -27.10719052120871098, -0.5475695427849570640, 2.295785794152556125 ) ) ;
#40873=DIRECTION ( 'NONE',  ( -1.000000000000000000, 0.000000000000000000, 0.000000000000000000 ) ) ;
#40879=CARTESIAN_POINT ( 'NONE',  ( -35.04834644901396956, -0.007161132384425688939, -0.01183641858480926831 ) ) ;
#40883=CARTESIAN_POINT ( 'NONE',  ( 2.000000000000001776, 0.000000000000000000, 0.000000000000000000 ) ) ;
#40885=CARTESIAN_POINT ( 'NONE',  ( 2.000000000000001776, -1.956810415765224187, 6.654767106875530303 ) ) ;
#40888=CARTESIAN_POINT ( 'NONE',  ( -27.08702828306176258, -2.226264228964706327, -0.5765135930309283063 ) ) ;
#40899=CIRCLE ( 'NONE', #53629, 2.899999999999994582 ) ;
#40901=CARTESIAN_POINT ( 'NONE',  ( -23.18047892478189453, 4.338318103648307833, -2.037851053449307948 ) ) ;
#40902=DIRECTION ( 'NONE',  ( -1.000000000000000000, 0.000000000000000000, 0.000000000000000000 ) ) ;
#40905=EDGE_CURVE ( 'NONE', #24684, #4330, #59803, .T. ) ;
#40912=LINE ( 'NONE', #25955, #52533 ) ;
#40915=ORIENTED_EDGE ( 'NONE', *, *, #43712, .T. ) ;
#40916=CARTESIAN_POINT ( 'NONE',  ( 0.000000000000000000, -1.865193240757140991, 6.552473556515165498 ) ) ;
#40922=CARTESIAN_POINT ( 'NONE',  ( 2.000000000000001776, 6.606214214351074254, 2.114938770769925647 ) ) ;
#40937=VECTOR ( 'NONE', #14325, 1000.000000000000000 ) ;
#40941=CARTESIAN_POINT ( 'NONE',  ( -16.00005080000000035, 0.000000000000000000, -2.999999999999995559 ) ) ;
#40945=VERTEX_POINT ( 'NONE', #5494 ) ;
#40947=EDGE_LOOP ( 'NONE', ( #30962, #54725, #10961, #50370 ) ) ;
#40950=ORIENTED_EDGE ( 'NONE', *, *, #101, .F. ) ;
#40953=ORIENTED_EDGE ( 'NONE', *, *, #23288, .T. ) ;
#40963=DIRECTION ( 'NONE',  ( -1.000000000000000000, 0.000000000000000000, 0.000000000000000000 ) ) ;
#40964=AXIS2_PLACEMENT_3D ( 'NONE', #35392, #51038, #50710 ) ;
#40974=CARTESIAN_POINT ( 'NONE',  ( -22.51237073810381162, -4.418556976583611906, 0.2145858836692225990 ) ) ;
#40985=CYLINDRICAL_SURFACE ( 'NONE', #56074, 2.899999999999994582 ) ;
#40995=CARTESIAN_POINT ( 'NONE',  ( 2.000000000000001776, 0.000000000000000000, 0.000000000000000000 ) ) ;
#41000=CARTESIAN_POINT ( 'NONE',  ( 2.000000000000001776, -1.018311147294094443, -6.861346417234492456 ) ) ;
#41003=CARTESIAN_POINT ( 'NONE',  ( 0.000000000000000000, 0.7281529553923131726, -7.464569195442812166 ) ) ;
#41005=ADVANCED_FACE ( 'NONE', ( #56008 ), #15514, .F. ) ;
#41008=ORIENTED_EDGE ( 'NONE', *, *, #54595, .T. ) ;
#41009=LINE ( 'NONE', #31034, #46093 ) ;
#41010=CARTESIAN_POINT ( 'NONE',  ( -22.27718112499583469, 3.412978993569800057, 1.380338971069110521 ) ) ;
#41011=CARTESIAN_POINT ( 'NONE',  ( -22.28169757117799321, 3.561623073126538586, -0.9841724999439870336 ) ) ;
#41018=EDGE_CURVE ( 'NONE', #12415, #10704, #19505, .T. ) ;
#41023=DIRECTION ( 'NONE',  ( -1.000000000000000000, 0.000000000000000000, 0.000000000000000000 ) ) ;
#41031=DIRECTION ( 'NONE',  ( 0.000000000000000000, 0.000000000000000000, 1.000000000000000000 ) ) ;
#41035=CARTESIAN_POINT ( 'NONE',  ( -22.28856623400852399, -0.9049353338066428165, 3.603818606161804716 ) ) ;
#41039=CIRCLE ( 'NONE', #51703, 2.899999999999996803 ) ;
#41041=DIRECTION ( 'NONE',  ( -1.000000000000000000, 0.000000000000000000, 0.000000000000000000 ) ) ;
#41046=LINE ( 'NONE', #46059, #57130 ) ;
#41050=CARTESIAN_POINT ( 'NONE',  ( 2.000000000000001776, 0.000000000000000000, 0.000000000000000000 ) ) ;
#41052=CARTESIAN_POINT ( 'NONE',  ( -22.29570301036918423, 0.8918611685731360206, -3.629130197778208888 ) ) ;
#41066=B_SPLINE_CURVE_WITH_KNOTS ( 'NONE', 3,
 ( #44451, #18234, #38501, #54128, #53811, #2949 ),
 .UNSPECIFIED., .F., .F.,
 ( 4, 2, 4 ),
 ( 0.0001654224980408265460, 0.0006219428995476446002, 0.001078463301054462817 ),
 .UNSPECIFIED. ) ;
#41074=CIRCLE ( 'NONE', #30446, 6.936499999999989896 ) ;
#41084=FACE_OUTER_BOUND ( 'NONE', #54663, .T. ) ;
#41092=CARTESIAN_POINT ( 'NONE',  ( -27.08704841010891684, 1.313007237775888125, 1.888108843317890528 ) ) ;
#41110=EDGE_LOOP ( 'NONE', ( #60005, #29098, #9291, #33519 ) ) ;
#41111=ORIENTED_EDGE ( 'NONE', *, *, #52632, .F. ) ;
#41115=DIRECTION ( 'NONE',  ( -1.000000000000000000, 0.000000000000000000, 0.000000000000000000 ) ) ;
#41119=CARTESIAN_POINT ( 'NONE',  ( -27.09602251845159415, 1.018053071731315429, -2.092130925171141076 ) ) ;
#41131=CARTESIAN_POINT ( 'NONE',  ( 0.000000000000000000, 0.000000000000000000, 0.000000000000000000 ) ) ;
#41132=DIRECTION ( 'NONE',  ( -1.000000000000000000, 0.000000000000000000, 0.000000000000000000 ) ) ;
#41135=EDGE_CURVE ( 'NONE', #14636, #59375, #62959, .T. ) ;
#41146=CARTESIAN_POINT ( 'NONE',  ( -35.04643116707788408, -0.004425962698862209721, 0.01135624435143547939 ) ) ;
#41149=CARTESIAN_POINT ( 'NONE',  ( -27.32337605527167312, -0.3676050637290663725, 2.988381643048326097 ) ) ;
#41152=DIRECTION ( 'NONE',  ( 0.000000000000000000, -0.6876994588534296460, 0.7259954919231248471 ) ) ;
#41156=CARTESIAN_POINT ( 'NONE',  ( -27.10512513516321320, -0.5469390009827510557, 2.289566223069553708 ) ) ;
#41159=DIRECTION ( 'NONE',  ( 1.000000000000000000, 0.000000000000000000, 0.000000000000000000 ) ) ;
#41165=VERTEX_POINT ( 'NONE', #27706 ) ;
#41166=AXIS2_PLACEMENT_3D ( 'NONE', #14375, #60585, #44619 ) ;
#41169=ORIENTED_EDGE ( 'NONE', *, *, #52465, .T. ) ;
#41170=CARTESIAN_POINT ( 'NONE',  ( 2.000000000000001776, 0.000000000000000000, 0.000000000000000000 ) ) ;
#41173=CARTESIAN_POINT ( 'NONE',  ( -27.15511094194038222, 2.092607239484540749, -1.375165223101512346 ) ) ;
#41174=CARTESIAN_POINT ( 'NONE',  ( 0.000000000000000000, -6.664893814313694875, -3.439359016433563898 ) ) ;
#41176=ORIENTED_EDGE ( 'NONE', *, *, #17340, .F. ) ;
#41177=EDGE_CURVE ( 'NONE', #23637, #20211, #49237, .T. ) ;
#41181=CARTESIAN_POINT ( 'NONE',  ( -22.27711351828769892, 2.547249869018266999, 2.657880562424656201 ) ) ;
#41200=ORIENTED_EDGE ( 'NONE', *, *, #962, .F. ) ;
#41214=DIRECTION ( 'NONE',  ( -1.000000000000000000, 0.000000000000000000, 0.000000000000000000 ) ) ;
#41235=AXIS2_PLACEMENT_3D ( 'NONE', #29844, #55125, #4930 ) ;
#41237=VECTOR ( 'NONE', #23649, 1000.000000000000000 ) ;
#41238=CARTESIAN_POINT ( 'NONE',  ( -35.04660725145885891, -0.008590646501108684455, -0.008800808525128425361 ) ) ;
#41240=CARTESIAN_POINT ( 'NONE',  ( -27.08416781016246588, 1.744495588874932279, -1.485424708116795722 ) ) ;
#41244=ORIENTED_EDGE ( 'NONE', *, *, #36690, .F. ) ;
#41247=CIRCLE ( 'NONE', #25310, 2.899999999999994582 ) ;
#41265=DIRECTION ( 'NONE',  ( -1.000000000000000000, 0.000000000000000000, 0.000000000000000000 ) ) ;
#41277=CARTESIAN_POINT ( 'NONE',  ( 2.000000000000001776, -6.812627895098285258, -0.04423456934733380197 ) ) ;
#41280=CARTESIAN_POINT ( 'NONE',  ( 2.000000000000001776, -3.155844197800145690, 6.177028383390419819 ) ) ;
#41281=CARTESIAN_POINT ( 'NONE',  ( 0.000000000000000000, -7.248432822490255667, 1.926193556692974429 ) ) ;
#41282=CARTESIAN_POINT ( 'NONE',  ( -27.09150307427447402, -0.1754204729056269008, -2.306459590995633135 ) ) ;
#41293=CARTESIAN_POINT ( 'NONE',  ( -27.08429572838383947, -2.279961732801590646, 0.2296550094122822017 ) ) ;
#41294=LINE ( 'NONE', #52292, #23829 ) ;
#41295=CARTESIAN_POINT ( 'NONE',  ( 2.000000000000001776, -5.396716205731451943, 4.158041573745051345 ) ) ;
#41306=ADVANCED_FACE ( 'NONE', ( #421 ), #60263, .T. ) ;
#41309=CARTESIAN_POINT ( 'NONE',  ( -27.08579483061179261, -0.9690219683526719585, 2.081508743190592092 ) ) ;
#41310=FACE_OUTER_BOUND ( 'NONE', #54660, .T. ) ;
#41311=CARTESIAN_POINT ( 'NONE',  ( 0.000000000000000000, -6.606214214351077807, 2.114938770769887455 ) ) ;
#41316=CARTESIAN_POINT ( 'NONE',  ( -23.18047892478189098, -2.738168160732679990, 3.933989833240137290 ) ) ;
#41317=AXIS2_PLACEMENT_3D ( 'NONE', #23813, #54722, #44378 ) ;
#41322=ORIENTED_EDGE ( 'NONE', *, *, #64471, .F. ) ;
#41323=CONICAL_SURFACE ( 'NONE', #23317, 2.214855479030549468, 1.249045772030607848 ) ;
#41325=CARTESIAN_POINT ( 'NONE',  ( 2.000000000000001776, 4.604744433234757572, -5.919993978425451608 ) ) ;
#41329=DIRECTION ( 'NONE',  ( -1.000000000000000000, 0.000000000000000000, 0.000000000000000000 ) ) ;
#41330=ORIENTED_EDGE ( 'NONE', *, *, #30145, .T. ) ;
#41335=CARTESIAN_POINT ( 'NONE',  ( -27.35552965826136429, -1.320216934008378473, -2.810569013793753346 ) ) ;
#41336=ADVANCED_FACE ( 'NONE', ( #40635 ), #54654, .T. ) ;
#41339=CARTESIAN_POINT ( 'NONE',  ( -22.27710395300133328, -3.562137928983395874, 0.9291085174899338384 ) ) ;
#41341=CARTESIAN_POINT ( 'NONE',  ( 1.000000000000000888, 0.08317740279931498670, 7.499538753794337431 ) ) ;
#41343=( BOUNDED_SURFACE ( )  B_SPLINE_SURFACE ( 3, 1, ( 
 ( #45013, #55655 ),
 ( #39694, #10090 ),
 ( #54979, #50666 ),
 ( #9407, #29696 ) ),
 .UNSPECIFIED., .F., .F., .F. ) 
 B_SPLINE_SURFACE_WITH_KNOTS ( ( 4, 4 ),
 ( 2, 2 ),
 ( 0.000000000000000000, 1.000000000000000000 ),
 ( 0.000000000000000000, 1.000000000000000000 ),
 .UNSPECIFIED. ) 
 GEOMETRIC_REPRESENTATION_ITEM ( )  RATIONAL_B_SPLINE_SURFACE ( (
 ( 1.000000000000000000, 1.000000000000000000),
 ( 0.8716676215708681896, 0.8964445200148167814),
 ( 0.8716676215708681896, 0.8964445200148167814),
 ( 1.000000000000000000, 1.000000000000000000) ) ) 
 REPRESENTATION_ITEM ( '' )  SURFACE ( )  );
#41359=ORIENTED_EDGE ( 'NONE', *, *, #8194, .T. ) ;
#41362=CARTESIAN_POINT ( 'NONE',  ( 2.000000000000001776, -6.935703035393428806, -0.1051458740708305362 ) ) ;
#41363=ORIENTED_EDGE ( 'NONE', *, *, #21347, .F. ) ;
#41366=EDGE_LOOP ( 'NONE', ( #49921, #61448, #1500, #3485 ) ) ;
#41372=CYLINDRICAL_SURFACE ( 'NONE', #9315, 2.899999999999994582 ) ;
#41373=EDGE_CURVE ( 'NONE', #34813, #39295, #4088, .T. ) ;
#41377=CARTESIAN_POINT ( 'NONE',  ( -22.27709082389155171, -0.8996430462092220859, -3.569727173833839640 ) ) ;
#41379=ORIENTED_EDGE ( 'NONE', *, *, #39929, .F. ) ;
#41381=VECTOR ( 'NONE', #36609, 1000.000000000000000 ) ;
#41382=EDGE_CURVE ( 'NONE', #9789, #30228, #4722, .T. ) ;
#41388=FACE_OUTER_BOUND ( 'NONE', #63217, .T. ) ;
#41390=CARTESIAN_POINT ( 'NONE',  ( -27.20164183316782314, 2.339520810540427043, 1.232966507052623895 ) ) ;
#41401=ORIENTED_EDGE ( 'NONE', *, *, #30529, .F. ) ;
#41403=DIRECTION ( 'NONE',  ( 0.000000000000000000, 0.7621620551276332423, 0.6473862847818313560 ) ) ;
#41404=DIRECTION ( 'NONE',  ( -1.000000000000000000, 0.000000000000000000, 0.000000000000000000 ) ) ;
#41408=LINE ( 'NONE', #55750, #34155 ) ;
#41434=CARTESIAN_POINT ( 'NONE',  ( -22.27721688985630522, -1.293557211780054006, 3.446999288411557227 ) ) ;
#41435=ORIENTED_EDGE ( 'NONE', *, *, #50095, .T. ) ;
#41436=ORIENTED_EDGE ( 'NONE', *, *, #13501, .T. ) ;
#41441=CARTESIAN_POINT ( 'NONE',  ( -27.08935880048753120, 0.5666837974575801296, -2.235999130317600336 ) ) ;
#41442=CARTESIAN_POINT ( 'NONE',  ( 1.000000000000000888, 1.693411908627200146, 7.306323022404582979 ) ) ;
#41443=CARTESIAN_POINT ( 'NONE',  ( -27.08506889328327816, 0.9597901767732768263, -2.083363953276920366 ) ) ;
#41444=CARTESIAN_POINT ( 'NONE',  ( -35.05175862995318425, -0.008949502803497905168, -0.008837625261055859216 ) ) ;
#41460=ORIENTED_EDGE ( 'NONE', *, *, #23344, .T. ) ;
#41461=VECTOR ( 'NONE', #37746, 1000.000000000000000 ) ;
#41472=CARTESIAN_POINT ( 'NONE',  ( 2.000000000000001776, 3.224464355699941720, -6.771471746881976728 ) ) ;
#41474=ADVANCED_FACE ( 'NONE', ( #32850 ), #63132, .T. ) ;
#41483=CARTESIAN_POINT ( 'NONE',  ( -35.04660725145885891, -0.01123650152077631907, -0.004999447127077803754 ) ) ;
#41486=CIRCLE ( 'NONE', #3327, 6.936499999999989008 ) ;
#41494=AXIS2_PLACEMENT_3D ( 'NONE', #44547, #64507, #23978 ) ;
#41495=CARTESIAN_POINT ( 'NONE',  ( -27.08423923533013422, -2.274768056034772279, 0.2759775751761906482 ) ) ;
#41496=FACE_OUTER_BOUND ( 'NONE', #19835, .T. ) ;
#41502=CARTESIAN_POINT ( 'NONE',  ( 0.000000000000000000, 0.000000000000000000, 0.000000000000000000 ) ) ;
#41512=EDGE_CURVE ( 'NONE', #15981, #14636, #7884, .T. ) ;
#41520=ORIENTED_EDGE ( 'NONE', *, *, #53241, .F. ) ;
#41527=ORIENTED_EDGE ( 'NONE', *, *, #62145, .T. ) ;
#41529=CIRCLE ( 'NONE', #106, 2.899999999999994582 ) ;
#41532=AXIS2_PLACEMENT_3D ( 'NONE', #44273, #64541, #19016 ) ;
#41537=CIRCLE ( 'NONE', #29854, 6.936499999999989008 ) ;
#41541=DIRECTION ( 'NONE',  ( -1.000000000000000000, 0.000000000000000000, 0.000000000000000000 ) ) ;
#41542=CARTESIAN_POINT ( 'NONE',  ( -27.10307689719060065, 0.6678239540327367552, 2.250862122746719152 ) ) ;
#41546=CARTESIAN_POINT ( 'NONE',  ( -27.08429572838383947, -0.2296550094122856711, -2.279961732801603080 ) ) ;
#41548=CARTESIAN_POINT ( 'NONE',  ( 2.000000000000001776, 3.859771122243047081, 5.613913289150030295 ) ) ;
#41549=EDGE_CURVE ( 'NONE', #25350, #4916, #29094, .T. ) ;
#41558=CARTESIAN_POINT ( 'NONE',  ( -27.10113028276028402, -0.6639289823109559840, -2.245923868550880886 ) ) ;
#41560=CARTESIAN_POINT ( 'NONE',  ( -35.05175862995318425, -0.01216930940958933782, -0.003178856583451253326 ) ) ;
#41561=ORIENTED_EDGE ( 'NONE', *, *, #6307, .T. ) ;
#41569=CIRCLE ( 'NONE', #26718, 7.499999999999988454 ) ;
#41572=CARTESIAN_POINT ( 'NONE',  ( -22.27384469013076185, 0.3730095848193410446, 3.663183248998782116 ) ) ;
#41581=VECTOR ( 'NONE', #45093, 1000.000000000000000 ) ;
#41594=CARTESIAN_POINT ( 'NONE',  ( 2.000000000000001776, 1.058508696395052517, -6.730038252034905355 ) ) ;
#41596=CARTESIAN_POINT ( 'NONE',  ( 2.000000000000001776, -6.662861565602071323, 1.421313227905616650 ) ) ;
#41608=EDGE_CURVE ( 'NONE', #42144, #23300, #59784, .T. ) ;
#41612=DIRECTION ( 'NONE',  ( 1.000000000000000000, -0.000000000000000000, -0.000000000000000000 ) ) ;
#41622=VERTEX_POINT ( 'NONE', #44158 ) ;
#41623=CARTESIAN_POINT ( 'NONE',  ( 2.000000000000001776, -6.883677378339461583, 0.8544109087185534079 ) ) ;
#41625=CARTESIAN_POINT ( 'NONE',  ( 2.000000000000001776, 1.865193240757184290, -6.552473556515182374 ) ) ;
#41637=AXIS2_PLACEMENT_3D ( 'NONE', #61346, #22101, #37392 ) ;
#41640=CIRCLE ( 'NONE', #1319, 6.936499999999989896 ) ;
#41646=CARTESIAN_POINT ( 'NONE',  ( -27.09150307427400861, -1.001311209615671549, 2.085162835056704189 ) ) ;
#41649=CARTESIAN_POINT ( 'NONE',  ( 2.000000000000001776, 2.480520636974191895, 6.345145617221231049 ) ) ;
#41667=B_SPLINE_CURVE_WITH_KNOTS ( 'NONE', 3,
 ( #65048, #49775, #24489, #19525, #57061, #30461, #6195, #863, #1202, #25154, #557, #60733, #31760, #50757, #15167, #62047, #45423, #40431, #5886 ),
 .UNSPECIFIED., .F., .F.,
 ( 4, 3, 3, 3, 3, 3, 4 ),
 ( 0.000000000000000000, 2.832085443540566458E-05, 4.217789847394524017E-05, 5.603488375045718604E-05, 6.989180858578818178E-05, 9.821094829918303128E-05, 0.0001178165571465086142 ),
 .UNSPECIFIED. ) ;
#41669=CARTESIAN_POINT ( 'NONE',  ( -22.70624764888619751, -3.282666355490664767, 4.097886656202270217 ) ) ;
#41672=EDGE_LOOP ( 'NONE', ( #19059, #25260, #43711, #51599 ) ) ;
#41680=DIRECTION ( 'NONE',  ( -1.000000000000000000, 0.000000000000000000, 0.000000000000000000 ) ) ;
#41684=AXIS2_PLACEMENT_3D ( 'NONE', #21979, #26312, #32275 ) ;
#41687=DIRECTION ( 'NONE',  ( -1.000000000000000000, 0.000000000000000000, 0.000000000000000000 ) ) ;
#41690=EDGE_CURVE ( 'NONE', #54252, #59964, #54841, .T. ) ;
#41695=CYLINDRICAL_SURFACE ( 'NONE', #2950, 7.499999999999988454 ) ;
#41698=ORIENTED_EDGE ( 'NONE', *, *, #1759, .F. ) ;
#41705=ORIENTED_EDGE ( 'NONE', *, *, #13511, .F. ) ;
#41716=AXIS2_PLACEMENT_3D ( 'NONE', #25645, #1037, #14994 ) ;
#41729=CARTESIAN_POINT ( 'NONE',  ( -22.27834755396594346, 2.305389312780943278, 2.876353066242370637 ) ) ;
#41735=DIRECTION ( 'NONE',  ( -1.000000000000000000, 0.000000000000000000, 0.000000000000000000 ) ) ;
#41736=CARTESIAN_POINT ( 'NONE',  ( 0.000000000000000000, 6.767909380267608022, -0.7805499053121014441 ) ) ;
#41760=DIRECTION ( 'NONE',  ( 0.000000000000000000, 0.8276889981568879007, 0.5611870653623863836 ) ) ;
#41778=ORIENTED_EDGE ( 'NONE', *, *, #60290, .F. ) ;
#41782=VERTEX_POINT ( 'NONE', #14891 ) ;
#41787=LINE ( 'NONE', #62382, #34744 ) ;
#41789=DIRECTION ( 'NONE',  ( -0.9582930651793754029, 0.08045274594386021827, 0.2742293873734361065 ) ) ;
#41790=AXIS2_PLACEMENT_3D ( 'NONE', #6298, #58145, #26899 ) ;
#41795=ORIENTED_EDGE ( 'NONE', *, *, #6838, .T. ) ;
#41796=CARTESIAN_POINT ( 'NONE',  ( 0.000000000000000000, -0.4804830611969332366, -6.919838746524582085 ) ) ;
#41797=CARTESIAN_POINT ( 'NONE',  ( -22.27384469013076185, -2.625926801827875412, 2.581192766446261722 ) ) ;
#41812=AXIS2_PLACEMENT_3D ( 'NONE', #1008, #21275, #15624 ) ;
#41817=CIRCLE ( 'NONE', #36505, 2.899999999999995026 ) ;
#41818=CARTESIAN_POINT ( 'NONE',  ( 0.000000000000000000, 0.000000000000000000, 0.000000000000000000 ) ) ;
#41837=ORIENTED_EDGE ( 'NONE', *, *, #28374, .F. ) ;
#41848=AXIS2_PLACEMENT_3D ( 'NONE', #32244, #32554, #31280 ) ;
#41850=CARTESIAN_POINT ( 'NONE',  ( 2.000000000000001776, 0.000000000000000000, 0.000000000000000000 ) ) ;
#41852=DIRECTION ( 'NONE',  ( 0.000000000000000000, 0.9635499925192219095, 0.2675283385292248073 ) ) ;
#41855=CARTESIAN_POINT ( 'NONE',  ( -27.08639648637162622, 1.635407781268146898, 1.614109828501612443 ) ) ;
#41857=CARTESIAN_POINT ( 'NONE',  ( 0.000000000000000000, 7.493043167941614513, -0.3229614270519962638 ) ) ;
#41858=CARTESIAN_POINT ( 'NONE',  ( -22.71097035706202760, 2.846599994298365743, -4.089776368546553798 ) ) ;
#41859=B_SPLINE_CURVE_WITH_KNOTS ( 'NONE', 3,
 ( #49602, #55572, #19982, #64859, #39607, #50262 ),
 .UNSPECIFIED., .F., .F.,
 ( 4, 2, 4 ),
 ( 0.000000000000000000, 0.0004528561986909411031, 0.0009057123973818822062 ),
 .UNSPECIFIED. ) ;
#41863=CARTESIAN_POINT ( 'NONE',  ( 0.000000000000000000, 4.962980376314068742, 4.846014654777798469 ) ) ;
#41869=ORIENTED_EDGE ( 'NONE', *, *, #44775, .F. ) ;
#41871=CARTESIAN_POINT ( 'NONE',  ( 2.000000000000001776, 0.000000000000000000, 0.000000000000000000 ) ) ;
#41877=DIRECTION ( 'NONE',  ( 0.000000000000000000, 0.000000000000000000, 1.000000000000000000 ) ) ;
#41883=CARTESIAN_POINT ( 'NONE',  ( 1.000000000000000888, 6.253963800348318003, -4.139799123620975685 ) ) ;
#41888=ADVANCED_FACE ( 'NONE', ( #16883 ), #18062, .F. ) ;
#41891=EDGE_CURVE ( 'NONE', #47105, #44216, #27006, .T. ) ;
#41896=CYLINDRICAL_SURFACE ( 'NONE', #61503, 6.936499999999988120 ) ;
#41906=CARTESIAN_POINT ( 'NONE',  ( -28.66013792860432119, -1.071635578228289587, -1.490739498621034720 ) ) ;
#41912=VERTEX_POINT ( 'NONE', #57465 ) ;
#41934=ORIENTED_EDGE ( 'NONE', *, *, #8270, .F. ) ;
#41936=DIRECTION ( 'NONE',  ( -1.000000000000000000, 0.000000000000000000, 0.000000000000000000 ) ) ;
#41943=CARTESIAN_POINT ( 'NONE',  ( 0.000000000000000000, -5.107597897712309098, -4.693343793638478978 ) ) ;
#41952=EDGE_CURVE ( 'NONE', #46346, #60499, #54445, .T. ) ;
#41957=CARTESIAN_POINT ( 'NONE',  ( 0.000000000000000000, -6.777474576704061171, -0.6925993764991672519 ) ) ;
#41962=EDGE_CURVE ( 'NONE', #16830, #21918, #23189, .T. ) ;
#41964=FACE_OUTER_BOUND ( 'NONE', #15036, .T. ) ;
#41966=EDGE_CURVE ( 'NONE', #32375, #61727, #38477, .T. ) ;
#41971=CIRCLE ( 'NONE', #6963, 7.499999999999988454 ) ;
#41983=FACE_OUTER_BOUND ( 'NONE', #33031, .T. ) ;
#41993=ORIENTED_EDGE ( 'NONE', *, *, #53889, .F. ) ;
#41996=CARTESIAN_POINT ( 'NONE',  ( -27.08429572838383947, -1.859677275556421927, 1.338867938658193424 ) ) ;
#42003=ORIENTED_EDGE ( 'NONE', *, *, #38711, .F. ) ;
#42006=CARTESIAN_POINT ( 'NONE',  ( -22.71097035706202405, -4.965150228107763297, -0.4203397252017324615 ) ) ;
#42009=CARTESIAN_POINT ( 'NONE',  ( 0.000000000000000000, 0.000000000000000000, 0.000000000000000000 ) ) ;
#42012=ADVANCED_FACE ( 'NONE', ( #54101 ), #49137, .T. ) ;
#42018=ORIENTED_EDGE ( 'NONE', *, *, #7441, .T. ) ;
#42027=B_SPLINE_CURVE_WITH_KNOTS ( 'NONE', 3,
 ( #31303, #45947, #35621, #56919, #10347, #36615 ),
 .UNSPECIFIED., .F., .F.,
 ( 4, 2, 4 ),
 ( 0.0002637379172192601240, 0.0009975831966643354445, 0.001731428476109410711 ),
 .UNSPECIFIED. ) ;
#42031=CARTESIAN_POINT ( 'NONE',  ( 0.000000000000000000, -6.201547234537033937, 2.820401998297862978 ) ) ;
#42046=ADVANCED_FACE ( 'NONE', ( #55074 ), #30768, .T. ) ;
#42051=DIRECTION ( 'NONE',  ( 0.000000000000000000, 0.000000000000000000, 1.000000000000000000 ) ) ;
#42057=VERTEX_POINT ( 'NONE', #55745 ) ;
#42074=FACE_OUTER_BOUND ( 'NONE', #17651, .T. ) ;
#42076=CYLINDRICAL_SURFACE ( 'NONE', #24467, 1.499999999999997780 ) ;
#42077=DIRECTION ( 'NONE',  ( -1.000000000000000000, 0.000000000000000000, 0.000000000000000000 ) ) ;
#42083=ORIENTED_EDGE ( 'NONE', *, *, #62442, .T. ) ;
#42084=EDGE_CURVE ( 'NONE', #19513, #50728, #3679, .T. ) ;
#42091=VERTEX_POINT ( 'NONE', #25469 ) ;
#42100=DIRECTION ( 'NONE',  ( -1.000000000000000000, 0.000000000000000000, 0.000000000000000000 ) ) ;
#42101=CARTESIAN_POINT ( 'NONE',  ( -22.51237073810381517, 0.9543406717316886834, -4.319597983500836236 ) ) ;
#42103=VERTEX_POINT ( 'NONE', #56051 ) ;
#42110=DIRECTION ( 'NONE',  ( 0.000000000000000000, 0.9635499925192219095, 0.2675283385292248073 ) ) ;
#42111=VECTOR ( 'NONE', #16008, 1000.000000000000000 ) ;
#42115=VERTEX_POINT ( 'NONE', #4883 ) ;
#42116=CARTESIAN_POINT ( 'NONE',  ( -27.09364415740217424, 0.1694361397562917371, 2.313349100776200817 ) ) ;
#42117=CIRCLE ( 'NONE', #21964, 7.499999999999988454 ) ;
#42118=EDGE_CURVE ( 'NONE', #4847, #15301, #65685, .T. ) ;
#42122=DIRECTION ( 'NONE',  ( -1.000000000000000000, 0.000000000000000000, 0.000000000000000000 ) ) ;
#42124=FACE_OUTER_BOUND ( 'NONE', #31332, .T. ) ;
#42128=CARTESIAN_POINT ( 'NONE',  ( -26.43258404273187878, 0.2934201954354447306, -3.465947334857406137 ) ) ;
#42129=DIRECTION ( 'NONE',  ( 1.000000000000000000, 1.685093406416449860E-16, -1.011030131491573426E-17 ) ) ;
#42141=ORIENTED_EDGE ( 'NONE', *, *, #27020, .T. ) ;
#42144=VERTEX_POINT ( 'NONE', #52061 ) ;
#42155=VERTEX_POINT ( 'NONE', #20815 ) ;
#42156=AXIS2_PLACEMENT_3D ( 'NONE', #47850, #27554, #16612 ) ;
#42158=DIRECTION ( 'NONE',  ( -1.000000000000000000, 0.000000000000000000, 0.000000000000000000 ) ) ;
#42163=ORIENTED_EDGE ( 'NONE', *, *, #50921, .T. ) ;
#42164=CARTESIAN_POINT ( 'NONE',  ( -22.31328051695926007, -0.8849444482787947042, 3.685074213229300621 ) ) ;
#42166=CARTESIAN_POINT ( 'NONE',  ( -10.00000000000000178, 0.000000000000000000, 0.000000000000000000 ) ) ;
#42167=ORIENTED_EDGE ( 'NONE', *, *, #43297, .T. ) ;
#42168=ORIENTED_EDGE ( 'NONE', *, *, #29050, .F. ) ;
#42175=CARTESIAN_POINT ( 'NONE',  ( -22.27706485742869091, -2.625261754997692876, 2.580541389029905819 ) ) ;
#42204=CARTESIAN_POINT ( 'NONE',  ( 2.000000000000001776, 0.000000000000000000, 0.000000000000000000 ) ) ;
#42209=AXIS2_PLACEMENT_3D ( 'NONE', #12961, #3338, #48555 ) ;
#42215=EDGE_CURVE ( 'NONE', #43782, #29713, #2633, .T. ) ;
#42221=EDGE_CURVE ( 'NONE', #46041, #23282, #21128, .T. ) ;
#42222=VERTEX_POINT ( 'NONE', #21817 ) ;
#42229=ORIENTED_EDGE ( 'NONE', *, *, #18876, .T. ) ;
#42244=LINE ( 'NONE', #11674, #19186 ) ;
#42253=DIRECTION ( 'NONE',  ( 0.000000000000000000, -0.3193015301359669600, -0.9476531711828067861 ) ) ;
#42257=ORIENTED_EDGE ( 'NONE', *, *, #31788, .F. ) ;
#42266=ORIENTED_EDGE ( 'NONE', *, *, #26475, .T. ) ;
#42286=ORIENTED_EDGE ( 'NONE', *, *, #18498, .F. ) ;
#42291=EDGE_CURVE ( 'NONE', #28521, #58714, #30830, .T. ) ;
#42294=ORIENTED_EDGE ( 'NONE', *, *, #33182, .F. ) ;
#42296=EDGE_CURVE ( 'NONE', #57422, #19640, #27427, .T. ) ;
#42297=ORIENTED_EDGE ( 'NONE', *, *, #26904, .F. ) ;
#42303=ADVANCED_FACE ( 'NONE', ( #42713 ), #22795, .T. ) ;
#42306=CARTESIAN_POINT ( 'NONE',  ( 0.000000000000000000, 5.860254403322073813, -3.474373880649762381 ) ) ;
#42308=DIRECTION ( 'NONE',  ( 0.000000000000000000, 0.000000000000000000, 1.000000000000000000 ) ) ;
#42311=AXIS2_PLACEMENT_3D ( 'NONE', #512, #824, #26104 ) ;
#42317=DIRECTION ( 'NONE',  ( -1.000000000000000000, 0.000000000000000000, 0.000000000000000000 ) ) ;
#42334=VERTEX_POINT ( 'NONE', #59339 ) ;
#42336=VECTOR ( 'NONE', #34181, 1000.000000000000000 ) ;
#42337=ORIENTED_EDGE ( 'NONE', *, *, #46016, .F. ) ;
#42342=DIRECTION ( 'NONE',  ( -1.000000000000000000, 0.000000000000000000, 0.000000000000000000 ) ) ;
#42344=CARTESIAN_POINT ( 'NONE',  ( -22.27722019117889474, -0.6494988092404023750, -3.623917154020615428 ) ) ;
#42346=CARTESIAN_POINT ( 'NONE',  ( 2.000000000000001776, -5.662015959325215952, 4.918493191653933394 ) ) ;
#42380=CARTESIAN_POINT ( 'NONE',  ( 2.000000000000001776, -1.865193240757140991, 6.552473556515165498 ) ) ;
#42390=VERTEX_POINT ( 'NONE', #45028 ) ;
#42391=CARTESIAN_POINT ( 'NONE',  ( -22.27722015946439171, 2.356370737780168589, 2.828901469906451194 ) ) ;
#42397=FACE_OUTER_BOUND ( 'NONE', #21923, .T. ) ;
#42398=EDGE_CURVE ( 'NONE', #15301, #42144, #2179, .T. ) ;
#42403=CARTESIAN_POINT ( 'NONE',  ( -27.08429572838383947, 0.9410937941434112108, -2.089332284968719922 ) ) ;
#42406=AXIS2_PLACEMENT_3D ( 'NONE', #50341, #10390, #56628 ) ;
#42411=DIRECTION ( 'NONE',  ( -1.000000000000000000, 0.000000000000000000, 0.000000000000000000 ) ) ;
#42420=CIRCLE ( 'NONE', #13757, 2.899999999999995470 ) ;
#42428=CIRCLE ( 'NONE', #40349, 6.936499999999989896 ) ;
#42429=DIRECTION ( 'NONE',  ( -1.000000000000000000, 0.000000000000000000, 0.000000000000000000 ) ) ;
#42436=FACE_OUTER_BOUND ( 'NONE', #61000, .T. ) ;
#42440=ORIENTED_EDGE ( 'NONE', *, *, #11273, .F. ) ;
#42442=CARTESIAN_POINT ( 'NONE',  ( 2.000000000000001776, 0.000000000000000000, 0.000000000000000000 ) ) ;
#42444=CARTESIAN_POINT ( 'NONE',  ( -26.74023318801843985, 0.2829279580742273259, -3.342010596062600758 ) ) ;
#42450=VERTEX_POINT ( 'NONE', #46344 ) ;
#42461=B_SPLINE_CURVE_WITH_KNOTS ( 'NONE', 3,
 ( #42800, #17552, #46573, #43123, #58790, #18205, #2608, #36256, #41240, #3246, #8218, #61524, #13209, #37822, #7905, #6349 ),
 .UNSPECIFIED., .F., .F.,
 ( 4, 3, 3, 3, 3, 4 ),
 ( 0.000000000000000000, 6.991367980366399674E-05, 0.0001398269368981363962, 0.0002097400188389094984, 0.0002811534801551362150, 0.0003526297678872492578 ),
 .UNSPECIFIED. ) ;
#42465=ORIENTED_EDGE ( 'NONE', *, *, #20060, .T. ) ;
#42468=CARTESIAN_POINT ( 'NONE',  ( -22.27384469013076185, 3.358914544760244869, 1.508555848190743287 ) ) ;
#42485=VERTEX_POINT ( 'NONE', #15418 ) ;
#42501=DIRECTION ( 'NONE',  ( -1.000000000000000000, 0.000000000000000000, 0.000000000000000000 ) ) ;
#42512=CARTESIAN_POINT ( 'NONE',  ( 2.000000000000001776, 0.000000000000000000, 0.000000000000000000 ) ) ;
#42513=LINE ( 'NONE', #58855, #54164 ) ;
#42515=CIRCLE ( 'NONE', #13840, 2.899999999999995026 ) ;
#42518=VECTOR ( 'NONE', #46158, 1000.000000000000000 ) ;
#42521=ORIENTED_EDGE ( 'NONE', *, *, #60686, .T. ) ;
#42525=CARTESIAN_POINT ( 'NONE',  ( -27.09229696323320624, -0.6397626223479085938, -2.225368503508858620 ) ) ;
#42527=ORIENTED_EDGE ( 'NONE', *, *, #46278, .F. ) ;
#42561=CARTESIAN_POINT ( 'NONE',  ( -22.30078715814471835, -0.2606204736986897363, -3.743307663037647615 ) ) ;
#42562=ORIENTED_EDGE ( 'NONE', *, *, #17215, .F. ) ;
#42563=CARTESIAN_POINT ( 'NONE',  ( -27.08419797710328680, -0.3221715127607973628, -2.268561579780439708 ) ) ;
#42567=CIRCLE ( 'NONE', #18206, 2.899999999999994582 ) ;
#42568=ORIENTED_EDGE ( 'NONE', *, *, #63706, .F. ) ;
#42571=CARTESIAN_POINT ( 'NONE',  ( 2.000000000000001776, 2.562706407243636075, 6.312399813420339179 ) ) ;
#42575=ADVANCED_FACE ( 'NONE', ( #43217 ), #3986, .T. ) ;
#42585=DIRECTION ( 'NONE',  ( 0.000000000000000000, 0.000000000000000000, 1.000000000000000000 ) ) ;
#42589=DIRECTION ( 'NONE',  ( -1.000000000000000000, 0.000000000000000000, 0.000000000000000000 ) ) ;
#42595=DIRECTION ( 'NONE',  ( -1.000000000000000000, 0.000000000000000000, 0.000000000000000000 ) ) ;
#42599=CARTESIAN_POINT ( 'NONE',  ( -27.08419797710328325, 2.125717714519606449, 0.8552720754636790046 ) ) ;
#42613=CARTESIAN_POINT ( 'NONE',  ( -27.08419797710328325, -0.8552720754637003209, 2.125717714519622881 ) ) ;
#42617=CARTESIAN_POINT ( 'NONE',  ( -22.31328051695926007, -2.748895659348118858, -2.608921479762132734 ) ) ;
#42619=VERTEX_POINT ( 'NONE', #28586 ) ;
#42620=CARTESIAN_POINT ( 'NONE',  ( -23.41523303002442091, 1.997501275420757949, 4.252418708693335603 ) ) ;
#42623=ORIENTED_EDGE ( 'NONE', *, *, #15645, .T. ) ;
#42628=CIRCLE ( 'NONE', #58591, 6.936499999999990784 ) ;
#42631=CARTESIAN_POINT ( 'NONE',  ( 0.000000000000000000, 4.409940824963425321, 5.354199675985255702 ) ) ;
#42632=EDGE_LOOP ( 'NONE', ( #5450, #61086, #47121, #16976 ) ) ;
#42635=CARTESIAN_POINT ( 'NONE',  ( -22.30527770659433173, -3.381761229713378558, -1.656864125491266604 ) ) ;
#42641=EDGE_LOOP ( 'NONE', ( #33374, #65028, #17734, #34491 ) ) ;
#42646=ORIENTED_EDGE ( 'NONE', *, *, #52308, .F. ) ;
#42668=AXIS2_PLACEMENT_3D ( 'NONE', #13272, #44176, #13574 ) ;
#42672=CARTESIAN_POINT ( 'NONE',  ( -22.29195009621226831, 1.030739959031474973, 3.580440466953051626 ) ) ;
#42673=CARTESIAN_POINT ( 'NONE',  ( 2.000000000000001776, 6.470132594555847660, -2.133363481234036296 ) ) ;
#42683=CARTESIAN_POINT ( 'NONE',  ( -22.29115169517546136, -3.075985640626798023, 2.098196790595514560 ) ) ;
#42686=CARTESIAN_POINT ( 'NONE',  ( -22.27384469013076185, 0.9224151068931638608, 3.564715702084478632 ) ) ;
#42687=CARTESIAN_POINT ( 'NONE',  ( 0.000000000000000000, 0.000000000000000000, 0.000000000000000000 ) ) ;
#42689=DIRECTION ( 'NONE',  ( -1.000000000000000000, 0.000000000000000000, 0.000000000000000000 ) ) ;
#42693=EDGE_CURVE ( 'NONE', #5798, #15336, #32966, .T. ) ;
#42700=CIRCLE ( 'NONE', #14046, 2.899999999999994582 ) ;
#42702=EDGE_CURVE ( 'NONE', #46041, #42334, #56337, .T. ) ;
#42704=CYLINDRICAL_SURFACE ( 'NONE', #14975, 2.899999999999994582 ) ;
#42713=FACE_OUTER_BOUND ( 'NONE', #17051, .T. ) ;
#42718=FACE_OUTER_BOUND ( 'NONE', #719, .T. ) ;
#42722=VECTOR ( 'NONE', #31888, 1000.000000000000000 ) ;
#42724=DIRECTION ( 'NONE',  ( 0.000000000000000000, 0.1081190184239417817, -0.9941379571543595972 ) ) ;
#42739=CARTESIAN_POINT ( 'NONE',  ( -22.27720387087365239, 3.639274226782813315, -0.5572161790459750907 ) ) ;
#42745=CARTESIAN_POINT ( 'NONE',  ( -27.08426504710140392, 0.6326154899769418360, -2.202478235133286333 ) ) ;
#42758=DIRECTION ( 'NONE',  ( 0.000000000000000000, -0.6876994588534142139, -0.7259954919231395021 ) ) ;
#42762=CARTESIAN_POINT ( 'NONE',  ( -27.10719052120871098, -1.962717903527672059, 1.310802520592011966 ) ) ;
#42774=DIRECTION ( 'NONE',  ( -1.000000000000000000, 0.000000000000000000, 0.000000000000000000 ) ) ;
#42777=EDGE_LOOP ( 'NONE', ( #56175, #24281, #29421, #46443 ) ) ;
#42782=DIRECTION ( 'NONE',  ( 0.000000000000000000, 0.000000000000000000, 1.000000000000000000 ) ) ;
#42783=CARTESIAN_POINT ( 'NONE',  ( -10.00000000000000178, 0.000000000000000000, 0.000000000000000000 ) ) ;
#42785=EDGE_CURVE ( 'NONE', #20437, #57759, #37508, .T. ) ;
#42789=LINE ( 'NONE', #13508, #24730 ) ;
#42800=CARTESIAN_POINT ( 'NONE',  ( -27.08429572838383947, 1.859677275556428810, -1.338867938658195200 ) ) ;
#42805=DIRECTION ( 'NONE',  ( 1.000000000000000000, -0.000000000000000000, -0.000000000000000000 ) ) ;
#42810=CARTESIAN_POINT ( 'NONE',  ( -22.76187086591099984, 1.734723475976807094E-15, -8.673617379884035472E-15 ) ) ;
#42816=CARTESIAN_POINT ( 'NONE',  ( 2.000000000000001776, -3.341639490130797530, 6.078525953551414673 ) ) ;
#42824=ORIENTED_EDGE ( 'NONE', *, *, #23948, .F. ) ;
#42825=DIRECTION ( 'NONE',  ( -1.000000000000000000, 0.000000000000000000, 0.000000000000000000 ) ) ;
#42840=ORIENTED_EDGE ( 'NONE', *, *, #58121, .T. ) ;
#42843=EDGE_CURVE ( 'NONE', #6053, #16234, #26583, .T. ) ;
#42844=VECTOR ( 'NONE', #61989, 1000.000000000000000 ) ;
#42849=CIRCLE ( 'NONE', #14167, 6.936499999999987232 ) ;
#42855=CYLINDRICAL_SURFACE ( 'NONE', #13531, 6.936499999999988120 ) ;
#42856=CIRCLE ( 'NONE', #24825, 7.499999999999988454 ) ;
#42857=CARTESIAN_POINT ( 'NONE',  ( -22.27720387087365239, 2.873095842208905459, -2.302200479844925596 ) ) ;
#42862=DIRECTION ( 'NONE',  ( 0.000000000000000000, 0.000000000000000000, 1.000000000000000000 ) ) ;
#42875=DIRECTION ( 'NONE',  ( 0.000000000000000000, 0.000000000000000000, 1.000000000000000000 ) ) ;
#42878=CARTESIAN_POINT ( 'NONE',  ( 2.000000000000001776, -3.979254915827401540, 5.681598592373737766 ) ) ;
#42883=AXIS2_PLACEMENT_3D ( 'NONE', #59778, #39479, #49167 ) ;
#42890=AXIS2_PLACEMENT_3D ( 'NONE', #41277, #63442, #6067 ) ;
#42891=AXIS2_PLACEMENT_3D ( 'NONE', #23430, #37741, #28740 ) ;
#42894=B_SPLINE_CURVE_WITH_KNOTS ( 'NONE', 3,
 ( #3955, #24215, #14544, #4616, #59801, #14234 ),
 .UNSPECIFIED., .F., .F.,
 ( 4, 2, 4 ),
 ( 0.000000000000000000, 0.0004528561986909231053, 0.0009057123973818462107 ),
 .UNSPECIFIED. ) ;
#42902=CARTESIAN_POINT ( 'NONE',  ( 0.000000000000000000, 5.396716205731433291, 4.158041573745082431 ) ) ;
#42910=EDGE_CURVE ( 'NONE', #51465, #41912, #48810, .T. ) ;
#42911=VERTEX_POINT ( 'NONE', #53132 ) ;
#42913=CARTESIAN_POINT ( 'NONE',  ( -22.28350523959500862, -0.3047406164877233814, -3.687952016964573421 ) ) ;
#42915=VERTEX_POINT ( 'NONE', #3261 ) ;
#42920=LINE ( 'NONE', #49568, #43040 ) ;
#42930=CARTESIAN_POINT ( 'NONE',  ( -27.10719052120871098, -0.6736837626858844796, -2.261993590776034235 ) ) ;
#42931=AXIS2_PLACEMENT_3D ( 'NONE', #5340, #9998, #30585 ) ;
#42937=CARTESIAN_POINT ( 'NONE',  ( -35.04834644901396956, 0.009049049589496429083, -0.01046409687785401256 ) ) ;
#42948=ORIENTED_EDGE ( 'NONE', *, *, #20860, .F. ) ;
#42954=LINE ( 'NONE', #63234, #12866 ) ;
#42956=ORIENTED_EDGE ( 'NONE', *, *, #29237, .T. ) ;
#42965=CYLINDRICAL_SURFACE ( 'NONE', #62799, 2.899999999999994582 ) ;
#42967=CARTESIAN_POINT ( 'NONE',  ( -22.28169757117798611, -2.633129923220811630, -2.592369810060399793 ) ) ;
#42974=CARTESIAN_POINT ( 'NONE',  ( -22.28482751661422867, 3.692400780723907872, -0.2989970708918196496 ) ) ;
#42975=CARTESIAN_POINT ( 'NONE',  ( -22.31328051695926007, 2.748895659348141507, 2.608921479762082551 ) ) ;
#42979=ORIENTED_EDGE ( 'NONE', *, *, #19629, .T. ) ;
#42986=ORIENTED_EDGE ( 'NONE', *, *, #58501, .T. ) ;
#42987=DIRECTION ( 'NONE',  ( 0.000000000000000000, 0.000000000000000000, 1.000000000000000000 ) ) ;
#42998=EDGE_LOOP ( 'NONE', ( #35181, #18868, #26000, #27346 ) ) ;
#42999=DIRECTION ( 'NONE',  ( 0.000000000000000000, 0.000000000000000000, 1.000000000000000000 ) ) ;
#43001=VECTOR ( 'NONE', #40902, 1000.000000000000000 ) ;
#43003=EDGE_LOOP ( 'NONE', ( #47784, #51853, #10387, #50904 ) ) ;
#43007=DIRECTION ( 'NONE',  ( 0.000000000000000000, 0.000000000000000000, 1.000000000000000000 ) ) ;
#43011=CARTESIAN_POINT ( 'NONE',  ( 2.000000000000001776, 4.976357229393922665, -4.652926418895522609 ) ) ;
#43015=CARTESIAN_POINT ( 'NONE',  ( 2.000000000000001776, -1.779948802829750543, -6.576141558201276993 ) ) ;
#43019=CARTESIAN_POINT ( 'NONE',  ( -22.28776923226071460, 3.350304995653733187, 1.601293944844088823 ) ) ;
#43023=DIRECTION ( 'NONE',  ( -1.000000000000000000, 0.000000000000000000, 0.000000000000000000 ) ) ;
#43024=AXIS2_PLACEMENT_3D ( 'NONE', #32389, #1825, #35501 ) ;
#43027=CARTESIAN_POINT ( 'NONE',  ( 2.000000000000001776, 7.248432822490290306, -1.926193556692970876 ) ) ;
#43028=CARTESIAN_POINT ( 'NONE',  ( -35.04709527796842394, -0.01232256164996302361, -0.001003525937983557048 ) ) ;
#43030=EDGE_CURVE ( 'NONE', #60601, #37253, #17870, .T. ) ;
#43031=DIRECTION ( 'NONE',  ( 0.000000000000000000, -0.8276889981568841259, -0.5611870653623918237 ) ) ;
#43032=DIRECTION ( 'NONE',  ( -1.000000000000000000, 0.000000000000000000, 0.000000000000000000 ) ) ;
#43039=CARTESIAN_POINT ( 'NONE',  ( 0.000000000000000000, 3.786546189469178092, 5.663561025469147303 ) ) ;
#43040=VECTOR ( 'NONE', #53893, 1000.000000000000000 ) ;
#43044=ORIENTED_EDGE ( 'NONE', *, *, #26026, .T. ) ;
#43046=DIRECTION ( 'NONE',  ( 0.000000000000000000, 0.000000000000000000, 1.000000000000000000 ) ) ;
#43050=DIRECTION ( 'NONE',  ( 0.000000000000000000, 0.000000000000000000, -1.000000000000000000 ) ) ;
#43051=FACE_OUTER_BOUND ( 'NONE', #40192, .T. ) ;
#43053=ORIENTED_EDGE ( 'NONE', *, *, #5397, .T. ) ;
#43075=CARTESIAN_POINT ( 'NONE',  ( -22.27721701579900682, 3.615531902032099065, -0.6950008646884262564 ) ) ;
#43080=ORIENTED_EDGE ( 'NONE', *, *, #47591, .T. ) ;
#43082=CARTESIAN_POINT ( 'NONE',  ( -22.27718112499583469, -0.5110808820053321933, -3.645895996548667917 ) ) ;
#43092=CARTESIAN_POINT ( 'NONE',  ( -22.28776923226071460, 3.061913732988073011, -2.100802264239969297 ) ) ;
#43094=CARTESIAN_POINT ( 'NONE',  ( -27.09483304420799143, -1.923212037696908627, 1.303111346475729126 ) ) ;
#43097=VERTEX_POINT ( 'NONE', #24839 ) ;
#43100=ORIENTED_EDGE ( 'NONE', *, *, #64340, .F. ) ;
#43104=ORIENTED_EDGE ( 'NONE', *, *, #63676, .T. ) ;
#43106=CARTESIAN_POINT ( 'NONE',  ( -27.09602251845210930, 0.1644056400645444449, 2.320865065108503433 ) ) ;
#43107=VERTEX_POINT ( 'NONE', #45119 ) ;
#43108=DIRECTION ( 'NONE',  ( -1.000000000000000000, 0.000000000000000000, 0.000000000000000000 ) ) ;
#43110=DIRECTION ( 'NONE',  ( 0.9582930651793755139, 0.1254087680151186046, -0.2568015617827263397 ) ) ;
#43123=CARTESIAN_POINT ( 'NONE',  ( -27.08421860617808008, 1.817782142550201208, -1.394838596205214332 ) ) ;
#43136=EDGE_LOOP ( 'NONE', ( #45117, #62983, #31654, #61240 ) ) ;
#43163=LINE ( 'NONE', #63440, #24710 ) ;
#43180=CARTESIAN_POINT ( 'NONE',  ( -22.27716857039623477, 2.705892286796408364, -2.496432241075900560 ) ) ;
#43191=VERTEX_POINT ( 'NONE', #47097 ) ;
#43207=ORIENTED_EDGE ( 'NONE', *, *, #17762, .F. ) ;
#43209=DIRECTION ( 'NONE',  ( -1.000000000000000000, 0.000000000000000000, 0.000000000000000000 ) ) ;
#43215=CARTESIAN_POINT ( 'NONE',  ( -27.08430792439081003, 2.215465963318196785, -0.5856059198894554285 ) ) ;
#43217=FACE_OUTER_BOUND ( 'NONE', #25568, .T. ) ;
#43219=CARTESIAN_POINT ( 'NONE',  ( -27.08639648637142017, -1.635407781266639660, -1.614109828502286570 ) ) ;
#43221=CARTESIAN_POINT ( 'NONE',  ( -22.28939870658739864, -2.099199915896300173, -3.068935452695167321 ) ) ;
#43231=ORIENTED_EDGE ( 'NONE', *, *, #30529, .T. ) ;
#43235=CARTESIAN_POINT ( 'NONE',  ( 2.000000000000001776, 5.662015959325269243, -4.918493191653929841 ) ) ;
#43245=CARTESIAN_POINT ( 'NONE',  ( 0.000000000000000000, 0.000000000000000000, 0.000000000000000000 ) ) ;
#43247=DIRECTION ( 'NONE',  ( 0.000000000000000000, 0.000000000000000000, -1.000000000000000000 ) ) ;
#43249=CARTESIAN_POINT ( 'NONE',  ( -22.71097035706202405, -4.965150228107763297, -0.4203397252017324615 ) ) ;
#43259=DIRECTION ( 'NONE',  ( 0.000000000000000000, 0.1764146379942750087, 0.9843159429275484262 ) ) ;
#43261=LINE ( 'NONE', #64217, #32289 ) ;
#43263=VERTEX_POINT ( 'NONE', #58049 ) ;
#43265=VECTOR ( 'NONE', #35776, 1000.000000000000000 ) ;
#43272=CARTESIAN_POINT ( 'NONE',  ( 2.000000000000001776, -3.073484823194281290, -6.841322316745092280 ) ) ;
#43273=VERTEX_POINT ( 'NONE', #18134 ) ;
#43276=EDGE_CURVE ( 'NONE', #55375, #32360, #7837, .T. ) ;
#43279=DIRECTION ( 'NONE',  ( 1.000000000000000000, 0.000000000000000000, 0.000000000000000000 ) ) ;
#43283=CARTESIAN_POINT ( 'NONE',  ( 2.000000000000001776, -6.777474576704061171, -0.6925993764991672519 ) ) ;
#43294=ORIENTED_EDGE ( 'NONE', *, *, #30462, .F. ) ;
#43297=EDGE_CURVE ( 'NONE', #42115, #41622, #35713, .T. ) ;
#43300=CIRCLE ( 'NONE', #22096, 7.499999999999988454 ) ;
#43310=CARTESIAN_POINT ( 'NONE',  ( 2.000000000000001776, 0.000000000000000000, 0.000000000000000000 ) ) ;
#43311=CARTESIAN_POINT ( 'NONE',  ( 2.000000000000001776, -3.786546189469129686, -5.663561025469209476 ) ) ;
#43312=ORIENTED_EDGE ( 'NONE', *, *, #1302, .T. ) ;
#43316=DIRECTION ( 'NONE',  ( -1.000000000000000000, 0.000000000000000000, 0.000000000000000000 ) ) ;
#43322=CARTESIAN_POINT ( 'NONE',  ( -10.00000000000000178, 0.000000000000000000, 0.000000000000000000 ) ) ;
#43337=CARTESIAN_POINT ( 'NONE',  ( -22.30078715814471835, 3.372109767220915266, 1.645949880549380850 ) ) ;
#43339=CARTESIAN_POINT ( 'NONE',  ( -22.28629837673888048, 2.102970853432577059, 3.055064048018781175 ) ) ;
#43345=AXIS2_PLACEMENT_3D ( 'NONE', #7214, #42129, #11881 ) ;
#43355=LINE ( 'NONE', #27741, #27750 ) ;
#43360=CARTESIAN_POINT ( 'NONE',  ( -22.27834755396594346, -0.5583491773602533570, -3.643689482009672798 ) ) ;
#43361=AXIS2_PLACEMENT_3D ( 'NONE', #43945, #8698, #39601 ) ;
#43365=AXIS2_PLACEMENT_3D ( 'NONE', #33114, #22834, #26823 ) ;
#43369=ORIENTED_EDGE ( 'NONE', *, *, #49684, .T. ) ;
#43371=CARTESIAN_POINT ( 'NONE',  ( -27.35552965826137140, -1.773915698030568366, 2.548625910254532112 ) ) ;
#43384=CARTESIAN_POINT ( 'NONE',  ( 2.000000000000001776, 0.4804830611970945520, -6.919838746524566986 ) ) ;
#43386=CARTESIAN_POINT ( 'NONE',  ( -28.67667724226168602, -0.1214114860980438498, -1.888227992976680980 ) ) ;
#43387=EDGE_LOOP ( 'NONE', ( #25229, #63748 ) ) ;
#43393=EDGE_LOOP ( 'NONE', ( #20832, #64180, #57901, #2560 ) ) ;
#43403=CARTESIAN_POINT ( 'NONE',  ( -22.27721038036499834, 0.5802312083658667241, 3.635620891621732298 ) ) ;
#43404=CARTESIAN_POINT ( 'NONE',  ( 0.000000000000000000, 0.000000000000000000, 0.000000000000000000 ) ) ;
#43410=DIRECTION ( 'NONE',  ( -1.000000000000000000, 0.000000000000000000, 0.000000000000000000 ) ) ;
#43412=CARTESIAN_POINT ( 'NONE',  ( -27.32337605527169089, -2.771816950947471714, 1.175835497774979643 ) ) ;
#43415=CARTESIAN_POINT ( 'NONE',  ( -27.09861164373156228, -1.936722219471109785, 1.303360234155833464 ) ) ;
#43419=DIRECTION ( 'NONE',  ( -1.000000000000000000, 0.000000000000000000, 0.000000000000000000 ) ) ;
#43422=CYLINDRICAL_SURFACE ( 'NONE', #53002, 2.899999999999994582 ) ;
#43428=CARTESIAN_POINT ( 'NONE',  ( -27.09252613521643127, 0.1722886739160412184, 2.309775830546432651 ) ) ;
#43430=EDGE_CURVE ( 'NONE', #57779, #6123, #50599, .T. ) ;
#43433=CARTESIAN_POINT ( 'NONE',  ( -27.09252613521643127, -2.086468883258537410, -1.005681546877608579 ) ) ;
#43444=DIRECTION ( 'NONE',  ( -1.000000000000000000, 0.000000000000000000, 0.000000000000000000 ) ) ;
#43472=CARTESIAN_POINT ( 'NONE',  ( -22.29018399051993882, 2.585196332786391160, -2.675685774027734887 ) ) ;
#43487=ORIENTED_EDGE ( 'NONE', *, *, #24965, .T. ) ;
#43489=ORIENTED_EDGE ( 'NONE', *, *, #52920, .F. ) ;
#43490=CARTESIAN_POINT ( 'NONE',  ( 2.000000000000001776, -4.604744433234619017, -5.919993978425545755 ) ) ;
#43492=EDGE_CURVE ( 'NONE', #23272, #22824, #14748, .T. ) ;
#43499=CARTESIAN_POINT ( 'NONE',  ( 2.000000000000001776, -2.480520636974233639, 6.345145617221206180 ) ) ;
#43508=EDGE_CURVE ( 'NONE', #18352, #15892, #21932, .T. ) ;
#43514=ADVANCED_FACE ( 'NONE', ( #4493 ), #26999, .F. ) ;
#43529=CYLINDRICAL_SURFACE ( 'NONE', #30775, 2.899999999999994582 ) ;
#43547=EDGE_CURVE ( 'NONE', #9429, #16636, #17707, .T. ) ;
#43548=FACE_OUTER_BOUND ( 'NONE', #5875, .T. ) ;
#43552=DIRECTION ( 'NONE',  ( -1.000000000000000000, 0.000000000000000000, 0.000000000000000000 ) ) ;
#43554=CARTESIAN_POINT ( 'NONE',  ( 1.000000000000000888, -3.073484823194374993, 6.841322316745024779 ) ) ;
#43555=COLOUR_RGB ( '', 0.09019608, 0.27058824, 0.51372549) ;
#43559=ORIENTED_EDGE ( 'NONE', *, *, #17249, .T. ) ;
#43560=CARTESIAN_POINT ( 'NONE',  ( -22.94572469358971034, 2.792384151940683346, -4.011883207821665742 ) ) ;
#43571=DIRECTION ( 'NONE',  ( 0.000000000000000000, 0.000000000000000000, 1.000000000000000000 ) ) ;
#43573=EDGE_CURVE ( 'NONE', #10064, #27787, #4332, .T. ) ;
#43574=CARTESIAN_POINT ( 'NONE',  ( -22.29382655386184808, 3.622626291186084035, 0.8947172055470357099 ) ) ;
#43579=ORIENTED_EDGE ( 'NONE', *, *, #61789, .F. ) ;
#43582=ORIENTED_EDGE ( 'NONE', *, *, #33814, .T. ) ;
#43583=ADVANCED_FACE ( 'NONE', ( #32349 ), #5812, .T. ) ;
#43596=CARTESIAN_POINT ( 'NONE',  ( -27.08421723179412410, 2.188590898430372356, 0.6782017488087717094 ) ) ;
#43598=AXIS2_PLACEMENT_3D ( 'NONE', #21829, #7161, #62356 ) ;
#43602=DIRECTION ( 'NONE',  ( 0.000000000000000000, 0.9289767198167924178, -0.3701381553399118451 ) ) ;
#43609=DIRECTION ( 'NONE',  ( 0.000000000000000000, 0.000000000000000000, 1.000000000000000000 ) ) ;
#43613=CIRCLE ( 'NONE', #29850, 6.936499999999988120 ) ;
#43615=EDGE_LOOP ( 'NONE', ( #30637, #18144, #43559, #20419 ) ) ;
#43624=CARTESIAN_POINT ( 'NONE',  ( -22.28939870658739864, 3.707376022556855499, -0.2834927284407640635 ) ) ;
#43636=ORIENTED_EDGE ( 'NONE', *, *, #55240, .F. ) ;
#43637=CARTESIAN_POINT ( 'NONE',  ( -22.27721701579900682, -2.409654355488384692, -2.783642043008656142 ) ) ;
#43649=AXIS2_PLACEMENT_3D ( 'NONE', #56748, #57719, #12142 ) ;
#43654=CARTESIAN_POINT ( 'NONE',  ( -22.70624764888619751, 3.282666355490694077, -4.097886656202270217 ) ) ;
#43655=CARTESIAN_POINT ( 'NONE',  ( 2.000000000000001776, 6.767909380267608022, -0.7805499053121014441 ) ) ;
#43658=EDGE_CURVE ( 'NONE', #14359, #26571, #709, .T. ) ;
#43660=AXIS2_PLACEMENT_3D ( 'NONE', #51332, #5782, #11080 ) ;
#43661=CYLINDRICAL_SURFACE ( 'NONE', #7949, 2.899999999999994582 ) ;
#43662=CARTESIAN_POINT ( 'NONE',  ( -22.27756824490284160, -3.555646273932175472, -0.9591204781040369998 ) ) ;
#43670=CARTESIAN_POINT ( 'NONE',  ( -27.35552965826137140, 2.810569013793760007, -1.320216934008374920 ) ) ;
#43697=CARTESIAN_POINT ( 'NONE',  ( 2.000000000000001776, 0.000000000000000000, 0.000000000000000000 ) ) ;
#43698=CARTESIAN_POINT ( 'NONE',  ( -26.74023318801843985, -1.425982498898169082, -3.035730054944089318 ) ) ;
#43699=EDGE_CURVE ( 'NONE', #13960, #18567, #41039, .T. ) ;
#43703=AXIS2_PLACEMENT_3D ( 'NONE', #20403, #55973, #25724 ) ;
#43705=CARTESIAN_POINT ( 'NONE',  ( -27.15511094194038222, 0.1446243978645498918, 2.499833641087588099 ) ) ;
#43711=ORIENTED_EDGE ( 'NONE', *, *, #58082, .F. ) ;
#43712=EDGE_CURVE ( 'NONE', #26006, #13578, #53779, .T. ) ;
#43714=DIRECTION ( 'NONE',  ( 0.000000000000000000, 0.8835120444460208278, 0.4684084406997939265 ) ) ;
#43716=ORIENTED_EDGE ( 'NONE', *, *, #33340, .T. ) ;
#43727=CARTESIAN_POINT ( 'NONE',  ( 0.000000000000000000, -5.396716205731396876, -4.158041573745144603 ) ) ;
#43731=ORIENTED_EDGE ( 'NONE', *, *, #21541, .F. ) ;
#43744=AXIS2_PLACEMENT_3D ( 'NONE', #45385, #40387, #9807 ) ;
#43754=AXIS2_PLACEMENT_3D ( 'NONE', #21830, #42077, #62357 ) ;
#43755=CARTESIAN_POINT ( 'NONE',  ( -22.76187086591099984, 1.734723475976807094E-15, -8.673617379884035472E-15 ) ) ;
#43757=CARTESIAN_POINT ( 'NONE',  ( -22.28939870658739864, 3.068935452695165544, -2.099199915896291291 ) ) ;
#43761=DIRECTION ( 'NONE',  ( 1.000000000000000000, 0.000000000000000000, 0.000000000000000000 ) ) ;
#43764=ORIENTED_EDGE ( 'NONE', *, *, #35157, .T. ) ;
#43769=PRESENTATION_STYLE_ASSIGNMENT (( #23490 ) ) ;
#43774=ORIENTED_EDGE ( 'NONE', *, *, #13862, .F. ) ;
#43776=ORIENTED_EDGE ( 'NONE', *, *, #49517, .T. ) ;
#43782=VERTEX_POINT ( 'NONE', #59941 ) ;
#43785=CARTESIAN_POINT ( 'NONE',  ( 2.000000000000001776, 6.767909380267589370, 0.7805499053121639497 ) ) ;
#43804=CIRCLE ( 'NONE', #9810, 6.936499999999989008 ) ;
#43819=B_SPLINE_CURVE_WITH_KNOTS ( 'NONE', 3,
 ( #29858, #4628, #50168, #13905, #65430, #19894, #60450, #14874, #5608, #25877, #15863, #46799, #40494, #30833, #1265, #611, #6249, #15549, #10235, #51497, #36500, #5943 ),
 .UNSPECIFIED., .F., .F.,
 ( 4, 3, 3, 3, 3, 3, 3, 4 ),
 ( 0.000000000000000000, 4.447697177976374735E-05, 6.624143997791376683E-05, 8.800576886944418142E-05, 0.0001097699864780915817, 0.0001315341395364400380, 0.0001760120188223304890, 0.0001867971373174766379 ),
 .UNSPECIFIED. ) ;
#43820=PRESENTATION_STYLE_ASSIGNMENT (( #60410 ) ) ;
#43821=CARTESIAN_POINT ( 'NONE',  ( -22.27710395300133683, 2.620347679538758801, -2.585700543510485616 ) ) ;
#43827=CIRCLE ( 'NONE', #53373, 2.899999999999997247 ) ;
#43838=DIRECTION ( 'NONE',  ( 0.000000000000000000, 0.3193015301359743985, 0.9476531711828043436 ) ) ;
#43839=CARTESIAN_POINT ( 'NONE',  ( -27.08871896697732140, -2.297279805116094753, 0.1856437051692867712 ) ) ;
#43846=CARTESIAN_POINT ( 'NONE',  ( 2.000000000000001776, 0.000000000000000000, 0.000000000000000000 ) ) ;
#43849=AXIS2_PLACEMENT_3D ( 'NONE', #9274, #34858, #49549 ) ;
#43856=CIRCLE ( 'NONE', #16228, 7.499999999999988454 ) ;
#43857=CIRCLE ( 'NONE', #45948, 7.499999999999988454 ) ;
#43859=LINE ( 'NONE', #64142, #48213 ) ;
#43863=DIRECTION ( 'NONE',  ( -1.000000000000000000, 0.000000000000000000, 0.000000000000000000 ) ) ;
#43867=AXIS2_PLACEMENT_3D ( 'NONE', #44102, #59392, #29148 ) ;
#43871=CARTESIAN_POINT ( 'NONE',  ( -22.29770266787582500, 2.703976473263656199, 2.588315884842612657 ) ) ;
#43876=DIRECTION ( 'NONE',  ( 0.000000000000000000, -0.9868265225415276953, 0.1617819965527552140 ) ) ;
#43885=CARTESIAN_POINT ( 'NONE',  ( -27.08429572838383947, 2.217805374070540125, -0.5764601019425888984 ) ) ;
#43891=CARTESIAN_POINT ( 'NONE',  ( -22.30625920655495165, -2.110841417170890466, -3.150098859949351571 ) ) ;
#43897=CARTESIAN_POINT ( 'NONE',  ( 0.000000000000000000, -3.805198749487460841, 5.799611601383201531 ) ) ;
#43909=CARTESIAN_POINT ( 'NONE',  ( -22.23402523511428086, 1.734723475976807094E-15, -8.673617379884035472E-15 ) ) ;
#43916=CARTESIAN_POINT ( 'NONE',  ( 0.000000000000000000, 0.000000000000000000, 0.000000000000000000 ) ) ;
#43917=VERTEX_POINT ( 'NONE', #36933 ) ;
#43920=CARTESIAN_POINT ( 'NONE',  ( 0.000000000000000000, -6.539067737394485214, -2.314222412769890713 ) ) ;
#43925=LINE ( 'NONE', #64511, #45727 ) ;
#43932=CARTESIAN_POINT ( 'NONE',  ( 2.000000000000001776, -2.469490258309472441, 6.482025155313308140 ) ) ;
#43935=FACE_OUTER_BOUND ( 'NONE', #33353, .T. ) ;
#43943=EDGE_CURVE ( 'NONE', #9689, #6901, #50938, .T. ) ;
#43944=VERTEX_POINT ( 'NONE', #15989 ) ;
#43945=CARTESIAN_POINT ( 'NONE',  ( 2.000000000000001776, -4.376687952327290354, -5.220963330856675633 ) ) ;
#43946=FACE_OUTER_BOUND ( 'NONE', #65348, .T. ) ;
#43951=AXIS2_PLACEMENT_3D ( 'NONE', #49778, #39795, #48809 ) ;
#43952=VECTOR ( 'NONE', #25222, 999.9999999999998863 ) ;
#43961=DIRECTION ( 'NONE',  ( -1.000000000000000000, 0.000000000000000000, 0.000000000000000000 ) ) ;
#43964=EDGE_CURVE ( 'NONE', #62360, #19513, #44266, .T. ) ;
#43965=ORIENTED_EDGE ( 'NONE', *, *, #9284, .T. ) ;
#43981=CARTESIAN_POINT ( 'NONE',  ( -22.27715239060371744, -2.513478159995845562, -2.689999469426704426 ) ) ;
#43982=DIRECTION ( 'NONE',  ( 0.000000000000000000, 0.000000000000000000, 1.000000000000000000 ) ) ;
#43992=CARTESIAN_POINT ( 'NONE',  ( 0.000000000000000000, 0.000000000000000000, 0.000000000000000000 ) ) ;
#44013=ORIENTED_EDGE ( 'NONE', *, *, #4807, .T. ) ;
#44015=CARTESIAN_POINT ( 'NONE',  ( -27.08429572838383947, 0.2296550094123047669, 2.279961732801582208 ) ) ;
#44017=CARTESIAN_POINT ( 'NONE',  ( -22.28776923226071460, 2.100802264239995942, 3.061913732988043702 ) ) ;
#44018=ADVANCED_FACE ( 'NONE', ( #53573 ), #62862, .T. ) ;
#44024=EDGE_LOOP ( 'NONE', ( #55330, #20199, #16313, #13078 ) ) ;
#44030=VECTOR ( 'NONE', #56103, 1000.000000000000000 ) ;
#44033=ORIENTED_EDGE ( 'NONE', *, *, #63593, .F. ) ;
#44036=FACE_OUTER_BOUND ( 'NONE', #53910, .T. ) ;
#44053=CARTESIAN_POINT ( 'NONE',  ( -35.05175862995318425, 0.01030783735684465130, -0.007207337213517919783 ) ) ;
#44057=DIRECTION ( 'NONE',  ( -1.000000000000000000, 0.000000000000000000, 0.000000000000000000 ) ) ;
#44060=LINE ( 'NONE', #64328, #28745 ) ;
#44061=FACE_OUTER_BOUND ( 'NONE', #61753, .T. ) ;
#44064=CARTESIAN_POINT ( 'NONE',  ( -22.27721038036499834, 2.320305412324252803, 2.858424446490910320 ) ) ;
#44073=VECTOR ( 'NONE', #34675, 1000.000000000000000 ) ;
#44076=DIRECTION ( 'NONE',  ( -1.000000000000000000, 0.000000000000000000, 0.000000000000000000 ) ) ;
#44079=CARTESIAN_POINT ( 'NONE',  ( -22.27722019110237284, 0.6492757894141428787, 3.623957119342502864 ) ) ;
#44083=ORIENTED_EDGE ( 'NONE', *, *, #25836, .F. ) ;
#44086=CARTESIAN_POINT ( 'NONE',  ( 2.000000000000001776, 6.643843315911821534, -1.507714007300717585 ) ) ;
#44087=EDGE_CURVE ( 'NONE', #49125, #17671, #42117, .T. ) ;
#44088=CARTESIAN_POINT ( 'NONE',  ( -22.28236030719477867, 3.035028179399219983, -2.111163412226028768 ) ) ;
#44091=CARTESIAN_POINT ( 'NONE',  ( 0.000000000000000000, -6.643843315911820646, 1.507714007300648307 ) ) ;
#44096=EDGE_CURVE ( 'NONE', #5306, #42222, #41074, .T. ) ;
#44097=DIRECTION ( 'NONE',  ( -1.000000000000000000, 0.000000000000000000, 0.000000000000000000 ) ) ;
#44101=CARTESIAN_POINT ( 'NONE',  ( 2.000000000000001776, 0.000000000000000000, 0.000000000000000000 ) ) ;
#44102=CARTESIAN_POINT ( 'NONE',  ( 2.000000000000001776, 0.000000000000000000, 0.000000000000000000 ) ) ;
#44109=CARTESIAN_POINT ( 'NONE',  ( -26.43258404273188233, -0.2934201954354099806, 3.465947334857387041 ) ) ;
#44117=EDGE_LOOP ( 'NONE', ( #50553, #53535, #65308, #57836 ) ) ;
#44118=CARTESIAN_POINT ( 'NONE',  ( -35.04709527796842394, -0.007030359780627049027, 0.01016988845956717791 ) ) ;
#44122=DIRECTION ( 'NONE',  ( -1.000000000000000000, 0.000000000000000000, 0.000000000000000000 ) ) ;
#44123=CARTESIAN_POINT ( 'NONE',  ( -22.46225619532220819, 4.233934615764574083, -0.1595555201818063817 ) ) ;
#44145=FILL_AREA_STYLE_COLOUR ( '', #62171 ) ;
#44148=CARTESIAN_POINT ( 'NONE',  ( -22.28856623400852399, 2.585606290939623797, -2.668530796663830973 ) ) ;
#44150=CARTESIAN_POINT ( 'NONE',  ( -22.30986928587821794, -1.665628047792428568, 3.392803916780406492 ) ) ;
#44158=CARTESIAN_POINT ( 'NONE',  ( 0.000000000000000000, 6.253963800348318003, -4.139799123620975685 ) ) ;
#44159=ORIENTED_EDGE ( 'NONE', *, *, #14573, .T. ) ;
#44161=CARTESIAN_POINT ( 'NONE',  ( 2.000000000000001776, 0.000000000000000000, 0.000000000000000000 ) ) ;
#44162=ADVANCED_FACE ( 'NONE', ( #39226 ), #59207, .T. ) ;
#44169=ORIENTED_EDGE ( 'NONE', *, *, #236, .T. ) ;
#44173=CARTESIAN_POINT ( 'NONE',  ( 0.000000000000000000, -5.097042323172487954, 5.501832381651415638 ) ) ;
#44176=DIRECTION ( 'NONE',  ( -1.000000000000000000, 0.000000000000000000, 0.000000000000000000 ) ) ;
#44187=DIRECTION ( 'NONE',  ( 1.000000000000000000, 0.000000000000000000, 0.000000000000000000 ) ) ;
#44189=B_SPLINE_CURVE_WITH_KNOTS ( 'NONE', 3,
 ( #38258, #34583, #54234, #24287, #8676, #39248, #28960, #49267 ),
 .UNSPECIFIED., .F., .F.,
 ( 4, 2, 2, 4 ),
 ( 0.000000000000000000, 0.0003639104015150029445, 0.0007278208030300058889, 0.001455641606060012428 ),
 .UNSPECIFIED. ) ;
#44191=CARTESIAN_POINT ( 'NONE',  ( 0.000000000000000000, 0.000000000000000000, 0.000000000000000000 ) ) ;
#44195=EDGE_CURVE ( 'NONE', #3384, #45709, #59861, .T. ) ;
#44196=DIRECTION ( 'NONE',  ( -1.000000000000000000, 0.000000000000000000, 0.000000000000000000 ) ) ;
#44204=EDGE_CURVE ( 'NONE', #10092, #11911, #27318, .T. ) ;
#44206=ORIENTED_EDGE ( 'NONE', *, *, #47537, .T. ) ;
#44215=EDGE_LOOP ( 'NONE', ( #54501, #44423, #25078, #61997 ) ) ;
#44216=VERTEX_POINT ( 'NONE', #3700 ) ;
#44219=DIRECTION ( 'NONE',  ( 1.000000000000000000, -0.000000000000000000, -0.000000000000000000 ) ) ;
#44228=DIRECTION ( 'NONE',  ( 0.000000000000000000, 0.8276889981568879007, 0.5611870653623863836 ) ) ;
#44231=CARTESIAN_POINT ( 'NONE',  ( 0.000000000000000000, -6.883677378339447372, -0.8544109087186817497 ) ) ;
#44246=DIRECTION ( 'NONE',  ( 0.000000000000000000, -0.8835120444460271560, 0.4684084406997820471 ) ) ;
#44248=VERTEX_POINT ( 'NONE', #18962 ) ;
#44253=EDGE_CURVE ( 'NONE', #32250, #61252, #6122, .T. ) ;
#44254=ORIENTED_EDGE ( 'NONE', *, *, #59747, .T. ) ;
#44263=CARTESIAN_POINT ( 'NONE',  ( -35.04709527796842394, -0.001082316405377065083, 0.01231589140597219578 ) ) ;
#44266=CIRCLE ( 'NONE', #11377, 6.936499999999987232 ) ;
#44272=EDGE_CURVE ( 'NONE', #39026, #53160, #61077, .T. ) ;
#44273=CARTESIAN_POINT ( 'NONE',  ( 2.000000000000001776, 0.000000000000000000, 0.000000000000000000 ) ) ;
#44275=CARTESIAN_POINT ( 'NONE',  ( 0.000000000000000000, -5.396716205731451943, 4.158041573745051345 ) ) ;
#44280=DIRECTION ( 'NONE',  ( 0.000000000000000000, -0.3193015301359669600, -0.9476531711828067861 ) ) ;
#44283=CARTESIAN_POINT ( 'NONE',  ( 0.000000000000000000, 6.586971819220387658, -3.586335490831350725 ) ) ;
#44291=CARTESIAN_POINT ( 'NONE',  ( -22.27709082389155171, -2.563977319272125133, -2.641652894015116715 ) ) ;
#44292=DIRECTION ( 'NONE',  ( 1.000000000000000000, 0.000000000000000000, 0.000000000000000000 ) ) ;
#44294=DIRECTION ( 'NONE',  ( -1.000000000000000000, 0.000000000000000000, 0.000000000000000000 ) ) ;
#44296=DIRECTION ( 'NONE',  ( 0.000000000000000000, -0.9289767198167949713, 0.3701381553399054614 ) ) ;
#44298=DIRECTION ( 'NONE',  ( 0.000000000000000000, 0.000000000000000000, 1.000000000000000000 ) ) ;
#44314=CARTESIAN_POINT ( 'NONE',  ( 0.000000000000000000, -3.155844197800055539, -6.177028383390492650 ) ) ;
#44316=ORIENTED_EDGE ( 'NONE', *, *, #48608, .F. ) ;
#44317=DIRECTION ( 'NONE',  ( -1.000000000000000000, 0.000000000000000000, 0.000000000000000000 ) ) ;
#44325=EDGE_CURVE ( 'NONE', #4816, #22798, #50689, .T. ) ;
#44329=CARTESIAN_POINT ( 'NONE',  ( 2.000000000000001776, -5.997115278587647147, 3.485633455389469226 ) ) ;
#44342=LINE ( 'NONE', #19090, #45270 ) ;
#44345=EDGE_CURVE ( 'NONE', #16346, #55528, #65564, .T. ) ;
#44365=ADVANCED_FACE ( 'NONE', ( #7170 ), #21502, .T. ) ;
#44369=CARTESIAN_POINT ( 'NONE',  ( -22.27720387087365239, 2.302200479844943359, 2.873095842208868156 ) ) ;
#44378=DIRECTION ( 'NONE',  ( 0.000000000000000000, 0.000000000000000000, -1.000000000000000000 ) ) ;
#44380=CARTESIAN_POINT ( 'NONE',  ( 1.000000000000000888, -3.937687286050851831, 6.383151168292441113 ) ) ;
#44383=ORIENTED_EDGE ( 'NONE', *, *, #37377, .T. ) ;
#44385=CIRCLE ( 'NONE', #51877, 2.899999999999995026 ) ;
#44392=ADVANCED_FACE ( 'NONE', ( #42397 ), #6869, .T. ) ;
#44400=LINE ( 'NONE', #20467, #47868 ) ;
#44407=CARTESIAN_POINT ( 'NONE',  ( 0.000000000000000000, -2.315790869867006219, -7.133520354428148025 ) ) ;
#44414=CARTESIAN_POINT ( 'NONE',  ( 0.000000000000000000, 0.000000000000000000, 0.000000000000000000 ) ) ;
#44419=CARTESIAN_POINT ( 'NONE',  ( -35.05175862995318425, 0.007207337213500572548, 0.01030783735683771241 ) ) ;
#44423=ORIENTED_EDGE ( 'NONE', *, *, #62003, .T. ) ;
#44450=( LENGTH_UNIT ( ) NAMED_UNIT ( * ) SI_UNIT ( .MILLI., .METRE. ) );
#44451=CARTESIAN_POINT ( 'NONE',  ( -27.35552965826137140, 0.2619431035392177365, -3.094132632038957276 ) ) ;
#44459=VERTEX_POINT ( 'NONE', #64653 ) ;
#44466=DIRECTION ( 'NONE',  ( 0.000000000000000000, 0.000000000000000000, 1.000000000000000000 ) ) ;
#44467=CARTESIAN_POINT ( 'NONE',  ( -27.08429572838383947, -1.632445743623433421, 1.608131779585712406 ) ) ;
#44469=EDGE_CURVE ( 'NONE', #43191, #40046, #47163, .T. ) ;
#44474=VERTEX_POINT ( 'NONE', #30076 ) ;
#44475=DIRECTION ( 'NONE',  ( 0.000000000000000000, 0.000000000000000000, -1.000000000000000000 ) ) ;
#44477=CIRCLE ( 'NONE', #15802, 6.936499999999987232 ) ;
#44479=CARTESIAN_POINT ( 'NONE',  ( -22.30625920655495165, -3.150098859949341357, 2.110841417170906009 ) ) ;
#44481=CARTESIAN_POINT ( 'NONE',  ( -27.10512513516317412, 1.618446180706347048, -1.709353012333662880 ) ) ;
#44482=DIRECTION ( 'NONE',  ( 0.000000000000000000, 0.000000000000000000, 1.000000000000000000 ) ) ;
#44483=DIRECTION ( 'NONE',  ( -1.000000000000000000, 0.000000000000000000, 0.000000000000000000 ) ) ;
#44493=CARTESIAN_POINT ( 'NONE',  ( 2.000000000000001776, 0.000000000000000000, 0.000000000000000000 ) ) ;
#44508=CARTESIAN_POINT ( 'NONE',  ( -24.42101984568203221, -3.884389025764515058, 1.824625598916869595 ) ) ;
#44510=CYLINDRICAL_SURFACE ( 'NONE', #57488, 2.899999999999994582 ) ;
#44511=EDGE_CURVE ( 'NONE', #12277, #42103, #9795, .T. ) ;
#44515=CARTESIAN_POINT ( 'NONE',  ( -27.09030469827880339, 2.221523195520540117, -0.6314616953885209272 ) ) ;
#44523=CARTESIAN_POINT ( 'NONE',  ( 2.000000000000001776, -4.570217215903314312, -5.218059682435693958 ) ) ;
#44535=ORIENTED_EDGE ( 'NONE', *, *, #24082, .F. ) ;
#44538=CARTESIAN_POINT ( 'NONE',  ( -27.08639648637141661, -2.223359598374791801, -0.5801562253478093067 ) ) ;
#44542=ORIENTED_EDGE ( 'NONE', *, *, #43964, .F. ) ;
#44543=CARTESIAN_POINT ( 'NONE',  ( 0.000000000000000000, 0.000000000000000000, 0.000000000000000000 ) ) ;
#44547=CARTESIAN_POINT ( 'NONE',  ( 2.000000000000001776, 0.000000000000000000, 0.000000000000000000 ) ) ;
#44548=CARTESIAN_POINT ( 'NONE',  ( -35.04709527796842394, 0.007095259204987700019, -0.01012471662515009030 ) ) ;
#44565=VERTEX_POINT ( 'NONE', #61986 ) ;
#44566=CARTESIAN_POINT ( 'NONE',  ( -35.04643116707788408, 0.001845126042312322800, 0.01204777744935429939 ) ) ;
#44570=CARTESIAN_POINT ( 'NONE',  ( 0.000000000000000000, 2.315790869867158985, -7.133520354428100951 ) ) ;
#44576=CIRCLE ( 'NONE', #21233, 2.899999999999994582 ) ;
#44588=ORIENTED_EDGE ( 'NONE', *, *, #65673, .F. ) ;
#44591=CARTESIAN_POINT ( 'NONE',  ( 2.000000000000001776, -5.888698556700776798, 3.665823448873372747 ) ) ;
#44592=DIRECTION ( 'NONE',  ( 0.000000000000000000, -0.9635499925192254622, 0.2675283385292119842 ) ) ;
#44602=VERTEX_POINT ( 'NONE', #51378 ) ;
#44613=ORIENTED_EDGE ( 'NONE', *, *, #58670, .F. ) ;
#44619=DIRECTION ( 'NONE',  ( 0.000000000000000000, 0.000000000000000000, 1.000000000000000000 ) ) ;
#44620=CARTESIAN_POINT ( 'NONE',  ( 0.000000000000000000, 0.000000000000000000, 0.000000000000000000 ) ) ;
#44621=CARTESIAN_POINT ( 'NONE',  ( 0.000000000000000000, -5.662015959325215952, 4.918493191653933394 ) ) ;
#44628=AXIS2_PLACEMENT_3D ( 'NONE', #60756, #30481, #40456 ) ;
#44629=ADVANCED_FACE ( 'NONE', ( #17420 ), #41695, .T. ) ;
#44630=ORIENTED_EDGE ( 'NONE', *, *, #62567, .T. ) ;
#44636=CARTESIAN_POINT ( 'NONE',  ( -22.31328051695926007, -2.608921479762108753, 2.748895659348124187 ) ) ;
#44638=CARTESIAN_POINT ( 'NONE',  ( 0.000000000000000000, 1.530946385938383614, 7.342084388195340594 ) ) ;
#44641=VECTOR ( 'NONE', #65365, 1000.000000000000000 ) ;
#44646=( BOUNDED_SURFACE ( )  B_SPLINE_SURFACE ( 3, 1, ( 
 ( #1939, #42468 ),
 ( #32176, #22206 ),
 ( #46194, #51523 ),
 ( #11262, #52501 ) ),
 .UNSPECIFIED., .F., .F., .F. ) 
 B_SPLINE_SURFACE_WITH_KNOTS ( ( 4, 4 ),
 ( 2, 2 ),
 ( 0.000000000000000000, 1.000000000000000000 ),
 ( 0.000000000000000000, 1.000000000000000000 ),
 .UNSPECIFIED. ) 
 GEOMETRIC_REPRESENTATION_ITEM ( )  RATIONAL_B_SPLINE_SURFACE ( (
 ( 1.000000000000000000, 1.000000000000000000),
 ( 0.9257577194822556033, 0.9980522942447415113),
 ( 0.9257577194822556033, 0.9980522942447415113),
 ( 1.000000000000000000, 1.000000000000000000) ) ) 
 REPRESENTATION_ITEM ( '' )  SURFACE ( )  );
#44654=VECTOR ( 'NONE', #37761, 1000.000000000000114 ) ;
#44663=DIRECTION ( 'NONE',  ( -1.000000000000000000, 0.000000000000000000, 0.000000000000000000 ) ) ;
#44673=VERTEX_POINT ( 'NONE', #49005 ) ;
#44685=VERTEX_POINT ( 'NONE', #12732 ) ;
#44687=CARTESIAN_POINT ( 'NONE',  ( -35.04834644901396956, 0.01211993185717642925, 0.006670072992069154237 ) ) ;
#44700=CARTESIAN_POINT ( 'NONE',  ( -22.28694879868232803, -0.9088670759107992936, 3.597828382597537011 ) ) ;
#44703=CARTESIAN_POINT ( 'NONE',  ( -35.04683013664716640, 0.009445816769477739447, 0.007968230201761825754 ) ) ;
#44708=CARTESIAN_POINT ( 'NONE',  ( 2.000000000000001776, 6.643843315911800218, 1.507714007300793968 ) ) ;
#44715=DIRECTION ( 'NONE',  ( 0.000000000000000000, 0.000000000000000000, 1.000000000000000000 ) ) ;
#44718=ADVANCED_FACE ( 'NONE', ( #33365 ), #63598, .T. ) ;
#44720=CIRCLE ( 'NONE', #56408, 6.936499999999990784 ) ;
#44733=CARTESIAN_POINT ( 'NONE',  ( -22.31328051695926007, -3.148362328073157190, 2.109671368890621679 ) ) ;
#44735=CARTESIAN_POINT ( 'NONE',  ( 2.000000000000001776, 0.000000000000000000, 0.000000000000000000 ) ) ;
#44754=LINE ( 'NONE', #30761, #17126 ) ;
#44756=ORIENTED_EDGE ( 'NONE', *, *, #53382, .F. ) ;
#44762=DIRECTION ( 'NONE',  ( -1.000000000000000000, 0.000000000000000000, 0.000000000000000000 ) ) ;
#44764=CARTESIAN_POINT ( 'NONE',  ( -22.28415773361649954, -0.9981933716384904232, -3.565377603762390546 ) ) ;
#44775=EDGE_CURVE ( 'NONE', #59375, #63362, #45400, .T. ) ;
#44776=DIRECTION ( 'NONE',  ( -1.000000000000000000, 0.000000000000000000, 0.000000000000000000 ) ) ;
#44777=CARTESIAN_POINT ( 'NONE',  ( -22.66110217412718342, 4.900671186447937089, 0.6585288088159688691 ) ) ;
#44784=VERTEX_POINT ( 'NONE', #9069 ) ;
#44787=VECTOR ( 'NONE', #50561, 1000.000000000000000 ) ;
#44794=ADVANCED_FACE ( 'NONE', ( #24353 ), #39975, .T. ) ;
#44796=ORIENTED_EDGE ( 'NONE', *, *, #6531, .T. ) ;
#44797=ORIENTED_EDGE ( 'NONE', *, *, #37438, .F. ) ;
#44800=DIRECTION ( 'NONE',  ( 1.000000000000000000, -0.000000000000000000, -0.000000000000000000 ) ) ;
#44804=AXIS2_PLACEMENT_3D ( 'NONE', #44854, #49225, #50190 ) ;
#44805=CARTESIAN_POINT ( 'NONE',  ( 0.000000000000000000, 6.160607635185464837, -4.277489166005534749 ) ) ;
#44808=DIRECTION ( 'NONE',  ( 1.000000000000000000, -0.000000000000000000, -0.000000000000000000 ) ) ;
#44812=ORIENTED_EDGE ( 'NONE', *, *, #36296, .T. ) ;
#44823=DIRECTION ( 'NONE',  ( 0.000000000000000000, 0.000000000000000000, -1.000000000000000000 ) ) ;
#44836=DIRECTION ( 'NONE',  ( -1.000000000000000000, 0.000000000000000000, 0.000000000000000000 ) ) ;
#44838=VERTEX_POINT ( 'NONE', #55270 ) ;
#44840=DIRECTION ( 'NONE',  ( -1.000000000000000000, 0.000000000000000000, 0.000000000000000000 ) ) ;
#44844=VECTOR ( 'NONE', #44840, 1000.000000000000000 ) ;
#44849=CARTESIAN_POINT ( 'NONE',  ( 2.000000000000001776, 2.473437528934141483, 7.080403010454977775 ) ) ;
#44854=CARTESIAN_POINT ( 'NONE',  ( 0.000000000000000000, -5.450255447309714896, -4.087611905901492371 ) ) ;
#44857=ADVANCED_FACE ( 'NONE', ( #5075 ), #19049, .T. ) ;
#44868=FACE_OUTER_BOUND ( 'NONE', #29730, .T. ) ;
#44886=ORIENTED_EDGE ( 'NONE', *, *, #9458, .F. ) ;
#44897=CARTESIAN_POINT ( 'NONE',  ( 2.000000000000001776, 5.769711778877324448, 4.791703871138532023 ) ) ;
#44915=EDGE_CURVE ( 'NONE', #59, #3146, #30536, .T. ) ;
#44919=CIRCLE ( 'NONE', #40649, 6.936499999999989008 ) ;
#44921=EDGE_CURVE ( 'NONE', #13767, #28521, #22957, .T. ) ;
#44927=DIRECTION ( 'NONE',  ( -1.000000000000000000, 0.000000000000000000, 0.000000000000000000 ) ) ;
#44934=CIRCLE ( 'NONE', #43849, 2.899999999999994582 ) ;
#44935=AXIS2_PLACEMENT_3D ( 'NONE', #30477, #20836, #61386 ) ;
#44941=ADVANCED_FACE ( 'NONE', ( #7997 ), #65604, .F. ) ;
#44944=CARTESIAN_POINT ( 'NONE',  ( -22.27711653538342773, -3.657713416444755783, 0.4190680140413455823 ) ) ;
#44948=ORIENTED_EDGE ( 'NONE', *, *, #36006, .T. ) ;
#44951=EDGE_LOOP ( 'NONE', ( #13460, #3844, #8071, #18230 ) ) ;
#44954=DIRECTION ( 'NONE',  ( -1.000000000000000000, 0.000000000000000000, 0.000000000000000000 ) ) ;
#44955=EDGE_LOOP ( 'NONE', ( #26314, #28515, #20496, #29708 ) ) ;
#44960=AXIS2_PLACEMENT_3D ( 'NONE', #26078, #62945, #36367 ) ;
#44965=CARTESIAN_POINT ( 'NONE',  ( 0.000000000000000000, -7.414200355365233364, -1.131208685655244350 ) ) ;
#44967=FACE_OUTER_BOUND ( 'NONE', #47905, .T. ) ;
#44981=CARTESIAN_POINT ( 'NONE',  ( -27.08704841010922593, -0.1930432016059823730, -2.291653842312389333 ) ) ;
#44985=ORIENTED_EDGE ( 'NONE', *, *, #20088, .T. ) ;
#44996=DIRECTION ( 'NONE',  ( -0.9582930651793755139, 0.06744057189511765138, -0.2777159889015695104 ) ) ;
#45006=FACE_OUTER_BOUND ( 'NONE', #14306, .T. ) ;
#45008=EDGE_LOOP ( 'NONE', ( #53039, #62152, #52071, #35835 ) ) ;
#45012=VECTOR ( 'NONE', #39497, 1000.000000000000000 ) ;
#45013=CARTESIAN_POINT ( 'NONE',  ( -35.05175862995318425, -0.005323180402361238350, 0.01139565579894724623 ) ) ;
#45015=ORIENTED_EDGE ( 'NONE', *, *, #10142, .T. ) ;
#45016=LINE ( 'NONE', #60971, #36260 ) ;
#45021=CARTESIAN_POINT ( 'NONE',  ( 2.000000000000001776, -7.387287142779360494, 1.295372019972132804 ) ) ;
#45022=EDGE_CURVE ( 'NONE', #13885, #3120, #26327, .T. ) ;
#45028=CARTESIAN_POINT ( 'NONE',  ( 0.000000000000000000, -5.217815162096798076, -5.387430271863655307 ) ) ;
#45031=CIRCLE ( 'NONE', #43951, 2.899999999999994582 ) ;
#45036=ORIENTED_EDGE ( 'NONE', *, *, #36412, .F. ) ;
#45038=CARTESIAN_POINT ( 'NONE',  ( -22.30625920655495165, -2.610366806364689651, 2.750410778797883982 ) ) ;
#45044=CARTESIAN_POINT ( 'NONE',  ( -27.05874794189610455, 2.503708927703406609E-30, 1.499999999999991562 ) ) ;
#45053=ORIENTED_EDGE ( 'NONE', *, *, #47728, .T. ) ;
#45054=CARTESIAN_POINT ( 'NONE',  ( -27.32337605527169089, 2.404211887218409949, 1.812546145273324028 ) ) ;
#45058=CARTESIAN_POINT ( 'NONE',  ( -22.28506771379528573, -0.2569416992704395830, -3.718191140878645218 ) ) ;
#45059=LINE ( 'NONE', #19795, #33387 ) ;
#45067=ORIENTED_EDGE ( 'NONE', *, *, #63208, .T. ) ;
#45069=AXIS2_PLACEMENT_3D ( 'NONE', #58101, #48460, #42782 ) ;
#45071=CARTESIAN_POINT ( 'NONE',  ( -22.29770266787582500, 0.8895590726607195409, -3.635870259503093838 ) ) ;
#45075=ADVANCED_FACE ( 'NONE', ( #27884 ), #5573, .T. ) ;
#45077=AXIS2_PLACEMENT_3D ( 'NONE', #59470, #54820, #9553 ) ;
#45081=FACE_OUTER_BOUND ( 'NONE', #48334, .T. ) ;
#45089=CIRCLE ( 'NONE', #61039, 2.899999999999994582 ) ;
#45093=DIRECTION ( 'NONE',  ( -1.000000000000000000, 0.000000000000000000, 0.000000000000000000 ) ) ;
#45095=AXIS2_PLACEMENT_3D ( 'NONE', #45623, #55626, #74 ) ;
#45097=CYLINDRICAL_SURFACE ( 'NONE', #1385, 2.899999999999994582 ) ;
#45098=CYLINDRICAL_SURFACE ( 'NONE', #57789, 2.899999999999994582 ) ;
#45099=AXIS2_PLACEMENT_3D ( 'NONE', #24419, #33431, #28428 ) ;
#45108=ORIENTED_EDGE ( 'NONE', *, *, #35028, .T. ) ;
#45115=ADVANCED_FACE ( 'NONE', ( #19861 ), #35475, .T. ) ;
#45117=ORIENTED_EDGE ( 'NONE', *, *, #48130, .T. ) ;
#45119=CARTESIAN_POINT ( 'NONE',  ( -27.08429572838383947, -1.338867938658200307, -1.859677275556420151 ) ) ;
#45123=CARTESIAN_POINT ( 'NONE',  ( -27.35552965826137140, 2.548625910254547655, 1.773915698030531951 ) ) ;
#45125=ORIENTED_EDGE ( 'NONE', *, *, #236, .F. ) ;
#45135=FACE_OUTER_BOUND ( 'NONE', #23429, .T. ) ;
#45137=CYLINDRICAL_SURFACE ( 'NONE', #63331, 7.499999999999988454 ) ;
#45139=ORIENTED_EDGE ( 'NONE', *, *, #34090, .T. ) ;
#45142=ORIENTED_EDGE ( 'NONE', *, *, #61916, .T. ) ;
#45144=ORIENTED_EDGE ( 'NONE', *, *, #58702, .F. ) ;
#45145=CARTESIAN_POINT ( 'NONE',  ( -27.08954555554413446, 2.300063521504144948, -0.1819824474943290971 ) ) ;
#45157=DIRECTION ( 'NONE',  ( -1.000000000000000000, 0.000000000000000000, 0.000000000000000000 ) ) ;
#45159=DIRECTION ( 'NONE',  ( -1.000000000000000000, 0.000000000000000000, 0.000000000000000000 ) ) ;
#45166=CARTESIAN_POINT ( 'NONE',  ( 2.000000000000001776, -1.754183803416586196, 6.711026108862235162 ) ) ;
#45174=CARTESIAN_POINT ( 'NONE',  ( -27.08456565417846917, 2.084650034356375858, 0.9533904527919445648 ) ) ;
#45176=ADVANCED_FACE ( 'NONE', ( #35782 ), #45137, .T. ) ;
#45177=FACE_OUTER_BOUND ( 'NONE', #17523, .T. ) ;
#45178=AXIS2_PLACEMENT_3D ( 'NONE', #40845, #35816, #26519 ) ;
#45191=VERTEX_POINT ( 'NONE', #47117 ) ;
#45196=CARTESIAN_POINT ( 'NONE',  ( -22.27713295444592845, -3.528329525272665634, -1.050517974989019221 ) ) ;
#45207=EDGE_CURVE ( 'NONE', #47458, #23272, #61264, .T. ) ;
#45209=CARTESIAN_POINT ( 'NONE',  ( -27.09602251845159415, 1.927725285105659880, -1.302811993375590172 ) ) ;
#45212=CARTESIAN_POINT ( 'NONE',  ( -35.05012975565874456, -0.01363945138522591922, 0.002839961651350852816 ) ) ;
#45214=DIRECTION ( 'NONE',  ( -1.000000000000000000, 0.000000000000000000, 0.000000000000000000 ) ) ;
#45217=CARTESIAN_POINT ( 'NONE',  ( -27.08430792439081003, -2.211452765398044473, -0.6005833784282822441 ) ) ;
#45224=ORIENTED_EDGE ( 'NONE', *, *, #23195, .F. ) ;
#45225=ORIENTED_EDGE ( 'NONE', *, *, #34213, .T. ) ;
#45230=CARTESIAN_POINT ( 'NONE',  ( -35.04709527796842394, -0.005292201869334239861, -0.01117341439756461274 ) ) ;
#45237=DIRECTION ( 'NONE',  ( 0.000000000000000000, 0.7621620551276332423, 0.6473862847818313560 ) ) ;
#45244=ADVANCED_FACE ( 'NONE', ( #36792 ), #11513, .T. ) ;
#45255=EDGE_CURVE ( 'NONE', #30228, #57752, #47463, .T. ) ;
#45257=CARTESIAN_POINT ( 'NONE',  ( 2.000000000000001776, 0.000000000000000000, 0.000000000000000000 ) ) ;
#45262=CARTESIAN_POINT ( 'NONE',  ( -27.35552965826137140, -0.2619431035391951434, 3.094132632038943065 ) ) ;
#45264=DIRECTION ( 'NONE',  ( -1.000000000000000000, 0.000000000000000000, 0.000000000000000000 ) ) ;
#45267=AXIS2_PLACEMENT_3D ( 'NONE', #39962, #44292, #49631 ) ;
#45269=CARTESIAN_POINT ( 'NONE',  ( -27.09729107899852352, -1.302895495071029419, -1.932259710108178430 ) ) ;
#45270=VECTOR ( 'NONE', #39697, 1000.000000000000000 ) ;
#45272=CARTESIAN_POINT ( 'NONE',  ( 1.000000000000000888, -6.936109781200648250, -2.853135311045116307 ) ) ;
#45275=EDGE_CURVE ( 'NONE', #666, #21047, #7380, .T. ) ;
#45279=ORIENTED_EDGE ( 'NONE', *, *, #4589, .T. ) ;
#45281=EDGE_CURVE ( 'NONE', #39745, #9785, #37560, .T. ) ;
#45291=CARTESIAN_POINT ( 'NONE',  ( -27.05874794189610455, -0.3907329275428090276, -2.180117559290211116 ) ) ;
#45297=VERTEX_POINT ( 'NONE', #33755 ) ;
#45299=FACE_OUTER_BOUND ( 'NONE', #28932, .T. ) ;
#45302=CYLINDRICAL_SURFACE ( 'NONE', #14482, 2.899999999999994582 ) ;
#45315=CARTESIAN_POINT ( 'NONE',  ( -27.08416974970326763, 0.4041872645907068629, 2.255186831366090772 ) ) ;
#45316=CARTESIAN_POINT ( 'NONE',  ( 0.000000000000000000, 2.562706407243739992, -6.312399813420325856 ) ) ;
#45317=AXIS2_PLACEMENT_3D ( 'NONE', #46768, #16184, #16831 ) ;
#45320=EDGE_CURVE ( 'NONE', #3030, #54788, #8492, .T. ) ;
#45329=EDGE_CURVE ( 'NONE', #3120, #22798, #64350, .T. ) ;
#45335=EDGE_CURVE ( 'NONE', #3708, #6580, #4218, .T. ) ;
#45336=ORIENTED_EDGE ( 'NONE', *, *, #55928, .F. ) ;
#45338=DIRECTION ( 'NONE',  ( -1.000000000000000000, 0.000000000000000000, 0.000000000000000000 ) ) ;
#45343=CARTESIAN_POINT ( 'NONE',  ( -35.04683013664716640, -0.006266879427269670538, -0.01065093278706642776 ) ) ;
#45344=CARTESIAN_POINT ( 'NONE',  ( -22.27716857039623477, 3.514919882996461187, 1.095155339732065913 ) ) ;
#45347=DIRECTION ( 'NONE',  ( -1.000000000000000000, 0.000000000000000000, 0.000000000000000000 ) ) ;
#45353=VECTOR ( 'NONE', #8655, 1000.000000000000000 ) ;
#45357=CARTESIAN_POINT ( 'NONE',  ( -35.04709527796842394, 0.01231589140598780829, 0.001082316405371860912 ) ) ;
#45359=CARTESIAN_POINT ( 'NONE',  ( -22.49803948133827447, -2.269619744675244188, -3.704553751086701485 ) ) ;
#45363=ORIENTED_EDGE ( 'NONE', *, *, #57427, .T. ) ;
#45364=ADVANCED_FACE ( 'NONE', ( #50634 ), #45302, .T. ) ;
#45366=ORIENTED_EDGE ( 'NONE', *, *, #44325, .T. ) ;
#45380=ORIENTED_EDGE ( 'NONE', *, *, #21921, .F. ) ;
#45384=CARTESIAN_POINT ( 'NONE',  ( -22.30398854582848145, 0.8844201765542331062, -3.656532484463044241 ) ) ;
#45385=CARTESIAN_POINT ( 'NONE',  ( 2.000000000000001776, 5.860254403322073813, -3.474373880649762381 ) ) ;
#45390=EDGE_CURVE ( 'NONE', #39365, #24342, #57340, .T. ) ;
#45392=ORIENTED_EDGE ( 'NONE', *, *, #34213, .F. ) ;
#45393=CARTESIAN_POINT ( 'NONE',  ( 2.000000000000001776, -5.860254403322033845, 3.474373880649773039 ) ) ;
#45400=CIRCLE ( 'NONE', #16730, 2.899999999999994582 ) ;
#45403=CARTESIAN_POINT ( 'NONE',  ( -27.08419797710328680, -2.125717714519619328, -0.8552720754637029854 ) ) ;
#45418=CARTESIAN_POINT ( 'NONE',  ( -22.31328051695926007, 3.781397440874590732, -0.2528478350593763024 ) ) ;
#45422=ORIENTED_EDGE ( 'NONE', *, *, #11622, .T. ) ;
#45423=CARTESIAN_POINT ( 'NONE',  ( -27.10307689719060420, 2.283215755731188068, 0.5470785519252191476 ) ) ;
#45425=AXIS2_PLACEMENT_3D ( 'NONE', #24438, #38431, #44715 ) ;
#45440=ORIENTED_EDGE ( 'NONE', *, *, #5069, .T. ) ;
#45452=ORIENTED_EDGE ( 'NONE', *, *, #23280, .T. ) ;
#45454=DIRECTION ( 'NONE',  ( -1.000000000000000000, 0.000000000000000000, 0.000000000000000000 ) ) ;
#45456=CARTESIAN_POINT ( 'NONE',  ( -27.08456565417852246, 2.282055114149009967, -0.2166646653333907935 ) ) ;
#45460=CARTESIAN_POINT ( 'NONE',  ( -27.08429572838383947, -0.9410937941433956677, 2.089332284968712816 ) ) ;
#45462=EDGE_LOOP ( 'NONE', ( #47614, #47919, #27152, #42824 ) ) ;
#45470=CARTESIAN_POINT ( 'NONE',  ( -28.67667724226168602, -1.840944188131431236, -0.4371157725390102389 ) ) ;
#45474=DIRECTION ( 'NONE',  ( 0.000000000000000000, 0.7621620551276333533, 0.6473862847818311339 ) ) ;
#45476=CIRCLE ( 'NONE', #923, 7.499999999999988454 ) ;
#45492=DIRECTION ( 'NONE',  ( -0.9606638835031803270, -0.07465901992591204850, 0.2674900627617601279 ) ) ;
#45494=CARTESIAN_POINT ( 'NONE',  ( -27.10113028276155944, -0.5479825692848022678, 2.276991616290404696 ) ) ;
#45500=DIRECTION ( 'NONE',  ( 0.000000000000000000, 0.000000000000000000, -1.000000000000000000 ) ) ;
#45502=VERTEX_POINT ( 'NONE', #7692 ) ;
#45508=CARTESIAN_POINT ( 'NONE',  ( -22.27722019094931127, -3.463038365117174333, -1.249795790945215312 ) ) ;
#45513=DIRECTION ( 'NONE',  ( -1.000000000000000000, 0.000000000000000000, 0.000000000000000000 ) ) ;
#45517=CARTESIAN_POINT ( 'NONE',  ( -35.05175862995318425, 0.003178856583447783879, -0.01216930940959627672 ) ) ;
#45520=CARTESIAN_POINT ( 'NONE',  ( -27.10128162969832388, 1.945744751330104272, -1.304299867634916010 ) ) ;
#45533=DIRECTION ( 'NONE',  ( -1.000000000000000000, 0.000000000000000000, 0.000000000000000000 ) ) ;
#45538=VECTOR ( 'NONE', #40742, 1000.000000000000000 ) ;
#45557=AXIS2_PLACEMENT_3D ( 'NONE', #18507, #28772, #33444 ) ;
#45585=VECTOR ( 'NONE', #45992, 1000.000000000000000 ) ;
#45589=FACE_OUTER_BOUND ( 'NONE', #5073, .T. ) ;
#45593=VERTEX_POINT ( 'NONE', #57588 ) ;
#45595=CARTESIAN_POINT ( 'NONE',  ( -27.10719052120871098, 2.355164825213508450, -0.1538293304135275597 ) ) ;
#45597=CARTESIAN_POINT ( 'NONE',  ( -22.27716857039623477, 0.8090275962000628152, 3.591587580807983127 ) ) ;
#45605=CIRCLE ( 'NONE', #12700, 7.499999999999988454 ) ;
#45615=LINE ( 'NONE', #55619, #25544 ) ;
#45616=CIRCLE ( 'NONE', #10577, 2.899999999999994582 ) ;
#45618=DIRECTION ( 'NONE',  ( -1.000000000000000000, 0.000000000000000000, 0.000000000000000000 ) ) ;
#45620=DIRECTION ( 'NONE',  ( -1.000000000000000000, 0.000000000000000000, 0.000000000000000000 ) ) ;
#45623=CARTESIAN_POINT ( 'NONE',  ( 0.000000000000000000, 0.000000000000000000, 0.000000000000000000 ) ) ;
#45632=ORIENTED_EDGE ( 'NONE', *, *, #59756, .T. ) ;
#45635=ORIENTED_EDGE ( 'NONE', *, *, #64808, .F. ) ;
#45639=CARTESIAN_POINT ( 'NONE',  ( -27.08588607604433207, -2.215240480751993868, 0.6046196991082962713 ) ) ;
#45642=VERTEX_POINT ( 'NONE', #42930 ) ;
#45646=CARTESIAN_POINT ( 'NONE',  ( -22.28506771379528573, 0.8783543640077344783, -3.622079238249916067 ) ) ;
#45649=ADVANCED_FACE ( 'NONE', ( #22665 ), #63210, .T. ) ;
#45651=FACE_OUTER_BOUND ( 'NONE', #16792, .T. ) ;
#45652=ADVANCED_FACE ( 'NONE', ( #48284 ), #24452, .F. ) ;
#45678=ORIENTED_EDGE ( 'NONE', *, *, #53503, .F. ) ;
#45679=ORIENTED_EDGE ( 'NONE', *, *, #53469, .F. ) ;
#45687=CARTESIAN_POINT ( 'NONE',  ( 2.000000000000001776, 0.4129979343797385294, 6.800241778083691457 ) ) ;
#45691=ORIENTED_EDGE ( 'NONE', *, *, #59765, .F. ) ;
#45709=VERTEX_POINT ( 'NONE', #44897 ) ;
#45714=DIRECTION ( 'NONE',  ( 0.000000000000000000, 0.000000000000000000, 1.000000000000000000 ) ) ;
#45719=CIRCLE ( 'NONE', #26632, 7.499999999999988454 ) ;
#45720=CARTESIAN_POINT ( 'NONE',  ( 2.000000000000001776, 0.3246585432986198727, 6.805031400696091914 ) ) ;
#45727=VECTOR ( 'NONE', #64207, 1000.000000000000000 ) ;
#45728=FACE_OUTER_BOUND ( 'NONE', #26745, .T. ) ;
#45731=DIRECTION ( 'NONE',  ( -1.000000000000000000, 0.000000000000000000, 0.000000000000000000 ) ) ;
#45738=VECTOR ( 'NONE', #64718, 1000.000000000000114 ) ;
#45739=VERTEX_POINT ( 'NONE', #65486 ) ;
#45741=FACE_OUTER_BOUND ( 'NONE', #49045, .T. ) ;
#45754=CARTESIAN_POINT ( 'NONE',  ( 0.000000000000000000, 0.000000000000000000, 0.000000000000000000 ) ) ;
#45755=CARTESIAN_POINT ( 'NONE',  ( -22.27719381268171261, -0.9326100520993095833, -3.561499689648256251 ) ) ;
#45756=LINE ( 'NONE', #26142, #48773 ) ;
#45781=DIRECTION ( 'NONE',  ( 0.000000000000000000, -0.1081190184239489566, 0.9941379571543588201 ) ) ;
#45791=CARTESIAN_POINT ( 'NONE',  ( 2.000000000000001776, -7.203928197742088813, -2.086484728383233289 ) ) ;
#45794=ADVANCED_FACE ( 'NONE', ( #57849 ), #56868, .T. ) ;
#45797=DIRECTION ( 'NONE',  ( 0.000000000000000000, 0.000000000000000000, 1.000000000000000000 ) ) ;
#45798=LINE ( 'NONE', #41442, #62819 ) ;
#45799=EDGE_CURVE ( 'NONE', #42911, #2803, #54904, .T. ) ;
#45806=ORIENTED_EDGE ( 'NONE', *, *, #38913, .F. ) ;
#45816=ADVANCED_FACE ( 'NONE', ( #27232 ), #12263, .T. ) ;
#45818=ORIENTED_EDGE ( 'NONE', *, *, #37377, .F. ) ;
#45820=AXIS2_PLACEMENT_3D ( 'NONE', #25206, #4632, #14876 ) ;
#45822=VERTEX_POINT ( 'NONE', #7267 ) ;
#45829=ORIENTED_EDGE ( 'NONE', *, *, #58482, .T. ) ;
#45830=CARTESIAN_POINT ( 'NONE',  ( 2.000000000000001776, -1.530946385938423582, 7.342084388195347699 ) ) ;
#45831=CARTESIAN_POINT ( 'NONE',  ( 0.000000000000000000, 0.000000000000000000, 0.000000000000000000 ) ) ;
#45836=AXIS2_PLACEMENT_3D ( 'NONE', #62380, #37786, #51783 ) ;
#45838=( BOUNDED_SURFACE ( )  B_SPLINE_SURFACE ( 3, 1, ( 
 ( #64577, #43654 ),
 ( #59620, #8101 ),
 ( #63944, #18420 ),
 ( #38686, #13400 ) ),
 .UNSPECIFIED., .F., .F., .F. ) 
 B_SPLINE_SURFACE_WITH_KNOTS ( ( 4, 4 ),
 ( 2, 2 ),
 ( 0.000000000000000000, 1.000000000000000000 ),
 ( 0.000000000000000000, 1.000000000000000000 ),
 .UNSPECIFIED. ) 
 GEOMETRIC_REPRESENTATION_ITEM ( )  RATIONAL_B_SPLINE_SURFACE ( (
 ( 1.000000000000000000, 1.000000000000000000),
 ( 0.8716676215708681896, 0.8964445200148167814),
 ( 0.8716676215708681896, 0.8964445200148167814),
 ( 1.000000000000000000, 1.000000000000000000) ) ) 
 REPRESENTATION_ITEM ( '' )  SURFACE ( )  );
#45840=DIRECTION ( 'NONE',  ( 1.000000000000000000, 0.000000000000000000, 0.000000000000000000 ) ) ;
#45846=CARTESIAN_POINT ( 'NONE',  ( -22.30625920655495165, -1.076742202099146839, -3.635849356906419416 ) ) ;
#45868=AXIS2_PLACEMENT_3D ( 'NONE', #31519, #26216, #15884 ) ;
#45869=CARTESIAN_POINT ( 'NONE',  ( -27.10422407540546885, 1.954655484500564588, -1.306850885988315003 ) ) ;
#45870=EDGE_CURVE ( 'NONE', #35715, #8602, #57046, .T. ) ;
#45877=CARTESIAN_POINT ( 'NONE',  ( 2.000000000000001776, -7.493043167941613625, 0.3229614270519164942 ) ) ;
#45892=LINE ( 'NONE', #21258, #44787 ) ;
#45893=CARTESIAN_POINT ( 'NONE',  ( -22.94572469358971034, 4.424217216616520787, -2.078200699019419062 ) ) ;
#45894=CARTESIAN_POINT ( 'NONE',  ( -22.27384469013076185, -1.508555848190757276, 3.358914544760229326 ) ) ;
#45900=CARTESIAN_POINT ( 'NONE',  ( -27.10719052120871098, 0.6736837626858914740, 2.261993590776020469 ) ) ;
#45907=CIRCLE ( 'NONE', #11893, 6.936499999999989008 ) ;
#45915=DIRECTION ( 'NONE',  ( -1.000000000000000000, 0.000000000000000000, 0.000000000000000000 ) ) ;
#45921=VECTOR ( 'NONE', #26161, 1000.000000000000000 ) ;
#45927=CARTESIAN_POINT ( 'NONE',  ( -35.04582288351658548, -0.006225574250549492823, 0.01107592729723125800 ) ) ;
#45933=EDGE_CURVE ( 'NONE', #53268, #38732, #18899, .T. ) ;
#45941=CIRCLE ( 'NONE', #48139, 6.936499999999989896 ) ;
#45943=ORIENTED_EDGE ( 'NONE', *, *, #53913, .T. ) ;
#45947=CARTESIAN_POINT ( 'NONE',  ( -22.65999102136914445, 1.886119913916099122, 4.450325798697146062 ) ) ;
#45948=AXIS2_PLACEMENT_3D ( 'NONE', #30383, #65607, #35683 ) ;
#45954=ORIENTED_EDGE ( 'NONE', *, *, #21145, .T. ) ;
#45955=CARTESIAN_POINT ( 'NONE',  ( -22.28121537037576871, 0.3168735205819809830, 3.680034389105500292 ) ) ;
#45956=EDGE_CURVE ( 'NONE', #55487, #30787, #1757, .T. ) ;
#45962=DIRECTION ( 'NONE',  ( -1.000000000000000000, 0.000000000000000000, 0.000000000000000000 ) ) ;
#45984=CARTESIAN_POINT ( 'NONE',  ( 2.000000000000001776, 0.000000000000000000, 0.000000000000000000 ) ) ;
#45986=CARTESIAN_POINT ( 'NONE',  ( 2.000000000000001776, -6.164400007374799095, 2.900694413976478536 ) ) ;
#45992=DIRECTION ( 'NONE',  ( 1.000000000000000000, -0.000000000000000000, -0.000000000000000000 ) ) ;
#45993=EDGE_LOOP ( 'NONE', ( #51518, #48563, #14601, #16820 ) ) ;
#45997=CIRCLE ( 'NONE', #47092, 6.936499999999988120 ) ;
#45999=CARTESIAN_POINT ( 'NONE',  ( -35.05012975565874456, -0.009279204628466307739, -0.01039213056760250956 ) ) ;
#46002=CIRCLE ( 'NONE', #17335, 2.899999999999994582 ) ;
#46009=VECTOR ( 'NONE', #49531, 1000.000000000000000 ) ;
#46016=EDGE_CURVE ( 'NONE', #8079, #11936, #27315, .T. ) ;
#46031=DIRECTION ( 'NONE',  ( 0.000000000000000000, 0.000000000000000000, 1.000000000000000000 ) ) ;
#46034=( BOUNDED_SURFACE ( )  B_SPLINE_SURFACE ( 3, 1, ( 
 ( #27100, #61675 ),
 ( #16134, #41729 ),
 ( #21458, #62023 ),
 ( #25795, #11463 ) ),
 .UNSPECIFIED., .F., .F., .F. ) 
 B_SPLINE_SURFACE_WITH_KNOTS ( ( 4, 4 ),
 ( 2, 2 ),
 ( 0.000000000000000000, 1.000000000000000000 ),
 ( 0.000000000000000000, 1.000000000000000000 ),
 .UNSPECIFIED. ) 
 GEOMETRIC_REPRESENTATION_ITEM ( )  RATIONAL_B_SPLINE_SURFACE ( (
 ( 1.000000000000000000, 1.000000000000000000),
 ( 0.9257577194822556033, 0.9980522942447415113),
 ( 0.9257577194822556033, 0.9980522942447415113),
 ( 1.000000000000000000, 1.000000000000000000) ) ) 
 REPRESENTATION_ITEM ( '' )  SURFACE ( )  );
#46039=ORIENTED_EDGE ( 'NONE', *, *, #61841, .T. ) ;
#46041=VERTEX_POINT ( 'NONE', #3941 ) ;
#46042=VECTOR ( 'NONE', #39933, 1000.000000000000000 ) ;
#46052=AXIS2_PLACEMENT_3D ( 'NONE', #233, #14506, #29807 ) ;
#46059=CARTESIAN_POINT ( 'NONE',  ( 1.000000000000000888, -7.493043167941613625, 0.3229614270519164942 ) ) ;
#46060=ORIENTED_EDGE ( 'NONE', *, *, #61208, .T. ) ;
#46063=B_SPLINE_CURVE_WITH_KNOTS ( 'NONE', 3,
 ( #49022, #3480, #39336, #33379, #63616, #54669, #27723, #23748, #23080, #43339, #44017, #64290, #58677, #48027, #59308, #13734, #18089, #34017, #54334, #38356, #22762, #19071 ),
 .UNSPECIFIED., .F., .F.,
 ( 4, 3, 3, 3, 3, 3, 3, 4 ),
 ( 0.000000000000000000, 4.447697177976273769E-05, 6.624143997791219474E-05, 8.800576886944384261E-05, 0.0001097699864780899689, 0.0001315341395364383575, 0.0001760120188223303806, 0.0001867971373174759061 ),
 .UNSPECIFIED. ) ;
#46093=VECTOR ( 'NONE', #17047, 1000.000000000000000 ) ;
#46099=CARTESIAN_POINT ( 'NONE',  ( -27.32343372485684796, -2.534722478175144289, -1.625341394141124773 ) ) ;
#46101=CIRCLE ( 'NONE', #35442, 2.899999999999994582 ) ;
#46110=EDGE_LOOP ( 'NONE', ( #64197, #53894, #20642, #6956 ) ) ;
#46114=ORIENTED_EDGE ( 'NONE', *, *, #62170, .F. ) ;
#46116=CARTESIAN_POINT ( 'NONE',  ( -27.09150307427401216, 1.305148381378462563, 1.909742362149637440 ) ) ;
#46130=DIRECTION ( 'NONE',  ( 0.000000000000000000, 0.000000000000000000, 1.000000000000000000 ) ) ;
#46133=DIRECTION ( 'NONE',  ( -1.000000000000000000, 0.000000000000000000, 0.000000000000000000 ) ) ;
#46134=CARTESIAN_POINT ( 'NONE',  ( -22.27722022243423794, -1.227876413014574952, 3.470949075637804970 ) ) ;
#46137=EDGE_CURVE ( 'NONE', #22708, #34425, #31873, .T. ) ;
#46144=CARTESIAN_POINT ( 'NONE',  ( -27.09048036756592026, 2.303144499688039470, -0.1785511875142904714 ) ) ;
#46147=CARTESIAN_POINT ( 'NONE',  ( 0.000000000000000000, 0.000000000000000000, 0.000000000000000000 ) ) ;
#46154=DIRECTION ( 'NONE',  ( 0.000000000000000000, 0.000000000000000000, 1.000000000000000000 ) ) ;
#46158=DIRECTION ( 'NONE',  ( -1.000000000000000000, 0.000000000000000000, 0.000000000000000000 ) ) ;
#46162=DIRECTION ( 'NONE',  ( 0.000000000000000000, 0.000000000000000000, 1.000000000000000000 ) ) ;
#46163=EDGE_CURVE ( 'NONE', #22582, #47105, #839, .T. ) ;
#46169=VERTEX_POINT ( 'NONE', #2221 ) ;
#46171=CARTESIAN_POINT ( 'NONE',  ( 0.000000000000000000, 0.000000000000000000, 0.000000000000000000 ) ) ;
#46174=CARTESIAN_POINT ( 'NONE',  ( -22.59983133926799326, 3.996991822164152719, 2.378226455340815448 ) ) ;
#46177=DIRECTION ( 'NONE',  ( 0.9606638835031803270, -0.02862840969242716124, -0.2762341707520462042 ) ) ;
#46179=CARTESIAN_POINT ( 'NONE',  ( 0.000000000000000000, -6.164400007374764456, -2.900694413976575792 ) ) ;
#46180=ORIENTED_EDGE ( 'NONE', *, *, #40149, .F. ) ;
#46187=EDGE_CURVE ( 'NONE', #11911, #61252, #41787, .T. ) ;
#46194=CARTESIAN_POINT ( 'NONE',  ( -35.04582288351658548, -0.01107592729725561699, -0.006225574250545745821 ) ) ;
#46196=CARTESIAN_POINT ( 'NONE',  ( -22.27719443589224113, -3.500848524682613760, -1.139586749255983911 ) ) ;
#46198=DIRECTION ( 'NONE',  ( 1.000000000000000000, 0.000000000000000000, 0.000000000000000000 ) ) ;
#46204=CARTESIAN_POINT ( 'NONE',  ( -22.27720412283625961, 2.444672752438211916, 2.752887114864203788 ) ) ;
#46206=AXIS2_PLACEMENT_3D ( 'NONE', #21412, #41687, #61977 ) ;
#46218=ORIENTED_EDGE ( 'NONE', *, *, #36465, .T. ) ;
#46221=ORIENTED_EDGE ( 'NONE', *, *, #5650, .F. ) ;
#46223=ORIENTED_EDGE ( 'NONE', *, *, #62442, .F. ) ;
#46228=AXIS2_PLACEMENT_3D ( 'NONE', #62903, #6093, #12355 ) ;
#46231=EDGE_LOOP ( 'NONE', ( #35690, #5261, #43776, #6634 ) ) ;
#46233=( BOUNDED_SURFACE ( )  B_SPLINE_SURFACE ( 3, 1, ( 
 ( #35209, #24259 ),
 ( #40879, #64806 ),
 ( #25572, #9958 ),
 ( #45517, #40196 ) ),
 .UNSPECIFIED., .F., .F., .F. ) 
 B_SPLINE_SURFACE_WITH_KNOTS ( ( 4, 4 ),
 ( 2, 2 ),
 ( 0.000000000000000000, 1.000000000000000000 ),
 ( 0.000000000000000000, 1.000000000000000000 ),
 .UNSPECIFIED. ) 
 GEOMETRIC_REPRESENTATION_ITEM ( )  RATIONAL_B_SPLINE_SURFACE ( (
 ( 1.000000000000000000, 1.000000000000000000),
 ( 0.8716676215708681896, 0.8964445200148164483),
 ( 0.8716676215708681896, 0.8964445200148164483),
 ( 1.000000000000000000, 1.000000000000000000) ) ) 
 REPRESENTATION_ITEM ( '' )  SURFACE ( )  );
#46234=ORIENTED_EDGE ( 'NONE', *, *, #2086, .T. ) ;
#46251=DIRECTION ( 'NONE',  ( 0.000000000000000000, 0.000000000000000000, 1.000000000000000000 ) ) ;
#46259=EDGE_CURVE ( 'NONE', #1482, #52904, #37454, .T. ) ;
#46274=ORIENTED_EDGE ( 'NONE', *, *, #59393, .T. ) ;
#46278=EDGE_CURVE ( 'NONE', #39065, #2509, #14570, .T. ) ;
#46280=ORIENTED_EDGE ( 'NONE', *, *, #33769, .F. ) ;
#46288=ORIENTED_EDGE ( 'NONE', *, *, #49803, .F. ) ;
#46301=CARTESIAN_POINT ( 'NONE',  ( 0.000000000000000000, 6.935703035393448346, -0.1051458740707923722 ) ) ;
#46304=EDGE_LOOP ( 'NONE', ( #43965, #5001, #59182, #44985 ) ) ;
#46315=CARTESIAN_POINT ( 'NONE',  ( 0.000000000000000000, 0.4129979343798200753, -6.800241778083709221 ) ) ;
#46325=CARTESIAN_POINT ( 'NONE',  ( -27.10422407540547241, -1.039355862229903282, 2.109093808474363119 ) ) ;
#46333=EDGE_CURVE ( 'NONE', #8848, #29500, #23174, .T. ) ;
#46343=EDGE_LOOP ( 'NONE', ( #12754, #55984, #18477, #60454 ) ) ;
#46344=CARTESIAN_POINT ( 'NONE',  ( 2.000000000000001776, -5.888698556700742159, -3.665823448873470003 ) ) ;
#46345=DIRECTION ( 'NONE',  ( 0.000000000000000000, 0.000000000000000000, 1.000000000000000000 ) ) ;
#46346=VERTEX_POINT ( 'NONE', #38099 ) ;
#46349=CARTESIAN_POINT ( 'NONE',  ( -27.28563798457902578, -1.413023339712117910, -2.528380693767751097 ) ) ;
#46352=CARTESIAN_POINT ( 'NONE',  ( -22.29978294495153435, -3.598607126810739132, 1.052446240539704814 ) ) ;
#46360=ORIENTED_EDGE ( 'NONE', *, *, #11135, .F. ) ;
#46362=VERTEX_POINT ( 'NONE', #63691 ) ;
#46369=EDGE_CURVE ( 'NONE', #52982, #52767, #7138, .T. ) ;
#46378=ORIENTED_EDGE ( 'NONE', *, *, #63655, .F. ) ;
#46391=CYLINDRICAL_SURFACE ( 'NONE', #59360, 6.936499999999988120 ) ;
#46394=EDGE_CURVE ( 'NONE', #11939, #54645, #30935, .T. ) ;
#46396=EDGE_CURVE ( 'NONE', #61330, #65638, #29489, .T. ) ;
#46407=FACE_OUTER_BOUND ( 'NONE', #35568, .T. ) ;
#46421=CARTESIAN_POINT ( 'NONE',  ( -27.35552965826137140, -3.094132632038958608, -0.2619431035392160156 ) ) ;
#46423=CARTESIAN_POINT ( 'NONE',  ( -35.04709527796842394, -0.001003525937983557048, 0.01232256164995608472 ) ) ;
#46436=EDGE_CURVE ( 'NONE', #32874, #10092, #35831, .T. ) ;
#46437=DIRECTION ( 'NONE',  ( 0.000000000000000000, 0.4198891015602657650, -0.9075754196709565624 ) ) ;
#46443=ORIENTED_EDGE ( 'NONE', *, *, #44915, .T. ) ;
#46445=ADVANCED_FACE ( 'NONE', ( #179 ), #9468, .T. ) ;
#46448=CARTESIAN_POINT ( 'NONE',  ( -27.08850691366480135, 0.5697889027535644191, -2.232573186527720743 ) ) ;
#46453=EDGE_CURVE ( 'NONE', #40758, #53254, #1886, .T. ) ;
#46460=FACE_OUTER_BOUND ( 'NONE', #13506, .T. ) ;
#46463=DIRECTION ( 'NONE',  ( -1.000000000000000000, 0.000000000000000000, 0.000000000000000000 ) ) ;
#46464=DIRECTION ( 'NONE',  ( 0.000000000000000000, 0.000000000000000000, 1.000000000000000000 ) ) ;
#46465=ORIENTED_EDGE ( 'NONE', *, *, #23340, .F. ) ;
#46471=ADVANCED_FACE ( 'NONE', ( #51715 ), #41372, .T. ) ;
#46472=LINE ( 'NONE', #51805, #11226 ) ;
#46477=DIRECTION ( 'NONE',  ( 0.000000000000000000, 0.9868265225415265851, -0.1617819965527618475 ) ) ;
#46478=CARTESIAN_POINT ( 'NONE',  ( 1.000000000000000888, -0.8935325819928070512, -7.446583077151393226 ) ) ;
#46479=B_SPLINE_CURVE_WITH_KNOTS ( 'NONE', 3,
 ( #41335, #51995, #46349, #790, #27048, #57307 ),
 .UNSPECIFIED., .F., .F.,
 ( 4, 2, 4 ),
 ( 0.0001654224980408343251, 0.0006219428995476489370, 0.001078463301054463468 ),
 .UNSPECIFIED. ) ;
#46493=DIRECTION ( 'NONE',  ( -1.000000000000000000, 0.000000000000000000, 0.000000000000000000 ) ) ;
#46496=CARTESIAN_POINT ( 'NONE',  ( -35.04683013664716640, 0.01075274318001804771, 0.006090538653935762686 ) ) ;
#46503=CARTESIAN_POINT ( 'NONE',  ( -22.31328051695926007, 2.608921479762127849, -2.748895659348120635 ) ) ;
#46505=DIRECTION ( 'NONE',  ( -0.9606638835031803270, 0.1984016392583671240, -0.1943236796486234874 ) ) ;
#46509=ORIENTED_EDGE ( 'NONE', *, *, #8169, .T. ) ;
#46512=CARTESIAN_POINT ( 'NONE',  ( 0.000000000000000000, 1.145812388885126820, 6.715725538143592743 ) ) ;
#46513=CARTESIAN_POINT ( 'NONE',  ( -27.05874794189610455, 1.734723475976807094E-15, -8.673617379884035472E-15 ) ) ;
#46518=ORIENTED_EDGE ( 'NONE', *, *, #22801, .T. ) ;
#46521=FACE_OUTER_BOUND ( 'NONE', #17244, .T. ) ;
#46537=ORIENTED_EDGE ( 'NONE', *, *, #45335, .F. ) ;
#46542=CARTESIAN_POINT ( 'NONE',  ( -27.09833916700227263, 0.6583442518269375654, 2.238843247505173828 ) ) ;
#46543=VECTOR ( 'NONE', #21433, 1000.000000000000114 ) ;
#46545=ADVANCED_FACE ( 'NONE', ( #26422 ), #31721, .T. ) ;
#46549=DIRECTION ( 'NONE',  ( 0.000000000000000000, 0.000000000000000000, 1.000000000000000000 ) ) ;
#46573=CARTESIAN_POINT ( 'NONE',  ( -27.08423923533013422, 1.832018136655364282, -1.376387618994801887 ) ) ;
#46576=EDGE_CURVE ( 'NONE', #13308, #46362, #43300, .T. ) ;
#46587=AXIS2_PLACEMENT_3D ( 'NONE', #58419, #19148, #23158 ) ;
#46594=EDGE_CURVE ( 'NONE', #65174, #26729, #25279, .T. ) ;
#46595=ORIENTED_EDGE ( 'NONE', *, *, #11703, .T. ) ;
#46600=ORIENTED_EDGE ( 'NONE', *, *, #18650, .T. ) ;
#46607=DIRECTION ( 'NONE',  ( 0.000000000000000000, 0.000000000000000000, 1.000000000000000000 ) ) ;
#46615=ORIENTED_EDGE ( 'NONE', *, *, #13674, .T. ) ;
#46618=CIRCLE ( 'NONE', #28524, 6.936499999999988120 ) ;
#46619=CYLINDRICAL_SURFACE ( 'NONE', #14714, 2.899999999999994582 ) ;
#46635=CARTESIAN_POINT ( 'NONE',  ( -22.27218376572352554, 0.9173404081777805086, -3.566922835983788787 ) ) ;
#46640=CARTESIAN_POINT ( 'NONE',  ( -27.09483304420744076, -1.013994808269844228, 2.090133548855273027 ) ) ;
#46648=CARTESIAN_POINT ( 'NONE',  ( -26.43258404273187523, -1.987083010659168592, 2.854888342447762906 ) ) ;
#46649=ADVANCED_FACE ( 'NONE', ( #49023 ), #12420, .T. ) ;
#46654=ORIENTED_EDGE ( 'NONE', *, *, #52632, .T. ) ;
#46658=VERTEX_POINT ( 'NONE', #23081 ) ;
#46661=ORIENTED_EDGE ( 'NONE', *, *, #821, .T. ) ;
#46668=CARTESIAN_POINT ( 'NONE',  ( -22.28694879868232448, -3.570244315741558871, 1.011812214896726791 ) ) ;
#46676=FACE_OUTER_BOUND ( 'NONE', #6366, .T. ) ;
#46695=VERTEX_POINT ( 'NONE', #48372 ) ;
#46699=DIRECTION ( 'NONE',  ( 0.000000000000000000, 0.000000000000000000, -1.000000000000000000 ) ) ;
#46703=DIRECTION ( 'NONE',  ( 0.000000000000000000, 0.000000000000000000, 1.000000000000000000 ) ) ;
#46708=AXIS2_PLACEMENT_3D ( 'NONE', #30670, #31344, #15053 ) ;
#46712=B_SPLINE_CURVE_WITH_KNOTS ( 'NONE', 3,
 ( #50514, #11246, #9935, #5623, #4957, #299, #55488, #14889, #25220, #55823, #5278, #625, #25548, #15563, #15880, #45494, #35826, #41156, #40854 ),
 .UNSPECIFIED., .F., .F.,
 ( 4, 3, 3, 3, 3, 3, 4 ),
 ( 0.000000000000000000, 2.832085443685182426E-05, 4.217789847592154422E-05, 5.603488375296287891E-05, 6.989180858882558772E-05, 9.821094830335149047E-05, 0.0001178165571463608645 ),
 .UNSPECIFIED. ) ;
#46713=AXIS2_PLACEMENT_3D ( 'NONE', #41502, #40873, #1304 ) ;
#46724=CARTESIAN_POINT ( 'NONE',  ( 2.000000000000001776, -3.152010634611648321, -6.039758645301327000 ) ) ;
#46728=DIRECTION ( 'NONE',  ( -1.000000000000000000, 0.000000000000000000, 0.000000000000000000 ) ) ;
#46739=ORIENTED_EDGE ( 'NONE', *, *, #9383, .F. ) ;
#46740=CYLINDRICAL_SURFACE ( 'NONE', #20355, 2.899999999999994582 ) ;
#46744=AXIS2_PLACEMENT_3D ( 'NONE', #40692, #45347, #55668 ) ;
#46766=ORIENTED_EDGE ( 'NONE', *, *, #4285, .T. ) ;
#46768=CARTESIAN_POINT ( 'NONE',  ( 0.000000000000000000, 6.767909380267589370, 0.7805499053121639497 ) ) ;
#46770=EDGE_CURVE ( 'NONE', #54645, #32746, #12668, .T. ) ;
#46792=ORIENTED_EDGE ( 'NONE', *, *, #37238, .T. ) ;
#46799=CARTESIAN_POINT ( 'NONE',  ( -22.28939870658739864, -3.707376022556851503, 0.2834927284407648407 ) ) ;
#46803=VERTEX_POINT ( 'NONE', #24718 ) ;
#46804=CYLINDRICAL_SURFACE ( 'NONE', #22939, 2.899999999999994582 ) ;
#46808=AXIS2_PLACEMENT_3D ( 'NONE', #58378, #22469, #63027 ) ;
#46824=EDGE_CURVE ( 'NONE', #12277, #7851, #4446, .T. ) ;
#46828=EDGE_LOOP ( 'NONE', ( #4947, #45452 ) ) ;
#46832=CARTESIAN_POINT ( 'NONE',  ( 2.000000000000001776, 1.225832621831852931, 6.827324998361547159 ) ) ;
#46836=CARTESIAN_POINT ( 'NONE',  ( 0.000000000000000000, -1.225832621831797420, -6.827324998361596009 ) ) ;
#46850=LINE ( 'NONE', #56855, #52450 ) ;
#46851=CARTESIAN_POINT ( 'NONE',  ( -22.65996813707686641, 2.607318832796713171, -4.069902221062751124 ) ) ;
#46862=EDGE_LOOP ( 'NONE', ( #3935, #45380, #24822, #12425 ) ) ;
#46866=CARTESIAN_POINT ( 'NONE',  ( -22.27711351828769892, -2.657880562424684179, 2.547249869018247015 ) ) ;
#46872=EDGE_LOOP ( 'NONE', ( #25936, #15101, #1797, #34866 ) ) ;
#46875=DIRECTION ( 'NONE',  ( 0.000000000000000000, 0.1081190184239352453, 0.9941379571543603744 ) ) ;
#46876=EDGE_LOOP ( 'NONE', ( #51292, #22326, #23227, #53650 ) ) ;
#46888=VERTEX_POINT ( 'NONE', #36962 ) ;
#46889=CARTESIAN_POINT ( 'NONE',  ( 0.000000000000000000, -6.767909380267597363, 2.119450094687866049 ) ) ;
#46896=ORIENTED_EDGE ( 'NONE', *, *, #40017, .F. ) ;
#46897=CARTESIAN_POINT ( 'NONE',  ( 0.000000000000000000, 6.160607635185406217, 4.277489166005578269 ) ) ;
#46910=ADVANCED_FACE ( 'NONE', ( #15691 ), #10865, .F. ) ;
#46916=ORIENTED_EDGE ( 'NONE', *, *, #51659, .T. ) ;
#46923=AXIS2_PLACEMENT_3D ( 'NONE', #12421, #52374, #2137 ) ;
#46927=DIRECTION ( 'NONE',  ( -0.3162277663656185012, -0.1673616205762862574, -0.9338040949457712125 ) ) ;
#46941=DIRECTION ( 'NONE',  ( 0.000000000000000000, 0.000000000000000000, 1.000000000000000000 ) ) ;
#46942=ADVANCED_FACE ( 'NONE', ( #62243 ), #40985, .T. ) ;
#46950=CARTESIAN_POINT ( 'NONE',  ( -27.35552965826137140, -2.548625910254533888, -1.773915698030580357 ) ) ;
#46953=EDGE_CURVE ( 'NONE', #49753, #11283, #22929, .T. ) ;
#46965=ORIENTED_EDGE ( 'NONE', *, *, #13093, .F. ) ;
#46973=DIRECTION ( 'NONE',  ( 1.000000000000000000, 0.000000000000000000, 0.000000000000000000 ) ) ;
#46978=CARTESIAN_POINT ( 'NONE',  ( -27.09602251845158705, -1.018053071731303660, 2.092130925171132638 ) ) ;
#46979=ADVANCED_FACE ( 'NONE', ( #26031 ), #63106, .F. ) ;
#46982=CARTESIAN_POINT ( 'NONE',  ( -22.51237073810381162, -3.719289647955757783, 2.395115314842892751 ) ) ;
#46984=CARTESIAN_POINT ( 'NONE',  ( 0.000000000000000000, -0.2704997240204360387, -6.931223712253490987 ) ) ;
#46993=ORIENTED_EDGE ( 'NONE', *, *, #22042, .T. ) ;
#47004=EDGE_CURVE ( 'NONE', #16340, #38810, #21038, .T. ) ;
#47007=ORIENTED_EDGE ( 'NONE', *, *, #12539, .F. ) ;
#47008=VERTEX_POINT ( 'NONE', #48527 ) ;
#47012=VERTEX_POINT ( 'NONE', #3649 ) ;
#47030=CARTESIAN_POINT ( 'NONE',  ( 2.000000000000001776, 0.000000000000000000, 0.000000000000000000 ) ) ;
#47047=LINE ( 'NONE', #57024, #21117 ) ;
#47049=CARTESIAN_POINT ( 'NONE',  ( 2.000000000000001776, -5.217815162096861137, 5.387430271863535403 ) ) ;
#47053=VECTOR ( 'NONE', #50605, 1000.000000000000000 ) ;
#47054=EDGE_CURVE ( 'NONE', #64495, #6128, #51883, .T. ) ;
#47061=CIRCLE ( 'NONE', #29017, 2.899999999999995470 ) ;
#47068=ORIENTED_EDGE ( 'NONE', *, *, #1550, .T. ) ;
#47069=CARTESIAN_POINT ( 'NONE',  ( -27.08426504710140392, 0.5533780324190830102, 2.223709847896192748 ) ) ;
#47074=CIRCLE ( 'NONE', #40697, 6.936499999999989896 ) ;
#47080=CARTESIAN_POINT ( 'NONE',  ( -35.05012975565874456, 0.01296790604419477931, 0.005092487515914018679 ) ) ;
#47081=EDGE_LOOP ( 'NONE', ( #23562, #34763, #20743, #36906 ) ) ;
#47083=DIRECTION ( 'NONE',  ( 0.000000000000000000, 0.1081190184239353008, 0.9941379571543603744 ) ) ;
#47089=ORIENTED_EDGE ( 'NONE', *, *, #65675, .F. ) ;
#47092=AXIS2_PLACEMENT_3D ( 'NONE', #50992, #1102, #5786 ) ;
#47097=CARTESIAN_POINT ( 'NONE',  ( -27.10719052120871098, 1.714424047991082389, 1.622102031466668093 ) ) ;
#47105=VERTEX_POINT ( 'NONE', #13269 ) ;
#47108=EDGE_LOOP ( 'NONE', ( #18971, #31575, #36234, #64555 ) ) ;
#47116=CYLINDRICAL_SURFACE ( 'NONE', #60600, 2.899999999999994582 ) ;
#47117=CARTESIAN_POINT ( 'NONE',  ( -27.35552965826137140, -1.773915698030568366, 2.548625910254532112 ) ) ;
#47119=ORIENTED_EDGE ( 'NONE', *, *, #63792, .T. ) ;
#47120=AXIS2_PLACEMENT_3D ( 'NONE', #6650, #32220, #46875 ) ;
#47121=ORIENTED_EDGE ( 'NONE', *, *, #27671, .F. ) ;
#47123=VERTEX_POINT ( 'NONE', #44173 ) ;
#47130=DIRECTION ( 'NONE',  ( -1.000000000000000000, 0.000000000000000000, 0.000000000000000000 ) ) ;
#47154=ADVANCED_FACE ( 'NONE', ( #8274 ), #31269, .F. ) ;
#47157=CIRCLE ( 'NONE', #3651, 2.899999999999995470 ) ;
#47163=B_SPLINE_CURVE_WITH_KNOTS ( 'NONE', 3,
 ( #20765, #24775, #60026, #35708, #45054, #4165 ),
 .UNSPECIFIED., .F., .F.,
 ( 4, 2, 4 ),
 ( 0.000000000000000000, 0.0004528561986909421331, 0.0009057123973818842662 ),
 .UNSPECIFIED. ) ;
#47168=AXIS2_PLACEMENT_3D ( 'NONE', #34436, #64671, #55718 ) ;
#47170=ORIENTED_EDGE ( 'NONE', *, *, #19228, .F. ) ;
#47175=CARTESIAN_POINT ( 'NONE',  ( -22.30625920655495165, -3.635849356906410534, 1.076742202099151946 ) ) ;
#47179=CARTESIAN_POINT ( 'NONE',  ( 2.000000000000001776, 0.000000000000000000, 0.000000000000000000 ) ) ;
#47183=CARTESIAN_POINT ( 'NONE',  ( 2.000000000000001776, 0.000000000000000000, 0.000000000000000000 ) ) ;
#47193=CARTESIAN_POINT ( 'NONE',  ( -27.32337605527168023, 1.175835497775001626, 2.771816950947462832 ) ) ;
#47198=DIRECTION ( 'NONE',  ( -1.000000000000000000, 0.000000000000000000, 0.000000000000000000 ) ) ;
#47201=CARTESIAN_POINT ( 'NONE',  ( -22.31328051695926007, 1.671726071983979711, -3.401210163132561082 ) ) ;
#47203=ORIENTED_EDGE ( 'NONE', *, *, #28693, .F. ) ;
#47208=VECTOR ( 'NONE', #38705, 1000.000000000000000 ) ;
#47219=CARTESIAN_POINT ( 'NONE',  ( -22.65996813707687707, -4.069902221062768000, -2.607318832796705177 ) ) ;
#47238=CARTESIAN_POINT ( 'NONE',  ( -27.08639648637141661, -0.6092497698725154454, -2.215564006614442416 ) ) ;
#47241=EDGE_LOOP ( 'NONE', ( #30884, #13322, #39432, #63158 ) ) ;
#47259=VERTEX_POINT ( 'NONE', #15535 ) ;
#47263=EDGE_CURVE ( 'NONE', #16108, #9767, #56099, .T. ) ;
#47280=LINE ( 'NONE', #57581, #15054 ) ;
#47288=ADVANCED_FACE ( 'NONE', ( #46460 ), #28727, .F. ) ;
#47297=CARTESIAN_POINT ( 'NONE',  ( 2.000000000000001776, -4.976357229393820525, -4.652926418895619420 ) ) ;
#47310=CARTESIAN_POINT ( 'NONE',  ( 2.000000000000001776, 0.000000000000000000, 0.000000000000000000 ) ) ;
#47312=DIRECTION ( 'NONE',  ( 0.000000000000000000, -0.3193015301359669600, -0.9476531711828067861 ) ) ;
#47317=AXIS2_PLACEMENT_3D ( 'NONE', #47310, #37303, #57616 ) ;
#47325=CARTESIAN_POINT ( 'NONE',  ( -22.27710395300133328, -2.585700543510490501, -2.620347679538754360 ) ) ;
#47326=ADVANCED_FACE ( 'NONE', ( #7198 ), #20183, .F. ) ;
#47330=CARTESIAN_POINT ( 'NONE',  ( 0.000000000000000000, 6.777474576704068276, 0.6925993764990892032 ) ) ;
#47333=DIRECTION ( 'NONE',  ( 0.000000000000000000, 0.9635499925192236859, -0.2675283385292183680 ) ) ;
#47343=CARTESIAN_POINT ( 'NONE',  ( -27.08423923533013777, -1.832018136655359841, 1.376387618994798112 ) ) ;
#47346=CARTESIAN_POINT ( 'NONE',  ( -22.28073302975500880, -3.560599703067827360, 0.9769664947681129252 ) ) ;
#47367=CARTESIAN_POINT ( 'NONE',  ( -22.27878402819508352, -3.562981801125738368, -0.9457981527432679503 ) ) ;
#47370=ORIENTED_EDGE ( 'NONE', *, *, #62641, .T. ) ;
#47372=ORIENTED_EDGE ( 'NONE', *, *, #22162, .T. ) ;
#47384=ORIENTED_EDGE ( 'NONE', *, *, #51224, .F. ) ;
#47386=B_SPLINE_CURVE_WITH_KNOTS ( 'NONE', 3,
 ( #14382, #9076, #29355, #49652, #64917, #39661, #34654, #54951, #24702, #41282, #14690, #4774, #21000, #44981, #16011, #10061, #35644, #15033, #10370 ),
 .UNSPECIFIED., .F., .F.,
 ( 4, 3, 3, 3, 3, 3, 4 ),
 ( 0.000000000000000000, 2.836829842860636775E-05, 4.224792512343439213E-05, 5.612066614708047458E-05, 6.998859278151889341E-05, 9.832141287888834162E-05, 0.0001178161482480083770 ),
 .UNSPECIFIED. ) ;
#47404=EDGE_CURVE ( 'NONE', #6123, #23282, #61431, .T. ) ;
#47407=ORIENTED_EDGE ( 'NONE', *, *, #31523, .F. ) ;
#47411=CARTESIAN_POINT ( 'NONE',  ( -35.04683013664716640, -0.007968230201740866825, 0.009445816769446301053 ) ) ;
#47417=ORIENTED_EDGE ( 'NONE', *, *, #49601, .F. ) ;
#47419=EDGE_CURVE ( 'NONE', #33111, #60601, #37670, .T. ) ;
#47421=FACE_OUTER_BOUND ( 'NONE', #47108, .T. ) ;
#47428=LINE ( 'NONE', #1863, #23600 ) ;
#47430=CYLINDRICAL_SURFACE ( 'NONE', #38298, 6.936499999999988120 ) ;
#47433=ORIENTED_EDGE ( 'NONE', *, *, #38711, .T. ) ;
#47457=CARTESIAN_POINT ( 'NONE',  ( 2.000000000000001776, 0.000000000000000000, 0.000000000000000000 ) ) ;
#47458=VERTEX_POINT ( 'NONE', #28798 ) ;
#47461=CARTESIAN_POINT ( 'NONE',  ( -22.30625920655495165, -2.610366806364689651, 2.750410778797883982 ) ) ;
#47463=CIRCLE ( 'NONE', #18789, 6.936499999999989896 ) ;
#47479=EDGE_CURVE ( 'NONE', #15336, #38388, #9404, .T. ) ;
#47485=DIRECTION ( 'NONE',  ( 0.000000000000000000, 0.000000000000000000, 1.000000000000000000 ) ) ;
#47492=VERTEX_POINT ( 'NONE', #44733 ) ;
#47495=CARTESIAN_POINT ( 'NONE',  ( -27.08423805673873019, -2.229265646063320894, 0.5302040644010340698 ) ) ;
#47501=CARTESIAN_POINT ( 'NONE',  ( -22.27706485742869091, -3.662257305743835012, 0.3729136217356029959 ) ) ;
#47502=DIRECTION ( 'NONE',  ( -1.000000000000000000, 0.000000000000000000, 0.000000000000000000 ) ) ;
#47504=ORIENTED_EDGE ( 'NONE', *, *, #20784, .T. ) ;
#47516=CARTESIAN_POINT ( 'NONE',  ( -22.59983133926798260, 2.378226455340867851, -3.996991822164138064 ) ) ;
#47517=CARTESIAN_POINT ( 'NONE',  ( -35.04683013664716640, 0.007968230201774052085, -0.009445816769469006849 ) ) ;
#47519=ORIENTED_EDGE ( 'NONE', *, *, #29848, .F. ) ;
#47521=ADVANCED_FACE ( 'NONE', ( #48452 ), #43422, .T. ) ;
#47525=EDGE_LOOP ( 'NONE', ( #28067, #42083, #48836, #15809 ) ) ;
#47527=DIRECTION ( 'NONE',  ( -1.000000000000000000, 0.000000000000000000, 0.000000000000000000 ) ) ;
#47528=DIRECTION ( 'NONE',  ( -1.000000000000000000, 0.000000000000000000, 0.000000000000000000 ) ) ;
#47532=DIRECTION ( 'NONE',  ( -1.000000000000000000, 0.000000000000000000, 0.000000000000000000 ) ) ;
#47537=EDGE_CURVE ( 'NONE', #60604, #58714, #57231, .T. ) ;
#47540=CYLINDRICAL_SURFACE ( 'NONE', #49377, 2.899999999999994582 ) ;
#47541=AXIS2_PLACEMENT_3D ( 'NONE', #33014, #49341, #48007 ) ;
#47544=AXIS2_PLACEMENT_3D ( 'NONE', #6011, #41541, #21266 ) ;
#47545=ORIENTED_EDGE ( 'NONE', *, *, #56412, .F. ) ;
#47550=DIRECTION ( 'NONE',  ( -1.000000000000000000, 0.000000000000000000, 0.000000000000000000 ) ) ;
#47557=FACE_OUTER_BOUND ( 'NONE', #6866, .T. ) ;
#47558=ORIENTED_EDGE ( 'NONE', *, *, #51358, .F. ) ;
#47565=ORIENTED_EDGE ( 'NONE', *, *, #58648, .T. ) ;
#47569=LINE ( 'NONE', #15977, #62593 ) ;
#47574=AXIS2_PLACEMENT_3D ( 'NONE', #33758, #13169, #65001 ) ;
#47591=EDGE_CURVE ( 'NONE', #17671, #45297, #25126, .T. ) ;
#47593=CYLINDRICAL_SURFACE ( 'NONE', #31711, 2.899999999999994582 ) ;
#47607=ADVANCED_FACE ( 'NONE', ( #45081 ), #39758, .T. ) ;
#47610=FACE_OUTER_BOUND ( 'NONE', #9815, .T. ) ;
#47614=ORIENTED_EDGE ( 'NONE', *, *, #26966, .T. ) ;
#47615=FACE_OUTER_BOUND ( 'NONE', #61230, .T. ) ;
#47617=AXIS2_PLACEMENT_3D ( 'NONE', #22154, #7184, #16838 ) ;
#47621=CARTESIAN_POINT ( 'NONE',  ( -27.05874794189610455, 0.3907329275428126913, 2.180117559290193796 ) ) ;
#47622=CYLINDRICAL_SURFACE ( 'NONE', #51237, 2.899999999999994582 ) ;
#47628=DIRECTION ( 'NONE',  ( -1.000000000000000000, 0.000000000000000000, 0.000000000000000000 ) ) ;
#47631=AXIS2_PLACEMENT_3D ( 'NONE', #49585, #4024, #24292 ) ;
#47634=CARTESIAN_POINT ( 'NONE',  ( -22.27706089016750468, -2.583072118615362012, -2.622757446538691806 ) ) ;
#47635=EDGE_CURVE ( 'NONE', #29113, #25350, #50413, .T. ) ;
#47640=EDGE_CURVE ( 'NONE', #52961, #19077, #15133, .T. ) ;
#47641=CARTESIAN_POINT ( 'NONE',  ( 2.000000000000001776, 0.000000000000000000, 0.000000000000000000 ) ) ;
#47660=VECTOR ( 'NONE', #33376, 1000.000000000000000 ) ;
#47661=ADVANCED_FACE ( 'NONE', ( #10803 ), #46391, .T. ) ;
#47663=DIRECTION ( 'NONE',  ( 0.000000000000000000, -0.1081190184239280011, -0.9941379571543611515 ) ) ;
#47666=DIRECTION ( 'NONE',  ( 0.000000000000000000, 0.000000000000000000, 1.000000000000000000 ) ) ;
#47668=ORIENTED_EDGE ( 'NONE', *, *, #28571, .F. ) ;
#47677=CARTESIAN_POINT ( 'NONE',  ( -35.04643116707788408, 0.01135624435143721411, 0.004425962698848331933 ) ) ;
#47690=DIRECTION ( 'NONE',  ( 0.000000000000000000, 0.000000000000000000, -1.000000000000000000 ) ) ;
#47700=CYLINDRICAL_SURFACE ( 'NONE', #20723, 2.899999999999994582 ) ;
#47702=CARTESIAN_POINT ( 'NONE',  ( -22.27834755396594346, 0.7418417409069284485, 3.610802913011835980 ) ) ;
#47709=ORIENTED_EDGE ( 'NONE', *, *, #58350, .F. ) ;
#47714=AXIS2_PLACEMENT_3D ( 'NONE', #20157, #56389, #40429 ) ;
#47715=EDGE_CURVE ( 'NONE', #46658, #24785, #52038, .T. ) ;
#47716=CARTESIAN_POINT ( 'NONE',  ( 2.000000000000001776, 0.000000000000000000, 0.000000000000000000 ) ) ;
#47723=CARTESIAN_POINT ( 'NONE',  ( -22.30625920655495165, -0.8854385781085337692, 3.687109008463850479 ) ) ;
#47728=EDGE_CURVE ( 'NONE', #35944, #47492, #54288, .T. ) ;
#47734=CIRCLE ( 'NONE', #56218, 1.499999999999997780 ) ;
#47738=CARTESIAN_POINT ( 'NONE',  ( 0.000000000000000000, 0.000000000000000000, 0.000000000000000000 ) ) ;
#47742=ORIENTED_EDGE ( 'NONE', *, *, #51177, .F. ) ;
#47743=DIRECTION ( 'NONE',  ( 0.000000000000000000, 0.000000000000000000, 1.000000000000000000 ) ) ;
#47756=ORIENTED_EDGE ( 'NONE', *, *, #26475, .F. ) ;
#47771=CARTESIAN_POINT ( 'NONE',  ( -27.09729107899852352, -1.932259710108171324, 1.302895495071016985 ) ) ;
#47774=CIRCLE ( 'NONE', #4244, 2.899999999999995914 ) ;
#47784=ORIENTED_EDGE ( 'NONE', *, *, #38674, .F. ) ;
#47786=DIRECTION ( 'NONE',  ( 1.000000000000000000, 0.000000000000000000, 0.000000000000000000 ) ) ;
#47802=DIRECTION ( 'NONE',  ( 0.000000000000000000, -0.1081190184239279733, -0.9941379571543611515 ) ) ;
#47811=ORIENTED_EDGE ( 'NONE', *, *, #26966, .F. ) ;
#47812=ORIENTED_EDGE ( 'NONE', *, *, #32203, .F. ) ;
#47813=FACE_OUTER_BOUND ( 'NONE', #2577, .T. ) ;
#47821=DIRECTION ( 'NONE',  ( 0.000000000000000000, 0.8835120444460207167, 0.4684084406997939265 ) ) ;
#47826=CARTESIAN_POINT ( 'NONE',  ( 2.000000000000001776, -5.107597897712309098, -4.693343793638478978 ) ) ;
#47833=CARTESIAN_POINT ( 'NONE',  ( -22.27706485742869091, -1.508175983031604606, 3.358064672837097753 ) ) ;
#47834=VERTEX_POINT ( 'NONE', #14077 ) ;
#47838=LINE ( 'NONE', #53817, #4255 ) ;
#47843=ORIENTED_EDGE ( 'NONE', *, *, #64670, .T. ) ;
#47849=ADVANCED_FACE ( 'NONE', ( #18452 ), #40580, .F. ) ;
#47850=CARTESIAN_POINT ( 'NONE',  ( 2.000000000000001776, 4.976357229393855164, 4.652926418895560801 ) ) ;
#47852=CYLINDRICAL_SURFACE ( 'NONE', #32014, 6.936499999999988120 ) ;
#47853=VECTOR ( 'NONE', #5023, 1000.000000000000000 ) ;
#47861=CARTESIAN_POINT ( 'NONE',  ( -22.27711653538342773, 2.958138731383647801, -2.191780254295670805 ) ) ;
#47865=AXIS2_PLACEMENT_3D ( 'NONE', #24107, #23799, #49410 ) ;
#47868=VECTOR ( 'NONE', #59388, 1000.000000000000000 ) ;
#47875=CARTESIAN_POINT ( 'NONE',  ( -27.08776759928964495, -0.6183458186125521117, -2.217308861843124035 ) ) ;
#47885=CARTESIAN_POINT ( 'NONE',  ( -22.46225619532221529, -1.978788174090782226, 3.746472695305350875 ) ) ;
#47887=UNCERTAINTY_MEASURE_WITH_UNIT (LENGTH_MEASURE( 1.000000000000000082E-05 ), #34154, 'distance_accuracy_value', 'NONE');
#47888=FACE_OUTER_BOUND ( 'NONE', #23467, .T. ) ;
#47897=ORIENTED_EDGE ( 'NONE', *, *, #4890, .F. ) ;
#47901=CARTESIAN_POINT ( 'NONE',  ( -27.08702828306176613, -1.639744581304558801, -1.612407531674189709 ) ) ;
#47902=CARTESIAN_POINT ( 'NONE',  ( 0.000000000000000000, 3.341639490130761114, 6.078525953551427996 ) ) ;
#47903=CARTESIAN_POINT ( 'NONE',  ( -22.29479313954897535, -2.096782908204890550, -3.090162644873553077 ) ) ;
#47905=EDGE_LOOP ( 'NONE', ( #21459, #6302, #65080, #62760 ) ) ;
#47913=AXIS2_PLACEMENT_3D ( 'NONE', #31901, #11631, #1994 ) ;
#47919=ORIENTED_EDGE ( 'NONE', *, *, #4589, .F. ) ;
#47922=VERTEX_POINT ( 'NONE', #8444 ) ;
#47925=AXIS2_PLACEMENT_3D ( 'NONE', #21174, #52104, #61738 ) ;
#47930=CARTESIAN_POINT ( 'NONE',  ( -22.29195009621226831, 3.616122380634898992, 0.8975732442595152349 ) ) ;
#47935=CARTESIAN_POINT ( 'NONE',  ( -22.66110217412718697, -4.192227617777427362, -2.622110956932569348 ) ) ;
#47937=ORIENTED_EDGE ( 'NONE', *, *, #37764, .T. ) ;
#47944=CARTESIAN_POINT ( 'NONE',  ( -35.04660725145885891, -0.001288602543478920958, -0.01223081933020915557 ) ) ;
#47945=ORIENTED_EDGE ( 'NONE', *, *, #36135, .T. ) ;
#47946=ADVANCED_FACE ( 'NONE', ( #10392 ), #4794, .T. ) ;
#47947=CIRCLE ( 'NONE', #34100, 2.899999999999995026 ) ;
#47949=AXIS2_PLACEMENT_3D ( 'NONE', #47716, #6503, #22439 ) ;
#47952=VERTEX_POINT ( 'NONE', #40006 ) ;
#47963=DIRECTION ( 'NONE',  ( 0.9606638835031803270, -0.2249116044183857577, 0.1629100154396148359 ) ) ;
#47975=DIRECTION ( 'NONE',  ( 1.000000000000000000, 0.000000000000000000, 0.000000000000000000 ) ) ;
#47978=ORIENTED_EDGE ( 'NONE', *, *, #6347, .F. ) ;
#47979=CARTESIAN_POINT ( 'NONE',  ( -22.31099767395441091, 3.774495463598467548, -0.2534174342804001445 ) ) ;
#47980=CARTESIAN_POINT ( 'NONE',  ( -22.59969328935897082, 3.618004136135768878, 2.921971394153407342 ) ) ;
#47987=DIRECTION ( 'NONE',  ( 1.000000000000000000, 0.000000000000000000, 0.000000000000000000 ) ) ;
#47990=CARTESIAN_POINT ( 'NONE',  ( -22.28350523959500862, -3.346230442873233013, -1.580062893038987948 ) ) ;
#47994=EDGE_CURVE ( 'NONE', #22369, #62776, #15396, .T. ) ;
#48006=VERTEX_POINT ( 'NONE', #25707 ) ;
#48007=DIRECTION ( 'NONE',  ( 0.000000000000000000, 0.3193015301359742875, 0.9476531711828043436 ) ) ;
#48018=ORIENTED_EDGE ( 'NONE', *, *, #25299, .F. ) ;
#48023=VERTEX_POINT ( 'NONE', #39686 ) ;
#48025=CARTESIAN_POINT ( 'NONE',  ( -22.28236030719477867, 3.345835236227605147, 1.572829798448300176 ) ) ;
#48027=CARTESIAN_POINT ( 'NONE',  ( -22.29290468048228036, 2.097193667172415399, 3.083035815361880427 ) ) ;
#48031=DIRECTION ( 'NONE',  ( 0.000000000000000000, 0.000000000000000000, 1.000000000000000000 ) ) ;
#48037=CIRCLE ( 'NONE', #28906, 2.899999999999997247 ) ;
#48041=AXIS2_PLACEMENT_3D ( 'NONE', #7824, #38053, #27424 ) ;
#48047=EDGE_CURVE ( 'NONE', #22824, #46888, #38174, .T. ) ;
#48057=DIRECTION ( 'NONE',  ( 0.000000000000000000, 0.000000000000000000, 1.000000000000000000 ) ) ;
#48087=CIRCLE ( 'NONE', #39717, 2.899999999999995026 ) ;
#48089=ORIENTED_EDGE ( 'NONE', *, *, #12043, .F. ) ;
#48090=CIRCLE ( 'NONE', #291, 1.499999999999998224 ) ;
#48091=ORIENTED_EDGE ( 'NONE', *, *, #18952, .F. ) ;
#48098=CARTESIAN_POINT ( 'NONE',  ( -27.08417473062937120, 0.7460375461499409999, -2.166271322019588830 ) ) ;
#48105=CARTESIAN_POINT ( 'NONE',  ( 2.000000000000001776, 0.000000000000000000, 0.000000000000000000 ) ) ;
#48112=CIRCLE ( 'NONE', #65069, 2.899999999999995470 ) ;
#48115=CARTESIAN_POINT ( 'NONE',  ( 2.000000000000001776, 0.000000000000000000, 0.000000000000000000 ) ) ;
#48116=CARTESIAN_POINT ( 'NONE',  ( -27.09602251845210930, -1.927725285107524611, 1.302811993375579069 ) ) ;
#48121=AXIS2_PLACEMENT_3D ( 'NONE', #38772, #53745, #53073 ) ;
#48130=EDGE_CURVE ( 'NONE', #22014, #62401, #57618, .T. ) ;
#48131=CARTESIAN_POINT ( 'NONE',  ( -27.08430418657511751, 0.2231435303617252952, 2.280643121250616190 ) ) ;
#48135=CARTESIAN_POINT ( 'NONE',  ( -22.27706485742869091, -3.547445275915918295, -0.9832726768967802178 ) ) ;
#48139=AXIS2_PLACEMENT_3D ( 'NONE', #24327, #54625, #44592 ) ;
#48141=CARTESIAN_POINT ( 'NONE',  ( -22.29382655386184453, -2.586160974799824874, 2.689927793811020429 ) ) ;
#48143=CARTESIAN_POINT ( 'NONE',  ( -23.41523303002442091, 0.3963225057405129759, -4.681453266967039006 ) ) ;
#48144=DIRECTION ( 'NONE',  ( -1.000000000000000000, 0.000000000000000000, 0.000000000000000000 ) ) ;
#48155=ORIENTED_EDGE ( 'NONE', *, *, #23379, .F. ) ;
#48159=CIRCLE ( 'NONE', #57744, 2.899999999999994582 ) ;
#48170=CARTESIAN_POINT ( 'NONE',  ( -27.08429572838383947, -2.217805374070538349, 0.5764601019425888984 ) ) ;
#48172=CARTESIAN_POINT ( 'NONE',  ( 0.000000000000000000, 0.000000000000000000, 0.000000000000000000 ) ) ;
#48184=CARTESIAN_POINT ( 'NONE',  ( -22.28694879868232803, 2.586016167700817991, -2.661377239830745367 ) ) ;
#48187=DIRECTION ( 'NONE',  ( 1.000000000000000000, 0.000000000000000000, 0.000000000000000000 ) ) ;
#48200=ORIENTED_EDGE ( 'NONE', *, *, #37912, .F. ) ;
#48203=AXIS2_PLACEMENT_3D ( 'NONE', #14340, #4389, #65215 ) ;
#48207=CARTESIAN_POINT ( 'NONE',  ( -27.10719052120871098, 2.355164825213508450, -0.1538293304135275597 ) ) ;
#48213=VECTOR ( 'NONE', #59475, 1000.000000000000000 ) ;
#48214=CYLINDRICAL_SURFACE ( 'NONE', #8516, 6.936499999999988120 ) ;
#48227=ORIENTED_EDGE ( 'NONE', *, *, #61812, .F. ) ;
#48232=CARTESIAN_POINT ( 'NONE',  ( -35.04643116707788408, 0.002453861112619928897, 0.01193867652719490802 ) ) ;
#48241=VECTOR ( 'NONE', #45214, 1000.000000000000000 ) ;
#48242=CARTESIAN_POINT ( 'NONE',  ( -22.38932658256919339, -1.810630688302289348, 3.587092141214295093 ) ) ;
#48243=EDGE_LOOP ( 'NONE', ( #41795, #54740, #38230, #34314 ) ) ;
#48248=AXIS2_PLACEMENT_3D ( 'NONE', #31321, #51622, #27548 ) ;
#48261=DIRECTION ( 'NONE',  ( -1.000000000000000000, 0.000000000000000000, 0.000000000000000000 ) ) ;
#48266=CARTESIAN_POINT ( 'NONE',  ( -10.00000000000000178, 0.000000000000000000, 0.000000000000000000 ) ) ;
#48270=CARTESIAN_POINT ( 'NONE',  ( -22.31328051695926007, -0.2528478350593797996, -3.781397440874599614 ) ) ;
#48279=ORIENTED_EDGE ( 'NONE', *, *, #47715, .T. ) ;
#48280=DIRECTION ( 'NONE',  ( 0.000000000000000000, 0.000000000000000000, 1.000000000000000000 ) ) ;
#48284=FACE_OUTER_BOUND ( 'NONE', #18061, .T. ) ;
#48285=CIRCLE ( 'NONE', #22776, 2.899999999999994582 ) ;
#48287=LINE ( 'NONE', #28620, #8562 ) ;
#48292=EDGE_CURVE ( 'NONE', #32746, #64838, #50285, .T. ) ;
#48297=CARTESIAN_POINT ( 'NONE',  ( 0.000000000000000000, 6.662861565602072211, 1.421313227905651289 ) ) ;
#48298=AXIS2_PLACEMENT_3D ( 'NONE', #37410, #858, #41403 ) ;
#48299=FACE_OUTER_BOUND ( 'NONE', #58384, .T. ) ;
#48301=ORIENTED_EDGE ( 'NONE', *, *, #23379, .T. ) ;
#48308=CARTESIAN_POINT ( 'NONE',  ( -22.23402523511428086, 0.6266381416564609230, 3.496364702451501216 ) ) ;
#48315=CYLINDRICAL_SURFACE ( 'NONE', #26523, 2.899999999999994582 ) ;
#48317=CARTESIAN_POINT ( 'NONE',  ( -27.08429572838383947, -0.6096735944848084010, 2.208905845566022208 ) ) ;
#48321=CIRCLE ( 'NONE', #43024, 2.899999999999995026 ) ;
#48326=DIRECTION ( 'NONE',  ( 1.000000000000000000, -0.000000000000000000, -0.000000000000000000 ) ) ;
#48332=DIRECTION ( 'NONE',  ( -1.000000000000000000, 0.000000000000000000, 0.000000000000000000 ) ) ;
#48334=EDGE_LOOP ( 'NONE', ( #11615, #12201, #52236, #53641 ) ) ;
#48337=DIRECTION ( 'NONE',  ( -1.000000000000000000, 0.000000000000000000, 0.000000000000000000 ) ) ;
#48339=CARTESIAN_POINT ( 'NONE',  ( -22.27706485742869091, -2.154081322712202873, -2.985151051101508468 ) ) ;
#48343=ORIENTED_EDGE ( 'NONE', *, *, #21145, .F. ) ;
#48345=CARTESIAN_POINT ( 'NONE',  ( 2.000000000000001776, 0.08317740279942427428, -7.499538753794372070 ) ) ;
#48351=ORIENTED_EDGE ( 'NONE', *, *, #1531, .F. ) ;
#48354=DIRECTION ( 'NONE',  ( 0.000000000000000000, 0.000000000000000000, 1.000000000000000000 ) ) ;
#48372=CARTESIAN_POINT ( 'NONE',  ( -27.08429572838383947, -2.208905845566027537, -0.6096735944848257205 ) ) ;
#48378=VERTEX_POINT ( 'NONE', #59211 ) ;
#48384=CARTESIAN_POINT ( 'NONE',  ( 2.000000000000001776, 3.937687286050817193, 6.383151168292468647 ) ) ;
#48402=VERTEX_POINT ( 'NONE', #13631 ) ;
#48404=CARTESIAN_POINT ( 'NONE',  ( 2.000000000000001776, -1.145812388885151023, 6.715725538143585638 ) ) ;
#48406=ORIENTED_EDGE ( 'NONE', *, *, #6526, .T. ) ;
#48414=ORIENTED_EDGE ( 'NONE', *, *, #12249, .T. ) ;
#48425=EDGE_CURVE ( 'NONE', #7386, #13124, #31808, .T. ) ;
#48430=CIRCLE ( 'NONE', #62177, 7.499999999999988454 ) ;
#48431=CARTESIAN_POINT ( 'NONE',  ( -22.27721688985630522, -0.6032462375556635337, -3.631967556481321857 ) ) ;
#48433=CARTESIAN_POINT ( 'NONE',  ( -22.59969328935894239, -4.339503524536120871, 1.672297795813938892 ) ) ;
#48437=ADVANCED_FACE ( 'NONE', ( #23298 ), #58565, .T. ) ;
#48444=DIRECTION ( 'NONE',  ( 0.000000000000000000, -0.6051742151937715697, 0.7960930657056388693 ) ) ;
#48452=FACE_OUTER_BOUND ( 'NONE', #39591, .T. ) ;
#48457=EDGE_CURVE ( 'NONE', #31241, #451, #59403, .T. ) ;
#48460=DIRECTION ( 'NONE',  ( -1.000000000000000000, 0.000000000000000000, 0.000000000000000000 ) ) ;
#48461=EDGE_CURVE ( 'NONE', #9767, #46346, #44576, .T. ) ;
#48462=CARTESIAN_POINT ( 'NONE',  ( -27.10719052120871098, -2.116547233941210138, -1.044362304621491377 ) ) ;
#48466=CARTESIAN_POINT ( 'NONE',  ( -24.42101984568203932, -0.3620223918248232642, 4.276292373951984693 ) ) ;
#48470=CARTESIAN_POINT ( 'NONE',  ( 2.000000000000001776, 3.073484823194340354, 6.841322316745045207 ) ) ;
#48481=ORIENTED_EDGE ( 'NONE', *, *, #9527, .F. ) ;
#48487=DIRECTION ( 'NONE',  ( 0.000000000000000000, 0.000000000000000000, 1.000000000000000000 ) ) ;
#48497=CARTESIAN_POINT ( 'NONE',  ( -22.28073302975501235, 2.595086548180011832, -2.626377654649338922 ) ) ;
#48498=CARTESIAN_POINT ( 'NONE',  ( 2.000000000000001776, -3.937687286050851831, 6.383151168292441113 ) ) ;
#48499=EDGE_CURVE ( 'NONE', #60906, #22351, #14290, .T. ) ;
#48500=DIRECTION ( 'NONE',  ( -1.000000000000000000, 0.000000000000000000, 0.000000000000000000 ) ) ;
#48516=CARTESIAN_POINT ( 'NONE',  ( -27.08506889328343803, -2.284141197253890088, 0.2104793012480277725 ) ) ;
#48518=DIRECTION ( 'NONE',  ( 0.000000000000000000, 0.000000000000000000, 1.000000000000000000 ) ) ;
#48523=EDGE_CURVE ( 'NONE', #47458, #5728, #42428, .T. ) ;
#48527=CARTESIAN_POINT ( 'NONE',  ( 2.000000000000001776, -2.473437528934186780, 7.080403010454960899 ) ) ;
#48528=CARTESIAN_POINT ( 'NONE',  ( -22.31328051695926007, 2.608921479762127849, -2.748895659348120635 ) ) ;
#48530=CYLINDRICAL_SURFACE ( 'NONE', #42668, 7.499999999999988454 ) ;
#48543=DIRECTION ( 'NONE',  ( -1.000000000000000000, 0.000000000000000000, 0.000000000000000000 ) ) ;
#48546=DIRECTION ( 'NONE',  ( 0.000000000000000000, 0.3193015301359806712, -0.9476531711828022342 ) ) ;
#48550=B_SPLINE_CURVE_WITH_KNOTS ( 'NONE', 3,
 ( #64430, #23567, #38520, #54146, #30423, #56018, #63771, #58841, #33541, #18901, #30096, #2968, #43839, #25434, #175, #48516, #28871, #53829, #61021 ),
 .UNSPECIFIED., .F., .F.,
 ( 4, 3, 3, 3, 3, 3, 4 ),
 ( 0.000000000000000000, 2.836829842860534115E-05, 4.224792512343245412E-05, 5.612066614707884827E-05, 6.998859278151770078E-05, 9.832141287888560401E-05, 0.0001178161482480192461 ),
 .UNSPECIFIED. ) ;
#48551=DIRECTION ( 'NONE',  ( 0.000000000000000000, 0.000000000000000000, 1.000000000000000000 ) ) ;
#48555=DIRECTION ( 'NONE',  ( 0.000000000000000000, -0.1081190184239279872, -0.9941379571543611515 ) ) ;
#48561=ORIENTED_EDGE ( 'NONE', *, *, #40505, .T. ) ;
#48563=ORIENTED_EDGE ( 'NONE', *, *, #18640, .F. ) ;
#48580=CARTESIAN_POINT ( 'NONE',  ( 0.000000000000000000, 2.469490258309515518, -6.482025155313297482 ) ) ;
#48596=CARTESIAN_POINT ( 'NONE',  ( 0.000000000000000000, 0.000000000000000000, 0.000000000000000000 ) ) ;
#48608=EDGE_CURVE ( 'NONE', #10092, #32250, #60838, .T. ) ;
#48610=VERTEX_POINT ( 'NONE', #45877 ) ;
#48618=ADVANCED_FACE ( 'NONE', ( #46521 ), #11921, .T. ) ;
#48629=CARTESIAN_POINT ( 'NONE',  ( -22.46509356695199600, -0.8809186187926192346, 4.154553862421305865 ) ) ;
#48643=ORIENTED_EDGE ( 'NONE', *, *, #41549, .T. ) ;
#48649=CARTESIAN_POINT ( 'NONE',  ( -22.30078715814471835, -3.372109767220907273, -1.645949880549425037 ) ) ;
#48676=CIRCLE ( 'NONE', #57168, 7.499999999999988454 ) ;
#48677=DIRECTION ( 'NONE',  ( -1.000000000000000000, 0.000000000000000000, 0.000000000000000000 ) ) ;
#48683=CARTESIAN_POINT ( 'NONE',  ( -22.28284753389937123, 0.9912969289936786055, 3.563226652211039180 ) ) ;
#48686=CIRCLE ( 'NONE', #53994, 7.499999999999988454 ) ;
#48687=DIRECTION ( 'NONE',  ( -1.000000000000000000, 0.000000000000000000, 0.000000000000000000 ) ) ;
#48688=FACE_OUTER_BOUND ( 'NONE', #35799, .T. ) ;
#48692=ORIENTED_EDGE ( 'NONE', *, *, #34940, .F. ) ;
#48717=CARTESIAN_POINT ( 'NONE',  ( -27.10719052120871098, -1.044362304621479165, 2.116547233941197703 ) ) ;
#48720=FACE_OUTER_BOUND ( 'NONE', #57826, .T. ) ;
#48733=CIRCLE ( 'NONE', #47544, 6.936499999999991672 ) ;
#48744=B_SPLINE_CURVE_WITH_KNOTS ( 'NONE', 3,
 ( #30543, #34857, #14904, #45196, #35539, #50846, #31219, #46196, #20244, #25236, #56485, #55505, #45508, #30865, #5293, #640, #5638, #29893, #21224, #25907, #20898, #65458 ),
 .UNSPECIFIED., .F., .F.,
 ( 4, 3, 3, 3, 3, 3, 3, 4 ),
 ( 0.000000000000000000, 6.990956068646571873E-05, 0.0001398191187764076656, 0.0002097286751720259625, 0.0002796382307041417933, 0.0003495477861619887723, 0.0004194573423310374110, 0.0005586102576333247961 ),
 .UNSPECIFIED. ) ;
#48746=CARTESIAN_POINT ( 'NONE',  ( 2.000000000000001776, -5.860254403322002759, -3.474373880649873403 ) ) ;
#48747=CARTESIAN_POINT ( 'NONE',  ( -27.08419642509983305, 0.7009209357102744731, -2.181485315953918924 ) ) ;
#48761=CARTESIAN_POINT ( 'NONE',  ( -27.08579483061203064, -1.879952013015653289, 1.318128465624906154 ) ) ;
#48765=DIRECTION ( 'NONE',  ( 0.000000000000000000, -0.9985334138511233748, -0.05413890858542835804 ) ) ;
#48768=CARTESIAN_POINT ( 'NONE',  ( -27.35552965826137140, 1.320216934008397569, 2.810569013793730697 ) ) ;
#48773=VECTOR ( 'NONE', #51091, 1000.000000000000000 ) ;
#48778=ORIENTED_EDGE ( 'NONE', *, *, #34854, .F. ) ;
#48785=CARTESIAN_POINT ( 'NONE',  ( -27.35552965826137140, -0.2619431035391951434, 3.094132632038943065 ) ) ;
#48799=EDGE_CURVE ( 'NONE', #25571, #22630, #47838, .T. ) ;
#48800=CARTESIAN_POINT ( 'NONE',  ( 1.000000000000000888, -0.08317740279924559776, -7.499538753794370294 ) ) ;
#48804=DIRECTION ( 'NONE',  ( -1.000000000000000000, -1.685093406416449860E-16, 1.011030131491573426E-17 ) ) ;
#48809=DIRECTION ( 'NONE',  ( 0.000000000000000000, 0.000000000000000000, -1.000000000000000000 ) ) ;
#48810=LINE ( 'NONE', #19187, #53207 ) ;
#48814=CIRCLE ( 'NONE', #13706, 7.499999999999988454 ) ;
#48816=ADVANCED_FACE ( 'NONE', ( #58828 ), #65242, .F. ) ;
#48823=CARTESIAN_POINT ( 'NONE',  ( -22.27756824490284515, 2.608445836294067899, -2.599719761044736899 ) ) ;
#48829=ORIENTED_EDGE ( 'NONE', *, *, #39437, .T. ) ;
#48834=ORIENTED_EDGE ( 'NONE', *, *, #62308, .F. ) ;
#48836=ORIENTED_EDGE ( 'NONE', *, *, #7322, .T. ) ;
#48840=VERTEX_POINT ( 'NONE', #22229 ) ;
#48842=CARTESIAN_POINT ( 'NONE',  ( -27.08702828306202548, -1.612407531673535122, 1.639744581306259441 ) ) ;
#48854=CARTESIAN_POINT ( 'NONE',  ( -27.08417473062937120, 1.503027223283688985, 1.729223128152638012 ) ) ;
#48865=CARTESIAN_POINT ( 'NONE',  ( -22.28506771379528573, -2.697635452840746684, -2.571716811880571107 ) ) ;
#48868=DIRECTION ( 'NONE',  ( 0.000000000000000000, -0.8276889981568956722, 0.5611870653623750593 ) ) ;
#48871=CARTESIAN_POINT ( 'NONE',  ( -22.29978294495153790, 2.710748743830190932, 2.590262069787936827 ) ) ;
#48873=B_SPLINE_CURVE_WITH_KNOTS ( 'NONE', 3,
 ( #34469, #65373, #9848, #65687, #60076, #30458, #20156, #24487, #40427, #15489, #60728, #10177, #44764, #50754, #19523, #5204, #25471, #39787, #45755, #34770, #20492, #40777 ),
 .UNSPECIFIED., .F., .F.,
 ( 4, 3, 3, 3, 3, 3, 3, 4 ),
 ( 0.000000000000000000, 4.455945684386670302E-05, 6.636307477203865976E-05, 8.816671873158680171E-05, 0.0001099660380492600289, 0.0001317545563165294228, 0.0001762613022895055323, 0.0001867992666138388333 ),
 .UNSPECIFIED. ) ;
#48883=CIRCLE ( 'NONE', #32950, 2.899999999999996358 ) ;
#48886=ORIENTED_EDGE ( 'NONE', *, *, #38456, .F. ) ;
#48887=CARTESIAN_POINT ( 'NONE',  ( -22.31328051695926007, -1.671726071983958839, 3.401210163132545539 ) ) ;
#48891=CARTESIAN_POINT ( 'NONE',  ( -27.09569413923794556, -1.680421072125452664, -1.607816962454774901 ) ) ;
#48893=EDGE_CURVE ( 'NONE', #49332, #63687, #14847, .T. ) ;
#48894=CARTESIAN_POINT ( 'NONE',  ( -35.04709527796842394, 0.01232256164996302361, 0.001003525937966209813 ) ) ;
#48901=AXIS2_PLACEMENT_3D ( 'NONE', #34538, #3972, #59181 ) ;
#48903=AXIS2_PLACEMENT_3D ( 'NONE', #60702, #15778, #36058 ) ;
#48909=CARTESIAN_POINT ( 'NONE',  ( -22.29677679919927868, -0.2674217835790838604, -3.730758197825084999 ) ) ;
#48912=CARTESIAN_POINT ( 'NONE',  ( 2.000000000000001776, 0.000000000000000000, 0.000000000000000000 ) ) ;
#48918=B_SPLINE_CURVE_WITH_KNOTS ( 'NONE', 3,
 ( #51225, #34895, #55201, #4696, #24957, #672 ),
 .UNSPECIFIED., .F., .F.,
 ( 4, 2, 4 ),
 ( 0.0002637379172190560772, 0.0009975831966641396376, 0.001731428476109223144 ),
 .UNSPECIFIED. ) ;
#48922=ORIENTED_EDGE ( 'NONE', *, *, #61119, .T. ) ;
#48926=CARTESIAN_POINT ( 'NONE',  ( -22.28169757117799321, 3.576542310004398928, 0.9284931499057018645 ) ) ;
#48952=EDGE_CURVE ( 'NONE', #63399, #59829, #48883, .T. ) ;
#48962=EDGE_CURVE ( 'NONE', #42103, #59964, #61211, .T. ) ;
#48968=VECTOR ( 'NONE', #25066, 1000.000000000000000 ) ;
#48975=CARTESIAN_POINT ( 'NONE',  ( -22.27704833740210333, 3.663709865074126881, -0.3581593033281141869 ) ) ;
#48977=CIRCLE ( 'NONE', #13907, 2.899999999999993694 ) ;
#48980=CIRCLE ( 'NONE', #17052, 7.499999999999988454 ) ;
#48985=CARTESIAN_POINT ( 'NONE',  ( -27.08429572838383947, 2.208905845566027537, 0.6096735944847788691 ) ) ;
#48998=ORIENTED_EDGE ( 'NONE', *, *, #43430, .T. ) ;
#49005=CARTESIAN_POINT ( 'NONE',  ( 0.000000000000000000, 5.097042323172460421, 5.501832381651443171 ) ) ;
#49009=VECTOR ( 'NONE', #13606, 1000.000000000000000 ) ;
#49012=AXIS2_PLACEMENT_3D ( 'NONE', #23024, #43279, #18028 ) ;
#49013=DIRECTION ( 'NONE',  ( -1.000000000000000000, 0.000000000000000000, 0.000000000000000000 ) ) ;
#49022=CARTESIAN_POINT ( 'NONE',  ( -22.27706485742869091, 2.154081322712221969, 2.985151051101477382 ) ) ;
#49023=FACE_OUTER_BOUND ( 'NONE', #48243, .T. ) ;
#49028=VECTOR ( 'NONE', #48543, 1000.000000000000000 ) ;
#49033=CARTESIAN_POINT ( 'NONE',  ( -27.08429572838383947, -1.608131779585707299, -1.632445743623455847 ) ) ;
#49045=EDGE_LOOP ( 'NONE', ( #22381, #19871, #8162, #16034 ) ) ;
#49047=DIRECTION ( 'NONE',  ( -1.000000000000000000, 0.000000000000000000, 0.000000000000000000 ) ) ;
#49049=EDGE_CURVE ( 'NONE', #49777, #10064, #24008, .T. ) ;
#49053=LINE ( 'NONE', #13438, #64862 ) ;
#49061=EDGE_LOOP ( 'NONE', ( #44254, #13607, #14022, #5711, #22300, #33731 ) ) ;
#49066=CIRCLE ( 'NONE', #14005, 2.899999999999994582 ) ;
#49074=VECTOR ( 'NONE', #30892, 1000.000000000000000 ) ;
#49080=CARTESIAN_POINT ( 'NONE',  ( -35.05175862995318425, -0.008837625261050655046, 0.008949502803489231550 ) ) ;
#49091=DIRECTION ( 'NONE',  ( -0.9582930651793754029, -0.2742293873734362175, 0.08045274594385933009 ) ) ;
#49100=DIRECTION ( 'NONE',  ( -1.000000000000000000, 0.000000000000000000, 0.000000000000000000 ) ) ;
#49105=CIRCLE ( 'NONE', #25722, 2.899999999999994582 ) ;
#49114=CIRCLE ( 'NONE', #53369, 6.936499999999990784 ) ;
#49122=CARTESIAN_POINT ( 'NONE',  ( -27.08456565417852602, -2.084650034355943315, -0.9533904527933274586 ) ) ;
#49125=VERTEX_POINT ( 'NONE', #32119 ) ;
#49126=CARTESIAN_POINT ( 'NONE',  ( -25.42680463514452427, -0.3277218550990526613, 3.871126486605850125 ) ) ;
#49127=CYLINDRICAL_SURFACE ( 'NONE', #9978, 2.899999999999994582 ) ;
#49128=EDGE_CURVE ( 'NONE', #30073, #50194, #56305, .T. ) ;
#49133=CARTESIAN_POINT ( 'NONE',  ( -22.70624764888619751, 5.190207123845774539, 0.7939291279022917536 ) ) ;
#49137=CYLINDRICAL_SURFACE ( 'NONE', #23836, 7.499999999999988454 ) ;
#49143=AXIS2_PLACEMENT_3D ( 'NONE', #62586, #53635, #32337 ) ;
#49144=DIRECTION ( 'NONE',  ( -1.000000000000000000, 0.000000000000000000, 0.000000000000000000 ) ) ;
#49150=CARTESIAN_POINT ( 'NONE',  ( 2.000000000000001776, -6.812627895098285258, 0.04423456934719675882 ) ) ;
#49165=CARTESIAN_POINT ( 'NONE',  ( -22.30078715814471835, -1.645949880549408162, 3.372109767220908605 ) ) ;
#49166=ORIENTED_EDGE ( 'NONE', *, *, #37438, .T. ) ;
#49167=DIRECTION ( 'NONE',  ( 0.000000000000000000, 0.000000000000000000, 1.000000000000000000 ) ) ;
#49172=CIRCLE ( 'NONE', #7762, 7.499999999999988454 ) ;
#49177=ORIENTED_EDGE ( 'NONE', *, *, #1276, .F. ) ;
#49179=DIRECTION ( 'NONE',  ( -1.000000000000000000, 0.000000000000000000, 0.000000000000000000 ) ) ;
#49183=CARTESIAN_POINT ( 'NONE',  ( 0.000000000000000000, 5.217815162096836268, 5.387430271863580700 ) ) ;
#49190=CARTESIAN_POINT ( 'NONE',  ( -35.04683013664716640, 0.002177781393214479368, -0.01216443238274463913 ) ) ;
#49194=CARTESIAN_POINT ( 'NONE',  ( 2.000000000000001776, -4.570217215903394248, 5.218059682435592705 ) ) ;
#49196=VECTOR ( 'NONE', #60097, 1000.000000000000000 ) ;
#49218=DIRECTION ( 'NONE',  ( -1.000000000000000000, 0.000000000000000000, 0.000000000000000000 ) ) ;
#49220=AXIS2_PLACEMENT_3D ( 'NONE', #63142, #31256, #54150 ) ;
#49221=DIRECTION ( 'NONE',  ( -1.000000000000000000, 0.000000000000000000, 0.000000000000000000 ) ) ;
#49225=DIRECTION ( 'NONE',  ( -1.000000000000000000, 0.000000000000000000, 0.000000000000000000 ) ) ;
#49226=DIRECTION ( 'NONE',  ( 0.000000000000000000, 0.000000000000000000, -1.000000000000000000 ) ) ;
#49228=ORIENTED_EDGE ( 'NONE', *, *, #50213, .F. ) ;
#49229=CARTESIAN_POINT ( 'NONE',  ( -27.10307689719060420, 2.250862122746726701, -0.6678239540327265411 ) ) ;
#49234=CARTESIAN_POINT ( 'NONE',  ( -22.31099767395440736, -2.106713667647941435, -3.142100240805198563 ) ) ;
#49236=AXIS2_PLACEMENT_3D ( 'NONE', #8554, #13534, #19534 ) ;
#49237=CIRCLE ( 'NONE', #61984, 7.499999999999988454 ) ;
#49246=CARTESIAN_POINT ( 'NONE',  ( 2.000000000000001776, -6.441884263200848615, 2.217201541069723891 ) ) ;
#49247=CARTESIAN_POINT ( 'NONE',  ( -35.04834644901396956, -0.01358669851862852156, -0.002604658385686434759 ) ) ;
#49251=CARTESIAN_POINT ( 'NONE',  ( 0.000000000000000000, 0.000000000000000000, 0.000000000000000000 ) ) ;
#49263=CARTESIAN_POINT ( 'NONE',  ( -22.28506771379528573, 1.050362426369367164, 3.575989816848450076 ) ) ;
#49264=CARTESIAN_POINT ( 'NONE',  ( 2.000000000000001776, 6.883677378339481123, -0.8544109087185395301 ) ) ;
#49266=CARTESIAN_POINT ( 'NONE',  ( 2.000000000000001776, 0.000000000000000000, 0.000000000000000000 ) ) ;
#49267=CARTESIAN_POINT ( 'NONE',  ( -22.71097035706202405, 0.4203397252017515573, -4.965150228107761521 ) ) ;
#49270=ORIENTED_EDGE ( 'NONE', *, *, #55042, .F. ) ;
#49271=CARTESIAN_POINT ( 'NONE',  ( 2.000000000000001776, 3.795144977083636739, 6.468916029978800886 ) ) ;
#49276=ORIENTED_EDGE ( 'NONE', *, *, #41608, .T. ) ;
#49300=AXIS2_PLACEMENT_3D ( 'NONE', #56053, #29468, #50106 ) ;
#49304=CARTESIAN_POINT ( 'NONE',  ( -22.71097035706203116, 4.965150228107710006, 0.4203397252017151420 ) ) ;
#49312=CARTESIAN_POINT ( 'NONE',  ( -27.08456565417852602, -1.328664661355672516, -1.867985369022553188 ) ) ;
#49315=CARTESIAN_POINT ( 'NONE',  ( -22.27722022243423794, -3.619868281251738207, 0.6721023714405491845 ) ) ;
#49320=ORIENTED_EDGE ( 'NONE', *, *, #46396, .T. ) ;
#49323=CARTESIAN_POINT ( 'NONE',  ( 2.000000000000001776, 0.000000000000000000, 0.000000000000000000 ) ) ;
#49326=AXIS2_PLACEMENT_3D ( 'NONE', #4444, #35326, #49983 ) ;
#49328=CARTESIAN_POINT ( 'NONE',  ( -22.27720412283625961, -2.444672752438193708, -2.752887114864236651 ) ) ;
#49331=CARTESIAN_POINT ( 'NONE',  ( 2.000000000000001776, -6.767909380267597363, -0.7805499053121327524 ) ) ;
#49332=VERTEX_POINT ( 'NONE', #41281 ) ;
#49337=ORIENTED_EDGE ( 'NONE', *, *, #48952, .T. ) ;
#49338=CARTESIAN_POINT ( 'NONE',  ( 2.000000000000001776, -3.155844197800145690, 6.177028383390419819 ) ) ;
#49339=ORIENTED_EDGE ( 'NONE', *, *, #26149, .T. ) ;
#49340=CIRCLE ( 'NONE', #37633, 2.899999999999994582 ) ;
#49341=DIRECTION ( 'NONE',  ( -1.000000000000000000, 0.000000000000000000, 0.000000000000000000 ) ) ;
#49352=DIRECTION ( 'NONE',  ( 0.000000000000000000, 0.000000000000000000, 1.000000000000000000 ) ) ;
#49356=VERTEX_POINT ( 'NONE', #17345 ) ;
#49363=CARTESIAN_POINT ( 'NONE',  ( -22.28169757117798966, 0.9841724999440121247, 3.561623073126532812 ) ) ;
#49372=CARTESIAN_POINT ( 'NONE',  ( -27.08419642509983305, -1.538761233743673795, -1.697757994346420940 ) ) ;
#49377=AXIS2_PLACEMENT_3D ( 'NONE', #37559, #12938, #32870 ) ;
#49384=ORIENTED_EDGE ( 'NONE', *, *, #55928, .T. ) ;
#49392=CARTESIAN_POINT ( 'NONE',  ( -22.27384469013076185, 3.548341908721028837, 0.9835229356381977039 ) ) ;
#49398=ORIENTED_EDGE ( 'NONE', *, *, #24653, .T. ) ;
#49403=ADVANCED_FACE ( 'NONE', ( #27628 ), #63527, .T. ) ;
#49405=CYLINDRICAL_SURFACE ( 'NONE', #10052, 2.899999999999994582 ) ;
#49407=CARTESIAN_POINT ( 'NONE',  ( -22.27706485742869091, 3.563814065926677710, -0.9221835209182235316 ) ) ;
#49410=DIRECTION ( 'NONE',  ( 0.000000000000000000, 0.000000000000000000, 1.000000000000000000 ) ) ;
#49416=EDGE_CURVE ( 'NONE', #44602, #28911, #41486, .T. ) ;
#49429=ORIENTED_EDGE ( 'NONE', *, *, #19701, .T. ) ;
#49432=CYLINDRICAL_SURFACE ( 'NONE', #2373, 2.899999999999994582 ) ;
#49434=DIRECTION ( 'NONE',  ( -1.000000000000000000, 0.000000000000000000, 0.000000000000000000 ) ) ;
#49442=DIRECTION ( 'NONE',  ( -1.000000000000000000, 0.000000000000000000, 0.000000000000000000 ) ) ;
#49451=CARTESIAN_POINT ( 'NONE',  ( -27.09150307427447757, -2.085162835057302821, -1.001311209617661291 ) ) ;
#49454=CARTESIAN_POINT ( 'NONE',  ( 0.000000000000000000, -4.915517050588371184, -4.717154614762162801 ) ) ;
#49473=EDGE_CURVE ( 'NONE', #41912, #42091, #37226, .T. ) ;
#49476=CARTESIAN_POINT ( 'NONE',  ( -28.67667724226168602, -1.695959153103724582, -0.8389685652162183205 ) ) ;
#49478=DIRECTION ( 'NONE',  ( -1.000000000000000000, 0.000000000000000000, 0.000000000000000000 ) ) ;
#49479=CARTESIAN_POINT ( 'NONE',  ( -23.18047892478189098, 3.933989833240163048, 2.738168160732657341 ) ) ;
#49491=DIRECTION ( 'NONE',  ( 0.000000000000000000, 0.6876994588534246500, -0.7259954919231293990 ) ) ;
#49496=EDGE_CURVE ( 'NONE', #35321, #36878, #48287, .T. ) ;
#49513=CARTESIAN_POINT ( 'NONE',  ( -22.59983133926799326, -4.058100437359466461, 2.272383229042392205 ) ) ;
#49517=EDGE_CURVE ( 'NONE', #34961, #50103, #43925, .T. ) ;
#49518=ORIENTED_EDGE ( 'NONE', *, *, #64493, .T. ) ;
#49522=ORIENTED_EDGE ( 'NONE', *, *, #39924, .T. ) ;
#49531=DIRECTION ( 'NONE',  ( -1.000000000000000000, 0.000000000000000000, 0.000000000000000000 ) ) ;
#49534=DIRECTION ( 'NONE',  ( 0.000000000000000000, 0.9635499925192236859, -0.2675283385292183680 ) ) ;
#49543=ORIENTED_EDGE ( 'NONE', *, *, #3419, .F. ) ;
#49545=CARTESIAN_POINT ( 'NONE',  ( -27.08702828306176258, 2.216258174335476561, -0.6138566972905349362 ) ) ;
#49549=DIRECTION ( 'NONE',  ( 0.000000000000000000, -0.2149704402110318713, 0.9766205557100849921 ) ) ;
#49551=DIRECTION ( 'NONE',  ( 0.000000000000000000, 0.000000000000000000, 1.000000000000000000 ) ) ;
#49553=EDGE_CURVE ( 'NONE', #51541, #22230, #26350, .T. ) ;
#49560=EDGE_CURVE ( 'NONE', #52831, #36393, #48980, .T. ) ;
#49564=CARTESIAN_POINT ( 'NONE',  ( 0.000000000000000000, 5.814643797626986910, -3.550179297009520063 ) ) ;
#49566=CARTESIAN_POINT ( 'NONE',  ( -22.71097035706202760, 2.846599994298365743, -4.089776368546553798 ) ) ;
#49568=CARTESIAN_POINT ( 'NONE',  ( 1.000000000000000888, -5.662015959325215952, 4.918493191653933394 ) ) ;
#49582=ORIENTED_EDGE ( 'NONE', *, *, #7253, .T. ) ;
#49585=CARTESIAN_POINT ( 'NONE',  ( 2.000000000000001776, 0.000000000000000000, 0.000000000000000000 ) ) ;
#49587=VERTEX_POINT ( 'NONE', #14304 ) ;
#49590=CARTESIAN_POINT ( 'NONE',  ( 0.000000000000000000, -0.4804830611970390408, 6.919838746524553663 ) ) ;
#49592=ORIENTED_EDGE ( 'NONE', *, *, #21396, .T. ) ;
#49593=CARTESIAN_POINT ( 'NONE',  ( -22.27218376572352554, 1.571356284315160501, -3.330959526935376225 ) ) ;
#49594=ORIENTED_EDGE ( 'NONE', *, *, #23288, .F. ) ;
#49601=EDGE_CURVE ( 'NONE', #43917, #36445, #40223, .T. ) ;
#49602=CARTESIAN_POINT ( 'NONE',  ( -27.10719052120871098, -1.622102031466687189, 1.714424047991066846 ) ) ;
#49608=FACE_OUTER_BOUND ( 'NONE', #46862, .T. ) ;
#49610=DIRECTION ( 'NONE',  ( -1.000000000000000000, 0.000000000000000000, 0.000000000000000000 ) ) ;
#49619=CARTESIAN_POINT ( 'NONE',  ( -22.27218376572352554, 3.026314224080938864, -2.099017427146244952 ) ) ;
#49621=DIRECTION ( 'NONE',  ( -1.000000000000000000, 0.000000000000000000, 0.000000000000000000 ) ) ;
#49627=CARTESIAN_POINT ( 'NONE',  ( 2.000000000000001776, 6.441884263200815752, 2.217201541069855786 ) ) ;
#49630=CARTESIAN_POINT ( 'NONE',  ( -22.27720387087365239, -2.302200479844928260, -2.873095842208896578 ) ) ;
#49631=DIRECTION ( 'NONE',  ( 0.000000000000000000, 0.000000000000000000, -1.000000000000000000 ) ) ;
#49633=DIRECTION ( 'NONE',  ( -1.000000000000000000, 0.000000000000000000, 0.000000000000000000 ) ) ;
#49650=FACE_OUTER_BOUND ( 'NONE', #10940, .T. ) ;
#49652=CARTESIAN_POINT ( 'NONE',  ( -27.09861164373156228, -0.1603819633258334043, -2.328930759213686752 ) ) ;
#49660=ORIENTED_EDGE ( 'NONE', *, *, #52214, .F. ) ;
#49662=DIRECTION ( 'NONE',  ( 0.000000000000000000, 0.9635499925192217985, 0.2675283385292246963 ) ) ;
#49663=CARTESIAN_POINT ( 'NONE',  ( -27.28573687977896256, -1.043905432732877392, -2.702109387930243578 ) ) ;
#49665=CARTESIAN_POINT ( 'NONE',  ( -22.30527770659433529, 1.656864125491268824, -3.381761229713376338 ) ) ;
#49667=DIRECTION ( 'NONE',  ( 0.000000000000000000, 0.000000000000000000, 1.000000000000000000 ) ) ;
#49678=CARTESIAN_POINT ( 'NONE',  ( 2.000000000000001776, 5.457833520448658327, 4.281014542496528463 ) ) ;
#49683=AXIS2_PLACEMENT_3D ( 'NONE', #42673, #10798, #46703 ) ;
#49684=EDGE_CURVE ( 'NONE', #37589, #22708, #15223, .T. ) ;
#49691=CARTESIAN_POINT ( 'NONE',  ( 0.000000000000000000, 0.000000000000000000, 0.000000000000000000 ) ) ;
#49692=CARTESIAN_POINT ( 'NONE',  ( -35.04582288351658548, 0.01092946910272441126, -0.006479247284622759000 ) ) ;
#49699=ORIENTED_EDGE ( 'NONE', *, *, #41962, .T. ) ;
#49701=VERTEX_POINT ( 'NONE', #6314 ) ;
#49708=CARTESIAN_POINT ( 'NONE',  ( -35.04660725145885891, 0.01191704700717466717, -0.003039313842370838965 ) ) ;
#49711=CARTESIAN_POINT ( 'NONE',  ( -22.27721688985630522, 2.338410344701265409, 2.843753050855849285 ) ) ;
#49717=CARTESIAN_POINT ( 'NONE',  ( -22.30861784526116054, -0.8834205920623459107, 3.671054459752214338 ) ) ;
#49725=ORIENTED_EDGE ( 'NONE', *, *, #64237, .F. ) ;
#49733=CYLINDRICAL_SURFACE ( 'NONE', #57214, 7.499999999999988454 ) ;
#49736=FACE_OUTER_BOUND ( 'NONE', #38579, .T. ) ;
#49740=ORIENTED_EDGE ( 'NONE', *, *, #33399, .T. ) ;
#49743=SURFACE_STYLE_FILL_AREA ( #23160 ) ;
#49750=CARTESIAN_POINT ( 'NONE',  ( 0.000000000000000000, 6.643843315911821534, -1.507714007300717585 ) ) ;
#49753=VERTEX_POINT ( 'NONE', #11934 ) ;
#49775=CARTESIAN_POINT ( 'NONE',  ( -27.08430792439081003, 2.211452765398042697, 0.6005833784282403887 ) ) ;
#49777=VERTEX_POINT ( 'NONE', #27898 ) ;
#49778=CARTESIAN_POINT ( 'NONE',  ( 0.000000000000000000, 3.230174184210159893, -5.998318953995314118 ) ) ;
#49792=DIRECTION ( 'NONE',  ( -0.9582930651793755139, 0.2742293873734353293, -0.08045274594386130074 ) ) ;
#49798=DIRECTION ( 'NONE',  ( -1.000000000000000000, 0.000000000000000000, 0.000000000000000000 ) ) ;
#49799=VECTOR ( 'NONE', #6811, 1000.000000000000000 ) ;
#49800=CARTESIAN_POINT ( 'NONE',  ( 0.000000000000000000, 0.000000000000000000, 0.000000000000000000 ) ) ;
#49803=EDGE_CURVE ( 'NONE', #5331, #24263, #14957, .T. ) ;
#49809=DIRECTION ( 'NONE',  ( -1.000000000000000000, 0.000000000000000000, 0.000000000000000000 ) ) ;
#49810=CARTESIAN_POINT ( 'NONE',  ( 2.000000000000001776, 1.754183803416544452, 6.711026108862249373 ) ) ;
#49812=CARTESIAN_POINT ( 'NONE',  ( 0.000000000000000000, 0.000000000000000000, 0.000000000000000000 ) ) ;
#49815=VECTOR ( 'NONE', #61943, 1000.000000000000000 ) ;
#49822=LINE ( 'NONE', #28552, #6365 ) ;
#49838=LINE ( 'NONE', #4288, #44844 ) ;
#49840=CARTESIAN_POINT ( 'NONE',  ( -27.09602251845159060, 2.092130925171141520, 1.018053071731282344 ) ) ;
#49843=CYLINDRICAL_SURFACE ( 'NONE', #2138, 2.899999999999994582 ) ;
#49854=CARTESIAN_POINT ( 'NONE',  ( 0.000000000000000000, -5.450255447309769963, 4.087611905901399112 ) ) ;
#49858=CARTESIAN_POINT ( 'NONE',  ( 0.000000000000000000, 0.000000000000000000, 0.000000000000000000 ) ) ;
#49859=ORIENTED_EDGE ( 'NONE', *, *, #9535, .T. ) ;
#49863=CARTESIAN_POINT ( 'NONE',  ( 0.000000000000000000, 6.250523986464036064, -3.007653927006531447 ) ) ;
#49866=CARTESIAN_POINT ( 'NONE',  ( -28.67667724226168602, -1.888227992976682756, 0.1214114860980369109 ) ) ;
#49869=ORIENTED_EDGE ( 'NONE', *, *, #48425, .T. ) ;
#49881=B_SPLINE_CURVE_WITH_KNOTS ( 'NONE', 3,
 ( #20136, #10158, #10812, #5861, #31099, #36415, #51412, #35422 ),
 .UNSPECIFIED., .F., .F.,
 ( 4, 2, 2, 4 ),
 ( 0.000000000000000000, 0.0003639104015150018603, 0.0007278208030300037205, 0.001455641606060010260 ),
 .UNSPECIFIED. ) ;
#49883=CARTESIAN_POINT ( 'NONE',  ( -27.09030469827879983, -2.239626370111428955, -0.5638997280370279253 ) ) ;
#49884=ORIENTED_EDGE ( 'NONE', *, *, #40260, .T. ) ;
#49887=ORIENTED_EDGE ( 'NONE', *, *, #49473, .T. ) ;
#49896=DIRECTION ( 'NONE',  ( -1.000000000000000000, 0.000000000000000000, 0.000000000000000000 ) ) ;
#49899=CARTESIAN_POINT ( 'NONE',  ( 2.000000000000001776, -5.107597897712365054, 4.693343793638375061 ) ) ;
#49900=ORIENTED_EDGE ( 'NONE', *, *, #29459, .F. ) ;
#49901=AXIS2_PLACEMENT_3D ( 'NONE', #56100, #24213, #19233 ) ;
#49906=DIRECTION ( 'NONE',  ( 0.000000000000000000, 0.000000000000000000, 1.000000000000000000 ) ) ;
#49907=DIRECTION ( 'NONE',  ( 0.000000000000000000, 0.000000000000000000, 1.000000000000000000 ) ) ;
#49908=CIRCLE ( 'NONE', #21215, 2.899999999999995470 ) ;
#49913=EDGE_CURVE ( 'NONE', #59829, #37286, #9687, .T. ) ;
#49916=CARTESIAN_POINT ( 'NONE',  ( 0.000000000000000000, -3.795144977083660720, 6.468916029978762694 ) ) ;
#49921=ORIENTED_EDGE ( 'NONE', *, *, #26381, .F. ) ;
#49925=EDGE_CURVE ( 'NONE', #28265, #7169, #37320, .T. ) ;
#49945=AXIS2_PLACEMENT_3D ( 'NONE', #58134, #3267, #53804 ) ;
#49961=VERTEX_POINT ( 'NONE', #24204 ) ;
#49964=EDGE_LOOP ( 'NONE', ( #56707, #4173, #60648, #64941 ) ) ;
#49966=CARTESIAN_POINT ( 'NONE',  ( -22.51237073810381517, 3.933875531624977828, 2.023441661740695618 ) ) ;
#49973=DIRECTION ( 'NONE',  ( -1.000000000000000000, 0.000000000000000000, 0.000000000000000000 ) ) ;
#49976=VERTEX_POINT ( 'NONE', #19220 ) ;
#49979=AXIS2_PLACEMENT_3D ( 'NONE', #49150, #39133, #59123 ) ;
#49980=VERTEX_POINT ( 'NONE', #50480 ) ;
#49982=CARTESIAN_POINT ( 'NONE',  ( -27.08417568107324058, 0.3682236895270734611, 2.261355310631410820 ) ) ;
#49983=DIRECTION ( 'NONE',  ( 0.000000000000000000, 0.000000000000000000, -1.000000000000000000 ) ) ;
#49992=EDGE_CURVE ( 'NONE', #1800, #12565, #54486, .T. ) ;
#49995=CARTESIAN_POINT ( 'NONE',  ( 0.000000000000000000, 1.225832621831856484, 6.827324998361554265 ) ) ;
#50000=VECTOR ( 'NONE', #23094, 1000.000000000000000 ) ;
#50004=VECTOR ( 'NONE', #54160, 1000.000000000000000 ) ;
#50019=CARTESIAN_POINT ( 'NONE',  ( -22.30398854582848145, 3.608860109585136922, -1.062335901716034758 ) ) ;
#50020=VERTEX_POINT ( 'NONE', #65725 ) ;
#50032=CARTESIAN_POINT ( 'NONE',  ( 2.000000000000001776, 6.662861565602083758, -1.421313227905602883 ) ) ;
#50041=CARTESIAN_POINT ( 'NONE',  ( 0.000000000000000000, -5.860254403322033845, 3.474373880649773039 ) ) ;
#50048=EDGE_CURVE ( 'NONE', #34961, #56217, #44720, .T. ) ;
#50057=CARTESIAN_POINT ( 'NONE',  ( 1.000000000000000888, 6.997684042076903310, 2.698595569414223849 ) ) ;
#50060=VERTEX_POINT ( 'NONE', #5241 ) ;
#50061=AXIS2_PLACEMENT_3D ( 'NONE', #48115, #6887, #38779 ) ;
#50065=CARTESIAN_POINT ( 'NONE',  ( -22.27713295444592845, 1.050517974989026104, -3.528329525272667411 ) ) ;
#50070=ADVANCED_FACE ( 'NONE', ( #16842 ), #62700, .F. ) ;
#50076=CARTESIAN_POINT ( 'NONE',  ( 2.000000000000001776, 6.606214214351110670, -2.114938770769863030 ) ) ;
#50080=DIRECTION ( 'NONE',  ( 0.000000000000000000, 0.9985334138511239299, -0.05413890858541457046 ) ) ;
#50094=AXIS2_PLACEMENT_3D ( 'NONE', #40513, #60808, #15246 ) ;
#50095=EDGE_CURVE ( 'NONE', #22010, #65658, #62756, .T. ) ;
#50102=EDGE_CURVE ( 'NONE', #53254, #45502, #1243, .T. ) ;
#50103=VERTEX_POINT ( 'NONE', #31168 ) ;
#50105=CARTESIAN_POINT ( 'NONE',  ( -22.59983133926797549, 4.650609684383191222, 0.06110861519532605202 ) ) ;
#50106=DIRECTION ( 'NONE',  ( 0.000000000000000000, 0.000000000000000000, 1.000000000000000000 ) ) ;
#50112=CARTESIAN_POINT ( 'NONE',  ( -22.59969328935897437, 0.7214993884004556879, -4.594269189967459255 ) ) ;
#50121=EDGE_LOOP ( 'NONE', ( #3011, #48351, #46654, #57843 ) ) ;
#50124=VERTEX_POINT ( 'NONE', #36478 ) ;
#50130=EDGE_CURVE ( 'NONE', #59008, #39168, #57526, .T. ) ;
#50136=ORIENTED_EDGE ( 'NONE', *, *, #54006, .F. ) ;
#50137=ORIENTED_EDGE ( 'NONE', *, *, #9979, .T. ) ;
#50141=CARTESIAN_POINT ( 'NONE',  ( 2.000000000000001776, -5.585096664091960150, 4.113602740025890547 ) ) ;
#50142=VERTEX_POINT ( 'NONE', #21523 ) ;
#50145=CARTESIAN_POINT ( 'NONE',  ( -27.10422407540546885, 1.039355862229912164, -2.109093808474372889 ) ) ;
#50151=ORIENTED_EDGE ( 'NONE', *, *, #50217, .F. ) ;
#50152=CARTESIAN_POINT ( 'NONE',  ( 2.000000000000001776, 6.164400007374793766, -2.900694413976553143 ) ) ;
#50162=CARTESIAN_POINT ( 'NONE',  ( 0.000000000000000000, 0.000000000000000000, 0.000000000000000000 ) ) ;
#50166=VERTEX_POINT ( 'NONE', #57099 ) ;
#50168=CARTESIAN_POINT ( 'NONE',  ( -22.27786964138239867, -3.667590411552013929, 0.3434379038477752277 ) ) ;
#50178=CARTESIAN_POINT ( 'NONE',  ( -22.28073302975501235, 2.626377654649359794, 2.595086548179975416 ) ) ;
#50185=CARTESIAN_POINT ( 'NONE',  ( 0.000000000000000000, 7.248432822490259220, 1.926193556693033271 ) ) ;
#50186=EDGE_CURVE ( 'NONE', #31213, #9689, #30918, .T. ) ;
#50189=CARTESIAN_POINT ( 'NONE',  ( 0.000000000000000000, -4.570217215903314312, -5.218059682435693958 ) ) ;
#50190=DIRECTION ( 'NONE',  ( 0.000000000000000000, -0.8835120444460272671, 0.4684084406997819916 ) ) ;
#50193=AXIS2_PLACEMENT_3D ( 'NONE', #13611, #2704, #63492 ) ;
#50194=VERTEX_POINT ( 'NONE', #63056 ) ;
#50195=ORIENTED_EDGE ( 'NONE', *, *, #12585, .T. ) ;
#50196=CARTESIAN_POINT ( 'NONE',  ( -27.08850691366480490, 2.218359546717756370, -0.6228349286848119393 ) ) ;
#50206=CARTESIAN_POINT ( 'NONE',  ( 2.000000000000001776, -6.936109781200651803, -2.853135311045104316 ) ) ;
#50209=ORIENTED_EDGE ( 'NONE', *, *, #6500, .F. ) ;
#50210=EDGE_LOOP ( 'NONE', ( #3368, #48886, #37612, #35857 ) ) ;
#50212=CARTESIAN_POINT ( 'NONE',  ( -27.08871896697694837, 1.896680818244936617, -1.309412067288129311 ) ) ;
#50213=EDGE_CURVE ( 'NONE', #25571, #20337, #4402, .T. ) ;
#50214=ORIENTED_EDGE ( 'NONE', *, *, #59765, .T. ) ;
#50217=EDGE_CURVE ( 'NONE', #28860, #65138, #37789, .T. ) ;
#50242=DIRECTION ( 'NONE',  ( 0.000000000000000000, -6.879075853011489629E-15, 1.000000000000000000 ) ) ;
#50250=ORIENTED_EDGE ( 'NONE', *, *, #53441, .T. ) ;
#50255=VECTOR ( 'NONE', #37283, 1000.000000000000000 ) ;
#50259=EDGE_LOOP ( 'NONE', ( #35689, #57863, #23818, #16424 ) ) ;
#50262=CARTESIAN_POINT ( 'NONE',  ( -27.35552965826137140, -1.773915698030568366, 2.548625910254532112 ) ) ;
#50268=CARTESIAN_POINT ( 'NONE',  ( -22.27218376572352554, 2.577901515391834764, -2.630375585211903733 ) ) ;
#50269=EDGE_CURVE ( 'NONE', #59063, #43191, #62712, .T. ) ;
#50272=CARTESIAN_POINT ( 'NONE',  ( 2.000000000000001776, 0.000000000000000000, 0.000000000000000000 ) ) ;
#50281=DIRECTION ( 'NONE',  ( 0.000000000000000000, 0.4198891015602657650, -0.9075754196709565624 ) ) ;
#50285=B_SPLINE_CURVE_WITH_KNOTS ( 'NONE', 3,
 ( #47201, #27222, #1956, #21593, #26562, #47516, #46851, #41858 ),
 .UNSPECIFIED., .F., .F.,
 ( 4, 2, 2, 4 ),
 ( 0.000000000000000000, 0.0003639104015150009929, 0.0007278208030300019858, 0.001455641606060005273 ),
 .UNSPECIFIED. ) ;
#50299=EDGE_LOOP ( 'NONE', ( #23806, #19372, #44535, #16597 ) ) ;
#50305=ORIENTED_EDGE ( 'NONE', *, *, #31860, .T. ) ;
#50307=ORIENTED_EDGE ( 'NONE', *, *, #18013, .T. ) ;
#50311=CARTESIAN_POINT ( 'NONE',  ( -35.05012975565874456, -0.004360246756757623493, 0.01323209221895336324 ) ) ;
#50314=CARTESIAN_POINT ( 'NONE',  ( -22.27722019117889829, 0.6493872998088092707, 3.623937139367928939 ) ) ;
#50320=CARTESIAN_POINT ( 'NONE',  ( 2.000000000000001776, 0.000000000000000000, 0.000000000000000000 ) ) ;
#50324=ORIENTED_EDGE ( 'NONE', *, *, #40148, .T. ) ;
#50341=CARTESIAN_POINT ( 'NONE',  ( 2.000000000000001776, 0.000000000000000000, 0.000000000000000000 ) ) ;
#50342=AXIS2_PLACEMENT_3D ( 'NONE', #17936, #27571, #23248 ) ;
#50347=ADVANCED_FACE ( 'NONE', ( #19484 ), #39414, .T. ) ;
#50353=ORIENTED_EDGE ( 'NONE', *, *, #20045, .F. ) ;
#50369=CIRCLE ( 'NONE', #41848, 2.899999999999993694 ) ;
#50370=ORIENTED_EDGE ( 'NONE', *, *, #1434, .T. ) ;
#50374=CARTESIAN_POINT ( 'NONE',  ( -22.70624764888619751, -2.702761586319157860, 4.501516772829871726 ) ) ;
#50376=CARTESIAN_POINT ( 'NONE',  ( -22.38932658256920405, -2.201197575855953659, -3.361598243548662879 ) ) ;
#50379=DIRECTION ( 'NONE',  ( 1.000000000000000000, 0.000000000000000000, 0.000000000000000000 ) ) ;
#50389=CARTESIAN_POINT ( 'NONE',  ( -22.28546858134833286, -0.9133285433746629600, 3.592117891549486242 ) ) ;
#50405=CARTESIAN_POINT ( 'NONE',  ( -22.28073302975500880, 0.9342220484184898810, -3.572053042948128088 ) ) ;
#50407=CARTESIAN_POINT ( 'NONE',  ( -22.27711653538342773, 1.465933162149084978, -3.377206745424994327 ) ) ;
#50412=VERTEX_POINT ( 'NONE', #40391 ) ;
#50413=LINE ( 'NONE', #522, #38126 ) ;
#50416=CARTESIAN_POINT ( 'NONE',  ( 0.000000000000000000, 6.664893814313781029, -3.439359016433444438 ) ) ;
#50417=CARTESIAN_POINT ( 'NONE',  ( -27.32343372485686572, -3.007804754713678808, -0.1402256980610577797 ) ) ;
#50439=DIRECTION ( 'NONE',  ( -1.000000000000000000, 0.000000000000000000, 0.000000000000000000 ) ) ;
#50449=CARTESIAN_POINT ( 'NONE',  ( -27.10422407540546885, 1.306850885988335209, 1.954655484500537277 ) ) ;
#50458=ORIENTED_EDGE ( 'NONE', *, *, #9664, .F. ) ;
#50477=CARTESIAN_POINT ( 'NONE',  ( -27.10128162969864363, 2.337214317750537340, -0.1566844438592116806 ) ) ;
#50480=CARTESIAN_POINT ( 'NONE',  ( 2.000000000000001776, 5.457833520448724940, -4.281014542496488495 ) ) ;
#50504=ORIENTED_EDGE ( 'NONE', *, *, #24947, .T. ) ;
#50505=CARTESIAN_POINT ( 'NONE',  ( -35.04643116707788408, -0.01193867652720878580, 0.002453861112621663620 ) ) ;
#50511=DIRECTION ( 'NONE',  ( 1.000000000000000000, 0.000000000000000000, 0.000000000000000000 ) ) ;
#50512=AXIS2_PLACEMENT_3D ( 'NONE', #14479, #23506, #34757 ) ;
#50513=ORIENTED_EDGE ( 'NONE', *, *, #3231, .T. ) ;
#50514=CARTESIAN_POINT ( 'NONE',  ( -27.08429572838383947, -0.6096735944848084010, 2.208905845566022208 ) ) ;
#50522=EDGE_CURVE ( 'NONE', #37286, #5947, #9745, .T. ) ;
#50525=DIRECTION ( 'NONE',  ( -1.000000000000000000, 0.000000000000000000, 0.000000000000000000 ) ) ;
#50529=CARTESIAN_POINT ( 'NONE',  ( 0.000000000000000000, 3.805198749487521681, -5.799611601383208637 ) ) ;
#50535=VERTEX_POINT ( 'NONE', #61663 ) ;
#50536=EDGE_CURVE ( 'NONE', #65336, #648, #57564, .T. ) ;
#50541=VERTEX_POINT ( 'NONE', #51400 ) ;
#50543=ORIENTED_EDGE ( 'NONE', *, *, #31216, .F. ) ;
#50546=DIRECTION ( 'NONE',  ( -1.000000000000000000, 0.000000000000000000, 0.000000000000000000 ) ) ;
#50547=EDGE_CURVE ( 'NONE', #42222, #19077, #39450, .T. ) ;
#50553=ORIENTED_EDGE ( 'NONE', *, *, #59896, .F. ) ;
#50555=ORIENTED_EDGE ( 'NONE', *, *, #34446, .F. ) ;
#50561=DIRECTION ( 'NONE',  ( -1.000000000000000000, 0.000000000000000000, 0.000000000000000000 ) ) ;
#50572=CARTESIAN_POINT ( 'NONE',  ( -27.08485414902838784, 0.5952588087544679052, 2.214586389210142059 ) ) ;
#50577=FACE_OUTER_BOUND ( 'NONE', #40507, .T. ) ;
#50579=ORIENTED_EDGE ( 'NONE', *, *, #4540, .F. ) ;
#50599=CIRCLE ( 'NONE', #28280, 2.899999999999995026 ) ;
#50605=DIRECTION ( 'NONE',  ( 1.000000000000000000, -0.000000000000000000, -0.000000000000000000 ) ) ;
#50607=VERTEX_POINT ( 'NONE', #32055 ) ;
#50617=DIRECTION ( 'NONE',  ( 0.000000000000000000, 0.3193015301359742875, 0.9476531711828043436 ) ) ;
#50619=CARTESIAN_POINT ( 'NONE',  ( -22.28350523959500862, 0.3047406164877414225, 3.687952016964565871 ) ) ;
#50622=CARTESIAN_POINT ( 'NONE',  ( -27.08935880048797529, 1.653090150968474781, 1.608762129669635721 ) ) ;
#50624=CARTESIAN_POINT ( 'NONE',  ( 0.000000000000000000, -1.865193240757054394, -6.552473556515217012 ) ) ;
#50631=EDGE_CURVE ( 'NONE', #18668, #39229, #12936, .T. ) ;
#50632=DIRECTION ( 'NONE',  ( 0.000000000000000000, 0.000000000000000000, 1.000000000000000000 ) ) ;
#50633=DIRECTION ( 'NONE',  ( -1.000000000000000000, 0.000000000000000000, 0.000000000000000000 ) ) ;
#50634=FACE_OUTER_BOUND ( 'NONE', #30168, .T. ) ;
#50637=CARTESIAN_POINT ( 'NONE',  ( -27.08419797710328325, 2.268561579780429494, -0.3221715127607987506 ) ) ;
#50641=EDGE_CURVE ( 'NONE', #50142, #22284, #18272, .T. ) ;
#50645=ORIENTED_EDGE ( 'NONE', *, *, #25800, .F. ) ;
#50650=CARTESIAN_POINT ( 'NONE',  ( -27.08418322526031119, 0.3452258100746978253, 2.265123059255399696 ) ) ;
#50656=CARTESIAN_POINT ( 'NONE',  ( 2.000000000000001776, 0.3246585432986198727, 6.805031400696091914 ) ) ;
#50666=CARTESIAN_POINT ( 'NONE',  ( -22.51237073810381517, 2.395115314842884757, 3.719289647955732914 ) ) ;
#50689=CIRCLE ( 'NONE', #10328, 2.899999999999995026 ) ;
#50690=ORIENTED_EDGE ( 'NONE', *, *, #60475, .F. ) ;
#50694=CARTESIAN_POINT ( 'NONE',  ( 2.000000000000001776, 0.000000000000000000, 0.000000000000000000 ) ) ;
#50695=( BOUNDED_SURFACE ( )  B_SPLINE_SURFACE ( 3, 1, ( 
 ( #32433, #52744 ),
 ( #28124, #19119 ),
 ( #24112, #23455 ),
 ( #49080, #17813 ) ),
 .UNSPECIFIED., .F., .F., .F. ) 
 B_SPLINE_SURFACE_WITH_KNOTS ( ( 4, 4 ),
 ( 2, 2 ),
 ( 0.000000000000000000, 1.000000000000000000 ),
 ( 0.000000000000000000, 1.000000000000000000 ),
 .UNSPECIFIED. ) 
 GEOMETRIC_REPRESENTATION_ITEM ( )  RATIONAL_B_SPLINE_SURFACE ( (
 ( 1.000000000000000000, 1.000000000000000000),
 ( 0.8716676215708681896, 0.8964445200148164483),
 ( 0.8716676215708681896, 0.8964445200148164483),
 ( 1.000000000000000000, 1.000000000000000000) ) ) 
 REPRESENTATION_ITEM ( '' )  SURFACE ( )  );
#50702=CARTESIAN_POINT ( 'NONE',  ( -10.00000000000000178, 0.000000000000000000, 0.000000000000000000 ) ) ;
#50707=EDGE_CURVE ( 'NONE', #28767, #28152, #40554, .T. ) ;
#50710=DIRECTION ( 'NONE',  ( 0.000000000000000000, 0.000000000000000000, 1.000000000000000000 ) ) ;
#50715=DIRECTION ( 'NONE',  ( -1.000000000000000000, 0.000000000000000000, 0.000000000000000000 ) ) ;
#50722=CARTESIAN_POINT ( 'NONE',  ( -22.27718150314433387, 1.117371044661096713, -3.507884203786629129 ) ) ;
#50728=VERTEX_POINT ( 'NONE', #64933 ) ;
#50743=CARTESIAN_POINT ( 'NONE',  ( 0.000000000000000000, 6.796153407501467569, -1.388283512725773772 ) ) ;
#50752=CARTESIAN_POINT ( 'NONE',  ( 0.000000000000000000, -6.201547234536999298, -2.820401998297984214 ) ) ;
#50754=CARTESIAN_POINT ( 'NONE',  ( -22.28284753389937123, -0.9912969289936532924, -3.563226652211067602 ) ) ;
#50757=CARTESIAN_POINT ( 'NONE',  ( -27.09569413923794556, 2.259195818742697703, 0.5521997980586177412 ) ) ;
#50762=CARTESIAN_POINT ( 'NONE',  ( -27.09483304420744787, 1.303111346475875010, 1.923212037694846055 ) ) ;
#50775=DIRECTION ( 'NONE',  ( -1.000000000000000000, 0.000000000000000000, 0.000000000000000000 ) ) ;
#50787=CARTESIAN_POINT ( 'NONE',  ( -27.10113028276028402, 0.5479825692853955710, -2.276991616286355935 ) ) ;
#50791=DIRECTION ( 'NONE',  ( 0.000000000000000000, 0.9985334138511240409, -0.05413890858541454271 ) ) ;
#50797=CARTESIAN_POINT ( 'NONE',  ( 2.000000000000001776, -3.224464355699868889, 6.771471746881965181 ) ) ;
#50801=DIRECTION ( 'NONE',  ( 0.000000000000000000, -0.4198891015602715382, 0.9075754196709537869 ) ) ;
#50816=AXIS2_PLACEMENT_3D ( 'NONE', #41625, #26336, #22315 ) ;
#50836=CARTESIAN_POINT ( 'NONE',  ( -22.27384469013076185, -0.9224151068931498720, -3.564715702084492399 ) ) ;
#50846=CARTESIAN_POINT ( 'NONE',  ( -22.27716857039623477, -3.514919882996453637, -1.095155339732105881 ) ) ;
#50856=CIRCLE ( 'NONE', #4146, 2.899999999999993694 ) ;
#50857=CARTESIAN_POINT ( 'NONE',  ( -27.09483304420744787, 1.923212037694859822, -1.303111346475867904 ) ) ;
#50858=ORIENTED_EDGE ( 'NONE', *, *, #47715, .F. ) ;
#50865=DIRECTION ( 'NONE',  ( 1.000000000000000000, -0.000000000000000000, -0.000000000000000000 ) ) ;
#50866=ORIENTED_EDGE ( 'NONE', *, *, #26156, .F. ) ;
#50869=CARTESIAN_POINT ( 'NONE',  ( 1.000000000000000888, 7.493043167941614513, -0.3229614270519962638 ) ) ;
#50874=AXIS2_PLACEMENT_3D ( 'NONE', #51407, #55047, #14468 ) ;
#50881=CARTESIAN_POINT ( 'NONE',  ( -35.04683013664716640, -0.004196202180954865246, -0.01162359816266951562 ) ) ;
#50884=( BOUNDED_SURFACE ( )  B_SPLINE_SURFACE ( 3, 1, ( 
 ( #9064, #34643 ),
 ( #64904, #18414 ),
 ( #23726, #29344 ),
 ( #18738, #7767 ) ),
 .UNSPECIFIED., .F., .F., .F. ) 
 B_SPLINE_SURFACE_WITH_KNOTS ( ( 4, 4 ),
 ( 2, 2 ),
 ( 0.000000000000000000, 1.000000000000000000 ),
 ( 0.000000000000000000, 1.000000000000000000 ),
 .UNSPECIFIED. ) 
 GEOMETRIC_REPRESENTATION_ITEM ( )  RATIONAL_B_SPLINE_SURFACE ( (
 ( 1.000000000000000000, 1.000000000000000000),
 ( 0.9932032654565553509, 0.8386279382598740284),
 ( 0.9932032654565553509, 0.8386279382598740284),
 ( 1.000000000000000000, 1.000000000000000000) ) ) 
 REPRESENTATION_ITEM ( '' )  SURFACE ( )  );
#50886=CARTESIAN_POINT ( 'NONE',  ( -27.09342121492585420, 0.6436068655225422042, 2.227768580955189925 ) ) ;
#50887=ORIENTED_EDGE ( 'NONE', *, *, #49803, .T. ) ;
#50893=VERTEX_POINT ( 'NONE', #61267 ) ;
#50902=ADVANCED_FACE ( 'NONE', ( #60609 ), #30662, .T. ) ;
#50904=ORIENTED_EDGE ( 'NONE', *, *, #20882, .F. ) ;
#50911=EDGE_CURVE ( 'NONE', #47922, #63874, #58519, .T. ) ;
#50915=FACE_OUTER_BOUND ( 'NONE', #46872, .T. ) ;
#50921=EDGE_CURVE ( 'NONE', #40113, #60906, #25547, .T. ) ;
#50925=DIRECTION ( 'NONE',  ( -1.000000000000000000, 0.000000000000000000, 0.000000000000000000 ) ) ;
#50927=CARTESIAN_POINT ( 'NONE',  ( 2.000000000000001776, -1.225832621831887792, 6.827324998361543607 ) ) ;
#50933=CARTESIAN_POINT ( 'NONE',  ( 1.000000000000000888, -3.073484823194281290, -6.841322316745092280 ) ) ;
#50938=LINE ( 'NONE', #31936, #6088 ) ;
#50942=AXIS2_PLACEMENT_3D ( 'NONE', #18097, #6239, #61747 ) ;
#50953=CARTESIAN_POINT ( 'NONE',  ( 2.000000000000001776, -4.915517050588371184, -4.717154614762162801 ) ) ;
#50958=CARTESIAN_POINT ( 'NONE',  ( -27.08426504710140392, 2.223709847896212732, -0.5533780324190695765 ) ) ;
#50962=CIRCLE ( 'NONE', #56259, 6.936499999999993449 ) ;
#50969=EDGE_CURVE ( 'NONE', #65490, #24851, #38868, .T. ) ;
#50974=CARTESIAN_POINT ( 'NONE',  ( -22.27945548916780183, 1.551028078364857343, -3.346394890313965753 ) ) ;
#50981=DIRECTION ( 'NONE',  ( -1.000000000000000000, 0.000000000000000000, 0.000000000000000000 ) ) ;
#50982=ADVANCED_FACE ( 'NONE', ( #2670 ), #48530, .T. ) ;
#50988=CARTESIAN_POINT ( 'NONE',  ( 0.000000000000000000, -1.018311147294196806, 6.861346417234461370 ) ) ;
#50992=CARTESIAN_POINT ( 'NONE',  ( 0.000000000000000000, 0.000000000000000000, 0.000000000000000000 ) ) ;
#50993=EDGE_CURVE ( 'NONE', #37253, #27036, #61160, .T. ) ;
#51002=LINE ( 'NONE', #5461, #22603 ) ;
#51003=CARTESIAN_POINT ( 'NONE',  ( -22.28546858134833641, 3.567529619157801868, -1.005093225210833330 ) ) ;
#51010=ORIENTED_EDGE ( 'NONE', *, *, #50186, .F. ) ;
#51011=ORIENTED_EDGE ( 'NONE', *, *, #50911, .T. ) ;
#51032=VECTOR ( 'NONE', #49218, 1000.000000000000000 ) ;
#51033=EDGE_CURVE ( 'NONE', #6128, #43782, #59162, .T. ) ;
#51038=DIRECTION ( 'NONE',  ( -1.000000000000000000, 0.000000000000000000, 0.000000000000000000 ) ) ;
#51039=DIRECTION ( 'NONE',  ( -1.000000000000000000, 0.000000000000000000, 0.000000000000000000 ) ) ;
#51046=EDGE_CURVE ( 'NONE', #18668, #24851, #13853, .T. ) ;
#51051=DIRECTION ( 'NONE',  ( 0.000000000000000000, 0.000000000000000000, 1.000000000000000000 ) ) ;
#51055=AXIS2_PLACEMENT_3D ( 'NONE', #32165, #27509, #16573 ) ;
#51062=AXIS2_PLACEMENT_3D ( 'NONE', #13005, #7344, #59224 ) ;
#51075=ADVANCED_FACE ( 'NONE', ( #60123 ), #65101, .T. ) ;
#51077=AXIS2_PLACEMENT_3D ( 'NONE', #7890, #37805, #32471 ) ;
#51082=( BOUNDED_SURFACE ( )  B_SPLINE_SURFACE ( 3, 1, ( 
 ( #45230, #65489 ),
 ( #50881, #5328 ),
 ( #40225, #55542 ),
 ( #25267, #45894 ) ),
 .UNSPECIFIED., .F., .F., .F. ) 
 B_SPLINE_SURFACE_WITH_KNOTS ( ( 4, 4 ),
 ( 2, 2 ),
 ( 0.000000000000000000, 1.000000000000000000 ),
 ( 0.000000000000000000, 1.000000000000000000 ),
 .UNSPECIFIED. ) 
 GEOMETRIC_REPRESENTATION_ITEM ( )  RATIONAL_B_SPLINE_SURFACE ( (
 ( 1.000000000000000000, 1.000000000000000000),
 ( 0.9932032654565553509, 0.8386279382598736953),
 ( 0.9932032654565553509, 0.8386279382598736953),
 ( 1.000000000000000000, 1.000000000000000000) ) ) 
 REPRESENTATION_ITEM ( '' )  SURFACE ( )  );
#51091=DIRECTION ( 'NONE',  ( -1.000000000000000000, 0.000000000000000000, 0.000000000000000000 ) ) ;
#51095=CARTESIAN_POINT ( 'NONE',  ( -22.94572469358971034, -4.870584850960110401, -0.4123340087948408894 ) ) ;
#51096=VERTEX_POINT ( 'NONE', #29219 ) ;
#51102=CARTESIAN_POINT ( 'NONE',  ( 2.000000000000001776, -3.341639490130703827, -6.078525953551491057 ) ) ;
#51107=VERTEX_POINT ( 'NONE', #39508 ) ;
#51114=DIRECTION ( 'NONE',  ( -1.000000000000000000, 0.000000000000000000, 0.000000000000000000 ) ) ;
#51117=EDGE_CURVE ( 'NONE', #49961, #8080, #9904, .T. ) ;
#51133=CIRCLE ( 'NONE', #4430, 2.899999999999994582 ) ;
#51134=CARTESIAN_POINT ( 'NONE',  ( -22.65999102136916576, -1.886119913916072255, -4.450325798697174484 ) ) ;
#51170=AXIS2_PLACEMENT_3D ( 'NONE', #43499, #62476, #53174 ) ;
#51177=EDGE_CURVE ( 'NONE', #3171, #3708, #42894, .T. ) ;
#51186=DIRECTION ( 'NONE',  ( -1.000000000000000000, 0.000000000000000000, 0.000000000000000000 ) ) ;
#51198=CARTESIAN_POINT ( 'NONE',  ( -27.09150307427401927, 1.909742362149659867, -1.305148381378450351 ) ) ;
#51202=CARTESIAN_POINT ( 'NONE',  ( -22.27713295444592845, 3.580881989303326129, -0.8543895091636388717 ) ) ;
#51210=AXIS2_PLACEMENT_3D ( 'NONE', #65248, #4419, #19717 ) ;
#51214=ORIENTED_EDGE ( 'NONE', *, *, #30666, .T. ) ;
#51224=EDGE_CURVE ( 'NONE', #30158, #17686, #35500, .T. ) ;
#51225=CARTESIAN_POINT ( 'NONE',  ( -22.71097035706202405, -2.846599994298329328, 4.089776368546542251 ) ) ;
#51228=AXIS2_PLACEMENT_3D ( 'NONE', #52761, #22494, #42758 ) ;
#51231=CARTESIAN_POINT ( 'NONE',  ( 0.000000000000000000, 5.769711778877384845, -4.791703871138491166 ) ) ;
#51237=AXIS2_PLACEMENT_3D ( 'NONE', #2416, #32315, #12037 ) ;
#51239=ORIENTED_EDGE ( 'NONE', *, *, #42084, .T. ) ;
#51241=ADVANCED_FACE ( 'NONE', ( #5254 ), #25520, .T. ) ;
#51243=DIRECTION ( 'NONE',  ( -1.000000000000000000, 0.000000000000000000, 0.000000000000000000 ) ) ;
#51247=EDGE_LOOP ( 'NONE', ( #10320, #60019, #41379, #53056, #61712, #34932 ) ) ;
#51253=AXIS2_PLACEMENT_3D ( 'NONE', #31118, #17719, #15805 ) ;
#51261=ORIENTED_EDGE ( 'NONE', *, *, #55003, .F. ) ;
#51265=CYLINDRICAL_SURFACE ( 'NONE', #55539, 2.899999999999994582 ) ;
#51267=ORIENTED_EDGE ( 'NONE', *, *, #3921, .F. ) ;
#51273=LINE ( 'NONE', #50933, #20632 ) ;
#51274=VECTOR ( 'NONE', #57449, 1000.000000000000000 ) ;
#51275=CARTESIAN_POINT ( 'NONE',  ( -22.27711351828769892, 0.8770428151440663456, 3.575417021793764416 ) ) ;
#51276=AXIS2_PLACEMENT_3D ( 'NONE', #49691, #55324, #39703 ) ;
#51281=ORIENTED_EDGE ( 'NONE', *, *, #4760, .F. ) ;
#51287=ORIENTED_EDGE ( 'NONE', *, *, #2086, .F. ) ;
#51288=CARTESIAN_POINT ( 'NONE',  ( 2.000000000000001776, -6.777474576704058506, 0.6925993764990423518 ) ) ;
#51291=FACE_OUTER_BOUND ( 'NONE', #38487, .T. ) ;
#51292=ORIENTED_EDGE ( 'NONE', *, *, #49553, .F. ) ;
#51293=DIRECTION ( 'NONE',  ( -1.000000000000000000, 0.000000000000000000, 0.000000000000000000 ) ) ;
#51298=DIRECTION ( 'NONE',  ( 0.000000000000000000, 0.000000000000000000, 1.000000000000000000 ) ) ;
#51308=EDGE_CURVE ( 'NONE', #8903, #332, #48977, .T. ) ;
#51327=AXIS2_PLACEMENT_3D ( 'NONE', #23812, #22820, #54395 ) ;
#51330=DIRECTION ( 'NONE',  ( -1.000000000000000000, 0.000000000000000000, 0.000000000000000000 ) ) ;
#51332=CARTESIAN_POINT ( 'NONE',  ( 2.000000000000001776, -6.812627895098285258, -0.04423456934733380197 ) ) ;
#51336=DIRECTION ( 'NONE',  ( -1.000000000000000000, 0.000000000000000000, 0.000000000000000000 ) ) ;
#51337=AXIS2_PLACEMENT_3D ( 'NONE', #17632, #12607, #62832 ) ;
#51339=ORIENTED_EDGE ( 'NONE', *, *, #4391, .F. ) ;
#51348=CARTESIAN_POINT ( 'NONE',  ( -22.27706485742869091, 3.563814065926677710, -0.9221835209182235316 ) ) ;
#51352=VERTEX_POINT ( 'NONE', #29026 ) ;
#51358=EDGE_CURVE ( 'NONE', #37217, #50194, #42567, .T. ) ;
#51360=LINE ( 'NONE', #15426, #55723 ) ;
#51370=CARTESIAN_POINT ( 'NONE',  ( -22.31328051695926007, -3.685074213229319717, -0.8849444482788241251 ) ) ;
#51372=ORIENTED_EDGE ( 'NONE', *, *, #14573, .F. ) ;
#51374=CARTESIAN_POINT ( 'NONE',  ( 2.000000000000001776, 3.155844197800189210, -6.177028383390422484 ) ) ;
#51377=EDGE_LOOP ( 'NONE', ( #27386, #52834, #21907, #31929 ) ) ;
#51378=CARTESIAN_POINT ( 'NONE',  ( 2.000000000000001776, -4.962980376314023445, -4.846014654777856201 ) ) ;
#51386=ORIENTED_EDGE ( 'NONE', *, *, #48523, .F. ) ;
#51388=EDGE_LOOP ( 'NONE', ( #27941, #16382, #7114, #51546 ) ) ;
#51389=EDGE_CURVE ( 'NONE', #27863, #45739, #55364, .T. ) ;
#51394=DIRECTION ( 'NONE',  ( 0.000000000000000000, 0.000000000000000000, -1.000000000000000000 ) ) ;
#51400=CARTESIAN_POINT ( 'NONE',  ( 2.000000000000001776, -4.472310526050724100, -6.020667617347421618 ) ) ;
#51404=EDGE_LOOP ( 'NONE', ( #12095, #9723, #60826, #5737 ) ) ;
#51407=CARTESIAN_POINT ( 'NONE',  ( 0.000000000000000000, 0.000000000000000000, 0.000000000000000000 ) ) ;
#51409=CARTESIAN_POINT ( 'NONE',  ( -22.28506771379528573, 3.348518833762387459, 1.636577531579554545 ) ) ;
#51411=CIRCLE ( 'NONE', #9942, 7.499999999999988454 ) ;
#51412=CARTESIAN_POINT ( 'NONE',  ( -22.65996813707689839, 2.220979297960725685, 4.292955455498893791 ) ) ;
#51418=CARTESIAN_POINT ( 'NONE',  ( -27.35552965826137140, 2.548625910254547655, 1.773915698030531951 ) ) ;
#51421=DIRECTION ( 'NONE',  ( -1.000000000000000000, 0.000000000000000000, 0.000000000000000000 ) ) ;
#51456=CARTESIAN_POINT ( 'NONE',  ( 0.000000000000000000, -6.441884263200848615, 2.217201541069723891 ) ) ;
#51464=ORIENTED_EDGE ( 'NONE', *, *, #59107, .T. ) ;
#51465=VERTEX_POINT ( 'NONE', #18315 ) ;
#51469=VERTEX_POINT ( 'NONE', #43897 ) ;
#51473=CARTESIAN_POINT ( 'NONE',  ( 2.000000000000001776, 0.000000000000000000, 0.000000000000000000 ) ) ;
#51494=ADVANCED_FACE ( 'NONE', ( #13310 ), #28595, .T. ) ;
#51497=CARTESIAN_POINT ( 'NONE',  ( -22.31099767395441091, -3.774495463598469769, 0.2534174342804084712 ) ) ;
#51501=CARTESIAN_POINT ( 'NONE',  ( -22.27834755396594346, 2.876353066242391510, -2.305389312780934841 ) ) ;
#51502=DIRECTION ( 'NONE',  ( 0.000000000000000000, 0.000000000000000000, 1.000000000000000000 ) ) ;
#51504=CARTESIAN_POINT ( 'NONE',  ( -22.65996813707688418, 4.069902221062769776, 2.607318832796647445 ) ) ;
#51512=DIRECTION ( 'NONE',  ( -1.000000000000000000, 0.000000000000000000, 0.000000000000000000 ) ) ;
#51518=ORIENTED_EDGE ( 'NONE', *, *, #30546, .T. ) ;
#51521=ORIENTED_EDGE ( 'NONE', *, *, #40315, .F. ) ;
#51522=DIRECTION ( 'NONE',  ( 0.000000000000000000, 0.000000000000000000, 1.000000000000000000 ) ) ;
#51523=CARTESIAN_POINT ( 'NONE',  ( -22.27834755396594346, 3.497967921180563877, 1.162947663292818623 ) ) ;
#51524=CIRCLE ( 'NONE', #580, 7.499999999999988454 ) ;
#51526=CARTESIAN_POINT ( 'NONE',  ( -28.66013792860432119, -1.306994062650338684, 1.289369452666812244 ) ) ;
#51533=DIRECTION ( 'NONE',  ( -1.000000000000000000, 0.000000000000000000, 0.000000000000000000 ) ) ;
#51536=CIRCLE ( 'NONE', #12196, 2.899999999999994582 ) ;
#51541=VERTEX_POINT ( 'NONE', #34237 ) ;
#51546=ORIENTED_EDGE ( 'NONE', *, *, #35849, .F. ) ;
#51561=CARTESIAN_POINT ( 'NONE',  ( -22.35190811654612020, -3.498661567523020821, -1.736165297231004434 ) ) ;
#51564=CARTESIAN_POINT ( 'NONE',  ( -27.08430792439081003, 0.5856059198894674189, 2.215465963318176357 ) ) ;
#51566=DIRECTION ( 'NONE',  ( -1.000000000000000000, 0.000000000000000000, 0.000000000000000000 ) ) ;
#51571=DIRECTION ( 'NONE',  ( -1.000000000000000000, 0.000000000000000000, 0.000000000000000000 ) ) ;
#51577=DIRECTION ( 'NONE',  ( 0.000000000000000000, 0.000000000000000000, 1.000000000000000000 ) ) ;
#51578=ORIENTED_EDGE ( 'NONE', *, *, #46163, .F. ) ;
#51584=ADVANCED_FACE ( 'NONE', ( #19931 ), #46233, .F. ) ;
#51592=ORIENTED_EDGE ( 'NONE', *, *, #31523, .T. ) ;
#51599=ORIENTED_EDGE ( 'NONE', *, *, #51308, .T. ) ;
#51606=ORIENTED_EDGE ( 'NONE', *, *, #178, .F. ) ;
#51609=ORIENTED_EDGE ( 'NONE', *, *, #30872, .F. ) ;
#51611=CARTESIAN_POINT ( 'NONE',  ( -22.28776923226071460, 0.2883912626656737754, 3.702096209084090983 ) ) ;
#51618=ORIENTED_EDGE ( 'NONE', *, *, #58654, .F. ) ;
#51622=DIRECTION ( 'NONE',  ( -1.000000000000000000, 0.000000000000000000, 0.000000000000000000 ) ) ;
#51637=CARTESIAN_POINT ( 'NONE',  ( -27.10719052120871098, -2.355164825213512003, 0.1538293304135223694 ) ) ;
#51642=ORIENTED_EDGE ( 'NONE', *, *, #39635, .T. ) ;
#51645=CARTESIAN_POINT ( 'NONE',  ( -35.04643116707788408, -0.009112266603810564858, 0.008094444324481878117 ) ) ;
#51646=CARTESIAN_POINT ( 'NONE',  ( 0.000000000000000000, -6.777474576704058506, 0.6925993764990423518 ) ) ;
#51654=CARTESIAN_POINT ( 'NONE',  ( -22.66110217412718697, -4.366928509133846781, 2.319520136975691482 ) ) ;
#51659=EDGE_CURVE ( 'NONE', #29418, #65490, #29860, .T. ) ;
#51678=ORIENTED_EDGE ( 'NONE', *, *, #8809, .T. ) ;
#51681=ADVANCED_FACE ( 'NONE', ( #7166 ), #27446, .T. ) ;
#51703=AXIS2_PLACEMENT_3D ( 'NONE', #3774, #60569, #19706 ) ;
#51709=EDGE_LOOP ( 'NONE', ( #47897, #20268, #54297, #49884 ) ) ;
#51711=CARTESIAN_POINT ( 'NONE',  ( -10.00000000000000178, 0.000000000000000000, 0.000000000000000000 ) ) ;
#51715=FACE_OUTER_BOUND ( 'NONE', #26408, .T. ) ;
#51720=CARTESIAN_POINT ( 'NONE',  ( -22.28350523959500862, -3.041489826385514572, 2.107889123925578367 ) ) ;
#51722=DIRECTION ( 'NONE',  ( -1.000000000000000000, 0.000000000000000000, 0.000000000000000000 ) ) ;
#51723=EDGE_CURVE ( 'NONE', #9280, #33968, #65022, .T. ) ;
#51724=CARTESIAN_POINT ( 'NONE',  ( -35.05012975565874456, 0.002073729464855276518, 0.01377677982613004053 ) ) ;
#51739=ORIENTED_EDGE ( 'NONE', *, *, #14222, .T. ) ;
#51752=EDGE_CURVE ( 'NONE', #27004, #50535, #61709, .T. ) ;
#51762=CARTESIAN_POINT ( 'NONE',  ( 0.000000000000000000, 0.8935325819928834346, 7.446583077151348817 ) ) ;
#51769=DIRECTION ( 'NONE',  ( 0.000000000000000000, 0.6876994588534246500, -0.7259954919231293990 ) ) ;
#51773=CARTESIAN_POINT ( 'NONE',  ( -22.31328051695926007, -3.401210163132568187, -1.671726071983963946 ) ) ;
#51776=ORIENTED_EDGE ( 'NONE', *, *, #22832, .T. ) ;
#51783=DIRECTION ( 'NONE',  ( 0.000000000000000000, 0.000000000000000000, -1.000000000000000000 ) ) ;
#51788=AXIS2_PLACEMENT_3D ( 'NONE', #21838, #1872, #36786 ) ;
#51790=ORIENTED_EDGE ( 'NONE', *, *, #2689, .F. ) ;
#51799=ORIENTED_EDGE ( 'NONE', *, *, #13110, .F. ) ;
#51805=CARTESIAN_POINT ( 'NONE',  ( 2.000000000000001776, 5.997115278587678233, -3.485633455389450130 ) ) ;
#51817=CIRCLE ( 'NONE', #7219, 2.899999999999995914 ) ;
#51822=DIRECTION ( 'NONE',  ( 0.000000000000000000, -0.6051742151937558045, -0.7960930657056509707 ) ) ;
#51824=CARTESIAN_POINT ( 'NONE',  ( -35.04660725145885891, 0.01123650152080950260, 0.004999447127041124761 ) ) ;
#51833=CARTESIAN_POINT ( 'NONE',  ( -27.08416813689868263, -2.257587568255724708, 0.3912215308406081782 ) ) ;
#51850=DIRECTION ( 'NONE',  ( -1.000000000000000000, 0.000000000000000000, 0.000000000000000000 ) ) ;
#51853=ORIENTED_EDGE ( 'NONE', *, *, #52293, .T. ) ;
#51854=ORIENTED_EDGE ( 'NONE', *, *, #61812, .T. ) ;
#51860=VERTEX_POINT ( 'NONE', #51370 ) ;
#51864=EDGE_CURVE ( 'NONE', #26639, #61504, #17151, .T. ) ;
#51871=AXIS2_PLACEMENT_3D ( 'NONE', #39935, #44927, #18702 ) ;
#51876=CARTESIAN_POINT ( 'NONE',  ( -27.08429572838383947, 0.5764601019426045525, 2.217805374070519253 ) ) ;
#51877=AXIS2_PLACEMENT_3D ( 'NONE', #43015, #62967, #7426 ) ;
#51883=CIRCLE ( 'NONE', #31669, 2.899999999999995026 ) ;
#51885=DIRECTION ( 'NONE',  ( 0.000000000000000000, 0.000000000000000000, 1.000000000000000000 ) ) ;
#51890=CARTESIAN_POINT ( 'NONE',  ( -27.08588607604433562, -0.6046196991082997130, -2.215240480751995644 ) ) ;
#51895=B_SPLINE_CURVE_WITH_KNOTS ( 'NONE', 3,
 ( #48462, #8858, #58430, #27833, #12515, #53103, #39104, #23502, #43433, #49451, #63080, #13818, #7892, #38462, #64373, #33140, #49122, #63388, #53770 ),
 .UNSPECIFIED., .F., .F.,
 ( 4, 3, 3, 3, 3, 3, 4 ),
 ( 1.226634733346813749E-18, 2.836829842860796018E-05, 4.224792512343430404E-05, 5.612066614708130128E-05, 6.998859278151969301E-05, 9.832141287888942582E-05, 0.0001178161482480163323 ),
 .UNSPECIFIED. ) ;
#51903=DIRECTION ( 'NONE',  ( 0.000000000000000000, 0.000000000000000000, 1.000000000000000000 ) ) ;
#51918=LINE ( 'NONE', #16975, #41381 ) ;
#51920=ORIENTED_EDGE ( 'NONE', *, *, #33904, .T. ) ;
#51928=DIRECTION ( 'NONE',  ( 0.000000000000000000, 0.000000000000000000, 1.000000000000000000 ) ) ;
#51930=CARTESIAN_POINT ( 'NONE',  ( -27.08417568107324058, -0.3682236895270647459, -2.261355310631429916 ) ) ;
#51945=DIRECTION ( 'NONE',  ( -1.000000000000000000, 0.000000000000000000, 0.000000000000000000 ) ) ;
#51956=VECTOR ( 'NONE', #28189, 1000.000000000000000 ) ;
#51979=ADVANCED_FACE ( 'NONE', ( #1481 ), #38003, .T. ) ;
#51987=ORIENTED_EDGE ( 'NONE', *, *, #16980, .F. ) ;
#51995=CARTESIAN_POINT ( 'NONE',  ( -27.32343372485685862, -1.382463360572550259, -2.674948176236203512 ) ) ;
#52004=CARTESIAN_POINT ( 'NONE',  ( 0.000000000000000000, 5.662015959325201742, 4.918493191653995567 ) ) ;
#52012=CARTESIAN_POINT ( 'NONE',  ( -10.00000000000000178, 0.000000000000000000, 0.000000000000000000 ) ) ;
#52017=CARTESIAN_POINT ( 'NONE',  ( -22.27384469013076185, -2.154627400808021509, -2.985904959940910874 ) ) ;
#52023=LINE ( 'NONE', #58002, #46543 ) ;
#52025=EDGE_CURVE ( 'NONE', #52648, #33594, #39444, .T. ) ;
#52030=CARTESIAN_POINT ( 'NONE',  ( 0.000000000000000000, -0.7281529553921430864, -7.464569195442815719 ) ) ;
#52038=LINE ( 'NONE', #37047, #64651 ) ;
#52041=CARTESIAN_POINT ( 'NONE',  ( 2.000000000000001776, 0.000000000000000000, 0.000000000000000000 ) ) ;
#52047=CARTESIAN_POINT ( 'NONE',  ( -27.08429572838383947, 2.217805374070540125, -0.5764601019425888984 ) ) ;
#52052=CARTESIAN_POINT ( 'NONE',  ( 2.000000000000001776, -6.936109781200700652, 2.853135311045000400 ) ) ;
#52053=AXIS2_PLACEMENT_3D ( 'NONE', #49800, #8572, #18891 ) ;
#52054=DIRECTION ( 'NONE',  ( 1.000000000000000000, -0.000000000000000000, -0.000000000000000000 ) ) ;
#52061=CARTESIAN_POINT ( 'NONE',  ( 0.000000000000000000, 5.662015959325264802, -4.918493191653922736 ) ) ;
#52066=CARTESIAN_POINT ( 'NONE',  ( 2.000000000000001776, -3.859771122242995123, -5.613913289150092467 ) ) ;
#52071=ORIENTED_EDGE ( 'NONE', *, *, #47635, .F. ) ;
#52074=CARTESIAN_POINT ( 'NONE',  ( -27.20102706715914209, -2.585824624629331492, -0.5453431011645174520 ) ) ;
#52075=DIRECTION ( 'NONE',  ( 0.000000000000000000, 0.000000000000000000, 1.000000000000000000 ) ) ;
#52082=CARTESIAN_POINT ( 'NONE',  ( 0.000000000000000000, 6.253963800348250501, 4.139799123621038746 ) ) ;
#52093=DIRECTION ( 'NONE',  ( 0.000000000000000000, 0.9289767198167924178, -0.3701381553399118451 ) ) ;
#52098=ORIENTED_EDGE ( 'NONE', *, *, #56558, .T. ) ;
#52103=CARTESIAN_POINT ( 'NONE',  ( -27.08430418657510685, 0.9470735946412849326, -2.086666645150412336 ) ) ;
#52104=DIRECTION ( 'NONE',  ( -1.000000000000000000, 0.000000000000000000, 0.000000000000000000 ) ) ;
#52108=AXIS2_PLACEMENT_3D ( 'NONE', #35127, #25495, #56417 ) ;
#52111=ADVANCED_FACE ( 'NONE', ( #29030 ), #50884, .F. ) ;
#52115=CARTESIAN_POINT ( 'NONE',  ( -35.04709527796842394, 0.001082316405385738700, -0.01231589140599127774 ) ) ;
#52119=CARTESIAN_POINT ( 'NONE',  ( 1.000000000000000888, -6.664893814313742837, 3.439359016433467087 ) ) ;
#52120=EDGE_CURVE ( 'NONE', #57823, #61028, #54343, .T. ) ;
#52130=DIRECTION ( 'NONE',  ( 0.000000000000000000, 0.9635499925192236859, -0.2675283385292183680 ) ) ;
#52135=ORIENTED_EDGE ( 'NONE', *, *, #60361, .T. ) ;
#52146=ORIENTED_EDGE ( 'NONE', *, *, #8194, .F. ) ;
#52150=FACE_OUTER_BOUND ( 'NONE', #7265, .T. ) ;
#52153=FACE_OUTER_BOUND ( 'NONE', #2518, .T. ) ;
#52155=EDGE_CURVE ( 'NONE', #55446, #62557, #58653, .T. ) ;
#52161=DIRECTION ( 'NONE',  ( 0.000000000000000000, -0.9289767198167871998, -0.3701381553399247792 ) ) ;
#52173=B_SPLINE_CURVE_WITH_KNOTS ( 'NONE', 3,
 ( #2064, #7052, #27325, #22328, #42599, #2413, #19002, #23014, #59246, #2758, #63886, #37960, #43596, #27648, #34285, #8365 ),
 .UNSPECIFIED., .F., .F.,
 ( 4, 3, 3, 3, 3, 4 ),
 ( 0.000000000000000000, 6.991367980366665303E-05, 0.0001398269368981414106, 0.0002097400188389170336, 0.0002811534801551458644, 0.0003526297678872614009 ),
 .UNSPECIFIED. ) ;
#52179=CIRCLE ( 'NONE', #33064, 2.899999999999994138 ) ;
#52186=ORIENTED_EDGE ( 'NONE', *, *, #43297, .F. ) ;
#52198=CARTESIAN_POINT ( 'NONE',  ( 2.000000000000001776, 0.000000000000000000, 0.000000000000000000 ) ) ;
#52202=CARTESIAN_POINT ( 'NONE',  ( 0.000000000000000000, 5.997115278587678233, -3.485633455389450130 ) ) ;
#52208=FACE_OUTER_BOUND ( 'NONE', #33746, .T. ) ;
#52214=EDGE_CURVE ( 'NONE', #44685, #65319, #33089, .T. ) ;
#52215=ORIENTED_EDGE ( 'NONE', *, *, #62566, .T. ) ;
#52217=ADVANCED_FACE ( 'NONE', ( #44967 ), #56244, .T. ) ;
#52219=ORIENTED_EDGE ( 'NONE', *, *, #43547, .F. ) ;
#52236=ORIENTED_EDGE ( 'NONE', *, *, #55344, .F. ) ;
#52245=ORIENTED_EDGE ( 'NONE', *, *, #19511, .F. ) ;
#52264=( BOUNDED_SURFACE ( )  B_SPLINE_SURFACE ( 3, 1, ( 
 ( #23991, #23004 ),
 ( #47944, #52924 ),
 ( #2402, #2748 ),
 ( #63536, #13018 ) ),
 .UNSPECIFIED., .F., .F., .F. ) 
 B_SPLINE_SURFACE_WITH_KNOTS ( ( 4, 4 ),
 ( 2, 2 ),
 ( 0.000000000000000000, 1.000000000000000000 ),
 ( 0.000000000000000000, 1.000000000000000000 ),
 .UNSPECIFIED. ) 
 GEOMETRIC_REPRESENTATION_ITEM ( )  RATIONAL_B_SPLINE_SURFACE ( (
 ( 1.000000000000000000, 1.000000000000000000),
 ( 0.9932032654565553509, 0.8386279382598740284),
 ( 0.9932032654565553509, 0.8386279382598740284),
 ( 1.000000000000000000, 1.000000000000000000) ) ) 
 REPRESENTATION_ITEM ( '' )  SURFACE ( )  );
#52270=ORIENTED_EDGE ( 'NONE', *, *, #27939, .T. ) ;
#52284=ORIENTED_EDGE ( 'NONE', *, *, #45390, .T. ) ;
#52287=FACE_OUTER_BOUND ( 'NONE', #36471, .T. ) ;
#52289=ORIENTED_EDGE ( 'NONE', *, *, #35349, .F. ) ;
#52292=CARTESIAN_POINT ( 'NONE',  ( 1.000000000000000888, 7.248432822490259220, 1.926193556693033271 ) ) ;
#52293=EDGE_CURVE ( 'NONE', #19282, #62401, #20383, .T. ) ;
#52296=ORIENTED_EDGE ( 'NONE', *, *, #23188, .T. ) ;
#52299=ORIENTED_EDGE ( 'NONE', *, *, #26904, .T. ) ;
#52300=CARTESIAN_POINT ( 'NONE',  ( -22.31328051695926007, 3.401210163132566411, 1.671726071983929307 ) ) ;
#52306=B_SPLINE_CURVE_WITH_KNOTS ( 'NONE', 3,
 ( #2820, #38355, #23747, #22761, #18437, #43670 ),
 .UNSPECIFIED., .F., .F.,
 ( 4, 2, 4 ),
 ( 0.000000000000000000, 0.0004528561986909402357, 0.0009057123973818806883 ),
 .UNSPECIFIED. ) ;
#52308=EDGE_CURVE ( 'NONE', #32446, #17391, #21473, .T. ) ;
#52309=AXIS2_PLACEMENT_3D ( 'NONE', #38188, #63782, #37554 ) ;
#52310=DIRECTION ( 'NONE',  ( 0.000000000000000000, 0.000000000000000000, 1.000000000000000000 ) ) ;
#52320=ORIENTED_EDGE ( 'NONE', *, *, #37244, .T. ) ;
#52326=CARTESIAN_POINT ( 'NONE',  ( 0.000000000000000000, 0.000000000000000000, 0.000000000000000000 ) ) ;
#52331=ORIENTED_EDGE ( 'NONE', *, *, #47004, .T. ) ;
#52333=AXIS2_PLACEMENT_3D ( 'NONE', #61221, #9343, #55906 ) ;
#52335=ORIENTED_EDGE ( 'NONE', *, *, #60475, .T. ) ;
#52337=DIRECTION ( 'NONE',  ( 1.000000000000000000, 0.000000000000000000, 0.000000000000000000 ) ) ;
#52345=CARTESIAN_POINT ( 'NONE',  ( -22.46509356695198889, -4.154553862421328070, -0.8809186187926377753 ) ) ;
#52355=EDGE_CURVE ( 'NONE', #61028, #10755, #2381, .T. ) ;
#52356=CARTESIAN_POINT ( 'NONE',  ( 2.000000000000001776, -6.338823199656690832, 2.816798305433647620 ) ) ;
#52357=EDGE_LOOP ( 'NONE', ( #42623, #28582, #4519, #9160 ) ) ;
#52360=CARTESIAN_POINT ( 'NONE',  ( -22.27719381268171261, -3.550654232855433357, -0.9730858478813990686 ) ) ;
#52370=DIRECTION ( 'NONE',  ( -0.9606638835031803270, -0.2689826995745344118, 0.06908842350339121363 ) ) ;
#52374=DIRECTION ( 'NONE',  ( 1.000000000000000000, 0.000000000000000000, 0.000000000000000000 ) ) ;
#52379=CARTESIAN_POINT ( 'NONE',  ( -22.29677679919927513, -3.097220482904027072, 2.096973157017371747 ) ) ;
#52385=VECTOR ( 'NONE', #3206, 1000.000000000000000 ) ;
#52399=FACE_OUTER_BOUND ( 'NONE', #44215, .T. ) ;
#52400=ORIENTED_EDGE ( 'NONE', *, *, #10474, .T. ) ;
#52404=CIRCLE ( 'NONE', #59853, 2.899999999999994582 ) ;
#52408=CYLINDRICAL_SURFACE ( 'NONE', #18290, 2.899999999999994582 ) ;
#52422=ORIENTED_EDGE ( 'NONE', *, *, #34090, .F. ) ;
#52423=CARTESIAN_POINT ( 'NONE',  ( -22.27722022243424149, 2.391991868237167917, 2.798846704197218482 ) ) ;
#52435=ORIENTED_EDGE ( 'NONE', *, *, #13862, .T. ) ;
#52448=DIRECTION ( 'NONE',  ( 1.000000000000000000, -0.000000000000000000, -0.000000000000000000 ) ) ;
#52450=VECTOR ( 'NONE', #36869, 1000.000000000000000 ) ;
#52451=DIRECTION ( 'NONE',  ( -1.000000000000000000, 0.000000000000000000, 0.000000000000000000 ) ) ;
#52457=CARTESIAN_POINT ( 'NONE',  ( -22.28506771379528573, -2.571716811880550679, 2.697635452840744463 ) ) ;
#52465=EDGE_CURVE ( 'NONE', #31213, #27713, #47280, .T. ) ;
#52473=CARTESIAN_POINT ( 'NONE',  ( -22.70624764888619751, 2.547047087672855259, 4.591418580540040928 ) ) ;
#52487=ORIENTED_EDGE ( 'NONE', *, *, #5118, .T. ) ;
#52500=CARTESIAN_POINT ( 'NONE',  ( -27.08418179957658367, -2.244544746853583295, 0.4604195552868128871 ) ) ;
#52501=CARTESIAN_POINT ( 'NONE',  ( -22.27384469013076185, 3.548341908721034166, 0.9835229356381993693 ) ) ;
#52513=VERTEX_POINT ( 'NONE', #44231 ) ;
#52517=CARTESIAN_POINT ( 'NONE',  ( -27.10307689719148172, 1.703783570823889093, 1.615391801699764374 ) ) ;
#52522=VERTEX_POINT ( 'NONE', #8665 ) ;
#52523=ORIENTED_EDGE ( 'NONE', *, *, #18769, .F. ) ;
#52530=ORIENTED_EDGE ( 'NONE', *, *, #10200, .F. ) ;
#52533=VECTOR ( 'NONE', #61193, 1000.000000000000000 ) ;
#52538=CARTESIAN_POINT ( 'NONE',  ( -22.31328051695926007, -3.401210163132568187, -1.671726071983963946 ) ) ;
#52539=EDGE_LOOP ( 'NONE', ( #63765, #35067, #15932, #7846 ) ) ;
#52542=CARTESIAN_POINT ( 'NONE',  ( -22.27718150314433387, 2.721613812022976031, -2.479231311682823957 ) ) ;
#52553=LINE ( 'NONE', #1991, #40180 ) ;
#52557=LINE ( 'NONE', #27924, #16945 ) ;
#52566=DIRECTION ( 'NONE',  ( -1.000000000000000000, 0.000000000000000000, 0.000000000000000000 ) ) ;
#52582=ADVANCED_FACE ( 'NONE', ( #25931 ), #55527, .T. ) ;
#52585=DIRECTION ( 'NONE',  ( -1.000000000000000000, 0.000000000000000000, 0.000000000000000000 ) ) ;
#52586=EDGE_CURVE ( 'NONE', #36878, #14755, #41640, .T. ) ;
#52589=VERTEX_POINT ( 'NONE', #39896 ) ;
#52593=CARTESIAN_POINT ( 'NONE',  ( 2.000000000000001776, 0.000000000000000000, 0.000000000000000000 ) ) ;
#52612=LINE ( 'NONE', #36641, #3509 ) ;
#52620=AXIS2_PLACEMENT_3D ( 'NONE', #48746, #28773, #3199 ) ;
#52622=EDGE_CURVE ( 'NONE', #35981, #12311, #40212, .T. ) ;
#52625=ORIENTED_EDGE ( 'NONE', *, *, #51033, .F. ) ;
#52627=CARTESIAN_POINT ( 'NONE',  ( 0.000000000000000000, -5.888698556700742159, -3.665823448873470003 ) ) ;
#52631=ORIENTED_EDGE ( 'NONE', *, *, #14107, .T. ) ;
#52632=EDGE_CURVE ( 'NONE', #662, #54975, #214, .T. ) ;
#52641=STYLED_ITEM ( 'NONE', ( #43820 ), #19082 ) ;
#52643=CARTESIAN_POINT ( 'NONE',  ( -22.71097035706202405, -0.4203397252017116448, 4.965150228107737540 ) ) ;
#52648=VERTEX_POINT ( 'NONE', #5315 ) ;
#52649=CARTESIAN_POINT ( 'NONE',  ( -22.27716857039623477, -3.591587580808000002, 0.8090275962000568200 ) ) ;
#52653=ORIENTED_EDGE ( 'NONE', *, *, #14563, .F. ) ;
#52659=VERTEX_POINT ( 'NONE', #15600 ) ;
#52672=DIRECTION ( 'NONE',  ( -1.000000000000000000, 0.000000000000000000, 0.000000000000000000 ) ) ;
#52677=CARTESIAN_POINT ( 'NONE',  ( -27.10719052120871098, 0.6736837626858914740, 2.261993590776020469 ) ) ;
#52691=CARTESIAN_POINT ( 'NONE',  ( -22.30861784526116054, 1.070462554923830245, 3.620936716852743764 ) ) ;
#52693=CARTESIAN_POINT ( 'NONE',  ( 2.000000000000001776, 1.779948802829816490, 6.576141558201244131 ) ) ;
#52695=VECTOR ( 'NONE', #9074, 1000.000000000000000 ) ;
#52701=CARTESIAN_POINT ( 'NONE',  ( -22.31099767395440736, -3.142100240805189237, 2.106713667647948540 ) ) ;
#52703=DIRECTION ( 'NONE',  ( 0.9582930651793754029, 0.2851010602429193685, -0.01979360193296059167 ) ) ;
#52713=CARTESIAN_POINT ( 'NONE',  ( -23.18047892478189453, -2.037851053449323935, -4.338318103648305168 ) ) ;
#52723=ORIENTED_EDGE ( 'NONE', *, *, #39752, .F. ) ;
#52727=CARTESIAN_POINT ( 'NONE',  ( 0.000000000000000000, -7.484036900328561615, -0.4890722589970097345 ) ) ;
#52730=DIRECTION ( 'NONE',  ( -1.000000000000000000, 0.000000000000000000, 0.000000000000000000 ) ) ;
#52731=VERTEX_POINT ( 'NONE', #41863 ) ;
#52737=DIRECTION ( 'NONE',  ( -1.000000000000000000, 0.000000000000000000, 0.000000000000000000 ) ) ;
#52744=CARTESIAN_POINT ( 'NONE',  ( -22.30625920655495165, -3.687109008463848703, -0.8854385781085442053 ) ) ;
#52761=CARTESIAN_POINT ( 'NONE',  ( 2.000000000000001776, 6.470132594555847660, -2.133363481234036296 ) ) ;
#52762=CARTESIAN_POINT ( 'NONE',  ( -27.08871896697694126, 0.9878677378267041176, -2.082324523415897577 ) ) ;
#52763=CARTESIAN_POINT ( 'NONE',  ( 2.000000000000001776, -6.662861565602053560, -1.421313227905724341 ) ) ;
#52767=VERTEX_POINT ( 'NONE', #63128 ) ;
#52775=ORIENTED_EDGE ( 'NONE', *, *, #43573, .F. ) ;
#52777=CARTESIAN_POINT ( 'NONE',  ( 0.000000000000000000, -0.08317740279924559776, -7.499538753794370294 ) ) ;
#52784=ORIENTED_EDGE ( 'NONE', *, *, #35083, .T. ) ;
#52788=CARTESIAN_POINT ( 'NONE',  ( 2.000000000000001776, -6.883677378339447372, -0.8544109087186817497 ) ) ;
#52789=CARTESIAN_POINT ( 'NONE',  ( 0.000000000000000000, 0.000000000000000000, 0.000000000000000000 ) ) ;
#52805=DIRECTION ( 'NONE',  ( 0.000000000000000000, 0.000000000000000000, 1.000000000000000000 ) ) ;
#52811=ORIENTED_EDGE ( 'NONE', *, *, #63625, .F. ) ;
#52831=VERTEX_POINT ( 'NONE', #22909 ) ;
#52832=CARTESIAN_POINT ( 'NONE',  ( 2.000000000000001776, 0.000000000000000000, 0.000000000000000000 ) ) ;
#52834=ORIENTED_EDGE ( 'NONE', *, *, #17485, .T. ) ;
#52837=EDGE_CURVE ( 'NONE', #61990, #23681, #34168, .T. ) ;
#52843=ORIENTED_EDGE ( 'NONE', *, *, #13348, .F. ) ;
#52854=DIRECTION ( 'NONE',  ( -1.000000000000000000, 0.000000000000000000, 0.000000000000000000 ) ) ;
#52863=ORIENTED_EDGE ( 'NONE', *, *, #62003, .F. ) ;
#52869=AXIS2_PLACEMENT_3D ( 'NONE', #35305, #55618, #20027 ) ;
#52879=CARTESIAN_POINT ( 'NONE',  ( -22.65999102136914445, 4.450325798697177149, -1.886119913916055602 ) ) ;
#52882=CARTESIAN_POINT ( 'NONE',  ( -22.28121537037576871, -2.114437713163344501, -3.028566507474733882 ) ) ;
#52884=ORIENTED_EDGE ( 'NONE', *, *, #49128, .T. ) ;
#52885=ORIENTED_EDGE ( 'NONE', *, *, #50993, .T. ) ;
#52890=CARTESIAN_POINT ( 'NONE',  ( 0.000000000000000000, 0.000000000000000000, 0.000000000000000000 ) ) ;
#52892=AXIS2_PLACEMENT_3D ( 'NONE', #13184, #17842, #58087 ) ;
#52901=ORIENTED_EDGE ( 'NONE', *, *, #62091, .F. ) ;
#52902=B_SPLINE_CURVE_WITH_KNOTS ( 'NONE', 3,
 ( #28253, #53197, #7643, #63807, #18288, #49840, #8617, #65120, #14560, #4950, #40503, #39855, #34838, #55144, #34206, #33881, #45174, #19258, #65752 ),
 .UNSPECIFIED., .F., .F.,
 ( 4, 3, 3, 3, 3, 3, 4 ),
 ( 0.000000000000000000, 2.836829843012721202E-05, 4.224792512550943312E-05, 5.612066614913196127E-05, 6.998859278354792356E-05, 9.832141288087241804E-05, 0.0001178161482478536071 ),
 .UNSPECIFIED. ) ;
#52904=VERTEX_POINT ( 'NONE', #2648 ) ;
#52907=CARTESIAN_POINT ( 'NONE',  ( 0.000000000000000000, -7.387287142779349836, 1.295372019972131028 ) ) ;
#52913=CARTESIAN_POINT ( 'NONE',  ( 0.000000000000000000, -6.997684042076877553, -2.698595569414293127 ) ) ;
#52920=EDGE_CURVE ( 'NONE', #50194, #2564, #43163, .T. ) ;
#52924=CARTESIAN_POINT ( 'NONE',  ( -22.27218376572352554, 2.630375585211922385, 2.577901515391789466 ) ) ;
#52927=ADVANCED_FACE ( 'NONE', ( #32846 ), #18894, .T. ) ;
#52929=CIRCLE ( 'NONE', #907, 7.499999999999988454 ) ;
#52934=DIRECTION ( 'NONE',  ( 0.000000000000000000, 0.9985334138511235968, 0.05413890858542115547 ) ) ;
#52938=EDGE_CURVE ( 'NONE', #34267, #39065, #31055, .T. ) ;
#52941=AXIS2_PLACEMENT_3D ( 'NONE', #30405, #497, #29733 ) ;
#52944=ADVANCED_FACE ( 'NONE', ( #60421 ), #54801, .T. ) ;
#52955=CARTESIAN_POINT ( 'NONE',  ( -22.30078715814471835, 3.743307663037642730, -0.2606204736986855175 ) ) ;
#52961=VERTEX_POINT ( 'NONE', #45791 ) ;
#52962=ORIENTED_EDGE ( 'NONE', *, *, #21541, .T. ) ;
#52963=CARTESIAN_POINT ( 'NONE',  ( -22.28236030719477512, -3.345835236227594933, -1.572829798448334815 ) ) ;
#52970=FACE_OUTER_BOUND ( 'NONE', #33774, .T. ) ;
#52975=DIRECTION ( 'NONE',  ( -1.000000000000000000, -1.685093406416449860E-16, 1.011030131491573426E-17 ) ) ;
#52982=VERTEX_POINT ( 'NONE', #55777 ) ;
#52990=CARTESIAN_POINT ( 'NONE',  ( -22.27834755396593991, -2.447855249718982495, -2.756126180273669846 ) ) ;
#53002=AXIS2_PLACEMENT_3D ( 'NONE', #45393, #25785, #36057 ) ;
#53009=ORIENTED_EDGE ( 'NONE', *, *, #32225, .F. ) ;
#53012=ADVANCED_FACE ( 'NONE', ( #35133 ), #39818, .T. ) ;
#53013=CARTESIAN_POINT ( 'NONE',  ( -28.67667724226168602, 1.888227992976679204, -0.1214114860980455846 ) ) ;
#53021=ORIENTED_EDGE ( 'NONE', *, *, #4837, .F. ) ;
#53022=CARTESIAN_POINT ( 'NONE',  ( -27.08416974970326407, 0.4151546250413345462, 2.253221199357843929 ) ) ;
#53023=CARTESIAN_POINT ( 'NONE',  ( 2.000000000000001776, 0.000000000000000000, 0.000000000000000000 ) ) ;
#53024=CARTESIAN_POINT ( 'NONE',  ( -26.43258404273188233, -1.478864324198220226, -3.148308537883193647 ) ) ;
#53026=DIRECTION ( 'NONE',  ( -1.000000000000000000, 0.000000000000000000, 0.000000000000000000 ) ) ;
#53036=CARTESIAN_POINT ( 'NONE',  ( -27.32343372485685151, -1.625341394141119222, 2.534722478175137184 ) ) ;
#53039=ORIENTED_EDGE ( 'NONE', *, *, #14168, .T. ) ;
#53056=ORIENTED_EDGE ( 'NONE', *, *, #5578, .T. ) ;
#53062=AXIS2_PLACEMENT_3D ( 'NONE', #17857, #12859, #53104 ) ;
#53067=CARTESIAN_POINT ( 'NONE',  ( -22.27722015946438816, -0.6262261846986509894, -3.628085906632226632 ) ) ;
#53073=DIRECTION ( 'NONE',  ( 0.000000000000000000, 0.000000000000000000, 1.000000000000000000 ) ) ;
#53080=DIRECTION ( 'NONE',  ( -1.000000000000000000, 0.000000000000000000, 0.000000000000000000 ) ) ;
#53087=CARTESIAN_POINT ( 'NONE',  ( 0.000000000000000000, 1.058508696395052517, -6.730038252034905355 ) ) ;
#53088=ORIENTED_EDGE ( 'NONE', *, *, #27593, .T. ) ;
#53096=ORIENTED_EDGE ( 'NONE', *, *, #46333, .T. ) ;
#53098=EDGE_CURVE ( 'NONE', #45593, #8268, #16526, .T. ) ;
#53103=CARTESIAN_POINT ( 'NONE',  ( -27.09602251845210930, -2.092130925172070999, -1.018053071732930803 ) ) ;
#53104=DIRECTION ( 'NONE',  ( 0.000000000000000000, 0.4198891015602657650, -0.9075754196709565624 ) ) ;
#53111=CIRCLE ( 'NONE', #37148, 7.499999999999988454 ) ;
#53112=VECTOR ( 'NONE', #24140, 1000.000000000000000 ) ;
#53116=CARTESIAN_POINT ( 'NONE',  ( -22.27834755396593991, -3.643689482009667913, 0.5583491773602463626 ) ) ;
#53132=CARTESIAN_POINT ( 'NONE',  ( 2.000000000000001776, 6.796153407501467569, -1.388283512725773772 ) ) ;
#53135=FACE_OUTER_BOUND ( 'NONE', #47241, .T. ) ;
#53147=ADVANCED_FACE ( 'NONE', ( #64354 ), #28451, .T. ) ;
#53153=ORIENTED_EDGE ( 'NONE', *, *, #3331, .T. ) ;
#53160=VERTEX_POINT ( 'NONE', #23474 ) ;
#53162=CARTESIAN_POINT ( 'NONE',  ( -22.27722022243423794, -2.798846704197242463, 2.391991868237150598 ) ) ;
#53174=DIRECTION ( 'NONE',  ( 0.000000000000000000, 0.000000000000000000, 1.000000000000000000 ) ) ;
#53179=CARTESIAN_POINT ( 'NONE',  ( 2.000000000000001776, -6.338823199656649088, -2.816798305433765748 ) ) ;
#53183=EDGE_CURVE ( 'NONE', #4358, #58669, #54476, .T. ) ;
#53185=CYLINDRICAL_SURFACE ( 'NONE', #50342, 2.899999999999994582 ) ;
#53187=CARTESIAN_POINT ( 'NONE',  ( 2.000000000000001776, 0.7281529553923113962, -7.464569195442801508 ) ) ;
#53191=CARTESIAN_POINT ( 'NONE',  ( -22.27218376572352554, -2.630375585211905953, -2.577901515391840537 ) ) ;
#53193=ORIENTED_EDGE ( 'NONE', *, *, #52155, .T. ) ;
#53196=AXIS2_PLACEMENT_3D ( 'NONE', #48596, #53249, #7696 ) ;
#53197=CARTESIAN_POINT ( 'NONE',  ( -27.10422407540546885, 2.109093808474372000, 1.039355862229879524 ) ) ;
#53200=AXIS2_PLACEMENT_3D ( 'NONE', #16674, #23308, #27298 ) ;
#53201=FACE_OUTER_BOUND ( 'NONE', #57262, .T. ) ;
#53207=VECTOR ( 'NONE', #64088, 1000.000000000000000 ) ;
#53215=CIRCLE ( 'NONE', #13887, 2.899999999999994582 ) ;
#53218=CARTESIAN_POINT ( 'NONE',  ( -22.30527770659433173, -2.100259071719460024, -3.125767038151211263 ) ) ;
#53224=AXIS2_PLACEMENT_3D ( 'NONE', #26897, #47198, #1644 ) ;
#53231=CARTESIAN_POINT ( 'NONE',  ( -22.30527770659433173, -0.2559941915621662401, -3.757123197210725962 ) ) ;
#53232=ORIENTED_EDGE ( 'NONE', *, *, #7197, .F. ) ;
#53235=CARTESIAN_POINT ( 'NONE',  ( 2.000000000000001776, -1.058508696395003890, 6.730038252034888480 ) ) ;
#53241=EDGE_CURVE ( 'NONE', #46803, #64819, #38094, .T. ) ;
#53243=ORIENTED_EDGE ( 'NONE', *, *, #16713, .T. ) ;
#53246=DIRECTION ( 'NONE',  ( 0.000000000000000000, -0.4198891015602717602, 0.9075754196709537869 ) ) ;
#53249=DIRECTION ( 'NONE',  ( -1.000000000000000000, 0.000000000000000000, 0.000000000000000000 ) ) ;
#53252=ORIENTED_EDGE ( 'NONE', *, *, #27410, .T. ) ;
#53254=VERTEX_POINT ( 'NONE', #2886 ) ;
#53257=VECTOR ( 'NONE', #17236, 1000.000000000000000 ) ;
#53265=VECTOR ( 'NONE', #52054, 1000.000000000000000 ) ;
#53268=VERTEX_POINT ( 'NONE', #23143 ) ;
#53278=CIRCLE ( 'NONE', #55397, 2.899999999999994582 ) ;
#53286=CARTESIAN_POINT ( 'NONE',  ( -22.29770266787582145, -2.703976473263631775, -2.588315884842665504 ) ) ;
#53288=EDGE_CURVE ( 'NONE', #22284, #46041, #49172, .T. ) ;
#53294=EDGE_CURVE ( 'NONE', #29586, #57905, #34284, .T. ) ;
#53295=CARTESIAN_POINT ( 'NONE',  ( -22.31328051695926007, 3.781397440874590732, -0.2528478350593763024 ) ) ;
#53300=ADVANCED_FACE ( 'NONE', ( #2215 ), #22489, .T. ) ;
#53301=ORIENTED_EDGE ( 'NONE', *, *, #37458, .T. ) ;
#53315=CYLINDRICAL_SURFACE ( 'NONE', #362, 2.899999999999994582 ) ;
#53321=CARTESIAN_POINT ( 'NONE',  ( -10.00000000000000178, 0.000000000000000000, 0.000000000000000000 ) ) ;
#53328=CIRCLE ( 'NONE', #44804, 2.899999999999995026 ) ;
#53330=FACE_OUTER_BOUND ( 'NONE', #51377, .T. ) ;
#53334=CARTESIAN_POINT ( 'NONE',  ( -22.28169757117798966, -3.576542310004382941, -0.9284931499057510473 ) ) ;
#53338=DIRECTION ( 'NONE',  ( -1.000000000000000000, 0.000000000000000000, 0.000000000000000000 ) ) ;
#53339=ORIENTED_EDGE ( 'NONE', *, *, #17276, .F. ) ;
#53342=ORIENTED_EDGE ( 'NONE', *, *, #21143, .F. ) ;
#53346=CARTESIAN_POINT ( 'NONE',  ( -22.28415773361649954, 0.9981933716385181787, 3.565377603762363012 ) ) ;
#53350=CIRCLE ( 'NONE', #3484, 2.899999999999996358 ) ;
#53352=DIRECTION ( 'NONE',  ( -1.000000000000000000, 0.000000000000000000, 0.000000000000000000 ) ) ;
#53353=CARTESIAN_POINT ( 'NONE',  ( -35.04683013664716640, -0.01216443238270097441, -0.002177781393209239635 ) ) ;
#53356=ADVANCED_FACE ( 'NONE', ( #5410 ), #30467, .F. ) ;
#53357=DIRECTION ( 'NONE',  ( 0.000000000000000000, 0.000000000000000000, 1.000000000000000000 ) ) ;
#53369=AXIS2_PLACEMENT_3D ( 'NONE', #24486, #3905, #24162 ) ;
#53373=AXIS2_PLACEMENT_3D ( 'NONE', #49564, #34244, #39227 ) ;
#53374=ORIENTED_EDGE ( 'NONE', *, *, #38275, .F. ) ;
#53382=EDGE_CURVE ( 'NONE', #37253, #33968, #21004, .T. ) ;
#53396=CARTESIAN_POINT ( 'NONE',  ( -22.27706485742869091, 2.580541389029920030, 2.625261754997667119 ) ) ;
#53404=SHAPE_DEFINITION_REPRESENTATION ( #23801, #13953 ) ;
#53418=DIRECTION ( 'NONE',  ( 0.000000000000000000, 0.000000000000000000, 1.000000000000000000 ) ) ;
#53428=CYLINDRICAL_SURFACE ( 'NONE', #22534, 2.899999999999994582 ) ;
#53429=CARTESIAN_POINT ( 'NONE',  ( -22.28629837673888048, 3.055064048018809153, -2.102970853432551301 ) ) ;
#53431=DIRECTION ( 'NONE',  ( -1.000000000000000000, 0.000000000000000000, 0.000000000000000000 ) ) ;
#53440=LINE ( 'NONE', #8199, #7502 ) ;
#53441=EDGE_CURVE ( 'NONE', #9429, #3201, #44919, .T. ) ;
#53443=CARTESIAN_POINT ( 'NONE',  ( -27.09729107899852707, 0.1622107421537268002, 2.324833743198334357 ) ) ;
#53452=CARTESIAN_POINT ( 'NONE',  ( -22.27719381268171261, -2.618044180756125439, 2.588413841766863843 ) ) ;
#53454=DIRECTION ( 'NONE',  ( -1.000000000000000000, 0.000000000000000000, 0.000000000000000000 ) ) ;
#53469=EDGE_CURVE ( 'NONE', #57350, #1853, #12658, .T. ) ;
#53470=AXIS2_PLACEMENT_3D ( 'NONE', #61855, #11964, #16316 ) ;
#53486=FACE_OUTER_BOUND ( 'NONE', #21311, .T. ) ;
#53489=DIRECTION ( 'NONE',  ( -1.000000000000000000, 0.000000000000000000, 0.000000000000000000 ) ) ;
#53493=LINE ( 'NONE', #12904, #27951 ) ;
#53498=CARTESIAN_POINT ( 'NONE',  ( -35.04660725145885891, 0.009947898977325340605, -0.007231372203147071014 ) ) ;
#53500=DIRECTION ( 'NONE',  ( -1.000000000000000000, 0.000000000000000000, 0.000000000000000000 ) ) ;
#53503=EDGE_CURVE ( 'NONE', #15336, #49701, #31961, .T. ) ;
#53505=ORIENTED_EDGE ( 'NONE', *, *, #2861, .F. ) ;
#53509=ORIENTED_EDGE ( 'NONE', *, *, #56022, .F. ) ;
#53512=CARTESIAN_POINT ( 'NONE',  ( -27.09229696323388126, -1.607344345646396278, 1.666734935102338833 ) ) ;
#53513=CIRCLE ( 'NONE', #34358, 6.936499999999989896 ) ;
#53525=CARTESIAN_POINT ( 'NONE',  ( -35.04834644901396956, -0.01211993185718040697, -0.006670072992065173914 ) ) ;
#53535=ORIENTED_EDGE ( 'NONE', *, *, #27381, .T. ) ;
#53542=ORIENTED_EDGE ( 'NONE', *, *, #12043, .T. ) ;
#53543=CARTESIAN_POINT ( 'NONE',  ( 0.000000000000000000, 6.767909380267608022, -0.7805499053121014441 ) ) ;
#53545=EDGE_CURVE ( 'NONE', #46888, #7394, #37464, .T. ) ;
#53548=CIRCLE ( 'NONE', #3671, 6.936499999999989896 ) ;
#53549=CYLINDRICAL_SURFACE ( 'NONE', #32910, 7.499999999999988454 ) ;
#53550=VERTEX_POINT ( 'NONE', #1733 ) ;
#53553=EDGE_CURVE ( 'NONE', #60601, #32845, #52612, .T. ) ;
#53563=CARTESIAN_POINT ( 'NONE',  ( -22.28506771379528573, -2.081613609299067580, -3.091577134491938050 ) ) ;
#53565=B_SPLINE_CURVE_WITH_KNOTS ( 'NONE', 3,
 ( #41996, #2097, #47343, #57649, #11729, #21054, #12066, #22368, #56668, #1121, #36362, #15731, #36011, #21402, #36689, #56309 ),
 .UNSPECIFIED., .F., .F.,
 ( 4, 3, 3, 3, 3, 4 ),
 ( 0.000000000000000000, 6.991367980366407805E-05, 0.0001398269368981363962, 0.0002097400188389097965, 0.0002811534801551364318, 0.0003526297678872492578 ),
 .UNSPECIFIED. ) ;
#53573=FACE_OUTER_BOUND ( 'NONE', #55299, .T. ) ;
#53575=ORIENTED_EDGE ( 'NONE', *, *, #1058, .F. ) ;
#53576=CARTESIAN_POINT ( 'NONE',  ( -24.42101984568203932, 2.451666775035126644, -3.522366633939671310 ) ) ;
#53589=CARTESIAN_POINT ( 'NONE',  ( -22.27384469013076185, 0.9224151068931638608, 3.564715702084478632 ) ) ;
#53603=AXIS2_PLACEMENT_3D ( 'NONE', #9502, #34467, #40775 ) ;
#53607=ORIENTED_EDGE ( 'NONE', *, *, #12940, .F. ) ;
#53617=ORIENTED_EDGE ( 'NONE', *, *, #15079, .F. ) ;
#53619=CIRCLE ( 'NONE', #13258, 2.899999999999994582 ) ;
#53624=CARTESIAN_POINT ( 'NONE',  ( -27.08417568107324058, -0.8117865859100323878, 2.142502990753197611 ) ) ;
#53626=ADVANCED_FACE ( 'NONE', ( #21342 ), #55134, .F. ) ;
#53628=CARTESIAN_POINT ( 'NONE',  ( -22.27706485742869091, -2.580541389029911148, -2.625261754997698205 ) ) ;
#53629=AXIS2_PLACEMENT_3D ( 'NONE', #51646, #46973, #1750 ) ;
#53634=CARTESIAN_POINT ( 'NONE',  ( -22.29479313954897890, 3.724550806388644109, -0.2707859422896706780 ) ) ;
#53635=DIRECTION ( 'NONE',  ( -1.000000000000000000, 0.000000000000000000, 0.000000000000000000 ) ) ;
#53641=ORIENTED_EDGE ( 'NONE', *, *, #14804, .T. ) ;
#53650=ORIENTED_EDGE ( 'NONE', *, *, #64184, .F. ) ;
#53670=CARTESIAN_POINT ( 'NONE',  ( -22.29570301036918423, -3.629130197778195122, -0.8918611685731365757 ) ) ;
#53678=CARTESIAN_POINT ( 'NONE',  ( -22.27710395300133683, 0.9291085174899564869, 3.562137928983401203 ) ) ;
#53682=EDGE_CURVE ( 'NONE', #52961, #37153, #62994, .T. ) ;
#53685=ORIENTED_EDGE ( 'NONE', *, *, #29967, .F. ) ;
#53701=VECTOR ( 'NONE', #50865, 1000.000000000000000 ) ;
#53712=FACE_OUTER_BOUND ( 'NONE', #25081, .T. ) ;
#53715=CARTESIAN_POINT ( 'NONE',  ( 0.000000000000000000, -1.693411908627245221, 7.306323022404576761 ) ) ;
#53719=DIRECTION ( 'NONE',  ( 0.9606638835031803270, -0.2535400141108140604, -0.1133241553124317708 ) ) ;
#53724=DIRECTION ( 'NONE',  ( -1.000000000000000000, 0.000000000000000000, 0.000000000000000000 ) ) ;
#53726=CARTESIAN_POINT ( 'NONE',  ( -22.27718112499583469, 2.265557025479522757, 2.901898111564422678 ) ) ;
#53729=ORIENTED_EDGE ( 'NONE', *, *, #55116, .T. ) ;
#53743=DIRECTION ( 'NONE',  ( -1.000000000000000000, 0.000000000000000000, 0.000000000000000000 ) ) ;
#53745=DIRECTION ( 'NONE',  ( -1.000000000000000000, 0.000000000000000000, 0.000000000000000000 ) ) ;
#53750=CIRCLE ( 'NONE', #36740, 2.899999999999995026 ) ;
#53753=CARTESIAN_POINT ( 'NONE',  ( -27.10422407540562162, -1.954655484501055085, 1.306850885988407596 ) ) ;
#53759=ORIENTED_EDGE ( 'NONE', *, *, #13436, .F. ) ;
#53760=EDGE_CURVE ( 'NONE', #8369, #49125, #14147, .T. ) ;
#53770=CARTESIAN_POINT ( 'NONE',  ( -27.08429572838383947, -2.089332284968714593, -0.9410937941434025511 ) ) ;
#53775=CARTESIAN_POINT ( 'NONE',  ( -22.27710395300133328, -2.620347679538745034, 2.585700543510492277 ) ) ;
#53779=CIRCLE ( 'NONE', #45267, 2.899999999999994582 ) ;
#53785=CARTESIAN_POINT ( 'NONE',  ( -35.04582288351658548, 0.01196488372921770960, -0.004274985098085598047 ) ) ;
#53801=DIRECTION ( 'NONE',  ( 0.000000000000000000, 0.000000000000000000, 1.000000000000000000 ) ) ;
#53804=DIRECTION ( 'NONE',  ( 0.000000000000000000, 0.000000000000000000, 1.000000000000000000 ) ) ;
#53810=CARTESIAN_POINT ( 'NONE',  ( -22.29770266787582500, 2.588315884842656178, -2.703976473263633995 ) ) ;
#53811=CARTESIAN_POINT ( 'NONE',  ( -27.15511094194037511, -0.1446243978645335992, -2.499833641087599201 ) ) ;
#53817=CARTESIAN_POINT ( 'NONE',  ( 18.00005080000000035, 0.000000000000000000, 1.499999999999997780 ) ) ;
#53821=EDGE_LOOP ( 'NONE', ( #9132, #53542, #45691, #45806 ) ) ;
#53826=VERTEX_POINT ( 'NONE', #49899 ) ;
#53829=CARTESIAN_POINT ( 'NONE',  ( -27.08430418657511041, -2.280643121250624628, 0.2231435303617014532 ) ) ;
#53831=LINE ( 'NONE', #8266, #36974 ) ;
#53833=AXIS2_PLACEMENT_3D ( 'NONE', #17327, #32915, #32583 ) ;
#53835=EDGE_LOOP ( 'NONE', ( #58309, #32497 ) ) ;
#53842=CARTESIAN_POINT ( 'NONE',  ( -27.09125059358711951, 1.607567221344183173, -1.662156772100930935 ) ) ;
#53844=CARTESIAN_POINT ( 'NONE',  ( 2.000000000000001776, 0.7281529553922108100, 7.464569195442779304 ) ) ;
#53856=CARTESIAN_POINT ( 'NONE',  ( -22.27384469013076185, 3.564715702084495952, -0.9224151068931343289 ) ) ;
#53861=CARTESIAN_POINT ( 'NONE',  ( 0.000000000000000000, -6.338823199656690832, 2.816798305433647620 ) ) ;
#53863=VERTEX_POINT ( 'NONE', #62471 ) ;
#53876=CARTESIAN_POINT ( 'NONE',  ( -27.10113028276028757, -1.697941299265485426, -1.613062633975405280 ) ) ;
#53881=VERTEX_POINT ( 'NONE', #52202 ) ;
#53888=CARTESIAN_POINT ( 'NONE',  ( -22.28121537037576871, -0.3168735205819631640, -3.680034389105507842 ) ) ;
#53889=EDGE_CURVE ( 'NONE', #26353, #5798, #40741, .T. ) ;
#53892=CARTESIAN_POINT ( 'NONE',  ( 0.000000000000000000, -3.230174184210094168, 5.998318953995296354 ) ) ;
#53893=DIRECTION ( 'NONE',  ( 1.000000000000000000, -0.000000000000000000, -0.000000000000000000 ) ) ;
#53894=ORIENTED_EDGE ( 'NONE', *, *, #34854, .T. ) ;
#53910=EDGE_LOOP ( 'NONE', ( #60979, #60579, #34644, #53193 ) ) ;
#53913=EDGE_CURVE ( 'NONE', #12705, #39365, #63141, .T. ) ;
#53915=DIRECTION ( 'NONE',  ( 0.000000000000000000, 0.000000000000000000, 1.000000000000000000 ) ) ;
#53921=ORIENTED_EDGE ( 'NONE', *, *, #49517, .F. ) ;
#53933=EDGE_CURVE ( 'NONE', #16541, #24026, #21631, .T. ) ;
#53939=CARTESIAN_POINT ( 'NONE',  ( 2.000000000000001776, 2.480520636974283821, -6.345145617221223944 ) ) ;
#53941=CARTESIAN_POINT ( 'NONE',  ( -22.30398854582847790, -2.724439933030904815, -2.594196582747015256 ) ) ;
#53950=ORIENTED_EDGE ( 'NONE', *, *, #3815, .F. ) ;
#53951=AXIS2_PLACEMENT_3D ( 'NONE', #14060, #53338, #9081 ) ;
#53957=CARTESIAN_POINT ( 'NONE',  ( -22.59983133926800036, -0.06110861519530256386, 4.650609684383217868 ) ) ;
#53968=LINE ( 'NONE', #28684, #5439 ) ;
#53971=ORIENTED_EDGE ( 'NONE', *, *, #40149, .T. ) ;
#53981=CARTESIAN_POINT ( 'NONE',  ( -27.28563798457901513, -2.528380693767725340, 1.413023339712126569 ) ) ;
#53983=AXIS2_PLACEMENT_3D ( 'NONE', #55780, #41115, #58078 ) ;
#53986=EDGE_CURVE ( 'NONE', #22284, #6123, #6008, .T. ) ;
#53987=ORIENTED_EDGE ( 'NONE', *, *, #46259, .F. ) ;
#53988=DIRECTION ( 'NONE',  ( 0.000000000000000000, 0.000000000000000000, 1.000000000000000000 ) ) ;
#53994=AXIS2_PLACEMENT_3D ( 'NONE', #46147, #47130, #26181 ) ;
#54002=CARTESIAN_POINT ( 'NONE',  ( -27.08417473062937120, -1.503027223283682101, -1.729223128152646671 ) ) ;
#54006=EDGE_CURVE ( 'NONE', #2871, #57207, #56659, .T. ) ;
#54011=ORIENTED_EDGE ( 'NONE', *, *, #59895, .T. ) ;
#54018=CARTESIAN_POINT ( 'NONE',  ( 0.000000000000000000, 0.000000000000000000, 0.000000000000000000 ) ) ;
#54024=EDGE_LOOP ( 'NONE', ( #21499, #29211, #10620, #37748 ) ) ;
#54028=ORIENTED_EDGE ( 'NONE', *, *, #18704, .F. ) ;
#54033=DIRECTION ( 'NONE',  ( 0.000000000000000000, -0.5155538571770110767, -0.8568571761675956022 ) ) ;
#54039=CARTESIAN_POINT ( 'NONE',  ( 0.000000000000000000, 2.664846396702499121, 6.404188155572998475 ) ) ;
#54041=ORIENTED_EDGE ( 'NONE', *, *, #5047, .F. ) ;
#54047=CARTESIAN_POINT ( 'NONE',  ( -22.71097035706202405, 0.4203397252017515573, -4.965150228107761521 ) ) ;
#54049=VECTOR ( 'NONE', #15466, 1000.000000000000000 ) ;
#54063=B_SPLINE_CURVE_WITH_KNOTS ( 'NONE', 3,
 ( #56712, #52691, #7119, #31415, #22406, #62314, #57342, #42672, #16460, #36727, #57026, #11447, #53346, #48683, #49363, #13099, #2485, #58331, #33700, #53678, #29055, #18756 ),
 .UNSPECIFIED., .F., .F.,
 ( 4, 3, 3, 3, 3, 3, 3, 4 ),
 ( 0.000000000000000000, 4.455945684386588987E-05, 6.636307477203692504E-05, 8.816671873158415896E-05, 0.0001099660380492575759, 0.0001317545563165277965, 0.0001762613022895024694, 0.0001867992666138357434 ),
 .UNSPECIFIED. ) ;
#54067=FACE_OUTER_BOUND ( 'NONE', #4403, .T. ) ;
#54085=FACE_OUTER_BOUND ( 'NONE', #46343, .T. ) ;
#54090=CARTESIAN_POINT ( 'NONE',  ( -22.27878402819508352, -2.600576127690917172, 2.612733676624896972 ) ) ;
#54091=FACE_OUTER_BOUND ( 'NONE', #28668, .T. ) ;
#54092=VECTOR ( 'NONE', #56505, 1000.000000000000000 ) ;
#54097=FACE_OUTER_BOUND ( 'NONE', #19744, .T. ) ;
#54101=FACE_OUTER_BOUND ( 'NONE', #12503, .T. ) ;
#54109=VERTEX_POINT ( 'NONE', #49183 ) ;
#54112=DIRECTION ( 'NONE',  ( -1.000000000000000000, 0.000000000000000000, 0.000000000000000000 ) ) ;
#54116=EDGE_CURVE ( 'NONE', #32831, #32332, #64751, .T. ) ;
#54119=ORIENTED_EDGE ( 'NONE', *, *, #61119, .F. ) ;
#54122=CARTESIAN_POINT ( 'NONE',  ( 2.000000000000001776, -6.935703035393428806, -0.1051458740708305362 ) ) ;
#54125=SURFACE_STYLE_FILL_AREA ( #64410 ) ;
#54128=CARTESIAN_POINT ( 'NONE',  ( -27.20164183316781248, -0.1019800881472461007, -2.642567708136698279 ) ) ;
#54130=CARTESIAN_POINT ( 'NONE',  ( -22.28776923226071460, -1.601293944844114359, 3.350304995653723417 ) ) ;
#54142=AXIS2_PLACEMENT_3D ( 'NONE', #48912, #63843, #33606 ) ;
#54146=CARTESIAN_POINT ( 'NONE',  ( -27.09861164373156228, -2.328930759213684976, 0.1603819633258212751 ) ) ;
#54150=DIRECTION ( 'NONE',  ( 0.000000000000000000, 0.8276889981568920085, -0.5611870653623801664 ) ) ;
#54160=DIRECTION ( 'NONE',  ( -1.000000000000000000, 0.000000000000000000, 0.000000000000000000 ) ) ;
#54163=VECTOR ( 'NONE', #47963, 1000.000000000000227 ) ;
#54164=VECTOR ( 'NONE', #17279, 1000.000000000000000 ) ;
#54173=ORIENTED_EDGE ( 'NONE', *, *, #206, .F. ) ;
#54176=CARTESIAN_POINT ( 'NONE',  ( 0.000000000000000000, 1.058508696394974358, 6.730038252034905355 ) ) ;
#54188=EDGE_CURVE ( 'NONE', #14567, #40113, #55117, .T. ) ;
#54191=DIRECTION ( 'NONE',  ( -1.000000000000000000, 0.000000000000000000, 0.000000000000000000 ) ) ;
#54201=CARTESIAN_POINT ( 'NONE',  ( -22.29115169517546136, -2.098196790595522998, -3.075985640626811790 ) ) ;
#54208=DIRECTION ( 'NONE',  ( -1.000000000000000000, -1.685093406416449860E-16, 1.011030131491573426E-17 ) ) ;
#54216=CARTESIAN_POINT ( 'NONE',  ( -26.43258404273187523, 1.987083010659177251, -2.854888342447755800 ) ) ;
#54218=EDGE_CURVE ( 'NONE', #37684, #22078, #56094, .T. ) ;
#54220=ORIENTED_EDGE ( 'NONE', *, *, #53241, .T. ) ;
#54226=ORIENTED_EDGE ( 'NONE', *, *, #5069, .F. ) ;
#54230=CARTESIAN_POINT ( 'NONE',  ( 2.000000000000001776, 0.000000000000000000, 0.000000000000000000 ) ) ;
#54234=CARTESIAN_POINT ( 'NONE',  ( -22.38932658256919694, -0.2254938976656423455, -4.011828264158265434 ) ) ;
#54235=ORIENTED_EDGE ( 'NONE', *, *, #3879, .F. ) ;
#54244=EDGE_CURVE ( 'NONE', #44838, #4743, #21082, .T. ) ;
#54252=VERTEX_POINT ( 'NONE', #45460 ) ;
#54254=CIRCLE ( 'NONE', #44628, 6.936499999999990784 ) ;
#54274=CARTESIAN_POINT ( 'NONE',  ( 0.000000000000000000, 0.000000000000000000, 0.000000000000000000 ) ) ;
#54283=ORIENTED_EDGE ( 'NONE', *, *, #29457, .T. ) ;
#54284=DIRECTION ( 'NONE',  ( -1.000000000000000000, 0.000000000000000000, 0.000000000000000000 ) ) ;
#54285=CARTESIAN_POINT ( 'NONE',  ( -22.27719412087655471, -3.642699606241631471, 0.5341638063191882502 ) ) ;
#54286=CARTESIAN_POINT ( 'NONE',  ( 2.000000000000001776, -0.8935325819929111901, 7.446583077151331942 ) ) ;
#54288=B_SPLINE_CURVE_WITH_KNOTS ( 'NONE', 3,
 ( #16124, #16774, #36408, #6484, #11149, #58018, #61667, #51720, #17110, #6165, #26760, #57352, #42683, #32699, #32060, #52379, #6823, #57693, #12114, #52701, #7125, #27403 ),
 .UNSPECIFIED., .F., .F.,
 ( 4, 3, 3, 3, 3, 3, 3, 4 ),
 ( 0.000000000000000000, 4.447697177976088099E-05, 6.624143997790994502E-05, 8.800576886943949225E-05, 0.0001097699864780839652, 0.0001315341395364316897, 0.0001760120188223209209, 0.0001867971373174606459 ),
 .UNSPECIFIED. ) ;
#54297=ORIENTED_EDGE ( 'NONE', *, *, #48799, .T. ) ;
#54298=CARTESIAN_POINT ( 'NONE',  ( -22.27718112499583469, -2.265557025479512099, -2.901898111564459093 ) ) ;
#54302=DIRECTION ( 'NONE',  ( -1.000000000000000000, 0.000000000000000000, 0.000000000000000000 ) ) ;
#54310=CIRCLE ( 'NONE', #4372, 6.936499999999990784 ) ;
#54314=DIRECTION ( 'NONE',  ( 0.000000000000000000, 0.000000000000000000, -1.000000000000000000 ) ) ;
#54329=EDGE_CURVE ( 'NONE', #55598, #3201, #16538, .T. ) ;
#54333=CYLINDRICAL_SURFACE ( 'NONE', #19594, 7.499999999999988454 ) ;
#54334=CARTESIAN_POINT ( 'NONE',  ( -22.30986928587821794, 2.105440358094968545, 3.138878161034310388 ) ) ;
#54339=CARTESIAN_POINT ( 'NONE',  ( 1.000000000000000888, -3.937687286050771895, -6.383151168292510391 ) ) ;
#54343=CIRCLE ( 'NONE', #14995, 7.499999999999988454 ) ;
#54346=ORIENTED_EDGE ( 'NONE', *, *, #27468, .T. ) ;
#54350=CYLINDRICAL_SURFACE ( 'NONE', #24652, 6.936499999999988120 ) ;
#54355=DIRECTION ( 'NONE',  ( -1.000000000000000000, 0.000000000000000000, 0.000000000000000000 ) ) ;
#54356=DIRECTION ( 'NONE',  ( 0.000000000000000000, -0.9635499925192201331, -0.2675283385292311356 ) ) ;
#54358=VECTOR ( 'NONE', #20120, 1000.000000000000000 ) ;
#54362=ORIENTED_EDGE ( 'NONE', *, *, #962, .T. ) ;
#54376=VERTEX_POINT ( 'NONE', #61741 ) ;
#54380=( BOUNDED_SURFACE ( )  B_SPLINE_SURFACE ( 3, 1, ( 
 ( #56757, #20825 ),
 ( #26150, #6198 ),
 ( #15496, #31455 ),
 ( #46423, #868 ) ),
 .UNSPECIFIED., .F., .F., .F. ) 
 B_SPLINE_SURFACE_WITH_KNOTS ( ( 4, 4 ),
 ( 2, 2 ),
 ( 0.000000000000000000, 1.000000000000000000 ),
 ( 0.000000000000000000, 1.000000000000000000 ),
 .UNSPECIFIED. ) 
 GEOMETRIC_REPRESENTATION_ITEM ( )  RATIONAL_B_SPLINE_SURFACE ( (
 ( 1.000000000000000000, 1.000000000000000000),
 ( 0.8716676215708681896, 0.8964445200148167814),
 ( 0.8716676215708681896, 0.8964445200148167814),
 ( 1.000000000000000000, 1.000000000000000000) ) ) 
 REPRESENTATION_ITEM ( '' )  SURFACE ( )  );
#54383=FACE_OUTER_BOUND ( 'NONE', #13704, .T. ) ;
#54389=AXIS2_PLACEMENT_3D ( 'NONE', #1084, #55641, #35972 ) ;
#54391=ORIENTED_EDGE ( 'NONE', *, *, #9524, .F. ) ;
#54395=DIRECTION ( 'NONE',  ( 0.000000000000000000, 0.000000000000000000, 1.000000000000000000 ) ) ;
#54399=ORIENTED_EDGE ( 'NONE', *, *, #16611, .F. ) ;
#54402=ORIENTED_EDGE ( 'NONE', *, *, #10077, .F. ) ;
#54406=ORIENTED_EDGE ( 'NONE', *, *, #64229, .F. ) ;
#54410=DIRECTION ( 'NONE',  ( 0.000000000000000000, 0.000000000000000000, 1.000000000000000000 ) ) ;
#54411=CARTESIAN_POINT ( 'NONE',  ( -22.30527770659433173, 3.125767038151207267, -2.100259071719456028 ) ) ;
#54412=EDGE_CURVE ( 'NONE', #21947, #18329, #11853, .T. ) ;
#54419=CARTESIAN_POINT ( 'NONE',  ( -27.20164183316779827, 1.409601201084051514, 2.237540722393148940 ) ) ;
#54440=ORIENTED_EDGE ( 'NONE', *, *, #35495, .F. ) ;
#54445=LINE ( 'NONE', #37827, #36591 ) ;
#54446=CARTESIAN_POINT ( 'NONE',  ( -22.35190811654613086, 3.898012445334707365, -0.2457675311904780890 ) ) ;
#54449=CIRCLE ( 'NONE', #17422, 7.499999999999988454 ) ;
#54456=ORIENTED_EDGE ( 'NONE', *, *, #10306, .T. ) ;
#54460=CARTESIAN_POINT ( 'NONE',  ( -27.10719052120871098, 0.5475695427849553987, -2.295785794152566339 ) ) ;
#54463=CARTESIAN_POINT ( 'NONE',  ( -26.74023318801843985, 2.752802096869884529, 1.916028097164389932 ) ) ;
#54471=ORIENTED_EDGE ( 'NONE', *, *, #5650, .T. ) ;
#54476=CIRCLE ( 'NONE', #60823, 6.936499999999992561 ) ;
#54477=ORIENTED_EDGE ( 'NONE', *, *, #39224, .T. ) ;
#54486=LINE ( 'NONE', #24530, #61715 ) ;
#54489=ORIENTED_EDGE ( 'NONE', *, *, #26381, .T. ) ;
#54501=ORIENTED_EDGE ( 'NONE', *, *, #62641, .F. ) ;
#54504=ORIENTED_EDGE ( 'NONE', *, *, #41608, .F. ) ;
#54510=DIRECTION ( 'NONE',  ( -1.000000000000000000, 0.000000000000000000, 0.000000000000000000 ) ) ;
#54512=CARTESIAN_POINT ( 'NONE',  ( 2.000000000000001776, 0.000000000000000000, 0.000000000000000000 ) ) ;
#54516=DIRECTION ( 'NONE',  ( -1.000000000000000000, 0.000000000000000000, 0.000000000000000000 ) ) ;
#54519=CIRCLE ( 'NONE', #25838, 2.899999999999996358 ) ;
#54521=DIRECTION ( 'NONE',  ( -1.000000000000000000, 0.000000000000000000, 0.000000000000000000 ) ) ;
#54522=CIRCLE ( 'NONE', #10986, 2.899999999999996358 ) ;
#54525=AXIS2_PLACEMENT_3D ( 'NONE', #30577, #4698, #9989 ) ;
#54533=ORIENTED_EDGE ( 'NONE', *, *, #51046, .F. ) ;
#54534=EDGE_LOOP ( 'NONE', ( #21312, #30373, #8727, #18313 ) ) ;
#54535=CARTESIAN_POINT ( 'NONE',  ( 0.000000000000000000, -5.888698556700776798, 3.665823448873372747 ) ) ;
#54536=EDGE_CURVE ( 'NONE', #55528, #47834, #62014, .T. ) ;
#54541=LINE ( 'NONE', #44523, #27483 ) ;
#54549=AXIS2_PLACEMENT_3D ( 'NONE', #50272, #4731, #55580 ) ;
#54557=DIRECTION ( 'NONE',  ( 0.000000000000000000, -0.3193015301359669600, -0.9476531711828067861 ) ) ;
#54558=CARTESIAN_POINT ( 'NONE',  ( 2.000000000000001776, 0.000000000000000000, 0.000000000000000000 ) ) ;
#54592=CARTESIAN_POINT ( 'NONE',  ( -22.28506771379528573, 1.636577531579587630, -3.348518833762368807 ) ) ;
#54595=EDGE_CURVE ( 'NONE', #59201, #25850, #34374, .T. ) ;
#54603=B_SPLINE_CURVE_WITH_KNOTS ( 'NONE', 3,
 ( #21558, #62114, #60803, #15240, #15561, #35822 ),
 .UNSPECIFIED., .F., .F.,
 ( 4, 2, 4 ),
 ( 0.000000000000000000, 0.0004528561986909333511, 0.0009057123973818667021 ),
 .UNSPECIFIED. ) ;
#54606=AXIS2_PLACEMENT_3D ( 'NONE', #47641, #17720, #63910 ) ;
#54621=CARTESIAN_POINT ( 'NONE',  ( -27.08704841010922948, -1.313007237774859615, -1.888108843319753261 ) ) ;
#54625=DIRECTION ( 'NONE',  ( -1.000000000000000000, 0.000000000000000000, 0.000000000000000000 ) ) ;
#54630=ORIENTED_EDGE ( 'NONE', *, *, #12218, .F. ) ;
#54641=CARTESIAN_POINT ( 'NONE',  ( -16.00005080000000035, 3.673940397442054445E-16, 2.999999999999995559 ) ) ;
#54645=VERTEX_POINT ( 'NONE', #9159 ) ;
#54650=ORIENTED_EDGE ( 'NONE', *, *, #63498, .F. ) ;
#54654=CYLINDRICAL_SURFACE ( 'NONE', #17372, 7.499999999999988454 ) ;
#54660=EDGE_LOOP ( 'NONE', ( #5571, #57305, #5052, #55280 ) ) ;
#54663=EDGE_LOOP ( 'NONE', ( #56794, #42527, #19145, #56756 ) ) ;
#54665=EDGE_CURVE ( 'NONE', #27434, #22936, #14247, .T. ) ;
#54666=CARTESIAN_POINT ( 'NONE',  ( -10.00000000000000178, 0.000000000000000000, 0.000000000000000000 ) ) ;
#54669=CARTESIAN_POINT ( 'NONE',  ( -22.28121537037576871, 2.114437713163361821, 3.028566507474710345 ) ) ;
#54670=CARTESIAN_POINT ( 'NONE',  ( -22.28121537037577227, 1.565596675942166671, -3.345440028056684945 ) ) ;
#54682=ORIENTED_EDGE ( 'NONE', *, *, #49496, .F. ) ;
#54695=EDGE_LOOP ( 'NONE', ( #41401, #51339, #39469, #55721 ) ) ;
#54706=CARTESIAN_POINT ( 'NONE',  ( 0.000000000000000000, 2.562706407243636075, 6.312399813420339179 ) ) ;
#54711=EDGE_LOOP ( 'NONE', ( #21189, #1264, #26103, #2647 ) ) ;
#54712=CARTESIAN_POINT ( 'NONE',  ( 0.000000000000000000, 0.000000000000000000, 0.000000000000000000 ) ) ;
#54722=DIRECTION ( 'NONE',  ( 1.000000000000000000, 0.000000000000000000, 0.000000000000000000 ) ) ;
#54725=ORIENTED_EDGE ( 'NONE', *, *, #60717, .T. ) ;
#54727=VERTEX_POINT ( 'NONE', #8731 ) ;
#54735=CARTESIAN_POINT ( 'NONE',  ( -22.29115169517546136, 3.075985640626810014, -2.098196790595514560 ) ) ;
#54739=VECTOR ( 'NONE', #37893, 1000.000000000000000 ) ;
#54740=ORIENTED_EDGE ( 'NONE', *, *, #28178, .T. ) ;
#54741=EDGE_CURVE ( 'NONE', #20276, #57966, #22769, .T. ) ;
#54742=DIRECTION ( 'NONE',  ( 0.000000000000000000, 0.000000000000000000, 1.000000000000000000 ) ) ;
#54746=EDGE_CURVE ( 'NONE', #61504, #60604, #51273, .T. ) ;
#54747=CIRCLE ( 'NONE', #12246, 2.899999999999994582 ) ;
#54758=EDGE_CURVE ( 'NONE', #3708, #24592, #8372, .T. ) ;
#54764=EDGE_LOOP ( 'NONE', ( #15669, #18695, #60916, #20102 ) ) ;
#54769=ORIENTED_EDGE ( 'NONE', *, *, #33340, .F. ) ;
#54775=LINE ( 'NONE', #4568, #37166 ) ;
#54778=CARTESIAN_POINT ( 'NONE',  ( -27.09252613521593744, 1.304094283669213095, 1.914180209340453409 ) ) ;
#54782=( BOUNDED_SURFACE ( )  B_SPLINE_SURFACE ( 3, 1, ( 
 ( #44419, #49133 ),
 ( #34463, #3591 ),
 ( #19832, #9184 ),
 ( #44118, #29462 ) ),
 .UNSPECIFIED., .F., .F., .F. ) 
 B_SPLINE_SURFACE_WITH_KNOTS ( ( 4, 4 ),
 ( 2, 2 ),
 ( 0.000000000000000000, 1.000000000000000000 ),
 ( 0.000000000000000000, 1.000000000000000000 ),
 .UNSPECIFIED. ) 
 GEOMETRIC_REPRESENTATION_ITEM ( )  RATIONAL_B_SPLINE_SURFACE ( (
 ( 1.000000000000000000, 1.000000000000000000),
 ( 0.8716676215708681896, 0.8964445200148167814),
 ( 0.8716676215708681896, 0.8964445200148167814),
 ( 1.000000000000000000, 1.000000000000000000) ) ) 
 REPRESENTATION_ITEM ( '' )  SURFACE ( )  );
#54788=VERTEX_POINT ( 'NONE', #34630 ) ;
#54801=CYLINDRICAL_SURFACE ( 'NONE', #25747, 2.899999999999994582 ) ;
#54812=ORIENTED_EDGE ( 'NONE', *, *, #65233, .F. ) ;
#54815=DIRECTION ( 'NONE',  ( 0.000000000000000000, 0.6051742151937661296, -0.7960930657056429771 ) ) ;
#54818=CARTESIAN_POINT ( 'NONE',  ( -22.31328051695926007, -3.148362328073157190, 2.109671368890621679 ) ) ;
#54820=DIRECTION ( 'NONE',  ( -1.000000000000000000, 0.000000000000000000, 0.000000000000000000 ) ) ;
#54822=ORIENTED_EDGE ( 'NONE', *, *, #26048, .F. ) ;
#54838=ORIENTED_EDGE ( 'NONE', *, *, #61695, .T. ) ;
#54840=ORIENTED_EDGE ( 'NONE', *, *, #29247, .F. ) ;
#54841=LINE ( 'NONE', #35529, #43952 ) ;
#54843=LINE ( 'NONE', #19913, #8707 ) ;
#54848=CARTESIAN_POINT ( 'NONE',  ( -27.08429572838383947, 0.9410937941434112108, -2.089332284968719922 ) ) ;
#54850=DIRECTION ( 'NONE',  ( -1.000000000000000000, 0.000000000000000000, 0.000000000000000000 ) ) ;
#54855=DIRECTION ( 'NONE',  ( -1.000000000000000000, 0.000000000000000000, 0.000000000000000000 ) ) ;
#54872=ADVANCED_FACE ( 'NONE', ( #17322 ), #36929, .T. ) ;
#54877=ORIENTED_EDGE ( 'NONE', *, *, #46594, .T. ) ;
#54892=ORIENTED_EDGE ( 'NONE', *, *, #12424, .F. ) ;
#54903=CARTESIAN_POINT ( 'NONE',  ( 0.000000000000000000, 0.000000000000000000, 0.000000000000000000 ) ) ;
#54904=CIRCLE ( 'NONE', #60218, 6.936499999999990784 ) ;
#54905=CARTESIAN_POINT ( 'NONE',  ( 0.000000000000000000, 1.018311147294260977, -6.861346417234475581 ) ) ;
#54915=CARTESIAN_POINT ( 'NONE',  ( -27.08506889328344158, -1.324351020478542029, -1.872884652028469432 ) ) ;
#54916=ORIENTED_EDGE ( 'NONE', *, *, #53545, .F. ) ;
#54922=ORIENTED_EDGE ( 'NONE', *, *, #23262, .T. ) ;
#54924=DIRECTION ( 'NONE',  ( -1.000000000000000000, 0.000000000000000000, 0.000000000000000000 ) ) ;
#54928=ORIENTED_EDGE ( 'NONE', *, *, #9823, .F. ) ;
#54932=ORIENTED_EDGE ( 'NONE', *, *, #15493, .F. ) ;
#54937=CARTESIAN_POINT ( 'NONE',  ( 2.000000000000001776, 5.107597897712416568, -4.693343793638371508 ) ) ;
#54951=CARTESIAN_POINT ( 'NONE',  ( -27.09364415740216714, -0.1694361397562798854, -2.313349100776210143 ) ) ;
#54958=ORIENTED_EDGE ( 'NONE', *, *, #16399, .T. ) ;
#54962=CARTESIAN_POINT ( 'NONE',  ( 2.000000000000001776, 3.155844197800107498, 6.177028383390443800 ) ) ;
#54966=CARTESIAN_POINT ( 'NONE',  ( -22.27704833740210333, 1.521679877253185875, -3.351945466913922367 ) ) ;
#54973=CARTESIAN_POINT ( 'NONE',  ( 0.000000000000000000, 0.4804830611970061227, 6.919838746524539452 ) ) ;
#54974=CARTESIAN_POINT ( 'NONE',  ( 2.000000000000001776, 6.164400007374793766, -2.900694413976553143 ) ) ;
#54975=VERTEX_POINT ( 'NONE', #56009 ) ;
#54979=CARTESIAN_POINT ( 'NONE',  ( -35.04834644901396956, -0.01306875526353248884, 0.004537648929124128358 ) ) ;
#54993=CARTESIAN_POINT ( 'NONE',  ( -22.27713295444592845, 3.528329525272667411, 1.050517974988984360 ) ) ;
#55002=CARTESIAN_POINT ( 'NONE',  ( -35.05012975565874456, 0.01363945138522194150, -0.002839961651364783513 ) ) ;
#55003=EDGE_CURVE ( 'NONE', #15374, #11147, #25105, .T. ) ;
#55019=CARTESIAN_POINT ( 'NONE',  ( -22.28073302975500525, -0.9342220484184691198, 3.572053042948124535 ) ) ;
#55023=DIRECTION ( 'NONE',  ( -1.000000000000000000, 0.000000000000000000, 0.000000000000000000 ) ) ;
#55031=EDGE_CURVE ( 'NONE', #14676, #63186, #45059, .T. ) ;
#55034=ORIENTED_EDGE ( 'NONE', *, *, #23344, .F. ) ;
#55037=CARTESIAN_POINT ( 'NONE',  ( -22.27756824490284160, 0.9591204781040340022, -3.555646273932179025 ) ) ;
#55040=CARTESIAN_POINT ( 'NONE',  ( -22.27715239060371744, 1.072868796692262761, -3.521735673127126098 ) ) ;
#55042=EDGE_CURVE ( 'NONE', #53863, #1800, #65225, .T. ) ;
#55043=DIRECTION ( 'NONE',  ( 0.000000000000000000, -0.1764146379942750087, -0.9843159429275484262 ) ) ;
#55044=ORIENTED_EDGE ( 'NONE', *, *, #56022, .T. ) ;
#55047=DIRECTION ( 'NONE',  ( -1.000000000000000000, 0.000000000000000000, 0.000000000000000000 ) ) ;
#55049=CARTESIAN_POINT ( 'NONE',  ( 0.000000000000000000, -4.444115772890149252, 5.163689623839303522 ) ) ;
#55066=VECTOR ( 'NONE', #5037, 1000.000000000000000 ) ;
#55073=AXIS2_PLACEMENT_3D ( 'NONE', #63218, #32944, #44246 ) ;
#55074=FACE_OUTER_BOUND ( 'NONE', #2942, .T. ) ;
#55084=CARTESIAN_POINT ( 'NONE',  ( -27.09048036756548328, 1.306202114107882339, 1.905306051557086322 ) ) ;
#55085=DIRECTION ( 'NONE',  ( -1.000000000000000000, 0.000000000000000000, 0.000000000000000000 ) ) ;
#55092=ORIENTED_EDGE ( 'NONE', *, *, #33652, .F. ) ;
#55097=AXIS2_PLACEMENT_3D ( 'NONE', #11632, #7293, #2336 ) ;
#55104=ORIENTED_EDGE ( 'NONE', *, *, #3971, .F. ) ;
#55108=CARTESIAN_POINT ( 'NONE',  ( -27.08776759928964495, 0.5731512436792131071, -2.229418711698792244 ) ) ;
#55116=EDGE_CURVE ( 'NONE', #59829, #47105, #12092, .T. ) ;
#55117=LINE ( 'NONE', #65091, #45012 ) ;
#55124=CARTESIAN_POINT ( 'NONE',  ( -22.27384469013076185, -2.985904959940905545, 2.154627400808026838 ) ) ;
#55125=DIRECTION ( 'NONE',  ( -1.000000000000000000, 0.000000000000000000, 0.000000000000000000 ) ) ;
#55126=CARTESIAN_POINT ( 'NONE',  ( -27.10113028276154878, 1.613062633976926730, -1.697941299269287940 ) ) ;
#55127=DIRECTION ( 'NONE',  ( -1.000000000000000000, 0.000000000000000000, 0.000000000000000000 ) ) ;
#55131=EDGE_LOOP ( 'NONE', ( #22204, #21935, #44756, #23939 ) ) ;
#55134=( BOUNDED_SURFACE ( )  B_SPLINE_SURFACE ( 3, 1, ( 
 ( #27633, #6388 ),
 ( #26658, #47935 ),
 ( #42937, #37944 ),
 ( #1073, #33933 ) ),
 .UNSPECIFIED., .F., .F., .F. ) 
 B_SPLINE_SURFACE_WITH_KNOTS ( ( 4, 4 ),
 ( 2, 2 ),
 ( 0.000000000000000000, 1.000000000000000000 ),
 ( 0.000000000000000000, 1.000000000000000000 ),
 .UNSPECIFIED. ) 
 GEOMETRIC_REPRESENTATION_ITEM ( )  RATIONAL_B_SPLINE_SURFACE ( (
 ( 1.000000000000000000, 1.000000000000000000),
 ( 0.8716676215708681896, 0.8964445200148167814),
 ( 0.8716676215708681896, 0.8964445200148167814),
 ( 1.000000000000000000, 1.000000000000000000) ) ) 
 REPRESENTATION_ITEM ( '' )  SURFACE ( )  );
#55135=ORIENTED_EDGE ( 'NONE', *, *, #31973, .T. ) ;
#55139=DIRECTION ( 'NONE',  ( 0.000000000000000000, -0.6876994588534143249, -0.7259954919231393911 ) ) ;
#55140=DIRECTION ( 'NONE',  ( -1.000000000000000000, 0.000000000000000000, 0.000000000000000000 ) ) ;
#55144=CARTESIAN_POINT ( 'NONE',  ( -27.08704841010891684, 2.081152044925695499, 0.9786466045353945375 ) ) ;
#55149=( BOUNDED_SURFACE ( )  B_SPLINE_SURFACE ( 3, 1, ( 
 ( #21393, #41669 ),
 ( #61962, #36682 ),
 ( #1778, #16722 ),
 ( #6432, #22040 ) ),
 .UNSPECIFIED., .F., .F., .F. ) 
 B_SPLINE_SURFACE_WITH_KNOTS ( ( 4, 4 ),
 ( 2, 2 ),
 ( 0.000000000000000000, 1.000000000000000000 ),
 ( 0.000000000000000000, 1.000000000000000000 ),
 .UNSPECIFIED. ) 
 GEOMETRIC_REPRESENTATION_ITEM ( )  RATIONAL_B_SPLINE_SURFACE ( (
 ( 1.000000000000000000, 1.000000000000000000),
 ( 0.8716676215708681896, 0.8964445200148167814),
 ( 0.8716676215708681896, 0.8964445200148167814),
 ( 1.000000000000000000, 1.000000000000000000) ) ) 
 REPRESENTATION_ITEM ( '' )  SURFACE ( )  );
#55151=AXIS2_PLACEMENT_3D ( 'NONE', #48297, #34273, #33939 ) ;
#55153=ORIENTED_EDGE ( 'NONE', *, *, #19130, .T. ) ;
#55161=DIRECTION ( 'NONE',  ( -1.000000000000000000, 0.000000000000000000, 0.000000000000000000 ) ) ;
#55171=ORIENTED_EDGE ( 'NONE', *, *, #10474, .F. ) ;
#55173=CARTESIAN_POINT ( 'NONE',  ( -22.65996813707687352, -0.2230532344361122188, 4.828298130757384676 ) ) ;
#55174=ORIENTED_EDGE ( 'NONE', *, *, #57127, .T. ) ;
#55186=CARTESIAN_POINT ( 'NONE',  ( -27.09569413923794556, -2.259195818742708806, -0.5521997980586369481 ) ) ;
#55189=DIRECTION ( 'NONE',  ( -1.000000000000000000, 0.000000000000000000, 0.000000000000000000 ) ) ;
#55195=DIRECTION ( 'NONE',  ( 0.000000000000000000, 0.000000000000000000, 1.000000000000000000 ) ) ;
#55200=CARTESIAN_POINT ( 'NONE',  ( -22.71097035706202405, 4.510116093748279376, -2.118550233809386896 ) ) ;
#55201=CARTESIAN_POINT ( 'NONE',  ( -22.59969328935896371, -2.921971394153427770, 3.618004136135737792 ) ) ;
#55219=VERTEX_POINT ( 'NONE', #21426 ) ;
#55229=CARTESIAN_POINT ( 'NONE',  ( -35.04834644901396956, -0.006670072992075125155, 0.01211993185716846860 ) ) ;
#55238=CIRCLE ( 'NONE', #23348, 2.899999999999995026 ) ;
#55240=EDGE_CURVE ( 'NONE', #37470, #57809, #13404, .T. ) ;
#55242=ORIENTED_EDGE ( 'NONE', *, *, #35521, .F. ) ;
#55252=EDGE_LOOP ( 'NONE', ( #40648, #50307, #11110, #2285 ) ) ;
#55256=ORIENTED_EDGE ( 'NONE', *, *, #58648, .F. ) ;
#55270=CARTESIAN_POINT ( 'NONE',  ( -22.71097035706202760, -2.118550233809395777, -4.510116093748293586 ) ) ;
#55280=ORIENTED_EDGE ( 'NONE', *, *, #56898, .T. ) ;
#55288=CARTESIAN_POINT ( 'NONE',  ( -22.27786964138239867, 1.536369256421363350, -3.347945419004150214 ) ) ;
#55289=ADVANCED_FACE ( 'NONE', ( #49650 ), #28696, .T. ) ;
#55296=FACE_OUTER_BOUND ( 'NONE', #6428, .T. ) ;
#55297=DIRECTION ( 'NONE',  ( 0.000000000000000000, 0.000000000000000000, 1.000000000000000000 ) ) ;
#55299=EDGE_LOOP ( 'NONE', ( #52270, #65221, #19718, #47668 ) ) ;
#55302=AXIS2_PLACEMENT_3D ( 'NONE', #29936, #38943, #59231 ) ;
#55304=AXIS2_PLACEMENT_3D ( 'NONE', #40995, #10728, #56635 ) ;
#55324=DIRECTION ( 'NONE',  ( -1.000000000000000000, 0.000000000000000000, 0.000000000000000000 ) ) ;
#55330=ORIENTED_EDGE ( 'NONE', *, *, #47640, .F. ) ;
#55332=ORIENTED_EDGE ( 'NONE', *, *, #24854, .T. ) ;
#55333=VECTOR ( 'NONE', #17129, 1000.000000000000000 ) ;
#55344=EDGE_CURVE ( 'NONE', #31156, #8369, #71, .T. ) ;
#55364=CIRCLE ( 'NONE', #64883, 7.499999999999988454 ) ;
#55367=CARTESIAN_POINT ( 'NONE',  ( 2.000000000000001776, 0.000000000000000000, 0.000000000000000000 ) ) ;
#55369=FACE_OUTER_BOUND ( 'NONE', #25916, .T. ) ;
#55370=DIRECTION ( 'NONE',  ( -1.000000000000000000, 0.000000000000000000, 0.000000000000000000 ) ) ;
#55374=VECTOR ( 'NONE', #8915, 1000.000000000000000 ) ;
#55375=VERTEX_POINT ( 'NONE', #34970 ) ;
#55381=EDGE_CURVE ( 'NONE', #11936, #18330, #11240, .T. ) ;
#55382=CARTESIAN_POINT ( 'NONE',  ( 0.000000000000000000, 0.000000000000000000, 0.000000000000000000 ) ) ;
#55383=AXIS2_PLACEMENT_3D ( 'NONE', #49854, #35189, #45500 ) ;
#55386=CARTESIAN_POINT ( 'NONE',  ( -28.66013792860432119, -1.826836065344825233, 0.1826938850344062559 ) ) ;
#55388=CARTESIAN_POINT ( 'NONE',  ( 2.000000000000001776, 3.786546189469178092, 5.663561025469147303 ) ) ;
#55396=CIRCLE ( 'NONE', #40537, 7.499999999999988454 ) ;
#55397=AXIS2_PLACEMENT_3D ( 'NONE', #13587, #44187, #61117 ) ;
#55408=CARTESIAN_POINT ( 'NONE',  ( 2.000000000000001776, 5.450255447309745982, 4.087611905901426645 ) ) ;
#55410=AXIS2_PLACEMENT_3D ( 'NONE', #23083, #48687, #6817 ) ;
#55414=ADVANCED_FACE ( 'NONE', ( #65259 ), #59960, .T. ) ;
#55421=CARTESIAN_POINT ( 'NONE',  ( -27.09729107899804745, 1.302895495070948151, 1.932259710106483341 ) ) ;
#55424=DIRECTION ( 'NONE',  ( -1.000000000000000000, 0.000000000000000000, 0.000000000000000000 ) ) ;
#55430=EDGE_LOOP ( 'NONE', ( #28559, #53342, #32848, #24150 ) ) ;
#55431=( NAMED_UNIT ( * ) SI_UNIT ( $, .STERADIAN. ) SOLID_ANGLE_UNIT ( ) );
#55434=VECTOR ( 'NONE', #35485, 1000.000000000000000 ) ;
#55436=CARTESIAN_POINT ( 'NONE',  ( 0.000000000000000000, -5.585096664091900642, -4.113602740025990911 ) ) ;
#55444=ORIENTED_EDGE ( 'NONE', *, *, #39553, .F. ) ;
#55445=CARTESIAN_POINT ( 'NONE',  ( -27.09833916700227263, 0.5492787772350139486, -2.268067253344199230 ) ) ;
#55446=VERTEX_POINT ( 'NONE', #41280 ) ;
#55447=CIRCLE ( 'NONE', #19343, 2.899999999999996358 ) ;
#55462=CARTESIAN_POINT ( 'NONE',  ( 2.000000000000001776, 6.812627895098307462, 2.855765430652717818 ) ) ;
#55469=ORIENTED_EDGE ( 'NONE', *, *, #9535, .F. ) ;
#55476=ORIENTED_EDGE ( 'NONE', *, *, #62816, .F. ) ;
#55481=CARTESIAN_POINT ( 'NONE',  ( -22.27878402819508707, 2.612733676624913848, 2.600576127690894523 ) ) ;
#55487=VERTEX_POINT ( 'NONE', #56602 ) ;
#55488=CARTESIAN_POINT ( 'NONE',  ( -27.08776759928996825, -0.5731512436777455033, 2.229418711700135169 ) ) ;
#55494=DIRECTION ( 'NONE',  ( -1.000000000000000000, 0.000000000000000000, 0.000000000000000000 ) ) ;
#55505=CARTESIAN_POINT ( 'NONE',  ( -22.27722022243423794, -3.470949075637794312, -1.227876413014593160 ) ) ;
#55506=DIRECTION ( 'NONE',  ( -1.000000000000000000, 0.000000000000000000, 0.000000000000000000 ) ) ;
#55510=DIRECTION ( 'NONE',  ( 0.9582930651793755139, -0.2851010602429190910, 0.01979360193296256579 ) ) ;
#55511=CYLINDRICAL_SURFACE ( 'NONE', #36060, 2.899999999999994582 ) ;
#55524=CARTESIAN_POINT ( 'NONE',  ( -27.10307689719060065, -2.283215755731203611, -0.5470785519252583384 ) ) ;
#55525=ORIENTED_EDGE ( 'NONE', *, *, #20882, .T. ) ;
#55526=ORIENTED_EDGE ( 'NONE', *, *, #18650, .F. ) ;
#55527=CYLINDRICAL_SURFACE ( 'NONE', #12974, 7.499999999999988454 ) ;
#55528=VERTEX_POINT ( 'NONE', #17344 ) ;
#55532=CIRCLE ( 'NONE', #28998, 6.936499999999989008 ) ;
#55539=AXIS2_PLACEMENT_3D ( 'NONE', #55908, #10666, #392 ) ;
#55541=DIRECTION ( 'NONE',  ( 0.000000000000000000, 0.000000000000000000, 1.000000000000000000 ) ) ;
#55542=CARTESIAN_POINT ( 'NONE',  ( -22.27218376572352554, -1.571356284315158502, 3.330959526935388659 ) ) ;
#55553=AXIS2_PLACEMENT_3D ( 'NONE', #42204, #15635, #16639 ) ;
#55558=ORIENTED_EDGE ( 'NONE', *, *, #13119, .F. ) ;
#55563=AXIS2_PLACEMENT_3D ( 'NONE', #28141, #23820, #27462 ) ;
#55569=VERTEX_POINT ( 'NONE', #13972 ) ;
#55572=CARTESIAN_POINT ( 'NONE',  ( -27.15525204139122906, -1.707635684994321279, 1.831989866434732273 ) ) ;
#55575=VECTOR ( 'NONE', #35077, 1000.000000000000000 ) ;
#55577=CARTESIAN_POINT ( 'NONE',  ( -35.04643116707788408, -0.01193867652720878580, 0.002453861112621663620 ) ) ;
#55580=DIRECTION ( 'NONE',  ( 0.000000000000000000, 0.6876994588534245390, -0.7259954919231297321 ) ) ;
#55581=VECTOR ( 'NONE', #64719, 1000.000000000000227 ) ;
#55583=EDGE_CURVE ( 'NONE', #55926, #3384, #7015, .T. ) ;
#55587=CARTESIAN_POINT ( 'NONE',  ( -27.09861164373156228, -1.303360234155845676, -1.936722219471114892 ) ) ;
#55593=AXIS2_PLACEMENT_3D ( 'NONE', #61754, #12200, #32468 ) ;
#55597=CIRCLE ( 'NONE', #51337, 2.899999999999994582 ) ;
#55598=VERTEX_POINT ( 'NONE', #17995 ) ;
#55612=CARTESIAN_POINT ( 'NONE',  ( 2.000000000000001776, 2.562706407243739992, -6.312399813420325856 ) ) ;
#55618=DIRECTION ( 'NONE',  ( -1.000000000000000000, 0.000000000000000000, 0.000000000000000000 ) ) ;
#55619=CARTESIAN_POINT ( 'NONE',  ( 2.000000000000001776, 1.225832621831950187, -6.827324998361564923 ) ) ;
#55626=DIRECTION ( 'NONE',  ( -1.000000000000000000, -0.000000000000000000, -0.000000000000000000 ) ) ;
#55637=DIRECTION ( 'NONE',  ( -1.000000000000000000, 0.000000000000000000, 0.000000000000000000 ) ) ;
#55638=CARTESIAN_POINT ( 'NONE',  ( -27.08935880048753120, -2.219773948423732435, 0.6272370006475057602 ) ) ;
#55641=DIRECTION ( 'NONE',  ( -1.000000000000000000, 0.000000000000000000, 0.000000000000000000 ) ) ;
#55642=EDGE_CURVE ( 'NONE', #31041, #65063, #22503, .T. ) ;
#55648=CARTESIAN_POINT ( 'NONE',  ( 0.000000000000000000, -7.493043167941588756, -0.3229614270520431152 ) ) ;
#55654=VECTOR ( 'NONE', #19223, 1000.000000000000000 ) ;
#55655=CARTESIAN_POINT ( 'NONE',  ( -22.70624764888619751, 1.907540768355125316, 4.891815784104529996 ) ) ;
#55663=ORIENTED_EDGE ( 'NONE', *, *, #56127, .F. ) ;
#55665=CARTESIAN_POINT ( 'NONE',  ( -22.27721038036499834, 3.438655654856790811, 1.315315479297472390 ) ) ;
#55666=CARTESIAN_POINT ( 'NONE',  ( -22.29382655386184808, 3.584644999358090889, -1.036465316386231850 ) ) ;
#55668=DIRECTION ( 'NONE',  ( 0.000000000000000000, 0.000000000000000000, 1.000000000000000000 ) ) ;
#55674=ORIENTED_EDGE ( 'NONE', *, *, #30837, .F. ) ;
#55676=EDGE_CURVE ( 'NONE', #59, #57650, #8343, .T. ) ;
#55677=ORIENTED_EDGE ( 'NONE', *, *, #12055, .F. ) ;
#55678=CARTESIAN_POINT ( 'NONE',  ( 2.000000000000001776, 1.530946385938383614, 7.342084388195340594 ) ) ;
#55685=DIRECTION ( 'NONE',  ( -1.000000000000000000, 0.000000000000000000, 0.000000000000000000 ) ) ;
#55687=DIRECTION ( 'NONE',  ( -1.000000000000000000, 0.000000000000000000, 0.000000000000000000 ) ) ;
#55698=CARTESIAN_POINT ( 'NONE',  ( 0.000000000000000000, 0.000000000000000000, 0.000000000000000000 ) ) ;
#55700=CARTESIAN_POINT ( 'NONE',  ( 2.000000000000001776, 4.409940824963425321, 5.354199675985255702 ) ) ;
#55705=DIRECTION ( 'NONE',  ( 0.000000000000000000, 0.3193015301359806157, -0.9476531711828021232 ) ) ;
#55712=CARTESIAN_POINT ( 'NONE',  ( -22.29018399051993882, 0.9010028109495269444, -3.609810019245846213 ) ) ;
#55714=CARTESIAN_POINT ( 'NONE',  ( -22.27716857039623477, 1.095155339732109212, -3.514919882996453193 ) ) ;
#55718=DIRECTION ( 'NONE',  ( 0.000000000000000000, 0.4198891015602656540, -0.9075754196709564514 ) ) ;
#55720=ADVANCED_FACE ( 'NONE', ( #30804 ), #10872, .T. ) ;
#55721=ORIENTED_EDGE ( 'NONE', *, *, #6347, .T. ) ;
#55723=VECTOR ( 'NONE', #30704, 1000.000000000000227 ) ;
#55730=DIRECTION ( 'NONE',  ( 0.000000000000000000, 0.2149704402110246271, -0.9766205557100866574 ) ) ;
#55745=CARTESIAN_POINT ( 'NONE',  ( -22.31328051695926007, 3.781397440874590732, -0.2528478350593763024 ) ) ;
#55750=CARTESIAN_POINT ( 'NONE',  ( 1.000000000000000888, 6.664893814313728626, 3.439359016433498173 ) ) ;
#55752=CARTESIAN_POINT ( 'NONE',  ( -24.42101984568203221, -4.276292373951995351, -0.3620223918248546835 ) ) ;
#55761=CIRCLE ( 'NONE', #39805, 2.899999999999996358 ) ;
#55762=ORIENTED_EDGE ( 'NONE', *, *, #27436, .F. ) ;
#55764=ORIENTED_EDGE ( 'NONE', *, *, #46953, .F. ) ;
#55770=VERTEX_POINT ( 'NONE', #30489 ) ;
#55771=CARTESIAN_POINT ( 'NONE',  ( -35.04709527796842394, 0.01120703303052542066, -0.005220632201003577721 ) ) ;
#55774=CARTESIAN_POINT ( 'NONE',  ( -22.27715526084302056, -1.423304177213873700, 3.395518526174210905 ) ) ;
#55777=CARTESIAN_POINT ( 'NONE',  ( -22.27706485742869091, 2.985151051101503583, -2.154081322712197544 ) ) ;
#55778=EDGE_CURVE ( 'NONE', #332, #983, #52929, .T. ) ;
#55780=CARTESIAN_POINT ( 'NONE',  ( 0.000000000000000000, 0.000000000000000000, 0.000000000000000000 ) ) ;
#55783=CIRCLE ( 'NONE', #32367, 6.936499999999995225 ) ;
#55787=EDGE_CURVE ( 'NONE', #28939, #10128, #19986, .T. ) ;
#55789=ORIENTED_EDGE ( 'NONE', *, *, #64868, .T. ) ;
#55792=CARTESIAN_POINT ( 'NONE',  ( 2.000000000000001776, -6.338823199656690832, 2.816798305433647620 ) ) ;
#55793=ADVANCED_FACE ( 'NONE', ( #12179 ), #22492, .T. ) ;
#55796=DIRECTION ( 'NONE',  ( 0.000000000000000000, 0.9289767198167925288, -0.3701381553399118451 ) ) ;
#55797=CARTESIAN_POINT ( 'NONE',  ( 1.000000000000000888, -1.693411908627144635, -7.306323022404617618 ) ) ;
#55804=CARTESIAN_POINT ( 'NONE',  ( 0.000000000000000000, -3.805198749487401777, -5.799611601383285020 ) ) ;
#55821=CIRCLE ( 'NONE', #50512, 6.936499999999989008 ) ;
#55823=CARTESIAN_POINT ( 'NONE',  ( -27.09030469827931853, -0.5638997280354804964, 2.239626370113432685 ) ) ;
#55826=CARTESIAN_POINT ( 'NONE',  ( -22.71097035706202405, -4.510116093748277599, 2.118550233809401107 ) ) ;
#55829=CIRCLE ( 'NONE', #27156, 2.899999999999996803 ) ;
#55835=CARTESIAN_POINT ( 'NONE',  ( 2.000000000000001776, 0.000000000000000000, 0.000000000000000000 ) ) ;
#55841=CARTESIAN_POINT ( 'NONE',  ( -22.31328051695926007, 1.076152733467212741, 3.633840107626929328 ) ) ;
#55846=CARTESIAN_POINT ( 'NONE',  ( -27.08954555554373300, 1.900922216191360148, -1.307633183325732640 ) ) ;
#55849=CARTESIAN_POINT ( 'NONE',  ( -22.27711351828769892, 3.575417021793781736, -0.8770428151440373687 ) ) ;
#55853=CARTESIAN_POINT ( 'NONE',  ( 1.000000000000000888, -4.604744433234619017, -5.919993978425545755 ) ) ;
#55857=EDGE_CURVE ( 'NONE', #57966, #3825, #7255, .T. ) ;
#55858=ORIENTED_EDGE ( 'NONE', *, *, #8285, .F. ) ;
#55865=DIRECTION ( 'NONE',  ( -1.000000000000000000, 0.000000000000000000, 0.000000000000000000 ) ) ;
#55872=ORIENTED_EDGE ( 'NONE', *, *, #9844, .T. ) ;
#55884=ORIENTED_EDGE ( 'NONE', *, *, #30107, .T. ) ;
#55893=CARTESIAN_POINT ( 'NONE',  ( 0.000000000000000000, 0.8935325819929771374, -7.446583077151355923 ) ) ;
#55896=CARTESIAN_POINT ( 'NONE',  ( -35.04643116707788408, -0.007621814750504232738, -0.009511118309140503824 ) ) ;
#55901=VECTOR ( 'NONE', #24415, 1000.000000000000000 ) ;
#55906=DIRECTION ( 'NONE',  ( 0.000000000000000000, -0.8835120444460178302, -0.4684084406997996997 ) ) ;
#55908=CARTESIAN_POINT ( 'NONE',  ( 2.000000000000001776, 0.3246585432987117992, -6.805031400696120336 ) ) ;
#55910=ORIENTED_EDGE ( 'NONE', *, *, #33206, .F. ) ;
#55916=DIRECTION ( 'NONE',  ( 0.000000000000000000, 0.6051742151937610226, 0.7960930657056469739 ) ) ;
#55917=ORIENTED_EDGE ( 'NONE', *, *, #42291, .F. ) ;
#55920=CYLINDRICAL_SURFACE ( 'NONE', #5732, 7.499999999999988454 ) ;
#55926=VERTEX_POINT ( 'NONE', #8499 ) ;
#55928=EDGE_CURVE ( 'NONE', #43917, #33557, #48676, .T. ) ;
#55932=CARTESIAN_POINT ( 'NONE',  ( -35.04709527796842394, -0.01117341439755767385, 0.005292201869320362073 ) ) ;
#55936=CARTESIAN_POINT ( 'NONE',  ( -23.47007829566609871, 4.659361080304749159, 0.3944522252365621484 ) ) ;
#55940=CARTESIAN_POINT ( 'NONE',  ( 0.000000000000000000, 0.000000000000000000, 0.000000000000000000 ) ) ;
#55943=CARTESIAN_POINT ( 'NONE',  ( 0.000000000000000000, 0.000000000000000000, 0.000000000000000000 ) ) ;
#55964=EDGE_LOOP ( 'NONE', ( #13963, #45067, #4515, #27617 ) ) ;
#55965=CARTESIAN_POINT ( 'NONE',  ( -27.09364415740165200, -1.009938549038089661, 2.088137158971413943 ) ) ;
#55968=CARTESIAN_POINT ( 'NONE',  ( 2.000000000000001776, 6.539067737394540281, -2.314222412769769033 ) ) ;
#55969=EDGE_LOOP ( 'NONE', ( #50324, #6548, #18672, #54362 ) ) ;
#55973=DIRECTION ( 'NONE',  ( -1.000000000000000000, 0.000000000000000000, 0.000000000000000000 ) ) ;
#55978=FACE_OUTER_BOUND ( 'NONE', #18788, .T. ) ;
#55984=ORIENTED_EDGE ( 'NONE', *, *, #11633, .T. ) ;
#55985=ORIENTED_EDGE ( 'NONE', *, *, #789, .T. ) ;
#55986=AXIS2_PLACEMENT_3D ( 'NONE', #8263, #49179, #43838 ) ;
#55993=CARTESIAN_POINT ( 'NONE',  ( -22.59983133926799681, -2.272383229042376662, -4.058100437359478008 ) ) ;
#56005=CARTESIAN_POINT ( 'NONE',  ( -22.28284753389937123, -0.9231250029035025229, 3.581493264753373040 ) ) ;
#56008=FACE_OUTER_BOUND ( 'NONE', #45462, .T. ) ;
#56009=CARTESIAN_POINT ( 'NONE',  ( 2.000000000000001776, -3.805198749487460841, 5.799611601383201531 ) ) ;
#56018=CARTESIAN_POINT ( 'NONE',  ( -27.09602251845210930, -2.320865065108512759, 0.1644056400645283189 ) ) ;
#56020=DIRECTION ( 'NONE',  ( -1.000000000000000000, 0.000000000000000000, 0.000000000000000000 ) ) ;
#56021=CARTESIAN_POINT ( 'NONE',  ( -22.27719412087655471, 1.358750377066217929, -3.421752300520414014 ) ) ;
#56022=EDGE_CURVE ( 'NONE', #4847, #23300, #64588, .T. ) ;
#56024=AXIS2_PLACEMENT_3D ( 'NONE', #17924, #58848, #22924 ) ;
#56025=VERTEX_POINT ( 'NONE', #9153 ) ;
#56027=CARTESIAN_POINT ( 'NONE',  ( 2.000000000000001776, 0.000000000000000000, 0.000000000000000000 ) ) ;
#56031=ADVANCED_FACE ( 'NONE', ( #29432 ), #49733, .T. ) ;
#56032=CARTESIAN_POINT ( 'NONE',  ( -27.20164183316782314, -2.642567708136704052, 0.1019800881472514298 ) ) ;
#56035=DIRECTION ( 'NONE',  ( -1.000000000000000000, 0.000000000000000000, 0.000000000000000000 ) ) ;
#56037=CARTESIAN_POINT ( 'NONE',  ( -27.08418179957658722, -2.174042548349536919, -0.7235373421492772295 ) ) ;
#56045=ORIENTED_EDGE ( 'NONE', *, *, #6607, .F. ) ;
#56050=EDGE_CURVE ( 'NONE', #28763, #28121, #46618, .T. ) ;
#56051=CARTESIAN_POINT ( 'NONE',  ( -22.27706485742869091, -0.9832726768967594566, 3.547445275915920071 ) ) ;
#56053=CARTESIAN_POINT ( 'NONE',  ( 2.000000000000001776, 0.000000000000000000, 0.000000000000000000 ) ) ;
#56055=ORIENTED_EDGE ( 'NONE', *, *, #13119, .T. ) ;
#56065=CARTESIAN_POINT ( 'NONE',  ( -27.10719052120871098, -2.295785794152564563, -0.5475695427849640584 ) ) ;
#56073=ORIENTED_EDGE ( 'NONE', *, *, #58242, .T. ) ;
#56074=AXIS2_PLACEMENT_3D ( 'NONE', #41295, #12933, #61580 ) ;
#56078=EDGE_CURVE ( 'NONE', #36827, #21425, #60417, .T. ) ;
#56090=CARTESIAN_POINT ( 'NONE',  ( -27.10422407540562517, 2.346206748218702121, -0.1544383239736422664 ) ) ;
#56094=LINE ( 'NONE', #9893, #14194 ) ;
#56095=ORIENTED_EDGE ( 'NONE', *, *, #64037, .T. ) ;
#56099=LINE ( 'NONE', #26186, #39126 ) ;
#56100=CARTESIAN_POINT ( 'NONE',  ( -27.05874794189610455, 1.734723475976807094E-15, -8.673617379884035472E-15 ) ) ;
#56103=DIRECTION ( 'NONE',  ( -0.9606638835031803270, 0.07465901992590978642, -0.2674900627617606830 ) ) ;
#56107=ORIENTED_EDGE ( 'NONE', *, *, #44325, .F. ) ;
#56109=CIRCLE ( 'NONE', #51871, 7.499999999999988454 ) ;
#56118=CARTESIAN_POINT ( 'NONE',  ( 2.000000000000001776, -5.814643797626954935, 3.550179297009551149 ) ) ;
#56126=ORIENTED_EDGE ( 'NONE', *, *, #49992, .F. ) ;
#56127=EDGE_CURVE ( 'NONE', #3146, #23034, #27476, .T. ) ;
#56129=ORIENTED_EDGE ( 'NONE', *, *, #48292, .F. ) ;
#56147=FACE_OUTER_BOUND ( 'NONE', #51388, .T. ) ;
#56148=DIRECTION ( 'NONE',  ( 0.000000000000000000, 0.000000000000000000, 1.000000000000000000 ) ) ;
#56152=CARTESIAN_POINT ( 'NONE',  ( -22.27716857039623477, 2.496432241075919212, 2.705892286796375945 ) ) ;
#56154=VECTOR ( 'NONE', #55510, 1000.000000000000114 ) ;
#56155=CARTESIAN_POINT ( 'NONE',  ( -27.09364415740165910, 1.918701019213897574, -1.303410551736464917 ) ) ;
#56158=CARTESIAN_POINT ( 'NONE',  ( -22.27711653538342773, 3.657713416444739352, -0.4190680140413353127 ) ) ;
#56163=DIRECTION ( 'NONE',  ( -1.000000000000000000, 0.000000000000000000, 0.000000000000000000 ) ) ;
#56168=AXIS2_PLACEMENT_3D ( 'NONE', #31801, #56795, #57423 ) ;
#56175=ORIENTED_EDGE ( 'NONE', *, *, #39769, .T. ) ;
#56181=VERTEX_POINT ( 'NONE', #30095 ) ;
#56192=CIRCLE ( 'NONE', #2041, 2.899999999999997247 ) ;
#56217=VERTEX_POINT ( 'NONE', #58006 ) ;
#56218=AXIS2_PLACEMENT_3D ( 'NONE', #56880, #25612, #20294 ) ;
#56220=DIRECTION ( 'NONE',  ( 1.000000000000000000, 0.000000000000000000, 0.000000000000000000 ) ) ;
#56222=FACE_OUTER_BOUND ( 'NONE', #29732, .T. ) ;
#56226=EDGE_CURVE ( 'NONE', #57752, #42222, #27719, .T. ) ;
#56229=CARTESIAN_POINT ( 'NONE',  ( -27.28563798457900447, 2.896153581097023366, 0.04047623855284953470 ) ) ;
#56244=CYLINDRICAL_SURFACE ( 'NONE', #8711, 2.899999999999994582 ) ;
#56252=DIRECTION ( 'NONE',  ( -1.000000000000000000, 0.000000000000000000, 0.000000000000000000 ) ) ;
#56253=DIRECTION ( 'NONE',  ( -1.000000000000000000, 0.000000000000000000, 0.000000000000000000 ) ) ;
#56257=CARTESIAN_POINT ( 'NONE',  ( 2.000000000000001776, 6.338823199656684615, 2.816798305433696470 ) ) ;
#56259=AXIS2_PLACEMENT_3D ( 'NONE', #49858, #19918, #33897 ) ;
#56268=CARTESIAN_POINT ( 'NONE',  ( -27.09833916700227263, -2.238843247505192480, 0.6583442518269273513 ) ) ;
#56279=ORIENTED_EDGE ( 'NONE', *, *, #31502, .F. ) ;
#56284=CARTESIAN_POINT ( 'NONE',  ( -35.05175862995318425, 0.005323180402356034180, -0.01139565579897153236 ) ) ;
#56288=EDGE_CURVE ( 'NONE', #43782, #47123, #12614, .T. ) ;
#56300=CARTESIAN_POINT ( 'NONE',  ( -22.27719381268171617, 3.561499689648256251, -0.9326100520993079179 ) ) ;
#56304=ORIENTED_EDGE ( 'NONE', *, *, #20271, .F. ) ;
#56305=CIRCLE ( 'NONE', #27640, 7.499999999999988454 ) ;
#56307=ORIENTED_EDGE ( 'NONE', *, *, #60114, .T. ) ;
#56309=CARTESIAN_POINT ( 'NONE',  ( -27.08429572838383947, -1.632445743623433421, 1.608131779585712406 ) ) ;
#56310=ORIENTED_EDGE ( 'NONE', *, *, #43276, .F. ) ;
#56312=CARTESIAN_POINT ( 'NONE',  ( 0.000000000000000000, 3.341639490130849488, -6.078525953551423555 ) ) ;
#56313=CARTESIAN_POINT ( 'NONE',  ( -22.29195009621226475, -3.580440466953070278, 1.030739959031457209 ) ) ;
#56314=CARTESIAN_POINT ( 'NONE',  ( 2.000000000000001776, 2.664846396702580833, -6.404188155572981600 ) ) ;
#56316=CYLINDRICAL_SURFACE ( 'NONE', #31153, 6.936499999999988120 ) ;
#56326=DIRECTION ( 'NONE',  ( 0.000000000000000000, 0.000000000000000000, 1.000000000000000000 ) ) ;
#56328=ORIENTED_EDGE ( 'NONE', *, *, #50993, .F. ) ;
#56332=AXIS2_PLACEMENT_3D ( 'NONE', #30215, #8621, #13598 ) ;
#56337=CIRCLE ( 'NONE', #1148, 7.499999999999988454 ) ;
#56338=EDGE_CURVE ( 'NONE', #2803, #29586, #2132, .T. ) ;
#56343=CARTESIAN_POINT ( 'NONE',  ( -24.42101984568203932, -3.522366633939671310, -2.451666775035121759 ) ) ;
#56344=ORIENTED_EDGE ( 'NONE', *, *, #5131, .T. ) ;
#56348=CARTESIAN_POINT ( 'NONE',  ( -22.27710395300133328, 0.9764373854729221369, -3.549456197028682869 ) ) ;
#56353=AXIS2_PLACEMENT_3D ( 'NONE', #13189, #17532, #38787 ) ;
#56361=CARTESIAN_POINT ( 'NONE',  ( -22.30625920655495165, 3.403091720605023962, 1.672644928563048472 ) ) ;
#56368=VECTOR ( 'NONE', #4482, 1000.000000000000000 ) ;
#56374=ADVANCED_FACE ( 'NONE', ( #59970 ), #28070, .T. ) ;
#56385=VERTEX_POINT ( 'NONE', #13095 ) ;
#56389=DIRECTION ( 'NONE',  ( -1.000000000000000000, 0.000000000000000000, 0.000000000000000000 ) ) ;
#56391=DIRECTION ( 'NONE',  ( 0.000000000000000000, 0.000000000000000000, 1.000000000000000000 ) ) ;
#56404=VERTEX_POINT ( 'NONE', #59305 ) ;
#56408=AXIS2_PLACEMENT_3D ( 'NONE', #10215, #30494, #50791 ) ;
#56409=ORIENTED_EDGE ( 'NONE', *, *, #18844, .T. ) ;
#56412=EDGE_CURVE ( 'NONE', #51352, #57823, #63957, .T. ) ;
#56417=DIRECTION ( 'NONE',  ( 0.000000000000000000, 0.000000000000000000, 1.000000000000000000 ) ) ;
#56419=CARTESIAN_POINT ( 'NONE',  ( -22.27720387087365239, -1.337073746937880614, 3.430312021254888322 ) ) ;
#56424=EDGE_LOOP ( 'NONE', ( #18244, #4777, #61617, #17164 ) ) ;
#56432=DIRECTION ( 'NONE',  ( 1.000000000000000000, 0.000000000000000000, 0.000000000000000000 ) ) ;
#56438=ADVANCED_FACE ( 'NONE', ( #23745 ), #58674, .T. ) ;
#56443=CARTESIAN_POINT ( 'NONE',  ( 2.000000000000001776, 1.145812388885126820, 6.715725538143592743 ) ) ;
#56444=CARTESIAN_POINT ( 'NONE',  ( -28.66013792860432119, -0.4872053345172048244, 1.770123732198246591 ) ) ;
#56449=ORIENTED_EDGE ( 'NONE', *, *, #33904, .F. ) ;
#56450=EDGE_CURVE ( 'NONE', #54975, #51469, #63612, .T. ) ;
#56453=ORIENTED_EDGE ( 'NONE', *, *, #30877, .F. ) ;
#56454=LINE ( 'NONE', #36823, #36191 ) ;
#56455=CYLINDRICAL_SURFACE ( 'NONE', #38856, 2.899999999999994582 ) ;
#56466=VECTOR ( 'NONE', #52370, 1000.000000000000000 ) ;
#56470=VERTEX_POINT ( 'NONE', #9085 ) ;
#56471=VECTOR ( 'NONE', #58808, 1000.000000000000000 ) ;
#56473=DIRECTION ( 'NONE',  ( 0.000000000000000000, -0.9289767198167950824, 0.3701381553399052948 ) ) ;
#56476=CIRCLE ( 'NONE', #64955, 2.214855479030549468 ) ;
#56479=ORIENTED_EDGE ( 'NONE', *, *, #11498, .T. ) ;
#56485=CARTESIAN_POINT ( 'NONE',  ( -22.27721701579900682, -3.478642907697087949, -1.205877546543716816 ) ) ;
#56495=AXIS2_PLACEMENT_3D ( 'NONE', #39536, #19605, #4963 ) ;
#56505=DIRECTION ( 'NONE',  ( 1.000000000000000000, -0.000000000000000000, -0.000000000000000000 ) ) ;
#56513=DIRECTION ( 'NONE',  ( -1.000000000000000000, 0.000000000000000000, 0.000000000000000000 ) ) ;
#56516=ORIENTED_EDGE ( 'NONE', *, *, #31860, .F. ) ;
#56519=LINE ( 'NONE', #6001, #8620 ) ;
#56531=CARTESIAN_POINT ( 'NONE',  ( 2.000000000000001776, -0.2704997240205401221, 6.931223712253438585 ) ) ;
#56535=DIRECTION ( 'NONE',  ( 0.000000000000000000, 0.9635499925192236859, -0.2675283385292184235 ) ) ;
#56558=EDGE_CURVE ( 'NONE', #58400, #4690, #24344, .T. ) ;
#56575=ORIENTED_EDGE ( 'NONE', *, *, #10244, .F. ) ;
#56580=LINE ( 'NONE', #26633, #33220 ) ;
#56586=ORIENTED_EDGE ( 'NONE', *, *, #59775, .F. ) ;
#56594=DIRECTION ( 'NONE',  ( -1.000000000000000000, 0.000000000000000000, 0.000000000000000000 ) ) ;
#56602=CARTESIAN_POINT ( 'NONE',  ( -27.08429572838383947, -1.632445743623433421, 1.608131779585712406 ) ) ;
#56612=ORIENTED_EDGE ( 'NONE', *, *, #50095, .F. ) ;
#56628=DIRECTION ( 'NONE',  ( 0.000000000000000000, -0.8276889981568956722, 0.5611870653623750593 ) ) ;
#56635=DIRECTION ( 'NONE',  ( 0.000000000000000000, -0.6876994588534143249, -0.7259954919231393911 ) ) ;
#56643=ADVANCED_FACE ( 'NONE', ( #47610 ), #22318, .T. ) ;
#56658=CARTESIAN_POINT ( 'NONE',  ( -22.27719412087655471, 3.421752300520425116, 1.358750377066169301 ) ) ;
#56659=CIRCLE ( 'NONE', #49220, 6.936499999999989008 ) ;
#56664=ORIENTED_EDGE ( 'NONE', *, *, #64656, .T. ) ;
#56668=CARTESIAN_POINT ( 'NONE',  ( -27.08416781016246588, -1.744495588874929393, 1.485424708116787507 ) ) ;
#56679=B_SPLINE_CURVE_WITH_KNOTS ( 'NONE', 3,
 ( #12774, #28408, #3161, #23426, #43705, #18467 ),
 .UNSPECIFIED., .F., .F.,
 ( 4, 2, 4 ),
 ( 0.0001654224980408412369, 0.0006219428995476526233, 0.001078463301054463901 ),
 .UNSPECIFIED. ) ;
#56680=CARTESIAN_POINT ( 'NONE',  ( 0.000000000000000000, 4.444115772890187444, -5.163689623839299081 ) ) ;
#56706=EDGE_CURVE ( 'NONE', #8645, #634, #35997, .T. ) ;
#56707=ORIENTED_EDGE ( 'NONE', *, *, #42296, .T. ) ;
#56712=CARTESIAN_POINT ( 'NONE',  ( -22.31328051695926007, 1.076152733467212741, 3.633840107626929328 ) ) ;
#56719=DIRECTION ( 'NONE',  ( -1.000000000000000000, 0.000000000000000000, 0.000000000000000000 ) ) ;
#56745=ORIENTED_EDGE ( 'NONE', *, *, #64411, .T. ) ;
#56748=CARTESIAN_POINT ( 'NONE',  ( 2.000000000000001776, 6.441884263200846839, -2.217201541069800275 ) ) ;
#56752=CARTESIAN_POINT ( 'NONE',  ( 2.000000000000001776, 0.000000000000000000, 0.000000000000000000 ) ) ;
#56754=ADVANCED_FACE ( 'NONE', ( #23002 ), #41323, .F. ) ;
#56756=ORIENTED_EDGE ( 'NONE', *, *, #64808, .T. ) ;
#56757=CARTESIAN_POINT ( 'NONE',  ( -35.05175862995318425, 0.01139565579896459346, 0.005323180402349095286 ) ) ;
#56768=CARTESIAN_POINT ( 'NONE',  ( 2.000000000000001776, 6.164400007374783108, 2.900694413976516728 ) ) ;
#56770=VECTOR ( 'NONE', #13502, 1000.000000000000000 ) ;
#56775=ORIENTED_EDGE ( 'NONE', *, *, #28693, .T. ) ;
#56782=EDGE_CURVE ( 'NONE', #18567, #57422, #58343, .T. ) ;
#56791=DIRECTION ( 'NONE',  ( 0.000000000000000000, 0.000000000000000000, -1.000000000000000000 ) ) ;
#56794=ORIENTED_EDGE ( 'NONE', *, *, #9823, .T. ) ;
#56795=DIRECTION ( 'NONE',  ( -1.000000000000000000, 0.000000000000000000, 0.000000000000000000 ) ) ;
#56818=CARTESIAN_POINT ( 'NONE',  ( -22.27710395300133683, 2.585700543510496718, 2.620347679538721941 ) ) ;
#56821=CARTESIAN_POINT ( 'NONE',  ( -28.66013792860432119, -0.1826938850344149434, -1.826836065344826787 ) ) ;
#56823=CARTESIAN_POINT ( 'NONE',  ( 2.000000000000001776, 0.000000000000000000, 0.000000000000000000 ) ) ;
#56825=CARTESIAN_POINT ( 'NONE',  ( -22.27218376572352554, 3.547715993389680023, -0.9890213205919581307 ) ) ;
#56836=CARTESIAN_POINT ( 'NONE',  ( -27.08417568107324058, -2.261355310631419702, 0.3682236895270578625 ) ) ;
#56837=CARTESIAN_POINT ( 'NONE',  ( 2.000000000000001776, -0.4129979343796691404, -6.800241778083718991 ) ) ;
#56839=DIRECTION ( 'NONE',  ( -1.000000000000000000, 0.000000000000000000, 0.000000000000000000 ) ) ;
#56853=CARTESIAN_POINT ( 'NONE',  ( -22.27720412283625961, 3.606406551442371100, -0.7407051501189783060 ) ) ;
#56855=CARTESIAN_POINT ( 'NONE',  ( 1.000000000000000888, -7.248432822490228133, -1.926193556693104547 ) ) ;
#56860=ORIENTED_EDGE ( 'NONE', *, *, #8285, .T. ) ;
#56861=ADVANCED_FACE ( 'NONE', ( #15938 ), #21619, .T. ) ;
#56868=CYLINDRICAL_SURFACE ( 'NONE', #42156, 2.899999999999994582 ) ;
#56871=CARTESIAN_POINT ( 'NONE',  ( -27.20164183316780182, 1.232966507052650318, -2.339520810540422602 ) ) ;
#56880=CARTESIAN_POINT ( 'NONE',  ( 2.000000000000001776, 0.000000000000000000, 0.000000000000000000 ) ) ;
#56884=CARTESIAN_POINT ( 'NONE',  ( 0.000000000000000000, -1.225832621831887792, 6.827324998361543607 ) ) ;
#56890=CARTESIAN_POINT ( 'NONE',  ( -27.09030469827880339, -0.6314616953885191508, -2.221523195520538341 ) ) ;
#56891=DIRECTION ( 'NONE',  ( -1.000000000000000000, 0.000000000000000000, 0.000000000000000000 ) ) ;
#56895=PLANE ( 'NONE',  #55553 ) ;
#56898=EDGE_CURVE ( 'NONE', #13688, #30158, #15832, .T. ) ;
#56900=CARTESIAN_POINT ( 'NONE',  ( 2.000000000000001776, 0.000000000000000000, 0.000000000000000000 ) ) ;
#56902=FACE_OUTER_BOUND ( 'NONE', #22234, .T. ) ;
#56908=EDGE_CURVE ( 'NONE', #44784, #6062, #48814, .T. ) ;
#56909=ORIENTED_EDGE ( 'NONE', *, *, #33303, .T. ) ;
#56919=CARTESIAN_POINT ( 'NONE',  ( -22.46509356695199600, 1.314379028669554472, 4.038408495643908580 ) ) ;
#56923=CARTESIAN_POINT ( 'NONE',  ( 0.000000000000000000, 0.000000000000000000, 0.000000000000000000 ) ) ;
#56927=CARTESIAN_POINT ( 'NONE',  ( -22.30527770659433173, 0.2559941915621863906, 3.757123197210709087 ) ) ;
#56938=CARTESIAN_POINT ( 'NONE',  ( -27.35552965826135008, 3.094132632038936404, 0.2619431035391969198 ) ) ;
#56962=CARTESIAN_POINT ( 'NONE',  ( 2.000000000000001776, -3.230174184210094168, 5.998318953995296354 ) ) ;
#56974=CARTESIAN_POINT ( 'NONE',  ( 2.000000000000001776, -0.7281529553922385656, 7.464569195442775751 ) ) ;
#56976=EDGE_CURVE ( 'NONE', #61504, #32257, #38151, .T. ) ;
#56978=CARTESIAN_POINT ( 'NONE',  ( -22.27721056931765631, 3.486117586310729433, 1.183805672860796188 ) ) ;
#56989=ORIENTED_EDGE ( 'NONE', *, *, #45933, .T. ) ;
#56991=CARTESIAN_POINT ( 'NONE',  ( -22.27756824490284160, -3.558840239148759910, 0.9472004376381163437 ) ) ;
#56994=EDGE_LOOP ( 'NONE', ( #8563, #54041, #44169, #65795 ) ) ;
#56995=DIRECTION ( 'NONE',  ( 0.000000000000000000, 0.9289767198167898643, 0.3701381553399183955 ) ) ;
#56999=DIRECTION ( 'NONE',  ( 0.000000000000000000, -0.7621620551276289124, -0.6473862847818364630 ) ) ;
#57000=ORIENTED_EDGE ( 'NONE', *, *, #56078, .F. ) ;
#57002=ORIENTED_EDGE ( 'NONE', *, *, #56976, .T. ) ;
#57008=EDGE_CURVE ( 'NONE', #64838, #20840, #191, .T. ) ;
#57022=ORIENTED_EDGE ( 'NONE', *, *, #3426, .T. ) ;
#57024=CARTESIAN_POINT ( 'NONE',  ( 2.000000000000001776, 4.409940824963509698, -5.354199675985237050 ) ) ;
#57026=CARTESIAN_POINT ( 'NONE',  ( -22.28694879868232803, 1.011812214896746998, 3.570244315741544661 ) ) ;
#57034=DIRECTION ( 'NONE',  ( 0.000000000000000000, 0.9635499925192219095, 0.2675283385292247518 ) ) ;
#57035=EDGE_CURVE ( 'NONE', #29113, #50541, #5230, .T. ) ;
#57040=ORIENTED_EDGE ( 'NONE', *, *, #29933, .F. ) ;
#57041=FACE_OUTER_BOUND ( 'NONE', #18671, .T. ) ;
#57045=DIRECTION ( 'NONE',  ( -1.000000000000000000, 0.000000000000000000, 0.000000000000000000 ) ) ;
#57046=CIRCLE ( 'NONE', #15636, 6.936499999999992561 ) ;
#57058=ADVANCED_FACE ( 'NONE', ( #40825 ), #61548, .F. ) ;
#57061=CARTESIAN_POINT ( 'NONE',  ( -27.08639648637141661, 2.223359598374790025, 0.5801562253477756670 ) ) ;
#57069=EDGE_CURVE ( 'NONE', #3618, #18279, #39505, .T. ) ;
#57080=CIRCLE ( 'NONE', #16863, 7.499999999999988454 ) ;
#57087=CARTESIAN_POINT ( 'NONE',  ( -22.27718112499583469, -1.380338971069141829, 3.412978993569784070 ) ) ;
#57090=EDGE_CURVE ( 'NONE', #65658, #19640, #34997, .T. ) ;
#57095=AXIS2_PLACEMENT_3D ( 'NONE', #61734, #42100, #16195 ) ;
#57099=CARTESIAN_POINT ( 'NONE',  ( 0.000000000000000000, 6.539067737394503865, 2.314222412769824544 ) ) ;
#57100=CARTESIAN_POINT ( 'NONE',  ( 0.000000000000000000, -6.338823199656649088, -2.816798305433765748 ) ) ;
#57108=CARTESIAN_POINT ( 'NONE',  ( -35.05012975565874456, 0.01089417657933950019, -0.008684292310216024449 ) ) ;
#57120=DIRECTION ( 'NONE',  ( -1.000000000000000000, 0.000000000000000000, 0.000000000000000000 ) ) ;
#57127=EDGE_CURVE ( 'NONE', #37616, #18279, #45605, .T. ) ;
#57130=VECTOR ( 'NONE', #50715, 1000.000000000000000 ) ;
#57139=DIRECTION ( 'NONE',  ( 0.000000000000000000, 0.000000000000000000, -1.000000000000000000 ) ) ;
#57146=ORIENTED_EDGE ( 'NONE', *, *, #13564, .T. ) ;
#57168=AXIS2_PLACEMENT_3D ( 'NONE', #34733, #34429, #3208 ) ;
#57179=DIRECTION ( 'NONE',  ( 0.000000000000000000, 0.1081190184239417679, -0.9941379571543595972 ) ) ;
#57186=CARTESIAN_POINT ( 'NONE',  ( 1.000000000000000888, -0.08317740279936355896, 7.499538753794337431 ) ) ;
#57189=ORIENTED_EDGE ( 'NONE', *, *, #6607, .T. ) ;
#57207=VERTEX_POINT ( 'NONE', #64937 ) ;
#57210=DIRECTION ( 'NONE',  ( 0.000000000000000000, 0.000000000000000000, 1.000000000000000000 ) ) ;
#57214=AXIS2_PLACEMENT_3D ( 'NONE', #51711, #60689, #45714 ) ;
#57215=LINE ( 'NONE', #26611, #55066 ) ;
#57222=AXIS2_PLACEMENT_3D ( 'NONE', #25334, #40290, #60582 ) ;
#57224=CARTESIAN_POINT ( 'NONE',  ( -22.46509356695200665, 4.038408495643943219, -1.314379028669518057 ) ) ;
#57227=CIRCLE ( 'NONE', #8378, 6.936499999999992561 ) ;
#57231=CIRCLE ( 'NONE', #50874, 7.499999999999988454 ) ;
#57243=ORIENTED_EDGE ( 'NONE', *, *, #26220, .F. ) ;
#57244=CARTESIAN_POINT ( 'NONE',  ( 1.000000000000000888, 3.795144977083718008, -6.468916029978776017 ) ) ;
#57246=LINE ( 'NONE', #37273, #16712 ) ;
#57249=ADVANCED_FACE ( 'NONE', ( #59648, #39345 ), #14075, .F. ) ;
#57251=VECTOR ( 'NONE', #36905, 1000.000000000000114 ) ;
#57256=EDGE_LOOP ( 'NONE', ( #5646, #16859, #53252, #7687 ) ) ;
#57262=EDGE_LOOP ( 'NONE', ( #63464, #44588, #51261, #62417 ) ) ;
#57266=CARTESIAN_POINT ( 'NONE',  ( -22.27834755396593991, -3.497967921180582973, -1.162947663292853706 ) ) ;
#57281=DIRECTION ( 'NONE',  ( -1.000000000000000000, 0.000000000000000000, 0.000000000000000000 ) ) ;
#57288=LINE ( 'NONE', #772, #23512 ) ;
#57294=DIRECTION ( 'NONE',  ( 0.000000000000000000, 0.000000000000000000, 1.000000000000000000 ) ) ;
#57297=( BOUNDED_SURFACE ( )  B_SPLINE_SURFACE ( 3, 1, ( 
 ( #29350, #19722 ),
 ( #50311, #419 ),
 ( #5076, #49966 ),
 ( #55932, #61243 ) ),
 .UNSPECIFIED., .F., .F., .F. ) 
 B_SPLINE_SURFACE_WITH_KNOTS ( ( 4, 4 ),
 ( 2, 2 ),
 ( 0.000000000000000000, 1.000000000000000000 ),
 ( 0.000000000000000000, 1.000000000000000000 ),
 .UNSPECIFIED. ) 
 GEOMETRIC_REPRESENTATION_ITEM ( )  RATIONAL_B_SPLINE_SURFACE ( (
 ( 1.000000000000000000, 1.000000000000000000),
 ( 0.8716676215708681896, 0.8964445200148167814),
 ( 0.8716676215708681896, 0.8964445200148167814),
 ( 1.000000000000000000, 1.000000000000000000) ) ) 
 REPRESENTATION_ITEM ( '' )  SURFACE ( )  );
#57298=AXIS2_PLACEMENT_3D ( 'NONE', #8125, #34674, #65279 ) ;
#57302=CYLINDRICAL_SURFACE ( 'NONE', #5516, 2.899999999999994582 ) ;
#57305=ORIENTED_EDGE ( 'NONE', *, *, #37646, .T. ) ;
#57306=ORIENTED_EDGE ( 'NONE', *, *, #45329, .F. ) ;
#57307=CARTESIAN_POINT ( 'NONE',  ( -27.10719052120871098, -1.310802520592025955, -1.962717903527680718 ) ) ;
#57311=CIRCLE ( 'NONE', #28638, 7.499999999999988454 ) ;
#57328=EDGE_CURVE ( 'NONE', #52513, #32250, #5277, .T. ) ;
#57331=CARTESIAN_POINT ( 'NONE',  ( 2.000000000000001776, 6.777474576704068276, 0.6925993764990892032 ) ) ;
#57332=CARTESIAN_POINT ( 'NONE',  ( -22.29770266787582145, -3.635870259503085844, -0.8895590726607217613 ) ) ;
#57333=VERTEX_POINT ( 'NONE', #63966 ) ;
#57340=B_SPLINE_CURVE_WITH_KNOTS ( 'NONE', 3,
 ( #25340, #26013, #61560, #30642, #35311, #30983 ),
 .UNSPECIFIED., .F., .F.,
 ( 4, 2, 4 ),
 ( 0.0002637379172017404469, 0.0009975831966478627272, 0.001731428476093984682 ),
 .UNSPECIFIED. ) ;
#57342=CARTESIAN_POINT ( 'NONE',  ( -22.29382655386184808, 1.036465316386264712, 3.584644999358078454 ) ) ;
#57350=VERTEX_POINT ( 'NONE', #44329 ) ;
#57352=CARTESIAN_POINT ( 'NONE',  ( -22.28939870658739864, -3.068935452695155774, 2.099199915896291291 ) ) ;
#57361=CARTESIAN_POINT ( 'NONE',  ( -27.08429572838383947, -2.208905845566027537, -0.6096735944848257205 ) ) ;
#57363=CARTESIAN_POINT ( 'NONE',  ( -27.08418179957658367, 0.4604195552868272645, 2.244544746853581962 ) ) ;
#57367=ADVANCED_FACE ( 'NONE', ( #55296 ), #9680, .F. ) ;
#57372=CARTESIAN_POINT ( 'NONE',  ( 2.000000000000001776, 0.000000000000000000, 0.000000000000000000 ) ) ;
#57374=DIRECTION ( 'NONE',  ( 0.000000000000000000, 0.000000000000000000, 1.000000000000000000 ) ) ;
#57394=ORIENTED_EDGE ( 'NONE', *, *, #62308, .T. ) ;
#57403=CARTESIAN_POINT ( 'NONE',  ( 2.000000000000001776, 6.767909380267608022, 2.119450094687893138 ) ) ;
#57404=CIRCLE ( 'NONE', #55304, 6.936499999999990784 ) ;
#57415=DIRECTION ( 'NONE',  ( -1.000000000000000000, 0.000000000000000000, 0.000000000000000000 ) ) ;
#57417=DIRECTION ( 'NONE',  ( -1.000000000000000000, 0.000000000000000000, 0.000000000000000000 ) ) ;
#57418=CARTESIAN_POINT ( 'NONE',  ( -22.30625920655495165, 0.8854385781085528651, -3.687109008463846926 ) ) ;
#57420=EDGE_CURVE ( 'NONE', #34013, #29113, #6372, .T. ) ;
#57422=VERTEX_POINT ( 'NONE', #25703 ) ;
#57423=DIRECTION ( 'NONE',  ( 0.000000000000000000, 0.9868265225415254749, 0.1617819965527686754 ) ) ;
#57427=EDGE_CURVE ( 'NONE', #24785, #44673, #14826, .T. ) ;
#57428=CARTESIAN_POINT ( 'NONE',  ( -22.51237073810381517, 3.263711251981947115, 2.986282257334718526 ) ) ;
#57438=DIRECTION ( 'NONE',  ( -1.000000000000000000, 0.000000000000000000, 0.000000000000000000 ) ) ;
#57449=DIRECTION ( 'NONE',  ( 1.000000000000000000, -0.000000000000000000, -0.000000000000000000 ) ) ;
#57456=AXIS2_PLACEMENT_3D ( 'NONE', #65201, #19, #19670 ) ;
#57465=CARTESIAN_POINT ( 'NONE',  ( 0.000000000000000000, 6.997684042076945055, -2.698595569414161677 ) ) ;
#57466=CARTESIAN_POINT ( 'NONE',  ( 0.000000000000000000, 0.000000000000000000, 0.000000000000000000 ) ) ;
#57472=ORIENTED_EDGE ( 'NONE', *, *, #23425, .F. ) ;
#57475=AXIS2_PLACEMENT_3D ( 'NONE', #43245, #2387, #43571 ) ;
#57476=CARTESIAN_POINT ( 'NONE',  ( -27.08421860617808008, -2.271664812096781727, 0.2990745872176354681 ) ) ;
#57483=EDGE_LOOP ( 'NONE', ( #65140, #26627, #54119, #26997 ) ) ;
#57488=AXIS2_PLACEMENT_3D ( 'NONE', #4302, #18941, #29245 ) ;
#57499=VERTEX_POINT ( 'NONE', #52300 ) ;
#57504=B_SPLINE_CURVE_WITH_KNOTS ( 'NONE', 3,
 ( #49566, #43560, #3703, #33271, #53576, #13954, #54216, #8022, #8660, #4002 ),
 .UNSPECIFIED., .F., .F.,
 ( 4, 3, 3, 4 ),
 ( 5.401523115762192401E-05, 0.0008136511341527791425, 0.004068255670953087148, 0.005063778443040924809 ),
 .UNSPECIFIED. ) ;
#57505=ORIENTED_EDGE ( 'NONE', *, *, #56226, .T. ) ;
#57509=AXIS2_PLACEMENT_3D ( 'NONE', #40723, #51039, #36716 ) ;
#57511=CARTESIAN_POINT ( 'NONE',  ( 2.000000000000001776, 0.000000000000000000, 0.000000000000000000 ) ) ;
#57516=VERTEX_POINT ( 'NONE', #11380 ) ;
#57526=CIRCLE ( 'NONE', #18212, 2.999999999999995559 ) ;
#57536=AXIS2_PLACEMENT_3D ( 'NONE', #20745, #41329, #11722 ) ;
#57543=EDGE_CURVE ( 'NONE', #27353, #36393, #31649, .T. ) ;
#57548=CARTESIAN_POINT ( 'NONE',  ( -22.31328051695926007, -1.671726071983958839, 3.401210163132545539 ) ) ;
#57553=VECTOR ( 'NONE', #49973, 1000.000000000000000 ) ;
#57556=CIRCLE ( 'NONE', #41637, 7.499999999999988454 ) ;
#57559=CARTESIAN_POINT ( 'NONE',  ( -27.08485414902839494, -1.622802444812894151, -1.620258667554023368 ) ) ;
#57564=CIRCLE ( 'NONE', #36272, 7.499999999999988454 ) ;
#57581=CARTESIAN_POINT ( 'NONE',  ( 2.000000000000001776, -5.585096664091900642, -4.113602740025990911 ) ) ;
#57586=CARTESIAN_POINT ( 'NONE',  ( 1.000000000000000888, 3.224464355699827145, 6.771471746881979392 ) ) ;
#57587=CARTESIAN_POINT ( 'NONE',  ( 2.000000000000001776, -6.935703035393425253, 0.1051458740707039013 ) ) ;
#57588=CARTESIAN_POINT ( 'NONE',  ( 2.000000000000001776, -5.457833520448679643, 4.281014542496493824 ) ) ;
#57589=VECTOR ( 'NONE', #45454, 1000.000000000000000 ) ;
#57609=AXIS2_PLACEMENT_3D ( 'NONE', #61361, #41404, #551 ) ;
#57615=AXIS2_PLACEMENT_3D ( 'NONE', #38170, #38511, #58831 ) ;
#57616=DIRECTION ( 'NONE',  ( 0.000000000000000000, 0.000000000000000000, 1.000000000000000000 ) ) ;
#57618=LINE ( 'NONE', #5774, #54092 ) ;
#57623=ADVANCED_FACE ( 'NONE', ( #64530 ), #38953, .T. ) ;
#57624=CIRCLE ( 'NONE', #59739, 2.899999999999995470 ) ;
#57625=CARTESIAN_POINT ( 'NONE',  ( -22.30625920655495165, -3.150098859949341357, 2.110841417170906009 ) ) ;
#57626=DIRECTION ( 'NONE',  ( 0.000000000000000000, -0.4198891015602528864, -0.9075754196709624466 ) ) ;
#57631=DIRECTION ( 'NONE',  ( 0.000000000000000000, 0.000000000000000000, 1.000000000000000000 ) ) ;
#57638=ORIENTED_EDGE ( 'NONE', *, *, #65406, .T. ) ;
#57649=CARTESIAN_POINT ( 'NONE',  ( -27.08421860617808363, -1.817782142550197655, 1.394838596205209225 ) ) ;
#57650=VERTEX_POINT ( 'NONE', #33308 ) ;
#57651=DIRECTION ( 'NONE',  ( 0.000000000000000000, -0.7621620551276288014, -0.6473862847818365740 ) ) ;
#57655=EDGE_CURVE ( 'NONE', #52589, #29418, #64619, .T. ) ;
#57674=ORIENTED_EDGE ( 'NONE', *, *, #61041, .T. ) ;
#57678=VECTOR ( 'NONE', #36180, 1000.000000000000000 ) ;
#57679=ORIENTED_EDGE ( 'NONE', *, *, #56782, .F. ) ;
#57680=CARTESIAN_POINT ( 'NONE',  ( 2.000000000000001776, -6.606214214351046721, -2.114938770769991372 ) ) ;
#57684=LINE ( 'NONE', #17440, #35239 ) ;
#57692=FACE_OUTER_BOUND ( 'NONE', #22811, .T. ) ;
#57693=CARTESIAN_POINT ( 'NONE',  ( -22.30527770659433173, -3.125767038151203714, 2.100259071719467130 ) ) ;
#57696=AXIS2_PLACEMENT_3D ( 'NONE', #16505, #26463, #62355 ) ;
#57704=CARTESIAN_POINT ( 'NONE',  ( 0.000000000000000000, 1.530946385938475762, -7.342084388195351252 ) ) ;
#57706=CARTESIAN_POINT ( 'NONE',  ( -24.42101984568203932, -1.824625598916879365, -3.884389025764522163 ) ) ;
#57710=CARTESIAN_POINT ( 'NONE',  ( 2.000000000000001776, -5.814643797626899868, -3.550179297009637747 ) ) ;
#57719=DIRECTION ( 'NONE',  ( -1.000000000000000000, 0.000000000000000000, 0.000000000000000000 ) ) ;
#57723=VERTEX_POINT ( 'NONE', #49916 ) ;
#57733=LINE ( 'NONE', #12154, #23435 ) ;
#57737=CIRCLE ( 'NONE', #11014, 7.499999999999988454 ) ;
#57744=AXIS2_PLACEMENT_3D ( 'NONE', #54176, #3668, #23932 ) ;
#57752=VERTEX_POINT ( 'NONE', #35254 ) ;
#57759=VERTEX_POINT ( 'NONE', #30284 ) ;
#57770=ORIENTED_EDGE ( 'NONE', *, *, #1480, .F. ) ;
#57779=VERTEX_POINT ( 'NONE', #4368 ) ;
#57786=CARTESIAN_POINT ( 'NONE',  ( 2.000000000000001776, 5.888698556700818543, -3.665823448873358981 ) ) ;
#57789=AXIS2_PLACEMENT_3D ( 'NONE', #61047, #57045, #10819 ) ;
#57797=CARTESIAN_POINT ( 'NONE',  ( 2.000000000000001776, 0.000000000000000000, 0.000000000000000000 ) ) ;
#57798=ORIENTED_EDGE ( 'NONE', *, *, #27535, .T. ) ;
#57805=B_SPLINE_CURVE_WITH_KNOTS ( 'NONE', 3,
 ( #59127, #8557, #49479, #28844, #13854, #14195, #28509, #54463, #39464, #45123 ),
 .UNSPECIFIED., .F., .F.,
 ( 4, 3, 3, 4 ),
 ( 5.401523115762189690E-05, 0.0008136511341527787088, 0.004068255670953088883, 0.005063778443040924809 ),
 .UNSPECIFIED. ) ;
#57809=VERTEX_POINT ( 'NONE', #46889 ) ;
#57821=ORIENTED_EDGE ( 'NONE', *, *, #3467, .T. ) ;
#57823=VERTEX_POINT ( 'NONE', #32546 ) ;
#57824=VECTOR ( 'NONE', #40425, 1000.000000000000000 ) ;
#57826=EDGE_LOOP ( 'NONE', ( #30480, #38926, #47811, #2677 ) ) ;
#57827=CARTESIAN_POINT ( 'NONE',  ( 0.000000000000000000, 5.888698556700773246, 3.665823448873418045 ) ) ;
#57836=ORIENTED_EDGE ( 'NONE', *, *, #61916, .F. ) ;
#57842=AXIS2_PLACEMENT_3D ( 'NONE', #50656, #29374, #49667 ) ;
#57843=ORIENTED_EDGE ( 'NONE', *, *, #56450, .T. ) ;
#57847=CARTESIAN_POINT ( 'NONE',  ( -22.27722015946438816, -2.828901469906474286, 2.356370737780152158 ) ) ;
#57849=FACE_OUTER_BOUND ( 'NONE', #29922, .T. ) ;
#57855=ORIENTED_EDGE ( 'NONE', *, *, #64914, .T. ) ;
#57857=CYLINDRICAL_SURFACE ( 'NONE', #51170, 2.899999999999994582 ) ;
#57860=CARTESIAN_POINT ( 'NONE',  ( -10.00000000000000178, 0.000000000000000000, 0.000000000000000000 ) ) ;
#57863=ORIENTED_EDGE ( 'NONE', *, *, #45933, .F. ) ;
#57868=DIRECTION ( 'NONE',  ( 0.000000000000000000, 0.000000000000000000, 1.000000000000000000 ) ) ;
#57878=EDGE_CURVE ( 'NONE', #27429, #1460, #52553, .T. ) ;
#57891=ORIENTED_EDGE ( 'NONE', *, *, #54244, .F. ) ;
#57895=CARTESIAN_POINT ( 'NONE',  ( -27.08429572838383947, -1.608131779585707299, -1.632445743623455847 ) ) ;
#57897=CARTESIAN_POINT ( 'NONE',  ( -22.30986928587821438, -2.105440358094953002, -3.138878161034341474 ) ) ;
#57901=ORIENTED_EDGE ( 'NONE', *, *, #34736, .T. ) ;
#57905=VERTEX_POINT ( 'NONE', #59169 ) ;
#57909=CARTESIAN_POINT ( 'NONE',  ( -27.08421860617808363, -0.2990745872176354681, -2.271664812096785280 ) ) ;
#57932=ORIENTED_EDGE ( 'NONE', *, *, #2965, .T. ) ;
#57934=CARTESIAN_POINT ( 'NONE',  ( 0.000000000000000000, -0.08317740279936355896, 7.499538753794337431 ) ) ;
#57938=VERTEX_POINT ( 'NONE', #22942 ) ;
#57944=CYLINDRICAL_SURFACE ( 'NONE', #62878, 6.936499999999988120 ) ;
#57946=CARTESIAN_POINT ( 'NONE',  ( -22.27706485742869091, -3.358064672837095976, -1.508175983031630585 ) ) ;
#57950=CARTESIAN_POINT ( 'NONE',  ( -22.30625920655495165, -2.110841417170890466, -3.150098859949351571 ) ) ;
#57951=LINE ( 'NONE', #31989, #13928 ) ;
#57953=CARTESIAN_POINT ( 'NONE',  ( 2.000000000000001776, -6.470132594555779271, -2.133363481234176628 ) ) ;
#57957=CARTESIAN_POINT ( 'NONE',  ( -22.29570301036918423, -2.696988360630593995, -2.586939527522312599 ) ) ;
#57962=AXIS2_PLACEMENT_3D ( 'NONE', #4287, #65436, #8950 ) ;
#57964=CARTESIAN_POINT ( 'NONE',  ( -22.28121537037576871, 3.680034389105501624, -0.3168735205819583900 ) ) ;
#57966=VERTEX_POINT ( 'NONE', #53187 ) ;
#57972=EDGE_LOOP ( 'NONE', ( #56586, #65626, #58138, #20025 ) ) ;
#57980=CARTESIAN_POINT ( 'NONE',  ( 2.000000000000001776, 0.000000000000000000, 0.000000000000000000 ) ) ;
#57998=CARTESIAN_POINT ( 'NONE',  ( -22.28415773361649954, -3.586804264761562333, -0.9182279841530253117 ) ) ;
#57999=ORIENTED_EDGE ( 'NONE', *, *, #3971, .T. ) ;
#58002=CARTESIAN_POINT ( 'NONE',  ( -28.67667724226168602, -1.574547667005685936, 1.049259427760459218 ) ) ;
#58006=CARTESIAN_POINT ( 'NONE',  ( 2.000000000000001776, 0.4804830611970061227, 6.919838746524539452 ) ) ;
#58015=AXIS2_PLACEMENT_3D ( 'NONE', #8455, #18774, #8135 ) ;
#58016=VERTEX_POINT ( 'NONE', #9563 ) ;
#58018=CARTESIAN_POINT ( 'NONE',  ( -22.28121537037576516, -3.028566507474731218, 2.114437713163338284 ) ) ;
#58026=CARTESIAN_POINT ( 'NONE',  ( -22.31328051695926007, 0.2528478350594092761, 3.781397440874584071 ) ) ;
#58031=CARTESIAN_POINT ( 'NONE',  ( 2.000000000000001776, -6.767909380267597363, 2.119450094687866049 ) ) ;
#58036=CARTESIAN_POINT ( 'NONE',  ( -35.04660725145885891, -0.008800808525089999501, 0.008590646501115670186 ) ) ;
#58043=DIRECTION ( 'NONE',  ( 0.000000000000000000, 0.000000000000000000, 1.000000000000000000 ) ) ;
#58048=CARTESIAN_POINT ( 'NONE',  ( 2.000000000000001776, 5.097042323172456868, 5.501832381651453829 ) ) ;
#58049=CARTESIAN_POINT ( 'NONE',  ( 0.000000000000000000, 4.409940824963509698, -5.354199675985237050 ) ) ;
#58070=( BOUNDED_SURFACE ( )  B_SPLINE_SURFACE ( 3, 1, ( 
 ( #62405, #62737 ),
 ( #16869, #58104 ),
 ( #12516, #11876 ),
 ( #32149, #52473 ) ),
 .UNSPECIFIED., .F., .F., .F. ) 
 B_SPLINE_SURFACE_WITH_KNOTS ( ( 4, 4 ),
 ( 2, 2 ),
 ( 0.000000000000000000, 1.000000000000000000 ),
 ( 0.000000000000000000, 1.000000000000000000 ),
 .UNSPECIFIED. ) 
 GEOMETRIC_REPRESENTATION_ITEM ( )  RATIONAL_B_SPLINE_SURFACE ( (
 ( 1.000000000000000000, 1.000000000000000000),
 ( 0.8716676215708681896, 0.8964445200148164483),
 ( 0.8716676215708681896, 0.8964445200148164483),
 ( 1.000000000000000000, 1.000000000000000000) ) ) 
 REPRESENTATION_ITEM ( '' )  SURFACE ( )  );
#58071=CARTESIAN_POINT ( 'NONE',  ( -22.27722019110237284, -0.6492757894141321096, -3.623957119342521516 ) ) ;
#58075=EDGE_LOOP ( 'NONE', ( #62774, #4320, #18248, #41169 ) ) ;
#58076=CARTESIAN_POINT ( 'NONE',  ( -10.00000000000000178, 0.000000000000000000, 0.000000000000000000 ) ) ;
#58078=DIRECTION ( 'NONE',  ( 0.000000000000000000, -0.9985334138511232638, -0.05413890858542831641 ) ) ;
#58082=EDGE_CURVE ( 'NONE', #8903, #13989, #40156, .T. ) ;
#58083=DIRECTION ( 'NONE',  ( -1.000000000000000000, 0.000000000000000000, 0.000000000000000000 ) ) ;
#58085=DIRECTION ( 'NONE',  ( -1.000000000000000000, 0.000000000000000000, 0.000000000000000000 ) ) ;
#58087=DIRECTION ( 'NONE',  ( 0.000000000000000000, 0.000000000000000000, 1.000000000000000000 ) ) ;
#58088=ORIENTED_EDGE ( 'NONE', *, *, #61536, .F. ) ;
#58101=CARTESIAN_POINT ( 'NONE',  ( 2.000000000000001776, 3.786546189469178092, 5.663561025469147303 ) ) ;
#58104=CARTESIAN_POINT ( 'NONE',  ( -22.51237073810381517, 1.333315726166114823, 4.218051923713566076 ) ) ;
#58121=EDGE_CURVE ( 'NONE', #49587, #42390, #10516, .T. ) ;
#58129=DIRECTION ( 'NONE',  ( -1.000000000000000000, 0.000000000000000000, 0.000000000000000000 ) ) ;
#58134=CARTESIAN_POINT ( 'NONE',  ( -10.00000000000000178, 0.000000000000000000, 0.000000000000000000 ) ) ;
#58138=ORIENTED_EDGE ( 'NONE', *, *, #49416, .T. ) ;
#58139=VECTOR ( 'NONE', #24527, 1000.000000000000000 ) ;
#58143=CARTESIAN_POINT ( 'NONE',  ( -22.28121537037576871, -1.565596675942153571, 3.345440028056702264 ) ) ;
#58144=ORIENTED_EDGE ( 'NONE', *, *, #37851, .F. ) ;
#58145=DIRECTION ( 'NONE',  ( -1.000000000000000000, 0.000000000000000000, 0.000000000000000000 ) ) ;
#58157=CARTESIAN_POINT ( 'NONE',  ( -22.27721056931765631, -2.768264578996974645, 2.427163553894365666 ) ) ;
#58163=ORIENTED_EDGE ( 'NONE', *, *, #58670, .T. ) ;
#58165=CARTESIAN_POINT ( 'NONE',  ( -22.27721688985630522, 2.843753050855884368, -2.338410344701251642 ) ) ;
#58183=ADVANCED_FACE ( 'NONE', ( #64996 ), #23463, .T. ) ;
#58207=CARTESIAN_POINT ( 'NONE',  ( -22.27706485742869091, -2.154081322712202873, -2.985151051101508468 ) ) ;
#58229=DIRECTION ( 'NONE',  ( -1.000000000000000000, 0.000000000000000000, 0.000000000000000000 ) ) ;
#58232=CARTESIAN_POINT ( 'NONE',  ( -22.28546858134833286, 3.592117891549500452, 0.9133285433746399784 ) ) ;
#58239=LINE ( 'NONE', #2397, #31715 ) ;
#58242=EDGE_CURVE ( 'NONE', #28860, #14144, #56192, .T. ) ;
#58247=B_SPLINE_CURVE_WITH_KNOTS ( 'NONE', 3,
 ( #52643, #18033, #38297, #48629, #63562, #58274 ),
 .UNSPECIFIED., .F., .F.,
 ( 4, 2, 4 ),
 ( 0.0002637379172192655451, 0.0009975831966643378297, 0.001731428476109410277 ),
 .UNSPECIFIED. ) ;
#58260=ORIENTED_EDGE ( 'NONE', *, *, #4123, .T. ) ;
#58269=CARTESIAN_POINT ( 'NONE',  ( -27.08421723179412410, -0.6782017488087908053, 2.188590898430377685 ) ) ;
#58274=CARTESIAN_POINT ( 'NONE',  ( -22.31328051695926007, -0.8849444482787947042, 3.685074213229300621 ) ) ;
#58282=CARTESIAN_POINT ( 'NONE',  ( -22.27945548916780183, 3.673577025288763398, -0.3299677273100581343 ) ) ;
#58309=ORIENTED_EDGE ( 'NONE', *, *, #41018, .F. ) ;
#58320=AXIS2_PLACEMENT_3D ( 'NONE', #35000, #18547, #33146 ) ;
#58321=ORIENTED_EDGE ( 'NONE', *, *, #56338, .T. ) ;
#58326=ADVANCED_FACE ( 'NONE', ( #25290 ), #41896, .T. ) ;
#58327=DIRECTION ( 'NONE',  ( 1.000000000000000000, 0.000000000000000000, 0.000000000000000000 ) ) ;
#58328=CARTESIAN_POINT ( 'NONE',  ( 2.000000000000001776, -6.906413915731192787, 0.6453518998147164121 ) ) ;
#58331=CARTESIAN_POINT ( 'NONE',  ( -22.27756824490284515, 0.9472004376381394364, 3.558840239148765239 ) ) ;
#58332=DIRECTION ( 'NONE',  ( 0.000000000000000000, 0.000000000000000000, 1.000000000000000000 ) ) ;
#58337=CARTESIAN_POINT ( 'NONE',  ( -35.04643116707788408, -0.01135624435144415301, -0.004425962698870883338 ) ) ;
#58338=EDGE_CURVE ( 'NONE', #25841, #4330, #31275, .T. ) ;
#58343=CIRCLE ( 'NONE', #60463, 7.499999999999988454 ) ;
#58344=FACE_OUTER_BOUND ( 'NONE', #27587, .T. ) ;
#58350=EDGE_CURVE ( 'NONE', #63668, #10675, #16635, .T. ) ;
#58353=DIRECTION ( 'NONE',  ( 0.000000000000000000, 0.6051742151937609115, 0.7960930657056469739 ) ) ;
#58355=AXIS2_PLACEMENT_3D ( 'NONE', #26950, #7303, #58531 ) ;
#58361=ORIENTED_EDGE ( 'NONE', *, *, #34679, .T. ) ;
#58362=EDGE_CURVE ( 'NONE', #4327, #30401, #13697, .T. ) ;
#58363=CARTESIAN_POINT ( 'NONE',  ( -10.00000000000000178, 0.000000000000000000, 0.000000000000000000 ) ) ;
#58372=CARTESIAN_POINT ( 'NONE',  ( 2.000000000000001776, 4.409940824963425321, 5.354199675985255702 ) ) ;
#58378=CARTESIAN_POINT ( 'NONE',  ( -10.00000000000000178, 0.000000000000000000, 0.000000000000000000 ) ) ;
#58383=ORIENTED_EDGE ( 'NONE', *, *, #25284, .F. ) ;
#58384=EDGE_LOOP ( 'NONE', ( #43489, #40740, #33903, #104 ) ) ;
#58400=VERTEX_POINT ( 'NONE', #40922 ) ;
#58406=CARTESIAN_POINT ( 'NONE',  ( 2.000000000000001776, -3.786546189469212731, 5.663561025469122434 ) ) ;
#58414=CARTESIAN_POINT ( 'NONE',  ( -10.00000000000000178, 0.000000000000000000, 0.000000000000000000 ) ) ;
#58419=CARTESIAN_POINT ( 'NONE',  ( 2.000000000000001776, -5.814643797626954935, 3.550179297009551149 ) ) ;
#58420=ADVANCED_FACE ( 'NONE', ( #26602 ), #23697, .F. ) ;
#58425=VERTEX_POINT ( 'NONE', #21635 ) ;
#58426=DIRECTION ( 'NONE',  ( 0.000000000000000000, 0.000000000000000000, -1.000000000000000000 ) ) ;
#58428=DIRECTION ( 'NONE',  ( 0.000000000000000000, 0.000000000000000000, 1.000000000000000000 ) ) ;
#58430=CARTESIAN_POINT ( 'NONE',  ( -27.10128162969864007, -2.102429195190290034, -1.032914450115358651 ) ) ;
#58432=ORIENTED_EDGE ( 'NONE', *, *, #50921, .F. ) ;
#58434=CARTESIAN_POINT ( 'NONE',  ( -22.71097035706202405, -0.4203397252017116448, 4.965150228107737540 ) ) ;
#58441=ORIENTED_EDGE ( 'NONE', *, *, #30030, .T. ) ;
#58448=CARTESIAN_POINT ( 'NONE',  ( 0.000000000000000000, 0.000000000000000000, 0.000000000000000000 ) ) ;
#58449=B_SPLINE_CURVE_WITH_KNOTS ( 'NONE', 3,
 ( #2250, #32479, #28479, #48143, #32800, #63086, #42128, #42444, #13203, #7213 ),
 .UNSPECIFIED., .F., .F.,
 ( 4, 3, 3, 4 ),
 ( 5.401523115762181559E-05, 0.0008136511341527790341, 0.004068255670953091485, 0.005063778443040924809 ),
 .UNSPECIFIED. ) ;
#58455=ORIENTED_EDGE ( 'NONE', *, *, #27331, .F. ) ;
#58459=DIRECTION ( 'NONE',  ( -1.000000000000000000, 0.000000000000000000, 0.000000000000000000 ) ) ;
#58465=ORIENTED_EDGE ( 'NONE', *, *, #64184, .T. ) ;
#58471=CARTESIAN_POINT ( 'NONE',  ( 2.000000000000001776, -5.769711778877344877, 4.791703871138500936 ) ) ;
#58473=CARTESIAN_POINT ( 'NONE',  ( -28.67667724226168602, -0.8389685652161974483, 1.695959153103712369 ) ) ;
#58479=ORIENTED_EDGE ( 'NONE', *, *, #20389, .F. ) ;
#58482=EDGE_CURVE ( 'NONE', #15892, #49980, #38143, .T. ) ;
#58484=ORIENTED_EDGE ( 'NONE', *, *, #38461, .F. ) ;
#58489=CARTESIAN_POINT ( 'NONE',  ( -27.10719052120871098, -1.622102031466687189, 1.714424047991066846 ) ) ;
#58491=CARTESIAN_POINT ( 'NONE',  ( 2.000000000000001776, 0.000000000000000000, 0.000000000000000000 ) ) ;
#58501=EDGE_CURVE ( 'NONE', #3623, #59877, #52557, .T. ) ;
#58502=CARTESIAN_POINT ( 'NONE',  ( -22.27834755396593991, -3.434702243602655081, -1.338300169228714420 ) ) ;
#58506=CARTESIAN_POINT ( 'NONE',  ( -27.08416813689868263, 1.467601568343278595, 1.759517419957071782 ) ) ;
#58513=CIRCLE ( 'NONE', #63739, 6.936499999999988120 ) ;
#58514=AXIS2_PLACEMENT_3D ( 'NONE', #36632, #51293, #46941 ) ;
#58519=CIRCLE ( 'NONE', #54389, 7.499999999999988454 ) ;
#58522=CARTESIAN_POINT ( 'NONE',  ( 2.000000000000001776, 0.000000000000000000, 0.000000000000000000 ) ) ;
#58526=CARTESIAN_POINT ( 'NONE',  ( -22.27706485742869091, -2.625261754997692876, 2.580541389029905819 ) ) ;
#58529=CARTESIAN_POINT ( 'NONE',  ( -22.49803948133826381, -2.073427785788362510, 3.817825231362851568 ) ) ;
#58531=DIRECTION ( 'NONE',  ( 0.000000000000000000, 0.000000000000000000, 1.000000000000000000 ) ) ;
#58538=AXIS2_PLACEMENT_3D ( 'NONE', #17777, #12765, #16474 ) ;
#58551=ORIENTED_EDGE ( 'NONE', *, *, #821, .F. ) ;
#58554=AXIS2_PLACEMENT_3D ( 'NONE', #18237, #48500, #2952 ) ;
#58559=DIRECTION ( 'NONE',  ( 0.000000000000000000, 0.000000000000000000, 1.000000000000000000 ) ) ;
#58560=VECTOR ( 'NONE', #7719, 1000.000000000000227 ) ;
#58561=CARTESIAN_POINT ( 'NONE',  ( -22.29479313954897890, -0.2707859422896734536, -3.724550806388652546 ) ) ;
#58565=CYLINDRICAL_SURFACE ( 'NONE', #13732, 6.936499999999988120 ) ;
#58566=CARTESIAN_POINT ( 'NONE',  ( 2.000000000000001776, 5.585096664091945939, 4.113602740025928739 ) ) ;
#58574=AXIS2_PLACEMENT_3D ( 'NONE', #65087, #64748, #14223 ) ;
#58576=LINE ( 'NONE', #57587, #34093 ) ;
#58589=LINE ( 'NONE', #37632, #31933 ) ;
#58591=AXIS2_PLACEMENT_3D ( 'NONE', #5466, #31370, #61295 ) ;
#58594=DIRECTION ( 'NONE',  ( -1.000000000000000000, 0.000000000000000000, 0.000000000000000000 ) ) ;
#58597=CIRCLE ( 'NONE', #28801, 2.899999999999996803 ) ;
#58600=ORIENTED_EDGE ( 'NONE', *, *, #20045, .T. ) ;
#58617=CARTESIAN_POINT ( 'NONE',  ( -27.08421860617808008, -0.8768262158915691717, 2.116856729767842005 ) ) ;
#58625=CIRCLE ( 'NONE', #28891, 2.899999999999994138 ) ;
#58628=CARTESIAN_POINT ( 'NONE',  ( 0.000000000000000000, -7.203928197742102135, 2.086484728383119158 ) ) ;
#58633=DIRECTION ( 'NONE',  ( -1.000000000000000000, 0.000000000000000000, 0.000000000000000000 ) ) ;
#58638=CARTESIAN_POINT ( 'NONE',  ( -22.29115169517546136, -3.355084543108104889, -1.614783311161204216 ) ) ;
#58645=DIRECTION ( 'NONE',  ( 0.000000000000000000, 0.000000000000000000, 1.000000000000000000 ) ) ;
#58648=EDGE_CURVE ( 'NONE', #56217, #10610, #19586, .T. ) ;
#58653=LINE ( 'NONE', #49338, #31990 ) ;
#58654=EDGE_CURVE ( 'NONE', #3120, #45709, #19084, .T. ) ;
#58663=DIRECTION ( 'NONE',  ( 0.000000000000000000, 0.000000000000000000, 1.000000000000000000 ) ) ;
#58664=DIRECTION ( 'NONE',  ( -1.000000000000000000, 0.000000000000000000, 0.000000000000000000 ) ) ;
#58665=CARTESIAN_POINT ( 'NONE',  ( -22.28694879868232448, -3.597828382597544117, -0.9088670759108156139 ) ) ;
#58668=DIRECTION ( 'NONE',  ( 0.000000000000000000, 0.8835120444460210498, 0.4684084406997938155 ) ) ;
#58669=VERTEX_POINT ( 'NONE', #3965 ) ;
#58670=EDGE_CURVE ( 'NONE', #42390, #6062, #24228, .T. ) ;
#58674=CYLINDRICAL_SURFACE ( 'NONE', #39150, 7.499999999999988454 ) ;
#58677=CARTESIAN_POINT ( 'NONE',  ( -22.29115169517546136, 2.098196790595542094, 3.075985640626778927 ) ) ;
#58692=DIRECTION ( 'NONE',  ( 0.000000000000000000, 0.5155538571770172940, 0.8568571761675919385 ) ) ;
#58702=EDGE_CURVE ( 'NONE', #62401, #11425, #10564, .T. ) ;
#58713=DIRECTION ( 'NONE',  ( -1.000000000000000000, 0.000000000000000000, 0.000000000000000000 ) ) ;
#58714=VERTEX_POINT ( 'NONE', #15230 ) ;
#58721=CIRCLE ( 'NONE', #36391, 2.899999999999995470 ) ;
#58732=CIRCLE ( 'NONE', #42891, 6.936499999999989896 ) ;
#58745=CARTESIAN_POINT ( 'NONE',  ( -22.27722019094931127, -0.6491642780571716953, -3.623977093944210637 ) ) ;
#58761=ORIENTED_EDGE ( 'NONE', *, *, #21396, .F. ) ;
#58769=CARTESIAN_POINT ( 'NONE',  ( 0.000000000000000000, 0.000000000000000000, 0.000000000000000000 ) ) ;
#58773=CYLINDRICAL_SURFACE ( 'NONE', #61682, 2.899999999999994582 ) ;
#58786=CARTESIAN_POINT ( 'NONE',  ( -27.08418179957658367, -0.4604195552868174390, -2.244544746853593065 ) ) ;
#58790=CARTESIAN_POINT ( 'NONE',  ( -27.08419797710328325, 1.803546201758821743, -1.413289504316735501 ) ) ;
#58808=DIRECTION ( 'NONE',  ( -1.000000000000000000, 0.000000000000000000, 0.000000000000000000 ) ) ;
#58811=AXIS2_PLACEMENT_3D ( 'NONE', #26581, #47532, #41877 ) ;
#58822=DIRECTION ( 'NONE',  ( -1.000000000000000000, 0.000000000000000000, 0.000000000000000000 ) ) ;
#58828=FACE_OUTER_BOUND ( 'NONE', #13421, .T. ) ;
#58831=DIRECTION ( 'NONE',  ( 0.000000000000000000, 0.000000000000000000, 1.000000000000000000 ) ) ;
#58832=EDGE_LOOP ( 'NONE', ( #40344, #60507, #33910, #33452 ) ) ;
#58838=EDGE_CURVE ( 'NONE', #25850, #8080, #13745, .T. ) ;
#58841=CARTESIAN_POINT ( 'NONE',  ( -27.09364415740217424, -2.313349100776211920, 0.1694361397562745286 ) ) ;
#58844=ADVANCED_FACE ( 'NONE', ( #42124 ), #58070, .F. ) ;
#58848=DIRECTION ( 'NONE',  ( 1.000000000000000000, 1.685093406416449860E-16, -1.011030131491573426E-17 ) ) ;
#58853=CARTESIAN_POINT ( 'NONE',  ( -22.39032720737626647, 2.746561316202170921, -2.936932155721168503 ) ) ;
#58854=CIRCLE ( 'NONE', #22705, 2.899999999999994582 ) ;
#58855=CARTESIAN_POINT ( 'NONE',  ( 2.000000000000001776, 4.962980376314068742, 4.846014654777798469 ) ) ;
#58856=CARTESIAN_POINT ( 'NONE',  ( -27.08429572838383947, 1.608131779585724619, 1.632445743623414325 ) ) ;
#58859=AXIS2_PLACEMENT_3D ( 'NONE', #5477, #31382, #11418 ) ;
#58920=CARTESIAN_POINT ( 'NONE',  ( -22.27706485742869091, 3.547445275915927176, 0.9832726768967369191 ) ) ;
#58948=CARTESIAN_POINT ( 'NONE',  ( 2.000000000000001776, 2.562706407243739992, -6.312399813420325856 ) ) ;
#58950=CARTESIAN_POINT ( 'NONE',  ( -27.08423923533013422, -0.8983804370399710582, 2.107995711831558872 ) ) ;
#58953=LINE ( 'NONE', #23689, #13419 ) ;
#58957=CARTESIAN_POINT ( 'NONE',  ( -22.71097035706202760, 2.118550233809425087, 4.510116093748266053 ) ) ;
#58960=CARTESIAN_POINT ( 'NONE',  ( -28.66013792860432119, -1.770123732198272570, -0.4872053345172134842 ) ) ;
#58962=ORIENTED_EDGE ( 'NONE', *, *, #64914, .F. ) ;
#58964=ORIENTED_EDGE ( 'NONE', *, *, #52622, .F. ) ;
#58966=ORIENTED_EDGE ( 'NONE', *, *, #61952, .F. ) ;
#58967=VERTEX_POINT ( 'NONE', #44407 ) ;
#58969=CARTESIAN_POINT ( 'NONE',  ( -22.29677679919927868, -3.364642266483117705, -1.633785040807715250 ) ) ;
#58981=CARTESIAN_POINT ( 'NONE',  ( 1.000000000000000888, -6.997684042076877553, -2.698595569414293127 ) ) ;
#58994=CARTESIAN_POINT ( 'NONE',  ( 0.000000000000000000, -3.073484823194374993, 6.841322316745024779 ) ) ;
#58995=ORIENTED_EDGE ( 'NONE', *, *, #9556, .T. ) ;
#59008=VERTEX_POINT ( 'NONE', #8520 ) ;
#59017=ADVANCED_FACE ( 'NONE', ( #39105 ), #34108, .T. ) ;
#59019=ADVANCED_FACE ( 'NONE', ( #26046 ), #1167, .F. ) ;
#59022=LINE ( 'NONE', #13434, #28285 ) ;
#59027=ORIENTED_EDGE ( 'NONE', *, *, #15319, .F. ) ;
#59032=ORIENTED_EDGE ( 'NONE', *, *, #60632, .F. ) ;
#59036=ORIENTED_EDGE ( 'NONE', *, *, #57655, .F. ) ;
#59063=VERTEX_POINT ( 'NONE', #24811 ) ;
#59064=CARTESIAN_POINT ( 'NONE',  ( -22.27711653538342773, 0.4190680140413665655, 3.657713416444722920 ) ) ;
#59075=CARTESIAN_POINT ( 'NONE',  ( -22.28023996335807411, 3.022323476748291604, -2.118259050016077616 ) ) ;
#59081=ORIENTED_EDGE ( 'NONE', *, *, #28374, .T. ) ;
#59084=ADVANCED_FACE ( 'NONE', ( #41310 ), #27023, .T. ) ;
#59087=ADVANCED_FACE ( 'NONE', ( #61278 ), #3314, .F. ) ;
#59091=LINE ( 'NONE', #27831, #56770 ) ;
#59092=DIRECTION ( 'NONE',  ( 0.000000000000000000, 0.000000000000000000, 1.000000000000000000 ) ) ;
#59100=AXIS2_PLACEMENT_3D ( 'NONE', #50032, #14432, #20421 ) ;
#59101=DIRECTION ( 'NONE',  ( -1.000000000000000000, 0.000000000000000000, 0.000000000000000000 ) ) ;
#59107=EDGE_CURVE ( 'NONE', #37744, #35944, #7373, .T. ) ;
#59110=CARTESIAN_POINT ( 'NONE',  ( 1.000000000000000888, -4.472310526050796931, 6.020667617347345235 ) ) ;
#59113=ADVANCED_FACE ( 'NONE', ( #38291 ), #48315, .T. ) ;
#59117=CARTESIAN_POINT ( 'NONE',  ( 2.000000000000001776, 4.962980376314141573, -4.846014654777754060 ) ) ;
#59119=ORIENTED_EDGE ( 'NONE', *, *, #9835, .T. ) ;
#59123=DIRECTION ( 'NONE',  ( 0.000000000000000000, -0.4198891015602717602, 0.9075754196709537869 ) ) ;
#59127=CARTESIAN_POINT ( 'NONE',  ( -22.71097035706202405, 4.089776368546564456, 2.846599994298306679 ) ) ;
#59132=( NAMED_UNIT ( * ) PLANE_ANGLE_UNIT ( ) SI_UNIT ( $, .RADIAN. ) );
#59133=CARTESIAN_POINT ( 'NONE',  ( -27.10719052120871098, -0.1538293304135310291, -2.355164825213519109 ) ) ;
#59140=ORIENTED_EDGE ( 'NONE', *, *, #64446, .F. ) ;
#59148=CARTESIAN_POINT ( 'NONE',  ( -27.08776759928997180, -1.611072893085645275, 1.644157618165822621 ) ) ;
#59160=CARTESIAN_POINT ( 'NONE',  ( 2.000000000000001776, 0.000000000000000000, 0.000000000000000000 ) ) ;
#59161=CARTESIAN_POINT ( 'NONE',  ( -27.09030469827931853, 1.608164674722576848, -1.657623467486017299 ) ) ;
#59162=LINE ( 'NONE', #49194, #2213 ) ;
#59163=FACE_OUTER_BOUND ( 'NONE', #2067, .T. ) ;
#59169=CARTESIAN_POINT ( 'NONE',  ( 0.000000000000000000, 7.248432822490286753, -1.926193556692960440 ) ) ;
#59179=CARTESIAN_POINT ( 'NONE',  ( -22.29018399051993882, 2.675685774027749986, 2.585196332786354301 ) ) ;
#59181=DIRECTION ( 'NONE',  ( 0.000000000000000000, 0.000000000000000000, 1.000000000000000000 ) ) ;
#59182=ORIENTED_EDGE ( 'NONE', *, *, #6500, .T. ) ;
#59199=CYLINDRICAL_SURFACE ( 'NONE', #63638, 2.899999999999994582 ) ;
#59201=VERTEX_POINT ( 'NONE', #702 ) ;
#59205=ORIENTED_EDGE ( 'NONE', *, *, #45799, .T. ) ;
#59206=EDGE_CURVE ( 'NONE', #30137, #30073, #10329, .T. ) ;
#59207=CYLINDRICAL_SURFACE ( 'NONE', #8150, 2.899999999999994582 ) ;
#59209=ORIENTED_EDGE ( 'NONE', *, *, #52025, .T. ) ;
#59211=CARTESIAN_POINT ( 'NONE',  ( -27.10719052120871098, 1.622102031466687189, -1.714424047991080613 ) ) ;
#59221=FACE_OUTER_BOUND ( 'NONE', #17823, .T. ) ;
#59223=CARTESIAN_POINT ( 'NONE',  ( -22.27710395300133683, 3.549456197028686866, 0.9764373854728822799 ) ) ;
#59224=DIRECTION ( 'NONE',  ( 0.000000000000000000, 0.000000000000000000, 1.000000000000000000 ) ) ;
#59231=DIRECTION ( 'NONE',  ( 0.000000000000000000, 0.000000000000000000, 1.000000000000000000 ) ) ;
#59237=AXIS2_PLACEMENT_3D ( 'NONE', #40389, #60693, #34737 ) ;
#59243=ORIENTED_EDGE ( 'NONE', *, *, #55857, .T. ) ;
#59244=DIRECTION ( 'NONE',  ( -1.000000000000000000, 0.000000000000000000, 0.000000000000000000 ) ) ;
#59246=CARTESIAN_POINT ( 'NONE',  ( -27.08416781016246588, 2.158663327075696081, 0.7680651426971605300 ) ) ;
#59256=DIRECTION ( 'NONE',  ( -1.000000000000000000, 0.000000000000000000, 0.000000000000000000 ) ) ;
#59257=FACE_OUTER_BOUND ( 'NONE', #61483, .T. ) ;
#59261=VECTOR ( 'NONE', #53743, 1000.000000000000000 ) ;
#59262=ORIENTED_EDGE ( 'NONE', *, *, #55857, .F. ) ;
#59265=VECTOR ( 'NONE', #48337, 1000.000000000000000 ) ;
#59267=CARTESIAN_POINT ( 'NONE',  ( 2.000000000000001776, 0.000000000000000000, 0.000000000000000000 ) ) ;
#59268=CARTESIAN_POINT ( 'NONE',  ( -22.27722015946438816, -3.628085906632222635, 0.6262261846986550973 ) ) ;
#59273=ORIENTED_EDGE ( 'NONE', *, *, #60717, .F. ) ;
#59277=CARTESIAN_POINT ( 'NONE',  ( -22.27719412087655471, -2.283949229175425533, -2.887588494201234202 ) ) ;
#59290=ORIENTED_EDGE ( 'NONE', *, *, #39939, .T. ) ;
#59300=AXIS2_PLACEMENT_3D ( 'NONE', #25504, #4919, #35789 ) ;
#59302=ORIENTED_EDGE ( 'NONE', *, *, #30597, .T. ) ;
#59303=EDGE_CURVE ( 'NONE', #48610, #26353, #53111, .T. ) ;
#59305=CARTESIAN_POINT ( 'NONE',  ( 2.000000000000001776, -7.493043167941588756, -0.3229614270520431152 ) ) ;
#59307=CARTESIAN_POINT ( 'NONE',  ( 0.000000000000000000, 3.979254915827449945, -5.681598592373734213 ) ) ;
#59308=CARTESIAN_POINT ( 'NONE',  ( -22.29479313954897890, 2.096782908204907869, 3.090162644873513997 ) ) ;
#59313=CIRCLE ( 'NONE', #43345, 3.552075659825890241 ) ;
#59339=CARTESIAN_POINT ( 'NONE',  ( 2.000000000000001776, 0.08317740279932192560, 7.499538753794337431 ) ) ;
#59340=CARTESIAN_POINT ( 'NONE',  ( -27.20164183316783024, -1.232966507052636329, 2.339520810540414164 ) ) ;
#59343=CARTESIAN_POINT ( 'NONE',  ( -22.30625920655495165, -0.2529928606556531290, -3.783486345733990674 ) ) ;
#59349=AXIS2_PLACEMENT_3D ( 'NONE', #30298, #14980, #24989 ) ;
#59350=DIRECTION ( 'NONE',  ( -1.000000000000000000, 0.000000000000000000, 0.000000000000000000 ) ) ;
#59351=CARTESIAN_POINT ( 'NONE',  ( 2.000000000000001776, -3.230174184210014232, -5.998318953995379843 ) ) ;
#59354=EDGE_LOOP ( 'NONE', ( #33187, #51011, #60202, #64525 ) ) ;
#59355=AXIS2_PLACEMENT_3D ( 'NONE', #50152, #24209, #44475 ) ;
#59360=AXIS2_PLACEMENT_3D ( 'NONE', #56027, #10468, #29759 ) ;
#59374=EDGE_CURVE ( 'NONE', #4778, #37616, #14818, .T. ) ;
#59375=VERTEX_POINT ( 'NONE', #53861 ) ;
#59379=CARTESIAN_POINT ( 'NONE',  ( -22.28482751661422867, 3.048214341614492451, -2.105139449411404851 ) ) ;
#59388=DIRECTION ( 'NONE',  ( -1.000000000000000000, 0.000000000000000000, 0.000000000000000000 ) ) ;
#59392=DIRECTION ( 'NONE',  ( -1.000000000000000000, 0.000000000000000000, 0.000000000000000000 ) ) ;
#59393=EDGE_CURVE ( 'NONE', #34255, #29292, #38802, .T. ) ;
#59401=CARTESIAN_POINT ( 'NONE',  ( -23.18047892478189453, -0.4043282704081303525, 4.776019214182007921 ) ) ;
#59403=CIRCLE ( 'NONE', #54142, 7.499999999999988454 ) ;
#59404=AXIS2_PLACEMENT_3D ( 'NONE', #14956, #64216, #49906 ) ;
#59417=ADVANCED_FACE ( 'NONE', ( #27266 ), #2345, .T. ) ;
#59419=CARTESIAN_POINT ( 'NONE',  ( 2.000000000000001776, -6.796153407501424049, -1.388283512725909219 ) ) ;
#59428=CARTESIAN_POINT ( 'NONE',  ( -22.71097035706202405, -4.089776368546547580, -2.846599994298351977 ) ) ;
#59442=ORIENTED_EDGE ( 'NONE', *, *, #44345, .T. ) ;
#59445=ADVANCED_FACE ( 'NONE', ( #53201 ), #43529, .T. ) ;
#59449=CARTESIAN_POINT ( 'NONE',  ( 0.000000000000000000, 0.000000000000000000, 0.000000000000000000 ) ) ;
#59450=ADVANCED_FACE ( 'NONE', ( #22271 ), #53549, .T. ) ;
#59453=ORIENTED_EDGE ( 'NONE', *, *, #49553, .T. ) ;
#59458=FACE_OUTER_BOUND ( 'NONE', #31678, .T. ) ;
#59462=ADVANCED_FACE ( 'NONE', ( #47557 ), #49843, .T. ) ;
#59468=CARTESIAN_POINT ( 'NONE',  ( -27.08850691366518504, 1.609738257842381559, -1.648570643966305260 ) ) ;
#59469=CARTESIAN_POINT ( 'NONE',  ( -27.08426571771018132, 1.357728109767524005, 1.845988025802319132 ) ) ;
#59470=CARTESIAN_POINT ( 'NONE',  ( 2.000000000000001776, -2.562706407243680928, 6.312399813420318750 ) ) ;
#59473=AXIS2_PLACEMENT_3D ( 'NONE', #32249, #32558, #48551 ) ;
#59475=DIRECTION ( 'NONE',  ( -1.000000000000000000, 0.000000000000000000, 0.000000000000000000 ) ) ;
#59476=EDGE_CURVE ( 'NONE', #14064, #43917, #55238, .T. ) ;
#59485=ORIENTED_EDGE ( 'NONE', *, *, #6262, .F. ) ;
#59489=CARTESIAN_POINT ( 'NONE',  ( -22.28415773361649954, 2.647149619609392879, 2.588610893123033829 ) ) ;
#59492=CARTESIAN_POINT ( 'NONE',  ( 2.000000000000001776, -6.643843315911796665, -1.507714007300762660 ) ) ;
#59499=FACE_OUTER_BOUND ( 'NONE', #61609, .T. ) ;
#59502=ORIENTED_EDGE ( 'NONE', *, *, #16801, .T. ) ;
#59513=ADVANCED_FACE ( 'NONE', ( #45177 ), #24567, .T. ) ;
#59514=ORIENTED_EDGE ( 'NONE', *, *, #64446, .T. ) ;
#59515=ORIENTED_EDGE ( 'NONE', *, *, #1550, .F. ) ;
#59523=CARTESIAN_POINT ( 'NONE',  ( 2.000000000000001776, 6.164400007374783108, 2.900694413976516728 ) ) ;
#59529=ORIENTED_EDGE ( 'NONE', *, *, #43699, .F. ) ;
#59532=EDGE_CURVE ( 'NONE', #1460, #42144, #23403, .T. ) ;
#59533=ORIENTED_EDGE ( 'NONE', *, *, #14342, .F. ) ;
#59534=CARTESIAN_POINT ( 'NONE',  ( 0.000000000000000000, 3.805198749487436416, 5.799611601383225512 ) ) ;
#59544=EDGE_LOOP ( 'NONE', ( #6248, #49522, #51678, #13582 ) ) ;
#59548=CYLINDRICAL_SURFACE ( 'NONE', #31664, 2.899999999999994582 ) ;
#59554=CARTESIAN_POINT ( 'NONE',  ( 2.000000000000001776, -6.997684042076874000, -2.698595569414309114 ) ) ;
#59559=EDGE_CURVE ( 'NONE', #26907, #32446, #65442, .T. ) ;
#59565=ADVANCED_FACE ( 'NONE', ( #64782 ), #29871, .T. ) ;
#59570=CARTESIAN_POINT ( 'NONE',  ( -35.05175862995318425, -0.01212835938694395432, 0.003331684148533478607 ) ) ;
#59573=CIRCLE ( 'NONE', #30880, 2.899999999999995914 ) ;
#59579=CARTESIAN_POINT ( 'NONE',  ( 2.000000000000001776, 0.000000000000000000, 0.000000000000000000 ) ) ;
#59590=CARTESIAN_POINT ( 'NONE',  ( 2.000000000000001776, 4.570217215903443986, -5.218059682435596258 ) ) ;
#59606=ORIENTED_EDGE ( 'NONE', *, *, #46278, .T. ) ;
#59620=CARTESIAN_POINT ( 'NONE',  ( -35.05012975565874456, 0.01323209221895734096, 0.004360246756757623493 ) ) ;
#59623=DIRECTION ( 'NONE',  ( 0.000000000000000000, 0.000000000000000000, 1.000000000000000000 ) ) ;
#59628=DIRECTION ( 'NONE',  ( 1.000000000000000000, 0.000000000000000000, 0.000000000000000000 ) ) ;
#59639=CARTESIAN_POINT ( 'NONE',  ( -22.31099767395441091, 1.667781795950537882, -3.395517675085595766 ) ) ;
#59640=AXIS2_PLACEMENT_3D ( 'NONE', #44708, #44076, #14130 ) ;
#59645=AXIS2_PLACEMENT_3D ( 'NONE', #13283, #54510, #28897 ) ;
#59648=FACE_BOUND ( 'NONE', #53835, .T. ) ;
#59651=CARTESIAN_POINT ( 'NONE',  ( -22.27218376572352554, 2.099017427146268044, 3.026314224080933091 ) ) ;
#59655=DIRECTION ( 'NONE',  ( -1.000000000000000000, 0.000000000000000000, 0.000000000000000000 ) ) ;
#59669=CARTESIAN_POINT ( 'NONE',  ( -35.04709527796842394, -0.005220632201001842998, -0.01120703303053409428 ) ) ;
#59682=DIRECTION ( 'NONE',  ( 0.000000000000000000, 0.000000000000000000, 1.000000000000000000 ) ) ;
#59687=CARTESIAN_POINT ( 'NONE',  ( -22.30625920655495165, -3.403091720605013748, -1.672644928563079780 ) ) ;
#59691=VERTEX_POINT ( 'NONE', #25891 ) ;
#59692=CARTESIAN_POINT ( 'NONE',  ( -22.71097035706202405, -2.846599994298329328, 4.089776368546542251 ) ) ;
#59693=VECTOR ( 'NONE', #10226, 1000.000000000000000 ) ;
#59697=B_SPLINE_CURVE_WITH_KNOTS ( 'NONE', 3,
 ( #55826, #60467, #14892, #35184, #44508, #39534, #10251, #30531, #65763, #20233 ),
 .UNSPECIFIED., .F., .F.,
 ( 4, 3, 3, 4 ),
 ( 5.401523115762577292E-05, 0.0008136511341527794677, 0.004068255670953088016, 0.005063778443040924809 ),
 .UNSPECIFIED. ) ;
#59705=ORIENTED_EDGE ( 'NONE', *, *, #61789, .T. ) ;
#59708=DIRECTION ( 'NONE',  ( 0.000000000000000000, 0.000000000000000000, 1.000000000000000000 ) ) ;
#59711=CARTESIAN_POINT ( 'NONE',  ( 0.000000000000000000, -1.754183803416586196, 6.711026108862235162 ) ) ;
#59713=EDGE_CURVE ( 'NONE', #50166, #21169, #35, .T. ) ;
#59728=CIRCLE ( 'NONE', #267, 6.936499999999991672 ) ;
#59730=DIRECTION ( 'NONE',  ( -1.000000000000000000, 0.000000000000000000, 0.000000000000000000 ) ) ;
#59739=AXIS2_PLACEMENT_3D ( 'NONE', #64755, #34516, #39503 ) ;
#59747=EDGE_CURVE ( 'NONE', #6336, #21047, #4954, .T. ) ;
#59751=AXIS2_PLACEMENT_3D ( 'NONE', #20078, #15078, #35358 ) ;
#59756=EDGE_CURVE ( 'NONE', #11939, #26744, #26525, .T. ) ;
#59765=EDGE_CURVE ( 'NONE', #48378, #37589, #54603, .T. ) ;
#59773=AXIS2_PLACEMENT_3D ( 'NONE', #25312, #50925, #50281 ) ;
#59775=EDGE_CURVE ( 'NONE', #49587, #24086, #1144, .T. ) ;
#59778=CARTESIAN_POINT ( 'NONE',  ( 0.000000000000000000, 0.000000000000000000, 0.000000000000000000 ) ) ;
#59784=LINE ( 'NONE', #38514, #40761 ) ;
#59799=CARTESIAN_POINT ( 'NONE',  ( 1.000000000000000888, -6.936109781200700652, 2.853135311045000400 ) ) ;
#59801=CARTESIAN_POINT ( 'NONE',  ( -27.32337605527166247, 2.988381643048321212, 0.3676050637290654288 ) ) ;
#59803=CIRCLE ( 'NONE', #51327, 7.499999999999988454 ) ;
#59817=CARTESIAN_POINT ( 'NONE',  ( -35.04660725145885891, 0.001288602543501626970, 0.01223081933018644978 ) ) ;
#59828=CIRCLE ( 'NONE', #44960, 2.899999999999995914 ) ;
#59829=VERTEX_POINT ( 'NONE', #48470 ) ;
#59849=ADVANCED_FACE ( 'NONE', ( #17218 ), #63089, .T. ) ;
#59851=LINE ( 'NONE', #14279, #23324 ) ;
#59853=AXIS2_PLACEMENT_3D ( 'NONE', #63627, #38373, #58692 ) ;
#59861=LINE ( 'NONE', #15189, #45353 ) ;
#59867=CARTESIAN_POINT ( 'NONE',  ( -27.08935880048752765, -2.235999130317592343, -0.5666837974575801296 ) ) ;
#59876=AXIS2_PLACEMENT_3D ( 'NONE', #1840, #12129, #7457 ) ;
#59877=VERTEX_POINT ( 'NONE', #63397 ) ;
#59890=ORIENTED_EDGE ( 'NONE', *, *, #15319, .T. ) ;
#59893=LINE ( 'NONE', #19967, #8954 ) ;
#59895=EDGE_CURVE ( 'NONE', #23681, #65266, #19165, .T. ) ;
#59896=EDGE_CURVE ( 'NONE', #22857, #45822, #17550, .T. ) ;
#59900=ORIENTED_EDGE ( 'NONE', *, *, #35965, .T. ) ;
#59904=DIRECTION ( 'NONE',  ( -1.000000000000000000, 0.000000000000000000, 0.000000000000000000 ) ) ;
#59906=ORIENTED_EDGE ( 'NONE', *, *, #12218, .T. ) ;
#59908=EDGE_CURVE ( 'NONE', #26907, #20276, #32964, .T. ) ;
#59921=AXIS2_PLACEMENT_3D ( 'NONE', #43846, #28547, #3300 ) ;
#59926=CARTESIAN_POINT ( 'NONE',  ( -22.27706485742869091, -3.662257305743835012, 0.3729136217356029959 ) ) ;
#59933=ORIENTED_EDGE ( 'NONE', *, *, #48893, .T. ) ;
#59941=CARTESIAN_POINT ( 'NONE',  ( 0.000000000000000000, -4.570217215903394248, 5.218059682435592705 ) ) ;
#59943=CARTESIAN_POINT ( 'NONE',  ( 0.000000000000000000, -5.662015959325143122, -4.918493191654053298 ) ) ;
#59945=CARTESIAN_POINT ( 'NONE',  ( 2.000000000000001776, 0.4129979343798200753, -6.800241778083709221 ) ) ;
#59950=EDGE_CURVE ( 'NONE', #65174, #44673, #9182, .T. ) ;
#59960=CYLINDRICAL_SURFACE ( 'NONE', #21883, 2.899999999999994582 ) ;
#59964=VERTEX_POINT ( 'NONE', #29460 ) ;
#59965=CLOSED_SHELL ( 'NONE', ( #9093, #56754, #3711, #7648, #44018, #59565, #18113, #37833, #56438, #17463, #31951, #56031, #35434, #22845, #10397, #53300, #28649, #10695, #29400, #62683, #51979, #56861, #27937, #26951, #20956, #14402, #42012, #24843, #53147, #44392, #50982, #6142, #59450, #13703, #27233, #50347, #62671, #44718, #28255, #65576, #52582, #42575, #9871, #31968, #44629, #26507, #45244, #51494, #61258, #3786, #45176, #4303, #21165, #15671, #9439, #35132, #41336, #49403, #7070, #42303, #45115, #10565, #36319, #2743, #48618, #37472, #32920, #19352, #19987, #47946, #44162, #3997, #20604, #26413, #47661, #39609, #46445, #34673, #63326, #17521, #38344, #18692, #14023, #61433, #54872, #14057, #745, #2957, #9067, #36656, #38898, #9965, #31410, #7617, #24780, #52927, #65285, #55414, #35993, #61444, #4457, #1784, #19081, #46545, #20133, #12580, #5602, #41306, #58183, #18046, #45075, #56374, #46649, #8386, #51681, #39825, #21705, #46471, #37369, #8411, #62151, #64414, #2696, #45649, #33483, #16100, #15309, #53012, #25215, #10614, #23841, #16373, #62661, #4234, #48437, #22526, #32865, #13238, #23511, #59417, #61128, #64031, #11856, #59017, #52944, #5175, #43583, #31096, #7999, #19132, #59445, #59084, #15376, #61049, #31079, #33966, #45364, #59113, #41474, #19760, #21079, #20469, #18325, #30427, #38598, #47607, #35834, #45816, #16476, #10301, #17562, #15327, #26224, #28441, #12350, #8777, #1444, #11367, #47521, #55793, #57623, #55289, #16969, #13917, #52217, #34437, #19683, #34511, #31594, #6231, #56643, #64242, #46942, #59462, #23651, #969, #1598, #10783, #50902, #25280, #51241, #13916, #44365, #61277, #12729, #21654, #58326, #7590, #4221, #3757, #60645, #51075, #22077, #60096, #36083, #34599, #21780, #11415, #60761, #11949, #44794, #42046, #45794, #4449, #26885, #2496, #15873, #11663, #33329, #24633, #4148, #44857, #61233, #6393, #9936, #34934, #2425, #55720, #31145, #59513, #29950, #35041, #59849, #64300, #24602, #40322, #57058, #60833, #57249, #2187, #51584, #33946, #41888, #61574, #46979, #63781, #33316, #903, #65064, #50070, #16282, #57367, #19238, #5017, #58420, #41005, #25432, #62379, #61352, #17425, #26264, #35887, #23710, #59087, #29290, #22599, #52111, #46910, #53626, #17161, #48816, #25461, #2047, #53356, #43514, #47154, #47326, #33978, #59019, #33942, #24382, #12510, #44941, #3039, #58844, #33424, #45652, #319, #4685, #47288, #47849, #9754, #36484, #36704, #35600, #63495, #20788, #39617, #5059 ) ) ;
#59967=DIRECTION ( 'NONE',  ( -1.000000000000000000, 0.000000000000000000, 0.000000000000000000 ) ) ;
#59970=FACE_OUTER_BOUND ( 'NONE', #40268, .T. ) ;
#59972=CARTESIAN_POINT ( 'NONE',  ( -27.08702828306176258, -2.216258174335476561, 0.6138566972905330488 ) ) ;
#59980=ORIENTED_EDGE ( 'NONE', *, *, #44345, .F. ) ;
#59982=CARTESIAN_POINT ( 'NONE',  ( -10.00000000000000178, 0.000000000000000000, 0.000000000000000000 ) ) ;
#59999=CARTESIAN_POINT ( 'NONE',  ( -22.27706485742869091, 3.547445275915927176, 0.9832726768967369191 ) ) ;
#60005=ORIENTED_EDGE ( 'NONE', *, *, #7443, .T. ) ;
#60014=DIRECTION ( 'NONE',  ( -1.000000000000000000, 0.000000000000000000, 0.000000000000000000 ) ) ;
#60019=ORIENTED_EDGE ( 'NONE', *, *, #45281, .F. ) ;
#60023=CARTESIAN_POINT ( 'NONE',  ( 2.000000000000001776, -6.250523986463956128, -3.007653927006670003 ) ) ;
#60024=VERTEX_POINT ( 'NONE', #852 ) ;
#60026=CARTESIAN_POINT ( 'NONE',  ( -27.20102706715913143, 1.966718264078106682, 1.765193291701696143 ) ) ;
#60034=ORIENTED_EDGE ( 'NONE', *, *, #21921, .T. ) ;
#60042=CARTESIAN_POINT ( 'NONE',  ( 2.000000000000001776, 1.956810415765184219, 6.654767106875543625 ) ) ;
#60055=FACE_OUTER_BOUND ( 'NONE', #43615, .T. ) ;
#60073=ORIENTED_EDGE ( 'NONE', *, *, #16671, .F. ) ;
#60076=CARTESIAN_POINT ( 'NONE',  ( -22.29770266787582500, -1.047554374660435439, -3.593535545924356089 ) ) ;
#60090=ORIENTED_EDGE ( 'NONE', *, *, #35610, .T. ) ;
#60096=ADVANCED_FACE ( 'NONE', ( #46407 ), #42704, .T. ) ;
#60097=DIRECTION ( 'NONE',  ( -1.000000000000000000, 0.000000000000000000, 0.000000000000000000 ) ) ;
#60101=DIRECTION ( 'NONE',  ( 0.000000000000000000, 0.000000000000000000, 1.000000000000000000 ) ) ;
#60113=DIRECTION ( 'NONE',  ( 0.9582930651793755139, 0.01979360193296375928, 0.2851010602429189245 ) ) ;
#60114=EDGE_CURVE ( 'NONE', #65638, #983, #63318, .T. ) ;
#60116=CARTESIAN_POINT ( 'NONE',  ( 2.000000000000001776, -1.754183803416492493, -6.711026108862277795 ) ) ;
#60123=FACE_OUTER_BOUND ( 'NONE', #46304, .T. ) ;
#60134=CYLINDRICAL_SURFACE ( 'NONE', #45820, 2.899999999999994582 ) ;
#60152=DIRECTION ( 'NONE',  ( -1.000000000000000000, 0.000000000000000000, 0.000000000000000000 ) ) ;
#60160=CARTESIAN_POINT ( 'NONE',  ( 2.000000000000001776, -7.484036900328550956, 0.4890722589968952150 ) ) ;
#60170=AXIS2_PLACEMENT_3D ( 'NONE', #42306, #52337, #16734 ) ;
#60176=CARTESIAN_POINT ( 'NONE',  ( -27.10113028276028757, -2.276991616286371478, -0.5479825692854007890 ) ) ;
#60178=VERTEX_POINT ( 'NONE', #32406 ) ;
#60202=ORIENTED_EDGE ( 'NONE', *, *, #33303, .F. ) ;
#60203=ORIENTED_EDGE ( 'NONE', *, *, #47263, .F. ) ;
#60204=EDGE_CURVE ( 'NONE', #13349, #39026, #24528, .T. ) ;
#60214=ORIENTED_EDGE ( 'NONE', *, *, #36659, .F. ) ;
#60218=AXIS2_PLACEMENT_3D ( 'NONE', #41871, #47527, #1658 ) ;
#60231=ORIENTED_EDGE ( 'NONE', *, *, #28748, .F. ) ;
#60232=LINE ( 'NONE', #45272, #63947 ) ;
#60239=ORIENTED_EDGE ( 'NONE', *, *, #64237, .T. ) ;
#60241=CIRCLE ( 'NONE', #37031, 7.499999999999988454 ) ;
#60244=ORIENTED_EDGE ( 'NONE', *, *, #42118, .F. ) ;
#60246=LINE ( 'NONE', #30323, #60820 ) ;
#60256=EDGE_CURVE ( 'NONE', #19077, #2801, #19219, .T. ) ;
#60258=EDGE_LOOP ( 'NONE', ( #56664, #25726, #45632, #19385 ) ) ;
#60263=CYLINDRICAL_SURFACE ( 'NONE', #11005, 6.936499999999988120 ) ;
#60264=CARTESIAN_POINT ( 'NONE',  ( -22.27722019117890895, -0.6493872998088024984, -3.623937139367951588 ) ) ;
#60266=EDGE_CURVE ( 'NONE', #29257, #59691, #49053, .T. ) ;
#60268=CARTESIAN_POINT ( 'NONE',  ( 0.000000000000000000, 6.664893814313728626, 3.439359016433498173 ) ) ;
#60269=CARTESIAN_POINT ( 'NONE',  ( 2.000000000000001776, -4.409940824963459960, 5.354199675985231721 ) ) ;
#60270=CARTESIAN_POINT ( 'NONE',  ( -27.32343372485685862, -2.674948176236188413, 1.382463360572558475 ) ) ;
#60280=CARTESIAN_POINT ( 'NONE',  ( -22.28939870658739864, 1.608176106660567983, -3.352428181135929997 ) ) ;
#60286=CYLINDRICAL_SURFACE ( 'NONE', #36614, 2.899999999999994582 ) ;
#60290=EDGE_CURVE ( 'NONE', #3684, #20446, #29831, .T. ) ;
#60302=CYLINDRICAL_SURFACE ( 'NONE', #24017, 2.899999999999994582 ) ;
#60305=AXIS2_PLACEMENT_3D ( 'NONE', #4247, #40806, #581 ) ;
#60312=ORIENTED_EDGE ( 'NONE', *, *, #18876, .F. ) ;
#60319=ORIENTED_EDGE ( 'NONE', *, *, #56127, .T. ) ;
#60343=ORIENTED_EDGE ( 'NONE', *, *, #43276, .T. ) ;
#60353=CARTESIAN_POINT ( 'NONE',  ( -22.27709082389155171, 1.005749854561714507, -3.541295940224341354 ) ) ;
#60358=CARTESIAN_POINT ( 'NONE',  ( 1.000000000000000888, -2.315790869867103474, 7.133520354428079635 ) ) ;
#60361=EDGE_CURVE ( 'NONE', #8080, #42619, #25573, .T. ) ;
#60370=CARTESIAN_POINT ( 'NONE',  ( 2.000000000000001776, 6.906413915731199005, -0.6453518998146886565 ) ) ;
#60373=CARTESIAN_POINT ( 'NONE',  ( 2.000000000000001776, 6.812627895098307462, -0.04423456934727655609 ) ) ;
#60392=ORIENTED_EDGE ( 'NONE', *, *, #60114, .F. ) ;
#60395=ORIENTED_EDGE ( 'NONE', *, *, #54218, .F. ) ;
#60397=EDGE_CURVE ( 'NONE', #43263, #18227, #5425, .T. ) ;
#60410=SURFACE_STYLE_USAGE ( .BOTH. , #39142 ) ;
#60411=CARTESIAN_POINT ( 'NONE',  ( 2.000000000000001776, 3.979254915827366901, 5.681598592373755530 ) ) ;
#60417=CIRCLE ( 'NONE', #42311, 6.936499999999992561 ) ;
#60421=FACE_OUTER_BOUND ( 'NONE', #10754, .T. ) ;
#60427=CARTESIAN_POINT ( 'NONE',  ( 0.000000000000000000, -1.754183803416492493, -6.711026108862277795 ) ) ;
#60433=CARTESIAN_POINT ( 'NONE',  ( 0.000000000000000000, 4.570217215903371155, 5.218059682435623792 ) ) ;
#60443=CARTESIAN_POINT ( 'NONE',  ( 0.000000000000000000, 1.779948802829816490, 6.576141558201244131 ) ) ;
#60448=ORIENTED_EDGE ( 'NONE', *, *, #48952, .F. ) ;
#60450=CARTESIAN_POINT ( 'NONE',  ( -22.28236030719477512, -3.683993210674363361, 0.3108070568283768376 ) ) ;
#60454=ORIENTED_EDGE ( 'NONE', *, *, #18332, .T. ) ;
#60459=B_SPLINE_CURVE_WITH_KNOTS ( 'NONE', 3,
 ( #10587, #40526, #36533, #65775, #41173, #61452 ),
 .UNSPECIFIED., .F., .F.,
 ( 4, 2, 4 ),
 ( 0.0001654224980408285247, 0.0006219428995476449255, 0.001078463301054461299 ),
 .UNSPECIFIED. ) ;
#60462=ORIENTED_EDGE ( 'NONE', *, *, #65175, .T. ) ;
#60463=AXIS2_PLACEMENT_3D ( 'NONE', #23662, #63871, #53915 ) ;
#60467=CARTESIAN_POINT ( 'NONE',  ( -22.94572469358970679, -4.424217216616509241, 2.078200699019450148 ) ) ;
#60469=CARTESIAN_POINT ( 'NONE',  ( 2.000000000000001776, 1.865193240757184290, -6.552473556515182374 ) ) ;
#60470=VERTEX_POINT ( 'NONE', #45021 ) ;
#60475=EDGE_CURVE ( 'NONE', #14035, #12068, #39423, .T. ) ;
#60481=LINE ( 'NONE', #64800, #19010 ) ;
#60489=DIRECTION ( 'NONE',  ( 1.000000000000000000, 1.685093406416449860E-16, -1.011030131491581592E-17 ) ) ;
#60499=VERTEX_POINT ( 'NONE', #56974 ) ;
#60500=CARTESIAN_POINT ( 'NONE',  ( 2.000000000000001776, 0.000000000000000000, 0.000000000000000000 ) ) ;
#60507=ORIENTED_EDGE ( 'NONE', *, *, #26048, .T. ) ;
#60521=ORIENTED_EDGE ( 'NONE', *, *, #30760, .T. ) ;
#60535=ORIENTED_EDGE ( 'NONE', *, *, #23340, .T. ) ;
#60536=EDGE_CURVE ( 'NONE', #52831, #47834, #16409, .T. ) ;
#60544=CARTESIAN_POINT ( 'NONE',  ( -22.30625920655495165, 2.610366806364701642, -2.750410778797873323 ) ) ;
#60547=AXIS2_PLACEMENT_3D ( 'NONE', #3672, #44196, #29540 ) ;
#60550=ORIENTED_EDGE ( 'NONE', *, *, #21227, .F. ) ;
#60551=CARTESIAN_POINT ( 'NONE',  ( -27.10128162969864007, -1.304299867635194232, -1.945744751331073497 ) ) ;
#60555=EDGE_CURVE ( 'NONE', #25882, #16541, #10756, .T. ) ;
#60562=VERTEX_POINT ( 'NONE', #19914 ) ;
#60569=DIRECTION ( 'NONE',  ( -1.000000000000000000, 0.000000000000000000, 0.000000000000000000 ) ) ;
#60570=VECTOR ( 'NONE', #42429, 1000.000000000000000 ) ;
#60571=DIRECTION ( 'NONE',  ( -1.000000000000000000, 0.000000000000000000, 0.000000000000000000 ) ) ;
#60574=CARTESIAN_POINT ( 'NONE',  ( -22.31099767395441091, 0.2534174342804221824, 3.774495463598458223 ) ) ;
#60578=CARTESIAN_POINT ( 'NONE',  ( -27.10512513516316702, 1.709353012333669319, 1.618446180706308635 ) ) ;
#60579=ORIENTED_EDGE ( 'NONE', *, *, #42785, .F. ) ;
#60582=DIRECTION ( 'NONE',  ( 0.000000000000000000, 0.7621620551276376831, -0.6473862847818260269 ) ) ;
#60585=DIRECTION ( 'NONE',  ( -1.000000000000000000, 0.000000000000000000, 0.000000000000000000 ) ) ;
#60594=DIRECTION ( 'NONE',  ( 0.000000000000000000, 0.5155538571770231782, -0.8568571761675882748 ) ) ;
#60598=EDGE_CURVE ( 'NONE', #57759, #57723, #18233, .T. ) ;
#60600=AXIS2_PLACEMENT_3D ( 'NONE', #43655, #22744, #43007 ) ;
#60601=VERTEX_POINT ( 'NONE', #8631 ) ;
#60604=VERTEX_POINT ( 'NONE', #24912 ) ;
#60607=CARTESIAN_POINT ( 'NONE',  ( -27.32337605527165891, -1.175835497774981198, -2.771816950947483704 ) ) ;
#60608=CARTESIAN_POINT ( 'NONE',  ( -22.27706485742869091, 1.508175983031630585, -3.358064672837109743 ) ) ;
#60609=FACE_OUTER_BOUND ( 'NONE', #45993, .T. ) ;
#60610=AXIS2_PLACEMENT_3D ( 'NONE', #10411, #15076, #25386 ) ;
#60614=AXIS2_PLACEMENT_3D ( 'NONE', #22493, #57415, #11845 ) ;
#60616=CARTESIAN_POINT ( 'NONE',  ( -22.27384469013076185, 0.9835229356382479970, -3.548341908721023952 ) ) ;
#60620=VECTOR ( 'NONE', #12906, 1000.000000000000114 ) ;
#60621=EDGE_CURVE ( 'NONE', #57809, #63687, #17124, .T. ) ;
#60622=AXIS2_PLACEMENT_3D ( 'NONE', #18990, #4703, #45237 ) ;
#60627=ORIENTED_EDGE ( 'NONE', *, *, #19973, .F. ) ;
#60629=FACE_OUTER_BOUND ( 'NONE', #17757, .T. ) ;
#60632=EDGE_CURVE ( 'NONE', #8461, #40758, #3981, .T. ) ;
#60633=CARTESIAN_POINT ( 'NONE',  ( 0.000000000000000000, -3.859771122243078167, 5.613913289150019637 ) ) ;
#60634=CARTESIAN_POINT ( 'NONE',  ( 0.000000000000000000, 0.000000000000000000, 0.000000000000000000 ) ) ;
#60645=ADVANCED_FACE ( 'NONE', ( #14896 ), #44510, .T. ) ;
#60646=ORIENTED_EDGE ( 'NONE', *, *, #44775, .T. ) ;
#60648=ORIENTED_EDGE ( 'NONE', *, *, #1517, .T. ) ;
#60666=ORIENTED_EDGE ( 'NONE', *, *, #62170, .T. ) ;
#60683=DIRECTION ( 'NONE',  ( -0.9606638835031802159, -0.2674900627617609605, -0.07465901992590913416 ) ) ;
#60686=EDGE_CURVE ( 'NONE', #49701, #7386, #47947, .T. ) ;
#60689=DIRECTION ( 'NONE',  ( -1.000000000000000000, 0.000000000000000000, 0.000000000000000000 ) ) ;
#60691=DIRECTION ( 'NONE',  ( -1.000000000000000000, 0.000000000000000000, 0.000000000000000000 ) ) ;
#60693=DIRECTION ( 'NONE',  ( -1.000000000000000000, 0.000000000000000000, 0.000000000000000000 ) ) ;
#60695=CARTESIAN_POINT ( 'NONE',  ( -27.05874794189610455, 1.734723475976807094E-15, -8.673617379884035472E-15 ) ) ;
#60702=CARTESIAN_POINT ( 'NONE',  ( 0.000000000000000000, 3.859771122243123465, -5.613913289150012531 ) ) ;
#60703=LINE ( 'NONE', #47621, #58560 ) ;
#60711=CARTESIAN_POINT ( 'NONE',  ( -27.08416813689867908, -2.150738950797701499, -0.7899859999124564380 ) ) ;
#60716=CARTESIAN_POINT ( 'NONE',  ( 0.000000000000000000, -0.3246585432986597852, 6.805031400696099020 ) ) ;
#60717=EDGE_CURVE ( 'NONE', #45739, #33077, #58597, .T. ) ;
#60728=CARTESIAN_POINT ( 'NONE',  ( -22.28694879868232803, -1.011812214896728346, -3.570244315741557983 ) ) ;
#60733=CARTESIAN_POINT ( 'NONE',  ( -27.09229696323320979, 2.247106967994373594, 0.5586335684093640674 ) ) ;
#60756=CARTESIAN_POINT ( 'NONE',  ( 2.000000000000001776, 0.000000000000000000, 0.000000000000000000 ) ) ;
#60758=CARTESIAN_POINT ( 'NONE',  ( -22.27720412283625961, -1.161733799004162293, 3.493592264983210516 ) ) ;
#60759=EDGE_LOOP ( 'NONE', ( #16657, #42257, #47119, #36385 ) ) ;
#60761=ADVANCED_FACE ( 'NONE', ( #15568 ), #1289, .T. ) ;
#60765=CARTESIAN_POINT ( 'NONE',  ( -27.08639648637141661, 0.5801562253478033115, -2.223359598374795354 ) ) ;
#60772=CARTESIAN_POINT ( 'NONE',  ( -22.59969328935897792, -1.672297795814008392, -4.339503524536198142 ) ) ;
#60790=DIRECTION ( 'NONE',  ( 1.000000000000000000, -0.000000000000000000, -0.000000000000000000 ) ) ;
#60794=ORIENTED_EDGE ( 'NONE', *, *, #55031, .T. ) ;
#60796=DIRECTION ( 'NONE',  ( -1.000000000000000000, 0.000000000000000000, 0.000000000000000000 ) ) ;
#60803=CARTESIAN_POINT ( 'NONE',  ( -27.20102706715913143, 1.765193291701727896, -1.966718264078090250 ) ) ;
#60806=VERTEX_POINT ( 'NONE', #10576 ) ;
#60808=DIRECTION ( 'NONE',  ( -1.000000000000000000, 0.000000000000000000, 0.000000000000000000 ) ) ;
#60820=VECTOR ( 'NONE', #60571, 1000.000000000000000 ) ;
#60823=AXIS2_PLACEMENT_3D ( 'NONE', #48105, #2563, #8179 ) ;
#60826=ORIENTED_EDGE ( 'NONE', *, *, #37307, .T. ) ;
#60827=CARTESIAN_POINT ( 'NONE',  ( 0.000000000000000000, 0.000000000000000000, 0.000000000000000000 ) ) ;
#60831=FACE_OUTER_BOUND ( 'NONE', #29201, .T. ) ;
#60833=ADVANCED_FACE ( 'NONE', ( #27511 ), #8632, .T. ) ;
#60838=LINE ( 'NONE', #26247, #28646 ) ;
#60839=LINE ( 'NONE', #55853, #53701 ) ;
#60844=CARTESIAN_POINT ( 'NONE',  ( 2.000000000000001776, -6.253963800348261159, 4.139799123620986343 ) ) ;
#60847=B_SPLINE_CURVE_WITH_KNOTS ( 'NONE', 3,
 ( #5777, #46325, #31348, #40667, #6409, #46978, #46640, #55965, #60964, #41646, #25710, #21026, #20722, #15398, #41309, #61589, #16036, #35668, #36330 ),
 .UNSPECIFIED., .F., .F.,
 ( 4, 3, 3, 3, 3, 3, 4 ),
 ( 0.000000000000000000, 2.836829843012736788E-05, 4.224792512551080192E-05, 5.612066614913364178E-05, 6.998859278355053920E-05, 9.832141288087331251E-05, 0.0001178161482478538510 ),
 .UNSPECIFIED. ) ;
#60857=CARTESIAN_POINT ( 'NONE',  ( -22.31328051695926007, -2.748895659348118858, -2.608921479762132734 ) ) ;
#60863=CARTESIAN_POINT ( 'NONE',  ( -27.08588607604432852, 0.6046196991083065964, 2.215240480751981877 ) ) ;
#60872=ORIENTED_EDGE ( 'NONE', *, *, #16302, .F. ) ;
#60878=CARTESIAN_POINT ( 'NONE',  ( -35.04709527796842394, -0.007095259204982495849, 0.01012471662512753889 ) ) ;
#60881=DIRECTION ( 'NONE',  ( -1.000000000000000000, 0.000000000000000000, 0.000000000000000000 ) ) ;
#60886=B_SPLINE_CURVE_WITH_KNOTS ( 'NONE', 3,
 ( #51418, #201, #61045, #41390, #15477, #35740 ),
 .UNSPECIFIED., .F., .F.,
 ( 4, 2, 4 ),
 ( 0.0001654224980408524042, 0.0006219428995476594538, 0.001078463301054466503 ),
 .UNSPECIFIED. ) ;
#60888=CARTESIAN_POINT ( 'NONE',  ( -22.30625920655495165, 0.2529928606556913206, 3.783486345733959588 ) ) ;
#60893=CIRCLE ( 'NONE', #1483, 7.499999999999988454 ) ;
#60896=VECTOR ( 'NONE', #36339, 1000.000000000000000 ) ;
#60901=LINE ( 'NONE', #15975, #15128 ) ;
#60906=VERTEX_POINT ( 'NONE', #18214 ) ;
#60911=CARTESIAN_POINT ( 'NONE',  ( -22.27706485742869091, 0.9221835209182547288, 3.563814065926663499 ) ) ;
#60916=ORIENTED_EDGE ( 'NONE', *, *, #29237, .F. ) ;
#60917=CIRCLE ( 'NONE', #408, 7.499999999999988454 ) ;
#60918=CARTESIAN_POINT ( 'NONE',  ( -27.08426571771018487, -0.2528330215897320321, -2.277536580310470793 ) ) ;
#60924=ORIENTED_EDGE ( 'NONE', *, *, #64368, .T. ) ;
#60932=CARTESIAN_POINT ( 'NONE',  ( 2.000000000000001776, -2.469490258309472441, 6.482025155313308140 ) ) ;
#60943=CIRCLE ( 'NONE', #15266, 2.899999999999994582 ) ;
#60950=AXIS2_PLACEMENT_3D ( 'NONE', #44275, #30946, #1368 ) ;
#60964=CARTESIAN_POINT ( 'NONE',  ( -27.09252613521593389, -1.005681546875654364, 2.086468883257830420 ) ) ;
#60966=EDGE_CURVE ( 'NONE', #25175, #24785, #25675, .T. ) ;
#60971=CARTESIAN_POINT ( 'NONE',  ( 1.000000000000000888, -6.997684042076912192, 2.698595569414189210 ) ) ;
#60972=DIRECTION ( 'NONE',  ( 0.000000000000000000, -0.9289767198167950824, 0.3701381553399052948 ) ) ;
#60979=ORIENTED_EDGE ( 'NONE', *, *, #64613, .F. ) ;
#60989=ORIENTED_EDGE ( 'NONE', *, *, #34278, .T. ) ;
#60993=CARTESIAN_POINT ( 'NONE',  ( -35.05175862995318425, 0.003331684148536948054, 0.01212835938693181126 ) ) ;
#61000=EDGE_LOOP ( 'NONE', ( #30421, #24031, #57040, #47504 ) ) ;
#61009=DIRECTION ( 'NONE',  ( 1.000000000000000000, 1.685093406416449860E-16, -1.011030131491573426E-17 ) ) ;
#61019=ORIENTED_EDGE ( 'NONE', *, *, #51752, .T. ) ;
#61021=CARTESIAN_POINT ( 'NONE',  ( -27.08429572838383947, -2.279961732801590646, 0.2296550094122822017 ) ) ;
#61023=CARTESIAN_POINT ( 'NONE',  ( 2.000000000000001776, 4.444115772890187444, -5.163689623839299081 ) ) ;
#61024=DIRECTION ( 'NONE',  ( 0.000000000000000000, 0.000000000000000000, 1.000000000000000000 ) ) ;
#61025=CARTESIAN_POINT ( 'NONE',  ( 0.000000000000000000, -6.767909380267593811, 0.7805499053120233954 ) ) ;
#61028=VERTEX_POINT ( 'NONE', #14817 ) ;
#61036=CARTESIAN_POINT ( 'NONE',  ( -27.28563798457902223, -2.896153581097044238, -0.04047623855284221417 ) ) ;
#61039=AXIS2_PLACEMENT_3D ( 'NONE', #36414, #65664, #14791 ) ;
#61041=EDGE_CURVE ( 'NONE', #32207, #3171, #41667, .T. ) ;
#61043=CARTESIAN_POINT ( 'NONE',  ( -27.08417473062937475, -2.166271322019585277, -0.7460375461499409999 ) ) ;
#61045=CARTESIAN_POINT ( 'NONE',  ( -27.28563798457902223, 2.487904455214894117, 1.483130241384891468 ) ) ;
#61046=CARTESIAN_POINT ( 'NONE',  ( 2.000000000000001776, 6.338823199656720142, -2.816798305433633853 ) ) ;
#61047=CARTESIAN_POINT ( 'NONE',  ( 2.000000000000001776, -6.767909380267597363, -0.7805499053121327524 ) ) ;
#61049=ADVANCED_FACE ( 'NONE', ( #5208 ), #46740, .T. ) ;
#61056=EDGE_CURVE ( 'NONE', #33077, #2794, #19327, .T. ) ;
#61060=DIRECTION ( 'NONE',  ( -1.000000000000000000, 0.000000000000000000, 0.000000000000000000 ) ) ;
#61077=LINE ( 'NONE', #15508, #43265 ) ;
#61082=CARTESIAN_POINT ( 'NONE',  ( 2.000000000000001776, -6.586971819220355684, 3.586335490831369821 ) ) ;
#61085=ORIENTED_EDGE ( 'NONE', *, *, #48962, .F. ) ;
#61086=ORIENTED_EDGE ( 'NONE', *, *, #59393, .F. ) ;
#61117=DIRECTION ( 'NONE',  ( 0.000000000000000000, 0.000000000000000000, -1.000000000000000000 ) ) ;
#61119=EDGE_CURVE ( 'NONE', #24026, #18208, #41408, .T. ) ;
#61123=CARTESIAN_POINT ( 'NONE',  ( 2.000000000000001776, 1.865193240757095916, 6.552473556515182374 ) ) ;
#61125=CARTESIAN_POINT ( 'NONE',  ( -22.31328051695926007, 3.401210163132566411, 1.671726071983929307 ) ) ;
#61128=ADVANCED_FACE ( 'NONE', ( #30773 ), #61365, .T. ) ;
#61145=DIRECTION ( 'NONE',  ( -1.000000000000000000, 0.000000000000000000, 0.000000000000000000 ) ) ;
#61160=B_SPLINE_CURVE_WITH_KNOTS ( 'NONE', 3,
 ( #33862, #59469, #22932, #63459, #33218, #2981, #8596, #58506, #17931, #48854, #63786, #18273, #38534, #26671, #28885, #58856 ),
 .UNSPECIFIED., .F., .F.,
 ( 4, 3, 3, 3, 3, 4 ),
 ( 0.000000000000000000, 6.991367980366391542E-05, 0.0001398269368981360167, 0.0002097400188389093628, 0.0002811534801551364318, 0.0003526297678872490409 ),
 .UNSPECIFIED. ) ;
#61166=DIRECTION ( 'NONE',  ( 0.000000000000000000, 0.000000000000000000, 1.000000000000000000 ) ) ;
#61167=CARTESIAN_POINT ( 'NONE',  ( -27.09342121492585065, -2.251107617621292967, -0.5565043948850181277 ) ) ;
#61176=EDGE_LOOP ( 'NONE', ( #43764, #14512, #18927, #9057 ) ) ;
#61177=DIRECTION ( 'NONE',  ( -1.000000000000000000, 0.000000000000000000, 0.000000000000000000 ) ) ;
#61180=CARTESIAN_POINT ( 'NONE',  ( -24.42101984568203576, 3.884389025764524384, -1.824625598916865155 ) ) ;
#61193=DIRECTION ( 'NONE',  ( 0.9606638835031803270, 0.2249116044183872010, -0.1629100154396133371 ) ) ;
#61198=ORIENTED_EDGE ( 'NONE', *, *, #19701, .F. ) ;
#61202=DIRECTION ( 'NONE',  ( 1.000000000000000000, -0.000000000000000000, -0.000000000000000000 ) ) ;
#61207=DIRECTION ( 'NONE',  ( 0.000000000000000000, 0.000000000000000000, 1.000000000000000000 ) ) ;
#61208=EDGE_CURVE ( 'NONE', #22936, #27434, #56476, .T. ) ;
#61211=B_SPLINE_CURVE_WITH_KNOTS ( 'NONE', 3,
 ( #5574, #25845, #31477, #26818, #35476, #15833, #1230, #21511, #60758, #251, #5913, #46134, #36111, #40807, #41434, #35783, #56419, #30484, #57087, #55774, #10867, #5231 ),
 .UNSPECIFIED., .F., .F.,
 ( 4, 3, 3, 3, 3, 3, 3, 4 ),
 ( 4.735866574735071843E-18, 6.990956068646401111E-05, 0.0001398191187764049009, 0.0002097286751720215444, 0.0002796382307041361554, 0.0003495477861619815082, 0.0004194573423310287374, 0.0005586102576333139540 ),
 .UNSPECIFIED. ) ;
#61221=CARTESIAN_POINT ( 'NONE',  ( 0.000000000000000000, 0.3246585432987117992, -6.805031400696120336 ) ) ;
#61230=EDGE_LOOP ( 'NONE', ( #28030, #50645, #62013, #57505 ) ) ;
#61233=ADVANCED_FACE ( 'NONE', ( #2175 ), #52408, .T. ) ;
#61240=ORIENTED_EDGE ( 'NONE', *, *, #7041, .T. ) ;
#61243=CARTESIAN_POINT ( 'NONE',  ( -22.30625920655495165, 3.403091720605023962, 1.672644928563048472 ) ) ;
#61250=CARTESIAN_POINT ( 'NONE',  ( 2.000000000000001776, 6.906413915731192787, 0.6453518998147528274 ) ) ;
#61252=VERTEX_POINT ( 'NONE', #52727 ) ;
#61253=CARTESIAN_POINT ( 'NONE',  ( -35.04834644901396956, 0.002604658385682454436, -0.01358669851862852156 ) ) ;
#61257=CARTESIAN_POINT ( 'NONE',  ( 2.000000000000001776, 6.160607635185464837, -4.277489166005534749 ) ) ;
#61258=ADVANCED_FACE ( 'NONE', ( #42718 ), #7476, .T. ) ;
#61264=CIRCLE ( 'NONE', #45317, 2.899999999999994582 ) ;
#61267=CARTESIAN_POINT ( 'NONE',  ( 0.000000000000000000, 3.979254915827366901, 5.681598592373755530 ) ) ;
#61277=ADVANCED_FACE ( 'NONE', ( #7832 ), #37750, .T. ) ;
#61278=FACE_OUTER_BOUND ( 'NONE', #19444, .T. ) ;
#61281=LINE ( 'NONE', #1099, #24314 ) ;
#61290=CIRCLE ( 'NONE', #22001, 2.899999999999994582 ) ;
#61293=CARTESIAN_POINT ( 'NONE',  ( -22.28073302975501235, 3.560599703067816701, -0.9769664947681093725 ) ) ;
#61294=EDGE_LOOP ( 'NONE', ( #19147, #56107, #5668, #2365 ) ) ;
#61295=DIRECTION ( 'NONE',  ( 0.000000000000000000, 0.3193015301359806157, -0.9476531711828021232 ) ) ;
#61309=CARTESIAN_POINT ( 'NONE',  ( -27.10719052120871098, 1.044362304621487825, -2.116547233941206585 ) ) ;
#61318=CARTESIAN_POINT ( 'NONE',  ( -22.27719381268171261, -0.9730858478813817491, 3.550654232855428027 ) ) ;
#61320=CARTESIAN_POINT ( 'NONE',  ( -35.04660725145885891, 0.008590646501148855446, 0.008800808525098732099 ) ) ;
#61324=LINE ( 'NONE', #16449, #37310 ) ;
#61330=VERTEX_POINT ( 'NONE', #53715 ) ;
#61332=LINE ( 'NONE', #26752, #11588 ) ;
#61333=CARTESIAN_POINT ( 'NONE',  ( -22.28856623400852399, 0.9049353338066689068, -3.603818606161816707 ) ) ;
#61335=CARTESIAN_POINT ( 'NONE',  ( -22.27721701579900682, 1.205877546543726364, -3.478642907697082620 ) ) ;
#61342=AXIS2_PLACEMENT_3D ( 'NONE', #34494, #49798, #15194 ) ;
#61346=CARTESIAN_POINT ( 'NONE',  ( 2.000000000000001776, 0.000000000000000000, 0.000000000000000000 ) ) ;
#61352=ADVANCED_FACE ( 'NONE', ( #48720 ), #2126, .F. ) ;
#61361=CARTESIAN_POINT ( 'NONE',  ( -10.00000000000000178, 0.000000000000000000, 0.000000000000000000 ) ) ;
#61365=CYLINDRICAL_SURFACE ( 'NONE', #5520, 6.936499999999988120 ) ;
#61371=CARTESIAN_POINT ( 'NONE',  ( -27.08506889328327816, 1.324351020479957564, 1.872884652026852725 ) ) ;
#61375=DIRECTION ( 'NONE',  ( -1.000000000000000000, 0.000000000000000000, 0.000000000000000000 ) ) ;
#61379=CIRCLE ( 'NONE', #7223, 2.899999999999995026 ) ;
#61382=CARTESIAN_POINT ( 'NONE',  ( 2.000000000000001776, -3.979254915827311390, -5.681598592373819478 ) ) ;
#61386=DIRECTION ( 'NONE',  ( 0.000000000000000000, -0.8835120444460178302, -0.4684084406997996997 ) ) ;
#61390=CARTESIAN_POINT ( 'NONE',  ( -22.30625920655495165, -0.8854385781085337692, 3.687109008463850479 ) ) ;
#61400=LINE ( 'NONE', #50141, #55434 ) ;
#61401=CARTESIAN_POINT ( 'NONE',  ( -27.08506889328343803, 2.284141197253897193, -0.2104793012480347114 ) ) ;
#61408=DIRECTION ( 'NONE',  ( -1.000000000000000000, 0.000000000000000000, 0.000000000000000000 ) ) ;
#61419=ORIENTED_EDGE ( 'NONE', *, *, #40574, .F. ) ;
#61428=CARTESIAN_POINT ( 'NONE',  ( -35.04582288351658548, -0.01092946910274502324, 0.006479247284604020517 ) ) ;
#61431=CIRCLE ( 'NONE', #24282, 7.499999999999988454 ) ;
#61433=ADVANCED_FACE ( 'NONE', ( #32961 ), #57944, .T. ) ;
#61436=VERTEX_POINT ( 'NONE', #8056 ) ;
#61442=DIRECTION ( 'NONE',  ( 0.000000000000000000, -0.9868265225415276953, 0.1617819965527552140 ) ) ;
#61443=AXIS2_PLACEMENT_3D ( 'NONE', #18363, #59244, #38625 ) ;
#61444=ADVANCED_FACE ( 'NONE', ( #27327 ), #47622, .T. ) ;
#61447=CARTESIAN_POINT ( 'NONE',  ( 2.000000000000001776, -6.662861565602071323, 1.421313227905616650 ) ) ;
#61448=ORIENTED_EDGE ( 'NONE', *, *, #13063, .T. ) ;
#61452=CARTESIAN_POINT ( 'NONE',  ( -27.10719052120871098, 1.962717903527675611, -1.310802520592017295 ) ) ;
#61454=CARTESIAN_POINT ( 'NONE',  ( 0.000000000000000000, 3.673940397442060361E-16, 3.000000000000000444 ) ) ;
#61462=DIRECTION ( 'NONE',  ( 0.000000000000000000, -0.4198891015602715382, 0.9075754196709537869 ) ) ;
#61467=CARTESIAN_POINT ( 'NONE',  ( -22.27706485742869091, 3.662257305743817692, -0.3729136217355926153 ) ) ;
#61468=VECTOR ( 'NONE', #59256, 1000.000000000000000 ) ;
#61475=ORIENTED_EDGE ( 'NONE', *, *, #5418, .F. ) ;
#61476=ORIENTED_EDGE ( 'NONE', *, *, #55787, .T. ) ;
#61483=EDGE_LOOP ( 'NONE', ( #61198, #16243, #47068, #51854 ) ) ;
#61490=CARTESIAN_POINT ( 'NONE',  ( -27.10719052120871098, 1.044362304621487825, -2.116547233941206585 ) ) ;
#61497=CARTESIAN_POINT ( 'NONE',  ( -27.08702828306176258, 0.6138566972905430408, 2.216258174335470787 ) ) ;
#61499=CARTESIAN_POINT ( 'NONE',  ( 2.000000000000001776, 0.000000000000000000, 0.000000000000000000 ) ) ;
#61503=AXIS2_PLACEMENT_3D ( 'NONE', #15318, #56891, #51577 ) ;
#61504=VERTEX_POINT ( 'NONE', #43272 ) ;
#61524=CARTESIAN_POINT ( 'NONE',  ( -27.08419642509982950, 1.697757994346406951, -1.538761233743668910 ) ) ;
#61536=EDGE_CURVE ( 'NONE', #63186, #28450, #23648, .T. ) ;
#61537=ORIENTED_EDGE ( 'NONE', *, *, #31598, .F. ) ;
#61540=AXIS2_PLACEMENT_3D ( 'NONE', #40497, #16219, #25208 ) ;
#61546=EDGE_LOOP ( 'NONE', ( #48778, #14280, #48018, #3023 ) ) ;
#61548=CONICAL_SURFACE ( 'NONE', #49901, 2.214855479030549468, 1.249045772030607848 ) ;
#61560=CARTESIAN_POINT ( 'NONE',  ( -22.59969328935886423, -3.618004136135291038, -2.921971394153373591 ) ) ;
#61564=CARTESIAN_POINT ( 'NONE',  ( -27.08426571771018487, 2.277536580310463243, -0.2528330215897251487 ) ) ;
#61574=ADVANCED_FACE ( 'NONE', ( #64152 ), #24654, .F. ) ;
#61580=DIRECTION ( 'NONE',  ( 0.000000000000000000, 0.000000000000000000, 1.000000000000000000 ) ) ;
#61589=CARTESIAN_POINT ( 'NONE',  ( -27.08506889328327816, -0.9597901767732647249, 2.083363953276908376 ) ) ;
#61593=CARTESIAN_POINT ( 'NONE',  ( -35.04834644901396956, 0.01306875526353248884, -0.004537648929138059922 ) ) ;
#61594=CARTESIAN_POINT ( 'NONE',  ( 0.000000000000000000, 6.812627895098307462, 2.855765430652722259 ) ) ;
#61601=ORIENTED_EDGE ( 'NONE', *, *, #34332, .T. ) ;
#61608=CARTESIAN_POINT ( 'NONE',  ( -22.30861784526116054, 3.620936716852761084, -1.070462554923803378 ) ) ;
#61609=EDGE_LOOP ( 'NONE', ( #46378, #55674, #54928, #63102 ) ) ;
#61617=ORIENTED_EDGE ( 'NONE', *, *, #7520, .T. ) ;
#61619=EDGE_CURVE ( 'NONE', #65138, #53550, #48037, .T. ) ;
#61640=DIRECTION ( 'NONE',  ( -1.000000000000000000, 0.000000000000000000, 0.000000000000000000 ) ) ;
#61643=VECTOR ( 'NONE', #43444, 1000.000000000000000 ) ;
#61652=EDGE_LOOP ( 'NONE', ( #47417, #49384, #52523, #55558 ) ) ;
#61653=CARTESIAN_POINT ( 'NONE',  ( -26.43258404273188589, -2.854888342447764238, -1.987083010659173699 ) ) ;
#61660=CARTESIAN_POINT ( 'NONE',  ( 2.000000000000001776, -6.441884263200848615, 2.217201541069723891 ) ) ;
#61663=CARTESIAN_POINT ( 'NONE',  ( 0.000000000000000000, 1.754183803416655474, -6.711026108862266248 ) ) ;
#61664=CARTESIAN_POINT ( 'NONE',  ( -22.27715239060371744, -0.8317362037004212283, -3.586346956688103660 ) ) ;
#61665=AXIS2_PLACEMENT_3D ( 'NONE', #35071, #49442, #13812 ) ;
#61667=CARTESIAN_POINT ( 'NONE',  ( -22.28236030719477512, -3.035028179399219983, 2.111163412226035430 ) ) ;
#61670=LINE ( 'NONE', #55386, #17293 ) ;
#61674=DIRECTION ( 'NONE',  ( -1.000000000000000000, 0.000000000000000000, 0.000000000000000000 ) ) ;
#61675=CARTESIAN_POINT ( 'NONE',  ( -22.27384469013076185, 2.154627400808035276, 2.985904959940879344 ) ) ;
#61679=CARTESIAN_POINT ( 'NONE',  ( 0.000000000000000000, 3.073484823194434057, -6.841322316745026555 ) ) ;
#61682=AXIS2_PLACEMENT_3D ( 'NONE', #23166, #43108, #58428 ) ;
#61683=EDGE_CURVE ( 'NONE', #29429, #47259, #65437, .T. ) ;
#61684=VECTOR ( 'NONE', #12233, 1000.000000000000000 ) ;
#61685=CARTESIAN_POINT ( 'NONE',  ( 1.000000000000000888, -7.484036900328550956, 0.4890722589968952150 ) ) ;
#61695=EDGE_CURVE ( 'NONE', #58669, #38796, #40575, .T. ) ;
#61697=ORIENTED_EDGE ( 'NONE', *, *, #29798, .T. ) ;
#61707=CARTESIAN_POINT ( 'NONE',  ( 2.000000000000001776, 0.000000000000000000, 0.000000000000000000 ) ) ;
#61709=CIRCLE ( 'NONE', #18265, 6.936499999999991672 ) ;
#61712=ORIENTED_EDGE ( 'NONE', *, *, #22042, .F. ) ;
#61715=VECTOR ( 'NONE', #44808, 1000.000000000000000 ) ;
#61719=EDGE_CURVE ( 'NONE', #59375, #41165, #45907, .T. ) ;
#61721=LINE ( 'NONE', #57403, #28816 ) ;
#61723=CIRCLE ( 'NONE', #30964, 6.936499999999989008 ) ;
#61724=CARTESIAN_POINT ( 'NONE',  ( -10.00000000000000178, 0.000000000000000000, 0.000000000000000000 ) ) ;
#61727=VERTEX_POINT ( 'NONE', #14559 ) ;
#61730=VERTEX_POINT ( 'NONE', #10560 ) ;
#61734=CARTESIAN_POINT ( 'NONE',  ( 0.000000000000000000, 4.976357229393855164, 4.652926418895560801 ) ) ;
#61738=DIRECTION ( 'NONE',  ( 0.000000000000000000, -0.6876994588534139918, -0.7259954919231395021 ) ) ;
#61740=CIRCLE ( 'NONE', #43660, 2.899999999999995026 ) ;
#61741=CARTESIAN_POINT ( 'NONE',  ( 0.000000000000000000, -3.795144977083577675, -6.468916029978841742 ) ) ;
#61747=DIRECTION ( 'NONE',  ( 0.000000000000000000, 0.000000000000000000, 1.000000000000000000 ) ) ;
#61751=CIRCLE ( 'NONE', #33079, 2.899999999999995026 ) ;
#61753=EDGE_LOOP ( 'NONE', ( #64058, #51799, #36900, #4547 ) ) ;
#61754=CARTESIAN_POINT ( 'NONE',  ( 0.000000000000000000, -3.859771122242995123, -5.613913289150092467 ) ) ;
#61759=CARTESIAN_POINT ( 'NONE',  ( -28.66013792860432119, -1.776574787184029169, 0.4631296695479288905 ) ) ;
#61770=CARTESIAN_POINT ( 'NONE',  ( -22.27756824490284515, 2.599719761044746669, 2.608445836294031928 ) ) ;
#61789=EDGE_CURVE ( 'NONE', #32257, #13767, #65010, .T. ) ;
#61791=CARTESIAN_POINT ( 'NONE',  ( -27.08418322526031119, -2.265123059255407689, 0.3452258100746847247 ) ) ;
#61802=CARTESIAN_POINT ( 'NONE',  ( 2.000000000000001776, 6.777474576704068276, 0.6925993764990892032 ) ) ;
#61806=CARTESIAN_POINT ( 'NONE',  ( -27.09030469827931853, 1.657623467486019075, 1.608164674722569965 ) ) ;
#61807=CARTESIAN_POINT ( 'NONE',  ( -22.27706485742869091, 3.563814065926677710, -0.9221835209182235316 ) ) ;
#61812=EDGE_CURVE ( 'NONE', #26639, #21973, #49838, .T. ) ;
#61813=ORIENTED_EDGE ( 'NONE', *, *, #1142, .F. ) ;
#61823=CARTESIAN_POINT ( 'NONE',  ( 2.000000000000001776, 2.473437528934240515, -7.080403010454960011 ) ) ;
#61829=ORIENTED_EDGE ( 'NONE', *, *, #12366, .T. ) ;
#61841=EDGE_CURVE ( 'NONE', #51096, #50020, #61884, .T. ) ;
#61849=CARTESIAN_POINT ( 'NONE',  ( -27.10512513516276911, -0.6711200423626885181, -2.256292013315177591 ) ) ;
#61851=CARTESIAN_POINT ( 'NONE',  ( -22.70624764888619751, -2.547047087672834387, -4.591418580540065797 ) ) ;
#61855=CARTESIAN_POINT ( 'NONE',  ( 2.000000000000001776, 0.000000000000000000, 0.000000000000000000 ) ) ;
#61865=FACE_OUTER_BOUND ( 'NONE', #56424, .T. ) ;
#61868=B_SPLINE_CURVE_WITH_KNOTS ( 'NONE', 3,
 ( #63927, #44291, #23713, #3773, #43981, #14031, #64255, #29333, #49328, #23368, #43637, #34322, #18402, #19036, #38981, #24032, #49630, #59277, #54298, #39299, #28039, #48339 ),
 .UNSPECIFIED., .F., .F.,
 ( 4, 3, 3, 3, 3, 3, 3, 4 ),
 ( 0.000000000000000000, 6.990956068646460742E-05, 0.0001398191187764047383, 0.0002097286751720217070, 0.0002796382307041362638, 0.0003495477861619818334, 0.0004194573423310300926, 0.0005586102576332987752 ),
 .UNSPECIFIED. ) ;
#61869=ORIENTED_EDGE ( 'NONE', *, *, #61619, .F. ) ;
#61875=LINE ( 'NONE', #50927, #38540 ) ;
#61884=CIRCLE ( 'NONE', #23693, 7.499999999999988454 ) ;
#61885=CARTESIAN_POINT ( 'NONE',  ( -22.27721056931765631, 0.7178530073137668888, 3.610969226755180728 ) ) ;
#61916=EDGE_CURVE ( 'NONE', #45822, #60806, #43856, .T. ) ;
#61918=CARTESIAN_POINT ( 'NONE',  ( 2.000000000000001776, -5.217815162096805182, -5.387430271863635767 ) ) ;
#61930=EDGE_CURVE ( 'NONE', #15285, #45739, #12208, .T. ) ;
#61942=DIRECTION ( 'NONE',  ( -1.000000000000000000, 0.000000000000000000, 0.000000000000000000 ) ) ;
#61943=DIRECTION ( 'NONE',  ( -1.000000000000000000, 0.000000000000000000, 0.000000000000000000 ) ) ;
#61947=CARTESIAN_POINT ( 'NONE',  ( 1.000000000000000888, -5.097042323172487954, 5.501832381651415638 ) ) ;
#61948=AXIS2_PLACEMENT_3D ( 'NONE', #10561, #30841, #11555 ) ;
#61952=EDGE_CURVE ( 'NONE', #5936, #17594, #7612, .T. ) ;
#61962=CARTESIAN_POINT ( 'NONE',  ( -35.05012975565874456, -0.01323209221896530161, -0.004360246756763594411 ) ) ;
#61971=CARTESIAN_POINT ( 'NONE',  ( -22.29770266787582145, -3.593535545924356533, 1.047554374660444321 ) ) ;
#61977=DIRECTION ( 'NONE',  ( 0.000000000000000000, 0.000000000000000000, 1.000000000000000000 ) ) ;
#61984=AXIS2_PLACEMENT_3D ( 'NONE', #7419, #3126, #64579 ) ;
#61986=CARTESIAN_POINT ( 'NONE',  ( -27.08429572838383947, 2.089332284968718145, 0.9410937941433747955 ) ) ;
#61989=DIRECTION ( 'NONE',  ( -1.000000000000000000, 0.000000000000000000, 0.000000000000000000 ) ) ;
#61990=VERTEX_POINT ( 'NONE', #28814 ) ;
#61997=ORIENTED_EDGE ( 'NONE', *, *, #46824, .F. ) ;
#62003=EDGE_CURVE ( 'NONE', #26234, #33347, #29058, .T. ) ;
#62005=CYLINDRICAL_SURFACE ( 'NONE', #30699, 2.899999999999994582 ) ;
#62013=ORIENTED_EDGE ( 'NONE', *, *, #45255, .T. ) ;
#62014=CIRCLE ( 'NONE', #15303, 2.899999999999994582 ) ;
#62017=EDGE_CURVE ( 'NONE', #28911, #24086, #42789, .T. ) ;
#62020=CARTESIAN_POINT ( 'NONE',  ( 2.000000000000001776, 0.000000000000000000, 0.000000000000000000 ) ) ;
#62023=CARTESIAN_POINT ( 'NONE',  ( -22.27834755396594346, 2.447855249718994930, 2.756126180273619219 ) ) ;
#62025=CARTESIAN_POINT ( 'NONE',  ( 2.000000000000001776, 4.962980376314141573, -4.846014654777754060 ) ) ;
#62027=DIRECTION ( 'NONE',  ( -1.000000000000000000, 0.000000000000000000, 0.000000000000000000 ) ) ;
#62033=DIRECTION ( 'NONE',  ( 0.000000000000000000, 0.000000000000000000, 1.000000000000000000 ) ) ;
#62047=CARTESIAN_POINT ( 'NONE',  ( -27.10113028276028757, 2.276991616286352382, 0.5479825692853625974 ) ) ;
#62052=CARTESIAN_POINT ( 'NONE',  ( 0.000000000000000000, -4.962980376314093611, 4.846014654777763830 ) ) ;
#62054=CYLINDRICAL_SURFACE ( 'NONE', #57696, 2.899999999999994582 ) ;
#62065=CARTESIAN_POINT ( 'NONE',  ( 2.000000000000001776, 5.396716205731433291, 4.158041573745082431 ) ) ;
#62087=CIRCLE ( 'NONE', #26021, 2.899999999999995914 ) ;
#62091=EDGE_CURVE ( 'NONE', #49961, #23637, #65049, .T. ) ;
#62099=ORIENTED_EDGE ( 'NONE', *, *, #40756, .T. ) ;
#62114=CARTESIAN_POINT ( 'NONE',  ( -27.15525204139121840, 1.707635684994321945, -1.831989866434744485 ) ) ;
#62118=CARTESIAN_POINT ( 'NONE',  ( -22.30625920655495165, 3.635849356906417640, -1.076742202099146839 ) ) ;
#62130=AXIS2_PLACEMENT_3D ( 'NONE', #44191, #9923, #48868 ) ;
#62145=EDGE_CURVE ( 'NONE', #9803, #30859, #24152, .T. ) ;
#62151=ADVANCED_FACE ( 'NONE', ( #45741 ), #45097, .T. ) ;
#62152=ORIENTED_EDGE ( 'NONE', *, *, #41549, .F. ) ;
#62157=CARTESIAN_POINT ( 'NONE',  ( -22.27715526084302056, -2.930376837866825124, 2.228953214080627632 ) ) ;
#62164=ORIENTED_EDGE ( 'NONE', *, *, #13736, .F. ) ;
#62166=VERTEX_POINT ( 'NONE', #9490 ) ;
#62170=EDGE_CURVE ( 'NONE', #9280, #27036, #29774, .T. ) ;
#62171=COLOUR_RGB ( '', 0.09019608, 0.27058824, 0.51372549) ;
#62172=DIRECTION ( 'NONE',  ( 0.000000000000000000, 0.000000000000000000, -1.000000000000000000 ) ) ;
#62177=AXIS2_PLACEMENT_3D ( 'NONE', #65359, #39433, #13821 ) ;
#62178=ORIENTED_EDGE ( 'NONE', *, *, #1759, .T. ) ;
#62212=CIRCLE ( 'NONE', #9147, 6.936499999999989008 ) ;
#62243=FACE_OUTER_BOUND ( 'NONE', #63666, .T. ) ;
#62261=CARTESIAN_POINT ( 'NONE',  ( -25.42680463514452072, -2.219378695194082152, 3.188632951113938852 ) ) ;
#62264=CYLINDRICAL_SURFACE ( 'NONE', #29942, 2.899999999999994582 ) ;
#62269=VERTEX_POINT ( 'NONE', #61679 ) ;
#62274=ORIENTED_EDGE ( 'NONE', *, *, #5565, .T. ) ;
#62286=LINE ( 'NONE', #37688, #6899 ) ;
#62304=ORIENTED_EDGE ( 'NONE', *, *, #13316, .F. ) ;
#62306=CARTESIAN_POINT ( 'NONE',  ( 1.000000000000000888, 4.604744433234757572, -5.919993978425451608 ) ) ;
#62308=EDGE_CURVE ( 'NONE', #6868, #34813, #62978, .T. ) ;
#62314=CARTESIAN_POINT ( 'NONE',  ( -22.29570301036918778, 1.042190670255910723, 3.588849529203719246 ) ) ;
#62315=EDGE_CURVE ( 'NONE', #44838, #7784, #27378, .T. ) ;
#62316=DIRECTION ( 'NONE',  ( 0.000000000000000000, 0.000000000000000000, 1.000000000000000000 ) ) ;
#62334=CYLINDRICAL_SURFACE ( 'NONE', #59876, 2.899999999999994582 ) ;
#62337=AXIS2_PLACEMENT_3D ( 'NONE', #62065, #16825, #16516 ) ;
#62339=CARTESIAN_POINT ( 'NONE',  ( 1.000000000000000888, -1.530946385938423582, 7.342084388195347699 ) ) ;
#62353=LINE ( 'NONE', #58372, #6789 ) ;
#62355=DIRECTION ( 'NONE',  ( 0.000000000000000000, 0.000000000000000000, 1.000000000000000000 ) ) ;
#62356=DIRECTION ( 'NONE',  ( 0.000000000000000000, 0.000000000000000000, 1.000000000000000000 ) ) ;
#62357=DIRECTION ( 'NONE',  ( 0.000000000000000000, -0.9985334138511232638, -0.05413890858542831641 ) ) ;
#62360=VERTEX_POINT ( 'NONE', #33404 ) ;
#62367=CIRCLE ( 'NONE', #18864, 2.899999999999995026 ) ;
#62376=ORIENTED_EDGE ( 'NONE', *, *, #30812, .T. ) ;
#62379=ADVANCED_FACE ( 'NONE', ( #23423 ), #11439, .F. ) ;
#62380=CARTESIAN_POINT ( 'NONE',  ( 0.000000000000000000, -6.767909380267597363, -0.7805499053121327524 ) ) ;
#62382=CARTESIAN_POINT ( 'NONE',  ( 1.000000000000000888, -7.484036900328561615, -0.4890722589970097345 ) ) ;
#62385=VECTOR ( 'NONE', #43209, 1000.000000000000000 ) ;
#62398=ORIENTED_EDGE ( 'NONE', *, *, #62645, .F. ) ;
#62399=EDGE_LOOP ( 'NONE', ( #25650, #7203, #45224, #51920 ) ) ;
#62400=CARTESIAN_POINT ( 'NONE',  ( -27.08456565417852246, 0.2166646653334106387, 2.282055114149001529 ) ) ;
#62401=VERTEX_POINT ( 'NONE', #39037 ) ;
#62405=CARTESIAN_POINT ( 'NONE',  ( -35.04709527796842394, 0.007095259204987700019, -0.01012471662515009030 ) ) ;
#62406=ORIENTED_EDGE ( 'NONE', *, *, #41952, .T. ) ;
#62417=ORIENTED_EDGE ( 'NONE', *, *, #28519, .T. ) ;
#62419=ORIENTED_EDGE ( 'NONE', *, *, #17360, .T. ) ;
#62442=EDGE_CURVE ( 'NONE', #46362, #21537, #15219, .T. ) ;
#62462=CARTESIAN_POINT ( 'NONE',  ( -22.27713295444592845, -2.673940016109006113, 2.530364014314291143 ) ) ;
#62471=CARTESIAN_POINT ( 'NONE',  ( 0.000000000000000000, -6.664893814313753495, 3.439359016433473748 ) ) ;
#62476=DIRECTION ( 'NONE',  ( -1.000000000000000000, 0.000000000000000000, 0.000000000000000000 ) ) ;
#62479=CARTESIAN_POINT ( 'NONE',  ( 2.000000000000001776, 6.606214214351074254, 2.114938770769925647 ) ) ;
#62494=DIRECTION ( 'NONE',  ( 0.000000000000000000, 0.3193015301359806712, -0.9476531711828022342 ) ) ;
#62498=CARTESIAN_POINT ( 'NONE',  ( -22.71097035706202405, -2.846599994298329328, 4.089776368546542251 ) ) ;
#62507=ORIENTED_EDGE ( 'NONE', *, *, #43508, .T. ) ;
#62510=DIRECTION ( 'NONE',  ( 0.000000000000000000, -0.5155538571770286183, 0.8568571761675851661 ) ) ;
#62516=ORIENTED_EDGE ( 'NONE', *, *, #9737, .F. ) ;
#62517=EDGE_CURVE ( 'NONE', #61730, #43263, #25818, .T. ) ;
#62527=CARTESIAN_POINT ( 'NONE',  ( -27.08423923533013777, -0.2759775751761929241, -2.274768056034775388 ) ) ;
#62543=DIRECTION ( 'NONE',  ( 0.9582930651793754029, 0.1596922922278031787, 0.2370079598497637219 ) ) ;
#62544=ORIENTED_EDGE ( 'NONE', *, *, #39437, .F. ) ;
#62556=CIRCLE ( 'NONE', #28584, 2.899999999999994582 ) ;
#62557=VERTEX_POINT ( 'NONE', #11394 ) ;
#62561=CARTESIAN_POINT ( 'NONE',  ( 2.000000000000001776, 6.767909380267589370, 0.7805499053121639497 ) ) ;
#62566=EDGE_CURVE ( 'NONE', #61436, #7150, #45997, .T. ) ;
#62567=EDGE_CURVE ( 'NONE', #29292, #45191, #17015, .T. ) ;
#62576=FACE_OUTER_BOUND ( 'NONE', #8427, .T. ) ;
#62578=EDGE_CURVE ( 'NONE', #47123, #64495, #21727, .T. ) ;
#62579=ORIENTED_EDGE ( 'NONE', *, *, #8526, .F. ) ;
#62586=CARTESIAN_POINT ( 'NONE',  ( 2.000000000000001776, 0.000000000000000000, 0.000000000000000000 ) ) ;
#62591=ORIENTED_EDGE ( 'NONE', *, *, #24082, .T. ) ;
#62593=VECTOR ( 'NONE', #11335, 1000.000000000000000 ) ;
#62597=CYLINDRICAL_SURFACE ( 'NONE', #22782, 7.499999999999988454 ) ;
#62598=CARTESIAN_POINT ( 'NONE',  ( -22.27706485742869091, -3.563814065926672381, 0.9221835209182321913 ) ) ;
#62600=LINE ( 'NONE', #41341, #29070 ) ;
#62601=VERTEX_POINT ( 'NONE', #15715 ) ;
#62605=CYLINDRICAL_SURFACE ( 'NONE', #3256, 7.499999999999988454 ) ;
#62635=ORIENTED_EDGE ( 'NONE', *, *, #18181, .F. ) ;
#62639=LINE ( 'NONE', #53013, #530 ) ;
#62640=CARTESIAN_POINT ( 'NONE',  ( 2.000000000000001776, -5.097042323172487954, 5.501832381651415638 ) ) ;
#62641=EDGE_CURVE ( 'NONE', #26234, #12277, #58247, .T. ) ;
#62643=VECTOR ( 'NONE', #23530, 1000.000000000000000 ) ;
#62645=EDGE_CURVE ( 'NONE', #24342, #4186, #26555, .T. ) ;
#62649=CARTESIAN_POINT ( 'NONE',  ( -27.08429572838383947, 0.5764601019426045525, 2.217805374070519253 ) ) ;
#62655=CYLINDRICAL_SURFACE ( 'NONE', #13929, 2.899999999999994582 ) ;
#62661=ADVANCED_FACE ( 'NONE', ( #62576 ), #32973, .T. ) ;
#62663=CARTESIAN_POINT ( 'NONE',  ( -35.04709527796842394, -0.007030359780627049027, 0.01016988845956717791 ) ) ;
#62670=DIRECTION ( 'NONE',  ( 0.000000000000000000, 0.000000000000000000, 1.000000000000000000 ) ) ;
#62671=ADVANCED_FACE ( 'NONE', ( #33326 ), #28335, .T. ) ;
#62680=DIRECTION ( 'NONE',  ( -1.000000000000000000, 0.000000000000000000, 0.000000000000000000 ) ) ;
#62683=ADVANCED_FACE ( 'NONE', ( #64871 ), #64543, .T. ) ;
#62685=CARTESIAN_POINT ( 'NONE',  ( 2.000000000000001776, 1.018311147294260977, -6.861346417234475581 ) ) ;
#62699=VECTOR ( 'NONE', #35945, 1000.000000000000227 ) ;
#62700=( BOUNDED_SURFACE ( )  B_SPLINE_SURFACE ( 3, 1, ( 
 ( #26180, #57418 ),
 ( #262, #42101 ),
 ( #10533, #36122 ),
 ( #41444, #11850 ) ),
 .UNSPECIFIED., .F., .F., .F. ) 
 B_SPLINE_SURFACE_WITH_KNOTS ( ( 4, 4 ),
 ( 2, 2 ),
 ( 0.000000000000000000, 1.000000000000000000 ),
 ( 0.000000000000000000, 1.000000000000000000 ),
 .UNSPECIFIED. ) 
 GEOMETRIC_REPRESENTATION_ITEM ( )  RATIONAL_B_SPLINE_SURFACE ( (
 ( 1.000000000000000000, 1.000000000000000000),
 ( 0.8716676215708681896, 0.8964445200148164483),
 ( 0.8716676215708681896, 0.8964445200148164483),
 ( 1.000000000000000000, 1.000000000000000000) ) ) 
 REPRESENTATION_ITEM ( '' )  SURFACE ( )  );
#62712=LINE ( 'NONE', #7873, #35172 ) ;
#62716=ORIENTED_EDGE ( 'NONE', *, *, #55778, .T. ) ;
#62737=CARTESIAN_POINT ( 'NONE',  ( -22.30625920655495165, 1.076742202099183254, 3.635849356906398544 ) ) ;
#62756=CIRCLE ( 'NONE', #47925, 2.899999999999996803 ) ;
#62760=ORIENTED_EDGE ( 'NONE', *, *, #10650, .T. ) ;
#62761=ORIENTED_EDGE ( 'NONE', *, *, #18013, .F. ) ;
#62766=CARTESIAN_POINT ( 'NONE',  ( -27.08426504710140392, -2.223709847896210512, 0.5533780324190709088 ) ) ;
#62771=EDGE_CURVE ( 'NONE', #10792, #16340, #24818, .T. ) ;
#62773=CARTESIAN_POINT ( 'NONE',  ( 0.000000000000000000, 1.693411908627200146, 7.306323022404582979 ) ) ;
#62774=ORIENTED_EDGE ( 'NONE', *, *, #5050, .F. ) ;
#62776=VERTEX_POINT ( 'NONE', #40259 ) ;
#62777=CARTESIAN_POINT ( 'NONE',  ( -27.10719052120871098, 0.6736837626858914740, 2.261993590776020469 ) ) ;
#62783=CARTESIAN_POINT ( 'NONE',  ( -27.08776759928996825, 1.644157618165827728, 1.611072893085636615 ) ) ;
#62794=EDGE_LOOP ( 'NONE', ( #51464, #22794, #60239, #1327 ) ) ;
#62799=AXIS2_PLACEMENT_3D ( 'NONE', #53939, #38966, #63243 ) ;
#62816=EDGE_CURVE ( 'NONE', #23443, #40945, #53513, .T. ) ;
#62818=CARTESIAN_POINT ( 'NONE',  ( 0.000000000000000000, 6.586971819220337032, 3.586335490831404460 ) ) ;
#62819=VECTOR ( 'NONE', #4921, 1000.000000000000000 ) ;
#62828=EDGE_CURVE ( 'NONE', #2095, #13885, #441, .T. ) ;
#62832=DIRECTION ( 'NONE',  ( 0.000000000000000000, 0.9868265225415265851, -0.1617819965527619031 ) ) ;
#62847=EDGE_CURVE ( 'NONE', #22815, #13989, #42849, .T. ) ;
#62850=CARTESIAN_POINT ( 'NONE',  ( 0.000000000000000000, 1.225832621831950187, -6.827324998361564923 ) ) ;
#62853=AXIS2_PLACEMENT_3D ( 'NONE', #60500, #45533, #35225 ) ;
#62854=CARTESIAN_POINT ( 'NONE',  ( -22.27384469013076185, -2.154627400808021509, -2.985904959940921088 ) ) ;
#62857=ORIENTED_EDGE ( 'NONE', *, *, #56338, .F. ) ;
#62858=ORIENTED_EDGE ( 'NONE', *, *, #42215, .T. ) ;
#62860=DIRECTION ( 'NONE',  ( 1.000000000000000000, 0.000000000000000000, 0.000000000000000000 ) ) ;
#62861=ORIENTED_EDGE ( 'NONE', *, *, #46369, .T. ) ;
#62862=CYLINDRICAL_SURFACE ( 'NONE', #53833, 2.899999999999994582 ) ;
#62863=AXIS2_PLACEMENT_3D ( 'NONE', #58406, #23479, #3555 ) ;
#62872=ORIENTED_EDGE ( 'NONE', *, *, #63676, .F. ) ;
#62873=DIRECTION ( 'NONE',  ( 0.000000000000000000, 0.000000000000000000, 1.000000000000000000 ) ) ;
#62878=AXIS2_PLACEMENT_3D ( 'NONE', #18022, #13354, #22020 ) ;
#62885=EDGE_CURVE ( 'NONE', #64819, #49332, #6795, .T. ) ;
#62886=ORIENTED_EDGE ( 'NONE', *, *, #6538, .F. ) ;
#62903=CARTESIAN_POINT ( 'NONE',  ( -10.00000000000000178, 0.000000000000000000, 0.000000000000000000 ) ) ;
#62908=DIRECTION ( 'NONE',  ( -1.000000000000000000, 0.000000000000000000, 0.000000000000000000 ) ) ;
#62915=CARTESIAN_POINT ( 'NONE',  ( -27.08417473062937120, -0.7460375461499253458, 2.166271322019566181 ) ) ;
#62925=CARTESIAN_POINT ( 'NONE',  ( -26.43258404273187523, 1.478864324198235769, 3.148308537883169222 ) ) ;
#62940=CARTESIAN_POINT ( 'NONE',  ( -22.29290468048228036, -3.357740900108097559, -1.621390503294487750 ) ) ;
#62942=DIRECTION ( 'NONE',  ( -1.000000000000000000, 0.000000000000000000, 0.000000000000000000 ) ) ;
#62945=DIRECTION ( 'NONE',  ( -1.000000000000000000, 0.000000000000000000, 0.000000000000000000 ) ) ;
#62950=DIRECTION ( 'NONE',  ( 0.000000000000000000, -0.1764146379942750642, -0.9843159429275485373 ) ) ;
#62959=LINE ( 'NONE', #52356, #42844 ) ;
#62963=CARTESIAN_POINT ( 'NONE',  ( -22.27706485742869091, -3.547445275915918295, -0.9832726768967802178 ) ) ;
#62966=EDGE_LOOP ( 'NONE', ( #65393, #47203, #63572, #62376 ) ) ;
#62967=DIRECTION ( 'NONE',  ( -1.000000000000000000, 0.000000000000000000, 0.000000000000000000 ) ) ;
#62976=LINE ( 'NONE', #26754, #56466 ) ;
#62978=CIRCLE ( 'NONE', #27956, 2.899999999999995470 ) ;
#62983=ORIENTED_EDGE ( 'NONE', *, *, #58702, .T. ) ;
#62987=AXIS2_PLACEMENT_3D ( 'NONE', #34780, #55085, #40790 ) ;
#62994=CIRCLE ( 'NONE', #25847, 7.499999999999988454 ) ;
#63003=ORIENTED_EDGE ( 'NONE', *, *, #63593, .T. ) ;
#63007=CYLINDRICAL_SURFACE ( 'NONE', #20092, 6.936499999999988120 ) ;
#63015=DIRECTION ( 'NONE',  ( -1.000000000000000000, 0.000000000000000000, 0.000000000000000000 ) ) ;
#63025=CIRCLE ( 'NONE', #41812, 2.899999999999995026 ) ;
#63027=DIRECTION ( 'NONE',  ( 0.000000000000000000, 0.000000000000000000, 1.000000000000000000 ) ) ;
#63032=CIRCLE ( 'NONE', #18501, 7.499999999999988454 ) ;
#63034=ORIENTED_EDGE ( 'NONE', *, *, #24965, .F. ) ;
#63043=CARTESIAN_POINT ( 'NONE',  ( -22.27722019094931127, 0.6491642780571855731, 3.623977093944191541 ) ) ;
#63046=ORIENTED_EDGE ( 'NONE', *, *, #455, .F. ) ;
#63056=CARTESIAN_POINT ( 'NONE',  ( 0.000000000000000000, -6.160607635185433750, 4.277489166005560506 ) ) ;
#63070=ORIENTED_EDGE ( 'NONE', *, *, #46436, .F. ) ;
#63080=CARTESIAN_POINT ( 'NONE',  ( -27.09048036756592026, -2.083857239073395373, -0.9969423855807594270 ) ) ;
#63082=ORIENTED_EDGE ( 'NONE', *, *, #101, .T. ) ;
#63086=CARTESIAN_POINT ( 'NONE',  ( -25.42680463514452072, 0.3277218550990906309, -3.871126486605867889 ) ) ;
#63087=CYLINDRICAL_SURFACE ( 'NONE', #63509, 2.899999999999994582 ) ;
#63089=CYLINDRICAL_SURFACE ( 'NONE', #15968, 6.936499999999988120 ) ;
#63090=ORIENTED_EDGE ( 'NONE', *, *, #54741, .F. ) ;
#63100=CIRCLE ( 'NONE', #42931, 7.499999999999988454 ) ;
#63102=ORIENTED_EDGE ( 'NONE', *, *, #48457, .T. ) ;
#63104=ORIENTED_EDGE ( 'NONE', *, *, #16789, .F. ) ;
#63106=( BOUNDED_SURFACE ( )  B_SPLINE_SURFACE ( 3, 1, ( 
 ( #17928, #38189 ),
 ( #53525, #20711 ),
 ( #7967, #11061 ),
 ( #28235, #11373 ) ),
 .UNSPECIFIED., .F., .F., .F. ) 
 B_SPLINE_SURFACE_WITH_KNOTS ( ( 4, 4 ),
 ( 2, 2 ),
 ( 0.000000000000000000, 1.000000000000000000 ),
 ( 0.000000000000000000, 1.000000000000000000 ),
 .UNSPECIFIED. ) 
 GEOMETRIC_REPRESENTATION_ITEM ( )  RATIONAL_B_SPLINE_SURFACE ( (
 ( 1.000000000000000000, 1.000000000000000000),
 ( 0.8716676215708681896, 0.8964445200148164483),
 ( 0.8716676215708681896, 0.8964445200148164483),
 ( 1.000000000000000000, 1.000000000000000000) ) ) 
 REPRESENTATION_ITEM ( '' )  SURFACE ( )  );
#63108=CARTESIAN_POINT ( 'NONE',  ( 2.000000000000001776, 0.000000000000000000, 0.000000000000000000 ) ) ;
#63126=ORIENTED_EDGE ( 'NONE', *, *, #24947, .F. ) ;
#63127=VERTEX_POINT ( 'NONE', #5540 ) ;
#63128=CARTESIAN_POINT ( 'NONE',  ( -22.31328051695926007, 3.148362328073167404, -2.109671368890616350 ) ) ;
#63132=CYLINDRICAL_SURFACE ( 'NONE', #36538, 6.936499999999988120 ) ;
#63133=ORIENTED_EDGE ( 'NONE', *, *, #30107, .F. ) ;
#63141=B_SPLINE_CURVE_WITH_KNOTS ( 'NONE', 3,
 ( #52538, #51561, #27559, #27238, #16287, #1334, #47219, #1665 ),
 .UNSPECIFIED., .F., .F.,
 ( 4, 2, 2, 4 ),
 ( 0.000000000000000000, 0.0003639104015149997461, 0.0007278208030299994922, 0.001455641606059999635 ),
 .UNSPECIFIED. ) ;
#63142=CARTESIAN_POINT ( 'NONE',  ( 2.000000000000001776, 0.000000000000000000, 0.000000000000000000 ) ) ;
#63146=FACE_OUTER_BOUND ( 'NONE', #1411, .T. ) ;
#63154=VECTOR ( 'NONE', #3956, 1000.000000000000000 ) ;
#63156=FACE_OUTER_BOUND ( 'NONE', #25044, .T. ) ;
#63158=ORIENTED_EDGE ( 'NONE', *, *, #50130, .T. ) ;
#63165=ORIENTED_EDGE ( 'NONE', *, *, #53288, .T. ) ;
#63171=CARTESIAN_POINT ( 'NONE',  ( 2.000000000000001776, -4.915517050588423587, 4.717154614762070430 ) ) ;
#63177=VECTOR ( 'NONE', #34957, 1000.000000000000000 ) ;
#63184=CARTESIAN_POINT ( 'NONE',  ( -27.10307689719060065, -1.703783570821478133, -1.615391801698475849 ) ) ;
#63186=VERTEX_POINT ( 'NONE', #37072 ) ;
#63199=LINE ( 'NONE', #33916, #32403 ) ;
#63208=EDGE_CURVE ( 'NONE', #51465, #25715, #35435, .T. ) ;
#63210=CYLINDRICAL_SURFACE ( 'NONE', #26288, 2.899999999999994582 ) ;
#63213=CARTESIAN_POINT ( 'NONE',  ( -27.15525204139121840, -1.831989866434736713, -1.707635684994332825 ) ) ;
#63217=EDGE_LOOP ( 'NONE', ( #4577, #941, #60666, #56328 ) ) ;
#63218=CARTESIAN_POINT ( 'NONE',  ( 0.000000000000000000, 0.000000000000000000, 0.000000000000000000 ) ) ;
#63234=CARTESIAN_POINT ( 'NONE',  ( 2.000000000000001776, 5.107597897712347290, 4.693343793638412365 ) ) ;
#63241=DIRECTION ( 'NONE',  ( -1.000000000000000000, 0.000000000000000000, 0.000000000000000000 ) ) ;
#63243=DIRECTION ( 'NONE',  ( 0.000000000000000000, 0.000000000000000000, 1.000000000000000000 ) ) ;
#63249=ORIENTED_EDGE ( 'NONE', *, *, #30338, .F. ) ;
#63256=CYLINDRICAL_SURFACE ( 'NONE', #16856, 2.899999999999994582 ) ;
#63261=CARTESIAN_POINT ( 'NONE',  ( -22.29479313954897890, -3.360948587163224310, -1.627767898183759332 ) ) ;
#63270=CARTESIAN_POINT ( 'NONE',  ( 2.000000000000001776, 0.000000000000000000, 0.000000000000000000 ) ) ;
#63277=CARTESIAN_POINT ( 'NONE',  ( 2.000000000000001776, 6.777474576704075382, -0.6925993764990371337 ) ) ;
#63278=ORIENTED_EDGE ( 'NONE', *, *, #55642, .T. ) ;
#63285=DIRECTION ( 'NONE',  ( -1.000000000000000000, 0.000000000000000000, 0.000000000000000000 ) ) ;
#63288=ORIENTED_EDGE ( 'NONE', *, *, #64868, .F. ) ;
#63293=CARTESIAN_POINT ( 'NONE',  ( -22.29115169517546136, 3.355084543108111994, 1.614783311161169577 ) ) ;
#63303=CARTESIAN_POINT ( 'NONE',  ( 2.000000000000001776, -6.201547234537033937, 2.820401998297862978 ) ) ;
#63307=DIRECTION ( 'NONE',  ( -1.000000000000000000, 0.000000000000000000, 0.000000000000000000 ) ) ;
#63310=CYLINDRICAL_SURFACE ( 'NONE', #58538, 2.899999999999994582 ) ;
#63315=CARTESIAN_POINT ( 'NONE',  ( -35.04643116707788408, -0.003844232202718234070, 0.01156612771643049375 ) ) ;
#63316=FACE_OUTER_BOUND ( 'NONE', #41672, .T. ) ;
#63318=LINE ( 'NONE', #62339, #55333 ) ;
#63322=FACE_OUTER_BOUND ( 'NONE', #7936, .T. ) ;
#63326=ADVANCED_FACE ( 'NONE', ( #63322 ), #23777, .T. ) ;
#63328=CARTESIAN_POINT ( 'NONE',  ( 2.000000000000001776, 0.000000000000000000, 0.000000000000000000 ) ) ;
#63331=AXIS2_PLACEMENT_3D ( 'NONE', #39814, #46133, #60101 ) ;
#63333=EDGE_CURVE ( 'NONE', #1853, #34412, #58732, .T. ) ;
#63343=LINE ( 'NONE', #7487, #40390 ) ;
#63344=ORIENTED_EDGE ( 'NONE', *, *, #46394, .T. ) ;
#63351=ORIENTED_EDGE ( 'NONE', *, *, #35309, .T. ) ;
#63353=CARTESIAN_POINT ( 'NONE',  ( -22.27722015946439171, 3.628085906632232849, -0.6262261846986482139 ) ) ;
#63358=CARTESIAN_POINT ( 'NONE',  ( -22.27715526084302056, -0.4651416883073714592, -3.652257391294517319 ) ) ;
#63362=VERTEX_POINT ( 'NONE', #32721 ) ;
#63368=CARTESIAN_POINT ( 'NONE',  ( -22.31099767395441091, 3.142100240805189681, -2.106713667647935662 ) ) ;
#63380=ORIENTED_EDGE ( 'NONE', *, *, #22821, .T. ) ;
#63382=ORIENTED_EDGE ( 'NONE', *, *, #37745, .T. ) ;
#63383=CARTESIAN_POINT ( 'NONE',  ( -27.08871896697731785, 0.1856437051692989004, 2.297279805116099638 ) ) ;
#63388=CARTESIAN_POINT ( 'NONE',  ( -27.08430418657510685, -2.086666645150138333, -0.9470735946419284179 ) ) ;
#63392=CARTESIAN_POINT ( 'NONE',  ( -22.30861784526116054, -2.600591904828400747, 2.737516124790397853 ) ) ;
#63397=CARTESIAN_POINT ( 'NONE',  ( 0.000000000000000000, -3.341639490130703827, -6.078525953551491057 ) ) ;
#63399=VERTEX_POINT ( 'NONE', #34386 ) ;
#63401=CARTESIAN_POINT ( 'NONE',  ( 2.000000000000001776, 4.962980376314068742, 4.846014654777798469 ) ) ;
#63413=EDGE_LOOP ( 'NONE', ( #42297, #8413, #46537, #47742 ) ) ;
#63429=CARTESIAN_POINT ( 'NONE',  ( -22.30398854582848145, 2.594196582747005930, -2.724439933030905259 ) ) ;
#63433=DIRECTION ( 'NONE',  ( 0.000000000000000000, 0.000000000000000000, -1.000000000000000000 ) ) ;
#63437=CARTESIAN_POINT ( 'NONE',  ( -22.27384469013075829, -3.663183248998797659, 0.3730095848193237251 ) ) ;
#63440=CARTESIAN_POINT ( 'NONE',  ( 1.000000000000000888, -6.160607635185433750, 4.277489166005560506 ) ) ;
#63441=ORIENTED_EDGE ( 'NONE', *, *, #30462, .T. ) ;
#63442=DIRECTION ( 'NONE',  ( -1.000000000000000000, 0.000000000000000000, 0.000000000000000000 ) ) ;
#63450=FACE_OUTER_BOUND ( 'NONE', #51709, .T. ) ;
#63453=CARTESIAN_POINT ( 'NONE',  ( 2.000000000000001776, -1.018311147294196806, 6.861346417234461370 ) ) ;
#63457=DIRECTION ( 'NONE',  ( -1.000000000000000000, 0.000000000000000000, 0.000000000000000000 ) ) ;
#63459=CARTESIAN_POINT ( 'NONE',  ( -27.08421860617808008, 1.394838596205212555, 1.817782142550182112 ) ) ;
#63464=ORIENTED_EDGE ( 'NONE', *, *, #13348, .T. ) ;
#63476=CARTESIAN_POINT ( 'NONE',  ( 2.000000000000001776, -1.693411908627144635, -7.306323022404617618 ) ) ;
#63477=AXIS2_PLACEMENT_3D ( 'NONE', #39751, #55370, #9157 ) ;
#63480=DIRECTION ( 'NONE',  ( 0.000000000000000000, 0.3193015301359742319, 0.9476531711828044546 ) ) ;
#63492=DIRECTION ( 'NONE',  ( 0.000000000000000000, 0.000000000000000000, 1.000000000000000000 ) ) ;
#63495=ADVANCED_FACE ( 'NONE', ( #55978 ), #27560, .F. ) ;
#63498=EDGE_CURVE ( 'NONE', #34267, #44216, #1380, .T. ) ;
#63505=ORIENTED_EDGE ( 'NONE', *, *, #7197, .T. ) ;
#63507=EDGE_CURVE ( 'NONE', #30401, #6868, #41009, .T. ) ;
#63509=AXIS2_PLACEMENT_3D ( 'NONE', #17862, #48144, #1275 ) ;
#63513=LINE ( 'NONE', #58566, #35601 ) ;
#63515=ORIENTED_EDGE ( 'NONE', *, *, #789, .F. ) ;
#63527=CYLINDRICAL_SURFACE ( 'NONE', #51062, 7.499999999999988454 ) ;
#63529=CYLINDRICAL_SURFACE ( 'NONE', #20400, 2.899999999999994582 ) ;
#63534=ORIENTED_EDGE ( 'NONE', *, *, #33652, .T. ) ;
#63536=CARTESIAN_POINT ( 'NONE',  ( -35.04709527796842394, 0.001082316405385738700, -0.01231589140599127774 ) ) ;
#63548=ORIENTED_EDGE ( 'NONE', *, *, #4123, .F. ) ;
#63556=DIRECTION ( 'NONE',  ( 0.000000000000000000, -0.2149704402110318713, 0.9766205557100849921 ) ) ;
#63561=CARTESIAN_POINT ( 'NONE',  ( 2.000000000000001776, 0.000000000000000000, 0.000000000000000000 ) ) ;
#63562=CARTESIAN_POINT ( 'NONE',  ( -22.39032720737627002, -0.9101257950220824622, 3.916738514147011685 ) ) ;
#63564=ORIENTED_EDGE ( 'NONE', *, *, #23214, .T. ) ;
#63565=DIRECTION ( 'NONE',  ( 0.000000000000000000, 0.000000000000000000, -1.000000000000000000 ) ) ;
#63568=DIRECTION ( 'NONE',  ( -1.000000000000000000, 0.000000000000000000, 0.000000000000000000 ) ) ;
#63572=ORIENTED_EDGE ( 'NONE', *, *, #58501, .F. ) ;
#63575=ORIENTED_EDGE ( 'NONE', *, *, #63949, .T. ) ;
#63584=DIRECTION ( 'NONE',  ( 0.000000000000000000, 0.000000000000000000, 1.000000000000000000 ) ) ;
#63593=EDGE_CURVE ( 'NONE', #55770, #36445, #48087, .T. ) ;
#63597=EDGE_LOOP ( 'NONE', ( #36992, #2477, #7145, #24352 ) ) ;
#63598=CYLINDRICAL_SURFACE ( 'NONE', #27358, 7.499999999999988454 ) ;
#63607=CIRCLE ( 'NONE', #36015, 2.899999999999995026 ) ;
#63608=ORIENTED_EDGE ( 'NONE', *, *, #48461, .F. ) ;
#63610=ORIENTED_EDGE ( 'NONE', *, *, #28431, .T. ) ;
#63612=LINE ( 'NONE', #38353, #47660 ) ;
#63613=CARTESIAN_POINT ( 'NONE',  ( -22.30527770659433173, 3.381761229713386552, 1.656864125491224193 ) ) ;
#63615=DIRECTION ( 'NONE',  ( 0.000000000000000000, 0.000000000000000000, 1.000000000000000000 ) ) ;
#63616=CARTESIAN_POINT ( 'NONE',  ( -22.28023996335807411, 2.118259050016095379, 3.022323476748264515 ) ) ;
#63625=EDGE_CURVE ( 'NONE', #14997, #21918, #37586, .T. ) ;
#63627=CARTESIAN_POINT ( 'NONE',  ( 2.000000000000001776, -3.786546189469212731, 5.663561025469122434 ) ) ;
#63638=AXIS2_PLACEMENT_3D ( 'NONE', #18311, #48261, #13615 ) ;
#63639=CARTESIAN_POINT ( 'NONE',  ( -10.00000000000000178, 0.000000000000000000, 0.000000000000000000 ) ) ;
#63647=DIRECTION ( 'NONE',  ( 0.000000000000000000, 0.000000000000000000, 1.000000000000000000 ) ) ;
#63652=EDGE_CURVE ( 'NONE', #55219, #42057, #23260, .T. ) ;
#63653=B_SPLINE_CURVE_WITH_KNOTS ( 'NONE', 3,
 ( #23294, #12637, #13625, #8325, #32916, #53888, #17979, #42913, #22977, #38239, #33601, #3363, #7677, #27961, #58561, #48909, #42561, #53231, #23631, #2717, #28599, #48270 ),
 .UNSPECIFIED., .F., .F.,
 ( 4, 3, 3, 3, 3, 3, 3, 4 ),
 ( 0.000000000000000000, 4.447697177976545497E-05, 6.624143997791643668E-05, 8.800576886944832850E-05, 0.0001097699864780960676, 0.0001315341395364451067, 0.0001760120188223387831, 0.0001867971373174843357 ),
 .UNSPECIFIED. ) ;
#63654=ORIENTED_EDGE ( 'NONE', *, *, #41966, .T. ) ;
#63655=EDGE_CURVE ( 'NONE', #4485, #451, #2436, .T. ) ;
#63656=CARTESIAN_POINT ( 'NONE',  ( 0.000000000000000000, 7.414200355365271555, -1.131208685655096691 ) ) ;
#63660=DIRECTION ( 'NONE',  ( -1.000000000000000000, 0.000000000000000000, 0.000000000000000000 ) ) ;
#63662=CYLINDRICAL_SURFACE ( 'NONE', #45099, 2.899999999999994582 ) ;
#63664=ORIENTED_EDGE ( 'NONE', *, *, #54758, .F. ) ;
#63666=EDGE_LOOP ( 'NONE', ( #1231, #19129, #41520, #7251 ) ) ;
#63668=VERTEX_POINT ( 'NONE', #2777 ) ;
#63674=VECTOR ( 'NONE', #24457, 1000.000000000000000 ) ;
#63676=EDGE_CURVE ( 'NONE', #54376, #44474, #54449, .T. ) ;
#63679=ORIENTED_EDGE ( 'NONE', *, *, #34370, .T. ) ;
#63680=CARTESIAN_POINT ( 'NONE',  ( -22.27706485742869091, 0.3729136217356220917, 3.662257305743802149 ) ) ;
#63684=FACE_OUTER_BOUND ( 'NONE', #16153, .T. ) ;
#63687=VERTEX_POINT ( 'NONE', #58628 ) ;
#63691=CARTESIAN_POINT ( 'NONE',  ( 2.000000000000001776, 2.315790869867166091, -7.133520354428107169 ) ) ;
#63694=CARTESIAN_POINT ( 'NONE',  ( -27.08871896697731785, -1.896680818246860412, 1.309412067287320847 ) ) ;
#63696=VECTOR ( 'NONE', #26793, 1000.000000000000000 ) ;
#63702=LINE ( 'NONE', #64045, #63674 ) ;
#63706=EDGE_CURVE ( 'NONE', #36273, #46695, #18387, .T. ) ;
#63713=EDGE_CURVE ( 'NONE', #27787, #22102, #22419, .T. ) ;
#63716=CARTESIAN_POINT ( 'NONE',  ( -22.28546858134833641, -2.587024666338645584, 2.654201075783120700 ) ) ;
#63722=CARTESIAN_POINT ( 'NONE',  ( 0.000000000000000000, -5.585096664091960150, 4.113602740025890547 ) ) ;
#63723=DIRECTION ( 'NONE',  ( -1.000000000000000000, 0.000000000000000000, 0.000000000000000000 ) ) ;
#63724=EDGE_LOOP ( 'NONE', ( #15813, #447, #37034, #41322 ) ) ;
#63729=DIRECTION ( 'NONE',  ( 1.000000000000000000, -0.000000000000000000, -0.000000000000000000 ) ) ;
#63739=AXIS2_PLACEMENT_3D ( 'NONE', #44735, #29145, #5180 ) ;
#63748=ORIENTED_EDGE ( 'NONE', *, *, #22801, .F. ) ;
#63751=CARTESIAN_POINT ( 'NONE',  ( -22.28415773361649954, 2.588610893123072021, -2.647149619609363569 ) ) ;
#63755=VERTEX_POINT ( 'NONE', #59590 ) ;
#63765=ORIENTED_EDGE ( 'NONE', *, *, #56412, .T. ) ;
#63769=CARTESIAN_POINT ( 'NONE',  ( -27.08850691366518859, -1.609738257842364462, 1.648570643966299265 ) ) ;
#63771=CARTESIAN_POINT ( 'NONE',  ( -27.09483304420799143, -2.317106154747429425, 0.1669215111592681211 ) ) ;
#63772=VECTOR ( 'NONE', #16216, 1000.000000000000114 ) ;
#63780=CARTESIAN_POINT ( 'NONE',  ( -22.27719443589224113, 2.737335337013115932, -2.462030382548423546 ) ) ;
#63781=ADVANCED_FACE ( 'NONE', ( #45589 ), #18261, .F. ) ;
#63782=DIRECTION ( 'NONE',  ( -1.000000000000000000, 0.000000000000000000, 0.000000000000000000 ) ) ;
#63786=CARTESIAN_POINT ( 'NONE',  ( -27.08418179957658367, 1.521007404704319388, 1.713622993062704714 ) ) ;
#63789=CIRCLE ( 'NONE', #53224, 2.899999999999995470 ) ;
#63792=EDGE_CURVE ( 'NONE', #8949, #15374, #45941, .T. ) ;
#63805=CARTESIAN_POINT ( 'NONE',  ( -22.27384469013076185, 3.663183248998794106, -0.3730095848193202279 ) ) ;
#63807=CARTESIAN_POINT ( 'NONE',  ( -27.09861164373112885, 2.097104182796081240, 1.025570525056623161 ) ) ;
#63820=ORIENTED_EDGE ( 'NONE', *, *, #44195, .T. ) ;
#63822=CARTESIAN_POINT ( 'NONE',  ( 0.000000000000000000, 0.000000000000000000, 0.000000000000000000 ) ) ;
#63829=CARTESIAN_POINT ( 'NONE',  ( -22.28023996335807411, -2.118259050016081613, -3.022323476748290716 ) ) ;
#63832=VERTEX_POINT ( 'NONE', #34623 ) ;
#63834=CIRCLE ( 'NONE', #25595, 2.899999999999995026 ) ;
#63836=CARTESIAN_POINT ( 'NONE',  ( 2.000000000000001776, -5.888698556700742159, -3.665823448873470003 ) ) ;
#63842=CARTESIAN_POINT ( 'NONE',  ( 0.000000000000000000, 0.000000000000000000, 0.000000000000000000 ) ) ;
#63843=DIRECTION ( 'NONE',  ( -1.000000000000000000, 0.000000000000000000, 0.000000000000000000 ) ) ;
#63845=ORIENTED_EDGE ( 'NONE', *, *, #4672, .T. ) ;
#63852=VECTOR ( 'NONE', #58083, 1000.000000000000000 ) ;
#63864=CARTESIAN_POINT ( 'NONE',  ( 2.000000000000001776, -5.585096664091900642, -4.113602740025990911 ) ) ;
#63867=AXIS2_PLACEMENT_3D ( 'NONE', #59945, #9059, #44296 ) ;
#63871=DIRECTION ( 'NONE',  ( -1.000000000000000000, 0.000000000000000000, 0.000000000000000000 ) ) ;
#63874=VERTEX_POINT ( 'NONE', #1374 ) ;
#63886=CARTESIAN_POINT ( 'NONE',  ( -27.08418179957658367, 2.174042548349535586, 0.7235373421492506951 ) ) ;
#63891=CARTESIAN_POINT ( 'NONE',  ( 0.000000000000000000, -6.906413915731167918, -0.6453518998148343178 ) ) ;
#63898=AXIS2_PLACEMENT_3D ( 'NONE', #65625, #55687, #10125 ) ;
#63904=DIRECTION ( 'NONE',  ( 0.000000000000000000, 0.000000000000000000, 1.000000000000000000 ) ) ;
#63910=DIRECTION ( 'NONE',  ( 0.000000000000000000, 0.000000000000000000, 1.000000000000000000 ) ) ;
#63927=CARTESIAN_POINT ( 'NONE',  ( -22.27706485742869091, -2.580541389029911148, -2.625261754997698205 ) ) ;
#63931=ORIENTED_EDGE ( 'NONE', *, *, #13597, .F. ) ;
#63939=CARTESIAN_POINT ( 'NONE',  ( 0.000000000000000000, -4.409940824963459960, 5.354199675985231721 ) ) ;
#63944=CARTESIAN_POINT ( 'NONE',  ( -35.04834644901396956, 0.01046409687784605365, 0.009049049589488470172 ) ) ;
#63947=VECTOR ( 'NONE', #30613, 1000.000000000000000 ) ;
#63949=EDGE_CURVE ( 'NONE', #1369, #58016, #16053, .T. ) ;
#63950=DIRECTION ( 'NONE',  ( 0.000000000000000000, 0.000000000000000000, 1.000000000000000000 ) ) ;
#63951=CARTESIAN_POINT ( 'NONE',  ( -22.28546858134833286, -3.592117891549503117, -0.9133285433746950455 ) ) ;
#63957=LINE ( 'NONE', #18434, #30652 ) ;
#63966=CARTESIAN_POINT ( 'NONE',  ( -27.08429572838383947, -0.6096735944848084010, 2.208905845566022208 ) ) ;
#63971=VECTOR ( 'NONE', #44219, 1000.000000000000000 ) ;
#63974=CARTESIAN_POINT ( 'NONE',  ( 2.000000000000001776, -1.693411908627248774, 7.306323022404580314 ) ) ;
#63975=DIRECTION ( 'NONE',  ( -1.000000000000000000, 0.000000000000000000, 0.000000000000000000 ) ) ;
#63983=CARTESIAN_POINT ( 'NONE',  ( 2.000000000000001776, 1.018311147294167274, 6.861346417234447159 ) ) ;
#63996=CARTESIAN_POINT ( 'NONE',  ( -27.28563798457903644, -1.483130241384912784, 2.487904455214888344 ) ) ;
#63998=VERTEX_POINT ( 'NONE', #14905 ) ;
#64009=ORIENTED_EDGE ( 'NONE', *, *, #61930, .F. ) ;
#64023=CARTESIAN_POINT ( 'NONE',  ( -27.08421723179412410, 0.6782017488087925816, -2.188590898430384790 ) ) ;
#64031=ADVANCED_FACE ( 'NONE', ( #18949 ), #4657, .T. ) ;
#64033=AXIS2_PLACEMENT_3D ( 'NONE', #15957, #26287, #62494 ) ;
#64037=EDGE_CURVE ( 'NONE', #37153, #3684, #44934, .T. ) ;
#64038=CARTESIAN_POINT ( 'NONE',  ( -22.29290468048228036, 3.083035815361912402, -2.097193667172387421 ) ) ;
#64039=AXIS2_PLACEMENT_3D ( 'NONE', #3608, #58459, #52805 ) ;
#64040=CARTESIAN_POINT ( 'NONE',  ( -27.09252613521643127, -1.914180209342509320, 1.304094283668840282 ) ) ;
#64045=CARTESIAN_POINT ( 'NONE',  ( 1.000000000000000888, 7.387287142779368487, -1.295372019972108601 ) ) ;
#64048=DIRECTION ( 'NONE',  ( 0.000000000000000000, 0.000000000000000000, 1.000000000000000000 ) ) ;
#64058=ORIENTED_EDGE ( 'NONE', *, *, #20194, .T. ) ;
#64061=CARTESIAN_POINT ( 'NONE',  ( -22.94572469358971389, -0.4123340087948151322, 4.870584850960092638 ) ) ;
#64067=EDGE_CURVE ( 'NONE', #43944, #10662, #11983, .T. ) ;
#64088=DIRECTION ( 'NONE',  ( -1.000000000000000000, 0.000000000000000000, 0.000000000000000000 ) ) ;
#64093=CARTESIAN_POINT ( 'NONE',  ( -27.10719052120871098, -1.962717903527672059, 1.310802520592011966 ) ) ;
#64101=CARTESIAN_POINT ( 'NONE',  ( -22.27706089016750113, 2.622757446538697579, -2.583072118615352242 ) ) ;
#64102=DIRECTION ( 'NONE',  ( -1.000000000000000000, 0.000000000000000000, 0.000000000000000000 ) ) ;
#64103=CIRCLE ( 'NONE', #42883, 7.499999999999988454 ) ;
#64104=CARTESIAN_POINT ( 'NONE',  ( -22.28023996335807411, -1.558279384310075510, 3.345627887484353913 ) ) ;
#64110=ORIENTED_EDGE ( 'NONE', *, *, #17360, .F. ) ;
#64111=CARTESIAN_POINT ( 'NONE',  ( 1.000000000000000888, 7.484036900328569608, -0.4890722589968761191 ) ) ;
#64122=CARTESIAN_POINT ( 'NONE',  ( 2.000000000000001776, 6.906413915731192787, 0.6453518998147528274 ) ) ;
#64124=DIRECTION ( 'NONE',  ( -0.9606638835031803270, -0.1984016392583687061, 0.1943236796486219886 ) ) ;
#64130=CARTESIAN_POINT ( 'NONE',  ( 2.000000000000001776, -6.586971819220303281, -3.586335490831480843 ) ) ;
#64135=CARTESIAN_POINT ( 'NONE',  ( -22.46225619532222595, -3.586917175123511381, 2.255146441673801405 ) ) ;
#64137=DIRECTION ( 'NONE',  ( 0.000000000000000000, 0.000000000000000000, 1.000000000000000000 ) ) ;
#64142=CARTESIAN_POINT ( 'NONE',  ( 2.000000000000001776, -2.664846396702537312, 6.404188155572974495 ) ) ;
#64152=FACE_OUTER_BOUND ( 'NONE', #24571, .T. ) ;
#64153=B_SPLINE_CURVE_WITH_KNOTS ( 'NONE', 3,
 ( #49304, #3752, #19348, #19013, #33961, #35270 ),
 .UNSPECIFIED., .F., .F.,
 ( 4, 2, 4 ),
 ( 0.0002637379172157169513, 0.0009975831966609807061, 0.001731428476106244407 ),
 .UNSPECIFIED. ) ;
#64155=CARTESIAN_POINT ( 'NONE',  ( -22.29382655386184808, 2.689927793811030643, 2.586160974799802226 ) ) ;
#64158=DIRECTION ( 'NONE',  ( -1.000000000000000000, 0.000000000000000000, 0.000000000000000000 ) ) ;
#64159=ORIENTED_EDGE ( 'NONE', *, *, #57035, .F. ) ;
#64160=DIRECTION ( 'NONE',  ( 0.000000000000000000, 0.9868265225415254749, 0.1617819965527686199 ) ) ;
#64165=AXIS2_PLACEMENT_3D ( 'NONE', #1285, #16571, #47485 ) ;
#64170=CARTESIAN_POINT ( 'NONE',  ( -27.10512513516275845, 2.256292013315186473, -0.6711200423626798583 ) ) ;
#64179=ORIENTED_EDGE ( 'NONE', *, *, #3993, .T. ) ;
#64180=ORIENTED_EDGE ( 'NONE', *, *, #62091, .T. ) ;
#64184=EDGE_CURVE ( 'NONE', #22230, #58425, #60459, .T. ) ;
#64192=DIRECTION ( 'NONE',  ( 0.000000000000000000, 0.000000000000000000, 1.000000000000000000 ) ) ;
#64197=ORIENTED_EDGE ( 'NONE', *, *, #22832, .F. ) ;
#64207=DIRECTION ( 'NONE',  ( -1.000000000000000000, 0.000000000000000000, 0.000000000000000000 ) ) ;
#64208=CARTESIAN_POINT ( 'NONE',  ( -22.59983133926798260, -4.650609684383241849, -0.06110861519531800984 ) ) ;
#64211=EDGE_LOOP ( 'NONE', ( #56126, #49270, #19930, #63564 ) ) ;
#64213=CYLINDRICAL_SURFACE ( 'NONE', #55302, 2.899999999999994582 ) ;
#64216=DIRECTION ( 'NONE',  ( -1.000000000000000000, 0.000000000000000000, 0.000000000000000000 ) ) ;
#64217=CARTESIAN_POINT ( 'NONE',  ( 2.000000000000001776, -1.018311147294094443, -6.861346417234492456 ) ) ;
#64223=CARTESIAN_POINT ( 'NONE',  ( -10.00000000000000178, 0.000000000000000000, 0.000000000000000000 ) ) ;
#64229=EDGE_CURVE ( 'NONE', #65410, #14359, #25908, .T. ) ;
#64232=CARTESIAN_POINT ( 'NONE',  ( -22.27384469013076185, 2.625926801827887846, -2.581192766446249731 ) ) ;
#64236=VECTOR ( 'NONE', #53352, 1000.000000000000000 ) ;
#64237=EDGE_CURVE ( 'NONE', #17594, #55487, #26545, .T. ) ;
#64239=CARTESIAN_POINT ( 'NONE',  ( -23.18047892478189453, 2.037851053449341698, 4.338318103648280299 ) ) ;
#64242=ADVANCED_FACE ( 'NONE', ( #37840 ), #37170, .T. ) ;
#64243=CARTESIAN_POINT ( 'NONE',  ( -22.27706485742869091, -3.563814065926672381, 0.9221835209182321913 ) ) ;
#64252=CARTESIAN_POINT ( 'NONE',  ( -22.28121537037576871, -3.345440028056690274, -1.565596675942159788 ) ) ;
#64255=CARTESIAN_POINT ( 'NONE',  ( -22.27718150314433387, -2.479231311682827066, -2.721613812022972478 ) ) ;
#64264=CARTESIAN_POINT ( 'NONE',  ( 2.000000000000001776, 0.000000000000000000, 0.000000000000000000 ) ) ;
#64287=CARTESIAN_POINT ( 'NONE',  ( -22.28939870658739864, 3.352428181135941543, 1.608176106660523130 ) ) ;
#64290=CARTESIAN_POINT ( 'NONE',  ( -22.28939870658739864, 2.099199915896319268, 3.068935452695135346 ) ) ;
#64299=( GEOMETRIC_REPRESENTATION_CONTEXT ( 3 ) GLOBAL_UNCERTAINTY_ASSIGNED_CONTEXT ( ( #47887 ) ) GLOBAL_UNIT_ASSIGNED_CONTEXT ( ( #34154, #14201, #55431 ) ) REPRESENTATION_CONTEXT ( 'NONE', 'WORKASPACE' ) );
#64300=ADVANCED_FACE ( 'NONE', ( #53135 ), #32178, .T. ) ;
#64307=CYLINDRICAL_SURFACE ( 'NONE', #8123, 6.936499999999988120 ) ;
#64309=CIRCLE ( 'NONE', #39868, 2.899999999999995914 ) ;
#64312=DIRECTION ( 'NONE',  ( 0.000000000000000000, 0.2149704402110246548, -0.9766205557100865464 ) ) ;
#64328=CARTESIAN_POINT ( 'NONE',  ( 2.000000000000001776, -6.906413915731192787, 0.6453518998147164121 ) ) ;
#64332=ORIENTED_EDGE ( 'NONE', *, *, #11703, .F. ) ;
#64340=EDGE_CURVE ( 'NONE', #50020, #34013, #11004, .T. ) ;
#64350=LINE ( 'NONE', #34969, #42111 ) ;
#64354=FACE_OUTER_BOUND ( 'NONE', #3615, .T. ) ;
#64357=DIRECTION ( 'NONE',  ( -1.000000000000000000, -1.685093406416449860E-16, 1.011030131491573426E-17 ) ) ;
#64360=CARTESIAN_POINT ( 'NONE',  ( -27.10719052120871098, -2.261993590776032459, 0.6736837626858792616 ) ) ;
#64364=ORIENTED_EDGE ( 'NONE', *, *, #26352, .F. ) ;
#64366=CARTESIAN_POINT ( 'NONE',  ( 0.000000000000000000, -6.160607635185357367, -4.277489166005654653 ) ) ;
#64368=EDGE_CURVE ( 'NONE', #22798, #3384, #60893, .T. ) ;
#64373=CARTESIAN_POINT ( 'NONE',  ( -27.08579483061203064, -2.081508743190409572, -0.9690219683547880436 ) ) ;
#64377=CARTESIAN_POINT ( 'NONE',  ( -22.28415773361650309, -2.588610893123045820, 2.647149619609370230 ) ) ;
#64384=VERTEX_POINT ( 'NONE', #3264 ) ;
#64385=LINE ( 'NONE', #14172, #34406 ) ;
#64389=DIRECTION ( 'NONE',  ( 0.000000000000000000, 0.000000000000000000, 1.000000000000000000 ) ) ;
#64407=LINE ( 'NONE', #54122, #4536 ) ;
#64410=FILL_AREA_STYLE ('',( #44145 ) ) ;
#64411=EDGE_CURVE ( 'NONE', #5936, #30787, #29480, .T. ) ;
#64412=CARTESIAN_POINT ( 'NONE',  ( -22.29195009621226831, 2.585382421603450442, -2.682867222693505749 ) ) ;
#64414=ADVANCED_FACE ( 'NONE', ( #19190 ), #39461, .T. ) ;
#64415=CARTESIAN_POINT ( 'NONE',  ( -22.31099767395441091, -1.667781795950512347, 3.395517675085599762 ) ) ;
#64421=ORIENTED_EDGE ( 'NONE', *, *, #38876, .F. ) ;
#64429=CARTESIAN_POINT ( 'NONE',  ( -27.08935880048797529, -1.608762129669640606, 1.653090150968469674 ) ) ;
#64430=CARTESIAN_POINT ( 'NONE',  ( -27.10719052120871098, -2.355164825213512003, 0.1538293304135223694 ) ) ;
#64439=CARTESIAN_POINT ( 'NONE',  ( -35.04660725145885891, 0.003326400506041530918, -0.01184012236748529200 ) ) ;
#64445=PRODUCT_DEFINITION ( 'UNKNOWN', '', #3767, #2005 ) ;
#64446=EDGE_CURVE ( 'NONE', #1625, #64819, #28007, .T. ) ;
#64448=CARTESIAN_POINT ( 'NONE',  ( 2.000000000000001776, 0.000000000000000000, 0.000000000000000000 ) ) ;
#64451=ORIENTED_EDGE ( 'NONE', *, *, #52837, .F. ) ;
#64461=LINE ( 'NONE', #18930, #46009 ) ;
#64463=CARTESIAN_POINT ( 'NONE',  ( 2.000000000000001776, 4.444115772890121718, 5.163689623839328391 ) ) ;
#64471=EDGE_CURVE ( 'NONE', #17391, #1614, #35381, .T. ) ;
#64476=ORIENTED_EDGE ( 'NONE', *, *, #11633, .F. ) ;
#64479=CARTESIAN_POINT ( 'NONE',  ( -27.09125059358653331, 2.223272438024538555, -0.6356863790372204726 ) ) ;
#64493=EDGE_CURVE ( 'NONE', #20149, #30137, #52404, .T. ) ;
#64495=VERTEX_POINT ( 'NONE', #62640 ) ;
#64503=CARTESIAN_POINT ( 'NONE',  ( 2.000000000000001776, -6.539067737394485214, -2.314222412769890713 ) ) ;
#64506=ORIENTED_EDGE ( 'NONE', *, *, #25777, .T. ) ;
#64507=DIRECTION ( 'NONE',  ( -1.000000000000000000, 0.000000000000000000, 0.000000000000000000 ) ) ;
#64510=CARTESIAN_POINT ( 'NONE',  ( -22.30398854582848145, 3.656532484463047350, 0.8844201765541789273 ) ) ;
#64511=CARTESIAN_POINT ( 'NONE',  ( 2.000000000000001776, 0.2704997240205054276, 6.931223712253452796 ) ) ;
#64519=ORIENTED_EDGE ( 'NONE', *, *, #52622, .T. ) ;
#64523=AXIS2_PLACEMENT_3D ( 'NONE', #10463, #30738, #51051 ) ;
#64525=ORIENTED_EDGE ( 'NONE', *, *, #927, .F. ) ;
#64530=FACE_OUTER_BOUND ( 'NONE', #61176, .T. ) ;
#64536=CARTESIAN_POINT ( 'NONE',  ( -22.51237073810381162, -3.263711251981912476, -2.986282257334758050 ) ) ;
#64540=LINE ( 'NONE', #4728, #61468 ) ;
#64541=DIRECTION ( 'NONE',  ( -1.000000000000000000, 0.000000000000000000, 0.000000000000000000 ) ) ;
#64542=CARTESIAN_POINT ( 'NONE',  ( 1.000000000000000888, -7.387287142779349836, 1.295372019972131028 ) ) ;
#64543=CYLINDRICAL_SURFACE ( 'NONE', #17323, 7.499999999999988454 ) ;
#64548=CIRCLE ( 'NONE', #4056, 2.899999999999996358 ) ;
#64551=CARTESIAN_POINT ( 'NONE',  ( -22.27721701579900682, -3.615531902032089295, 0.6950008646884325847 ) ) ;
#64553=CIRCLE ( 'NONE', #22094, 2.899999999999994582 ) ;
#64555=ORIENTED_EDGE ( 'NONE', *, *, #16302, .T. ) ;
#64561=ORIENTED_EDGE ( 'NONE', *, *, #58362, .T. ) ;
#64562=CARTESIAN_POINT ( 'NONE',  ( 0.000000000000000000, -1.530946385938423582, 7.342084388195347699 ) ) ;
#64566=ORIENTED_EDGE ( 'NONE', *, *, #34321, .F. ) ;
#64570=DIRECTION ( 'NONE',  ( -1.000000000000000000, 0.000000000000000000, 0.000000000000000000 ) ) ;
#64573=EDGE_LOOP ( 'NONE', ( #49740, #47089, #53301, #6909 ) ) ;
#64577=CARTESIAN_POINT ( 'NONE',  ( -35.05175862995318425, 0.01253051761585140256, -0.001087818442121676887 ) ) ;
#64579=DIRECTION ( 'NONE',  ( 0.000000000000000000, 0.000000000000000000, 1.000000000000000000 ) ) ;
#64582=CARTESIAN_POINT ( 'NONE',  ( 2.000000000000001776, -2.480520636974139936, -6.345145617221269241 ) ) ;
#64583=CARTESIAN_POINT ( 'NONE',  ( 0.000000000000000000, 6.643843315911800218, 1.507714007300793968 ) ) ;
#64585=ORIENTED_EDGE ( 'NONE', *, *, #35520, .F. ) ;
#64588=CIRCLE ( 'NONE', #35910, 7.499999999999988454 ) ;
#64598=EDGE_CURVE ( 'NONE', #41782, #16541, #12762, .T. ) ;
#64600=AXIS2_PLACEMENT_3D ( 'NONE', #31282, #5033, #61207 ) ;
#64613=EDGE_CURVE ( 'NONE', #57759, #62557, #5709, .T. ) ;
#64615=ORIENTED_EDGE ( 'NONE', *, *, #35849, .T. ) ;
#64619=CIRCLE ( 'NONE', #43361, 2.899999999999995026 ) ;
#64626=CARTESIAN_POINT ( 'NONE',  ( 2.000000000000001776, -3.805198749487401777, -5.799611601383285020 ) ) ;
#64632=ORIENTED_EDGE ( 'NONE', *, *, #59206, .T. ) ;
#64641=( BOUNDED_SURFACE ( )  B_SPLINE_SURFACE ( 3, 1, ( 
 ( #47677, #52017 ),
 ( #38012, #33023 ),
 ( #32371, #52990 ),
 ( #32041, #37704 ) ),
 .UNSPECIFIED., .F., .F., .F. ) 
 B_SPLINE_SURFACE_WITH_KNOTS ( ( 4, 4 ),
 ( 2, 2 ),
 ( 0.000000000000000000, 1.000000000000000000 ),
 ( 0.000000000000000000, 1.000000000000000000 ),
 .UNSPECIFIED. ) 
 GEOMETRIC_REPRESENTATION_ITEM ( )  RATIONAL_B_SPLINE_SURFACE ( (
 ( 1.000000000000000000, 1.000000000000000000),
 ( 0.9257577194822556033, 0.9980522942447415113),
 ( 0.9257577194822556033, 0.9980522942447415113),
 ( 1.000000000000000000, 1.000000000000000000) ) ) 
 REPRESENTATION_ITEM ( '' )  SURFACE ( )  );
#64642=CARTESIAN_POINT ( 'NONE',  ( -22.27218376572352554, -3.330959526935390880, -1.571356284315152285 ) ) ;
#64651=VECTOR ( 'NONE', #56719, 1000.000000000000000 ) ;
#64653=CARTESIAN_POINT ( 'NONE',  ( -27.10719052120871098, -2.116547233941210138, -1.044362304621491377 ) ) ;
#64656=EDGE_CURVE ( 'NONE', #34425, #54645, #35597, .T. ) ;
#64664=CARTESIAN_POINT ( 'NONE',  ( 2.000000000000001776, 0.000000000000000000, 0.000000000000000000 ) ) ;
#64670=EDGE_CURVE ( 'NONE', #57350, #20149, #17371, .T. ) ;
#64671=DIRECTION ( 'NONE',  ( -1.000000000000000000, 0.000000000000000000, 0.000000000000000000 ) ) ;
#64677=CARTESIAN_POINT ( 'NONE',  ( -27.10719052120871098, 1.310802520592036391, 1.962717903527646079 ) ) ;
#64706=VERTEX_POINT ( 'NONE', #40589 ) ;
#64713=DIRECTION ( 'NONE',  ( -1.000000000000000000, 0.000000000000000000, 0.000000000000000000 ) ) ;
#64718=DIRECTION ( 'NONE',  ( 0.9582930651793755139, -0.2568015617827265618, -0.1254087680151175499 ) ) ;
#64719=DIRECTION ( 'NONE',  ( -0.9582930651793754029, 0.1972632429577076685, -0.2067888154783172894 ) ) ;
#64744=CARTESIAN_POINT ( 'NONE',  ( 2.000000000000001776, -5.450255447309769963, 4.087611905901399112 ) ) ;
#64746=LINE ( 'NONE', #34173, #55374 ) ;
#64747=CARTESIAN_POINT ( 'NONE',  ( -27.08430792439084556, -1.625846845508331695, 1.614882584890338757 ) ) ;
#64748=DIRECTION ( 'NONE',  ( -1.000000000000000000, 0.000000000000000000, 0.000000000000000000 ) ) ;
#64751=LINE ( 'NONE', #28875, #55654 ) ;
#64755=CARTESIAN_POINT ( 'NONE',  ( 2.000000000000001776, -3.786546189469129686, -5.663561025469209476 ) ) ;
#64759=CARTESIAN_POINT ( 'NONE',  ( -22.38932658256920760, -3.361598243548632237, 2.201197575855957211 ) ) ;
#64765=ORIENTED_EDGE ( 'NONE', *, *, #38512, .T. ) ;
#64775=DIRECTION ( 'NONE',  ( -1.000000000000000000, 0.000000000000000000, 0.000000000000000000 ) ) ;
#64778=EDGE_CURVE ( 'NONE', #42091, #25715, #27262, .T. ) ;
#64782=FACE_OUTER_BOUND ( 'NONE', #38169, .T. ) ;
#64786=ORIENTED_EDGE ( 'NONE', *, *, #55240, .T. ) ;
#64788=DIRECTION ( 'NONE',  ( 0.000000000000000000, 0.6051742151937609115, 0.7960930657056469739 ) ) ;
#64796=DIRECTION ( 'NONE',  ( -1.000000000000000000, 0.000000000000000000, 0.000000000000000000 ) ) ;
#64800=CARTESIAN_POINT ( 'NONE',  ( 2.000000000000001776, 1.754183803416655474, -6.711026108862266248 ) ) ;
#64805=ORIENTED_EDGE ( 'NONE', *, *, #45320, .T. ) ;
#64806=CARTESIAN_POINT ( 'NONE',  ( -22.51237073810381517, 4.218051923713606932, -1.333315726166068194 ) ) ;
#64808=EDGE_CURVE ( 'NONE', #52522, #31241, #50369, .T. ) ;
#64819=VERTEX_POINT ( 'NONE', #37577 ) ;
#64823=DIRECTION ( 'NONE',  ( -1.000000000000000000, 0.000000000000000000, 0.000000000000000000 ) ) ;
#64828=AXIS2_PLACEMENT_3D ( 'NONE', #11424, #36701, #6449 ) ;
#64830=CARTESIAN_POINT ( 'NONE',  ( -22.30625920655495165, 1.076742202099183254, 3.635849356906398544 ) ) ;
#64831=CARTESIAN_POINT ( 'NONE',  ( -26.43258404273186812, 3.148308537883197200, -1.478864324198215119 ) ) ;
#64838=VERTEX_POINT ( 'NONE', #1689 ) ;
#64841=VECTOR ( 'NONE', #55127, 1000.000000000000000 ) ;
#64859=CARTESIAN_POINT ( 'NONE',  ( -27.28573687977896611, -1.818142657385560801, 2.255103317860390977 ) ) ;
#64862=VECTOR ( 'NONE', #14417, 1000.000000000000000 ) ;
#64868=EDGE_CURVE ( 'NONE', #28939, #1614, #45031, .T. ) ;
#64869=FACE_OUTER_BOUND ( 'NONE', #60258, .T. ) ;
#64871=FACE_OUTER_BOUND ( 'NONE', #37706, .T. ) ;
#64872=CIRCLE ( 'NONE', #22408, 2.899999999999995914 ) ;
#64876=CARTESIAN_POINT ( 'NONE',  ( -27.10719052120871098, -1.310802520592025955, -1.962717903527680718 ) ) ;
#64878=VECTOR ( 'NONE', #17076, 1000.000000000000000 ) ;
#64880=DIRECTION ( 'NONE',  ( -1.000000000000000000, 0.000000000000000000, 0.000000000000000000 ) ) ;
#64883=AXIS2_PLACEMENT_3D ( 'NONE', #2456, #33355, #44298 ) ;
#64887=EDGE_LOOP ( 'NONE', ( #63515, #41934, #8989, #10871 ) ) ;
#64896=DIRECTION ( 'NONE',  ( -1.000000000000000000, 0.000000000000000000, 0.000000000000000000 ) ) ;
#64904=CARTESIAN_POINT ( 'NONE',  ( -35.04660725145885891, 0.007231372203155804479, 0.009947898977290411948 ) ) ;
#64914=EDGE_CURVE ( 'NONE', #29381, #19030, #18316, .T. ) ;
#64916=VECTOR ( 'NONE', #27753, 999.9999999999998863 ) ;
#64917=CARTESIAN_POINT ( 'NONE',  ( -27.09729107899852352, -0.1622107421537205552, -2.324833743198346347 ) ) ;
#64919=CARTESIAN_POINT ( 'NONE',  ( -27.35552965826136429, -2.810569013793742688, 1.320216934008381804 ) ) ;
#64922=CARTESIAN_POINT ( 'NONE',  ( 0.000000000000000000, 6.338823199656720142, -2.816798305433633853 ) ) ;
#64933=CARTESIAN_POINT ( 'NONE',  ( 0.000000000000000000, -5.097042323172408906, -5.501832381651512449 ) ) ;
#64937=CARTESIAN_POINT ( 'NONE',  ( 2.000000000000001776, 3.979254915827366901, 5.681598592373755530 ) ) ;
#64941=ORIENTED_EDGE ( 'NONE', *, *, #37851, .T. ) ;
#64947=CIRCLE ( 'NONE', #36287, 6.936499999999991672 ) ;
#64955=AXIS2_PLACEMENT_3D ( 'NONE', #32419, #26791, #18128 ) ;
#64956=VECTOR ( 'NONE', #741, 1000.000000000000000 ) ;
#64957=CIRCLE ( 'NONE', #22502, 2.899999999999994582 ) ;
#64959=CARTESIAN_POINT ( 'NONE',  ( 2.000000000000001776, 0.000000000000000000, 0.000000000000000000 ) ) ;
#64969=ORIENTED_EDGE ( 'NONE', *, *, #43492, .F. ) ;
#64988=FACE_OUTER_BOUND ( 'NONE', #21073, .T. ) ;
#64989=AXIS2_PLACEMENT_3D ( 'NONE', #26189, #46463, #11535 ) ;
#64992=CARTESIAN_POINT ( 'NONE',  ( -22.27706089016750113, -0.9798385173596184661, 3.548384797797526691 ) ) ;
#64994=CARTESIAN_POINT ( 'NONE',  ( -35.04709527796842394, 0.01016988845958452514, 0.007030359780618375409 ) ) ;
#64996=FACE_OUTER_BOUND ( 'NONE', #54534, .T. ) ;
#65001=DIRECTION ( 'NONE',  ( 0.000000000000000000, 0.9635499925192236859, -0.2675283385292184235 ) ) ;
#65004=ORIENTED_EDGE ( 'NONE', *, *, #10550, .F. ) ;
#65007=CARTESIAN_POINT ( 'NONE',  ( -22.27878402819508352, 0.9457981527432597346, -3.562981801125743697 ) ) ;
#65009=CARTESIAN_POINT ( 'NONE',  ( -22.27720387087365239, 1.337073746937897711, -3.430312021254875443 ) ) ;
#65010=CIRCLE ( 'NONE', #7693, 2.899999999999995026 ) ;
#65022=B_SPLINE_CURVE_WITH_KNOTS ( 'NONE', 3,
 ( #53396, #12805, #41181, #27135, #35852, #56152, #10595, #5647, #46204, #11823, #32106, #52423, #1867, #42391, #49711, #44064, #44369, #23453, #53726, #18802, #24422, #8819 ),
 .UNSPECIFIED., .F., .F.,
 ( 4, 3, 3, 3, 3, 3, 3, 4 ),
 ( 0.000000000000000000, 6.990956068646337414E-05, 0.0001398191187764040878, 0.0002097286751720215986, 0.0002796382307041359386, 0.0003495477861619810745, 0.0004194573423310289542, 0.0005586102576333142793 ),
 .UNSPECIFIED. ) ;
#65023=AXIS2_PLACEMENT_3D ( 'NONE', #5730, #10679, #51928 ) ;
#65028=ORIENTED_EDGE ( 'NONE', *, *, #26273, .F. ) ;
#65031=CARTESIAN_POINT ( 'NONE',  ( 2.000000000000001776, -6.643843315911820646, 1.507714007300648307 ) ) ;
#65048=CARTESIAN_POINT ( 'NONE',  ( -27.08429572838383947, 2.208905845566027537, 0.6096735944847788691 ) ) ;
#65049=CIRCLE ( 'NONE', #35340, 2.899999999999995026 ) ;
#65053=EDGE_LOOP ( 'NONE', ( #4958, #59243, #49339, #55789 ) ) ;
#65061=CARTESIAN_POINT ( 'NONE',  ( -27.35552965826137140, 2.810569013793760007, -1.320216934008374920 ) ) ;
#65063=VERTEX_POINT ( 'NONE', #36446 ) ;
#65064=ADVANCED_FACE ( 'NONE', ( #228 ), #54380, .F. ) ;
#65069=AXIS2_PLACEMENT_3D ( 'NONE', #56837, #12234, #52161 ) ;
#65080=ORIENTED_EDGE ( 'NONE', *, *, #53469, .T. ) ;
#65087=CARTESIAN_POINT ( 'NONE',  ( 2.000000000000001776, 0.000000000000000000, 0.000000000000000000 ) ) ;
#65091=CARTESIAN_POINT ( 'NONE',  ( 2.000000000000001776, -2.469490258309361419, -6.482025155313371201 ) ) ;
#65101=CYLINDRICAL_SURFACE ( 'NONE', #4357, 2.899999999999994582 ) ;
#65120=CARTESIAN_POINT ( 'NONE',  ( -27.09364415740165555, 2.088137158971423268, 1.009938549038068567 ) ) ;
#65138=VERTEX_POINT ( 'NONE', #62052 ) ;
#65140=ORIENTED_EDGE ( 'NONE', *, *, #64598, .F. ) ;
#65174=VERTEX_POINT ( 'NONE', #58048 ) ;
#65175=EDGE_CURVE ( 'NONE', #28152, #25175, #62353, .T. ) ;
#65182=EDGE_CURVE ( 'NONE', #52513, #27353, #60943, .T. ) ;
#65194=AXIS2_PLACEMENT_3D ( 'NONE', #34595, #9, #49907 ) ;
#65197=ORIENTED_EDGE ( 'NONE', *, *, #55583, .T. ) ;
#65199=CARTESIAN_POINT ( 'NONE',  ( 1.000000000000000888, -0.7281529553921430864, -7.464569195442815719 ) ) ;
#65201=CARTESIAN_POINT ( 'NONE',  ( 0.000000000000000000, -6.643843315911796665, -1.507714007300762660 ) ) ;
#65213=DIRECTION ( 'NONE',  ( 0.000000000000000000, 0.000000000000000000, 1.000000000000000000 ) ) ;
#65215=DIRECTION ( 'NONE',  ( 0.000000000000000000, -0.5155538571770286183, 0.8568571761675851661 ) ) ;
#65221=ORIENTED_EDGE ( 'NONE', *, *, #51117, .T. ) ;
#65225=CIRCLE ( 'NONE', #36572, 7.499999999999988454 ) ;
#65230=ORIENTED_EDGE ( 'NONE', *, *, #3428, .F. ) ;
#65231=ORIENTED_EDGE ( 'NONE', *, *, #23764, .F. ) ;
#65233=EDGE_CURVE ( 'NONE', #23443, #21834, #28756, .T. ) ;
#65242=( BOUNDED_SURFACE ( )  B_SPLINE_SURFACE ( 3, 1, ( 
 ( #7945, #17589 ),
 ( #47517, #33529 ),
 ( #37856, #7256 ),
 ( #27541, #63437 ) ),
 .UNSPECIFIED., .F., .F., .F. ) 
 B_SPLINE_SURFACE_WITH_KNOTS ( ( 4, 4 ),
 ( 2, 2 ),
 ( 0.000000000000000000, 1.000000000000000000 ),
 ( 0.000000000000000000, 1.000000000000000000 ),
 .UNSPECIFIED. ) 
 GEOMETRIC_REPRESENTATION_ITEM ( )  RATIONAL_B_SPLINE_SURFACE ( (
 ( 1.000000000000000000, 1.000000000000000000),
 ( 0.9932032654565553509, 0.8386279382598736953),
 ( 0.9932032654565553509, 0.8386279382598736953),
 ( 1.000000000000000000, 1.000000000000000000) ) ) 
 REPRESENTATION_ITEM ( '' )  SURFACE ( )  );
#65246=DIRECTION ( 'NONE',  ( 0.000000000000000000, 0.000000000000000000, 1.000000000000000000 ) ) ;
#65247=ORIENTED_EDGE ( 'NONE', *, *, #54006, .T. ) ;
#65248=CARTESIAN_POINT ( 'NONE',  ( 2.000000000000001776, 0.000000000000000000, 0.000000000000000000 ) ) ;
#65251=CARTESIAN_POINT ( 'NONE',  ( 2.000000000000001776, 1.956810415765184219, 6.654767106875543625 ) ) ;
#65258=DIRECTION ( 'NONE',  ( -1.000000000000000000, 0.000000000000000000, 0.000000000000000000 ) ) ;
#65259=FACE_OUTER_BOUND ( 'NONE', #24525, .T. ) ;
#65261=CARTESIAN_POINT ( 'NONE',  ( -27.08429572838383947, 2.217805374070540125, -0.5764601019425888984 ) ) ;
#65266=VERTEX_POINT ( 'NONE', #39379 ) ;
#65270=ORIENTED_EDGE ( 'NONE', *, *, #22626, .F. ) ;
#65279=DIRECTION ( 'NONE',  ( -1.977578355587678392E-17, 0.1764146379942750364, 0.9843159429275484262 ) ) ;
#65285=ADVANCED_FACE ( 'NONE', ( #33735 ), #49405, .T. ) ;
#65295=CARTESIAN_POINT ( 'NONE',  ( -27.10719052120871098, 0.1538293304135379680, 2.355164825213503121 ) ) ;
#65301=ORIENTED_EDGE ( 'NONE', *, *, #55381, .T. ) ;
#65307=EDGE_LOOP ( 'NONE', ( #34578, #62886, #12768, #26712 ) ) ;
#65308=ORIENTED_EDGE ( 'NONE', *, *, #38897, .F. ) ;
#65312=DIRECTION ( 'NONE',  ( 0.000000000000000000, -6.879075853011489629E-15, 1.000000000000000000 ) ) ;
#65315=CARTESIAN_POINT ( 'NONE',  ( 2.000000000000001776, 0.000000000000000000, 0.000000000000000000 ) ) ;
#65319=VERTEX_POINT ( 'NONE', #19450 ) ;
#65321=ORIENTED_EDGE ( 'NONE', *, *, #60966, .F. ) ;
#65322=DIRECTION ( 'NONE',  ( 1.000000000000000000, 0.000000000000000000, 0.000000000000000000 ) ) ;
#65325=CARTESIAN_POINT ( 'NONE',  ( -22.29770266787582500, -0.8895590726606950049, 3.635870259503088064 ) ) ;
#65331=CYLINDRICAL_SURFACE ( 'NONE', #52620, 2.899999999999994582 ) ;
#65333=ORIENTED_EDGE ( 'NONE', *, *, #58242, .F. ) ;
#65336=VERTEX_POINT ( 'NONE', #63656 ) ;
#65348=EDGE_LOOP ( 'NONE', ( #33983, #17802, #1909, #57679 ) ) ;
#65351=CIRCLE ( 'NONE', #18690, 3.552075659825890241 ) ;
#65354=EDGE_CURVE ( 'NONE', #47008, #45297, #29142, .T. ) ;
#65358=VERTEX_POINT ( 'NONE', #56312 ) ;
#65359=CARTESIAN_POINT ( 'NONE',  ( 0.000000000000000000, 0.000000000000000000, 0.000000000000000000 ) ) ;
#65365=DIRECTION ( 'NONE',  ( -1.000000000000000000, 0.000000000000000000, 0.000000000000000000 ) ) ;
#65373=CARTESIAN_POINT ( 'NONE',  ( -22.30861784526115699, -1.070462554923801601, -3.620936716852776627 ) ) ;
#65381=FACE_OUTER_BOUND ( 'NONE', #34576, .T. ) ;
#65393=ORIENTED_EDGE ( 'NONE', *, *, #2861, .T. ) ;
#65400=EDGE_CURVE ( 'NONE', #50412, #48610, #49340, .T. ) ;
#65406=EDGE_CURVE ( 'NONE', #58425, #52767, #51360, .T. ) ;
#65410=VERTEX_POINT ( 'NONE', #55678 ) ;
#65417=DIRECTION ( 'NONE',  ( 0.000000000000000000, -0.1081190184239280011, -0.9941379571543611515 ) ) ;
#65418=B_SPLINE_CURVE_WITH_KNOTS ( 'NONE', 3,
 ( #23365, #23046, #18399, #7753, #18054, #64252, #52963, #47990, #39882, #8084, #38316, #38664, #58638, #62940, #63261, #58969, #48649, #42635, #28351, #13381, #13062, #33666 ),
 .UNSPECIFIED., .F., .F.,
 ( 4, 3, 3, 3, 3, 3, 3, 4 ),
 ( 0.000000000000000000, 4.447697177976158572E-05, 6.624143997791090725E-05, 8.800576886944027830E-05, 0.0001097699864780866350, 0.0001315341395364341833, 0.0001760120188223243090, 0.0001867971373174694279 ),
 .UNSPECIFIED. ) ;
#65430=CARTESIAN_POINT ( 'NONE',  ( -22.28023996335807411, -3.676538434326165561, 0.3233044107360762420 ) ) ;
#65436=DIRECTION ( 'NONE',  ( -1.000000000000000000, 0.000000000000000000, 0.000000000000000000 ) ) ;
#65437=LINE ( 'NONE', #290, #27858 ) ;
#65442=LINE ( 'NONE', #29238, #51032 ) ;
#65446=ORIENTED_EDGE ( 'NONE', *, *, #27389, .T. ) ;
#65458=CARTESIAN_POINT ( 'NONE',  ( -22.27706485742869091, -3.358064672837095976, -1.508175983031630585 ) ) ;
#65479=ORIENTED_EDGE ( 'NONE', *, *, #36269, .F. ) ;
#65486=CARTESIAN_POINT ( 'NONE',  ( 2.000000000000001776, -0.8935325819928070512, -7.446583077151393226 ) ) ;
#65489=CARTESIAN_POINT ( 'NONE',  ( -22.30625920655495165, -1.672644928563074451, 3.403091720605004866 ) ) ;
#65490=VERTEX_POINT ( 'NONE', #793 ) ;
#65517=AXIS2_PLACEMENT_3D ( 'NONE', #32752, #12165, #22478 ) ;
#65520=CARTESIAN_POINT ( 'NONE',  ( 1.000000000000000888, 6.586971819220387658, -3.586335490831350725 ) ) ;
#65521=EDGE_CURVE ( 'NONE', #63755, #63127, #6833, .T. ) ;
#65526=ORIENTED_EDGE ( 'NONE', *, *, #30837, .T. ) ;
#65527=CARTESIAN_POINT ( 'NONE',  ( -27.09150307427447757, -1.305148381377968070, -1.909742362151680917 ) ) ;
#65531=CARTESIAN_POINT ( 'NONE',  ( -22.27715526084302056, -3.652257391294512878, 0.4651416883073748454 ) ) ;
#65536=ORIENTED_EDGE ( 'NONE', *, *, #44253, .F. ) ;
#65538=CARTESIAN_POINT ( 'NONE',  ( -27.15511094194037867, 2.499833641087587655, -0.1446243978645330164 ) ) ;
#65559=DIRECTION ( 'NONE',  ( -1.000000000000000000, 0.000000000000000000, 0.000000000000000000 ) ) ;
#65563=CARTESIAN_POINT ( 'NONE',  ( 2.000000000000001776, 6.662861565602083758, -1.421313227905602883 ) ) ;
#65564=CIRCLE ( 'NONE', #51788, 6.936499999999988120 ) ;
#65566=CARTESIAN_POINT ( 'NONE',  ( -27.08423923533013422, 2.274768056034765173, -0.2759775751761893714 ) ) ;
#65567=DIRECTION ( 'NONE',  ( -1.000000000000000000, 0.000000000000000000, 0.000000000000000000 ) ) ;
#65570=CARTESIAN_POINT ( 'NONE',  ( -22.66110217412718697, -4.941631093908260830, -0.1747008913564142285 ) ) ;
#65576=ADVANCED_FACE ( 'NONE', ( #7399 ), #62597, .T. ) ;
#65579=CARTESIAN_POINT ( 'NONE',  ( -27.10719052120871098, -0.6736837626858844796, -2.261993590776034235 ) ) ;
#65580=CARTESIAN_POINT ( 'NONE',  ( -22.30986928587821794, 1.665628047792451216, -3.392803916780399831 ) ) ;
#65604=( BOUNDED_SURFACE ( )  B_SPLINE_SURFACE ( 3, 1, ( 
 ( #3977, #17956 ),
 ( #24240, #38217 ),
 ( #33889, #33244 ),
 ( #23269, #34217 ) ),
 .UNSPECIFIED., .F., .F., .F. ) 
 B_SPLINE_SURFACE_WITH_KNOTS ( ( 4, 4 ),
 ( 2, 2 ),
 ( 0.000000000000000000, 1.000000000000000000 ),
 ( 0.000000000000000000, 1.000000000000000000 ),
 .UNSPECIFIED. ) 
 GEOMETRIC_REPRESENTATION_ITEM ( )  RATIONAL_B_SPLINE_SURFACE ( (
 ( 1.000000000000000000, 1.000000000000000000),
 ( 0.9257577194822556033, 0.9980522942447415113),
 ( 0.9257577194822556033, 0.9980522942447415113),
 ( 1.000000000000000000, 1.000000000000000000) ) ) 
 REPRESENTATION_ITEM ( '' )  SURFACE ( )  );
#65606=CARTESIAN_POINT ( 'NONE',  ( -22.30625920655495165, 3.687109008463850479, 0.8854385781085043483 ) ) ;
#65607=DIRECTION ( 'NONE',  ( -1.000000000000000000, 0.000000000000000000, 0.000000000000000000 ) ) ;
#65613=ORIENTED_EDGE ( 'NONE', *, *, #46594, .F. ) ;
#65616=ORIENTED_EDGE ( 'NONE', *, *, #38456, .T. ) ;
#65625=CARTESIAN_POINT ( 'NONE',  ( 2.000000000000001776, -4.976357229393820525, -4.652926418895619420 ) ) ;
#65626=ORIENTED_EDGE ( 'NONE', *, *, #35099, .F. ) ;
#65635=DIRECTION ( 'NONE',  ( 0.000000000000000000, 0.000000000000000000, 1.000000000000000000 ) ) ;
#65638=VERTEX_POINT ( 'NONE', #64562 ) ;
#65644=ORIENTED_EDGE ( 'NONE', *, *, #5047, .T. ) ;
#65654=CARTESIAN_POINT ( 'NONE',  ( -22.27721056931765631, 1.183805672860844815, -3.486117586310724104 ) ) ;
#65658=VERTEX_POINT ( 'NONE', #8399 ) ;
#65659=DIRECTION ( 'NONE',  ( 0.000000000000000000, 0.000000000000000000, 1.000000000000000000 ) ) ;
#65664=DIRECTION ( 'NONE',  ( -1.000000000000000000, 0.000000000000000000, 0.000000000000000000 ) ) ;
#65673=EDGE_CURVE ( 'NONE', #11147, #58967, #55761, .T. ) ;
#65675=EDGE_CURVE ( 'NONE', #4186, #51107, #61868, .T. ) ;
#65680=CARTESIAN_POINT ( 'NONE',  ( -27.20164183316783024, -2.339520810540427931, -1.232966507052649430 ) ) ;
#65685=LINE ( 'NONE', #20154, #57824 ) ;
#65687=CARTESIAN_POINT ( 'NONE',  ( -22.29978294495153790, -1.052446240539694378, -3.598607126810737356 ) ) ;
#65698=CARTESIAN_POINT ( 'NONE',  ( 0.000000000000000000, -6.936109781200700652, 2.853135311045000400 ) ) ;
#65702=ORIENTED_EDGE ( 'NONE', *, *, #45281, .T. ) ;
#65716=ORIENTED_EDGE ( 'NONE', *, *, #241, .T. ) ;
#65720=CARTESIAN_POINT ( 'NONE',  ( -27.10719052120871098, 0.5475695427849553987, -2.295785794152566339 ) ) ;
#65721=CARTESIAN_POINT ( 'NONE',  ( -27.08430418657511751, 2.280643121250624628, -0.2231435303617068100 ) ) ;
#65725=CARTESIAN_POINT ( 'NONE',  ( 2.000000000000001776, -3.937687286050771895, -6.383151168292510391 ) ) ;
#65739=DIRECTION ( 'NONE',  ( -0.9582930651793755139, 0.2777159889015691219, 0.06744057189511871997 ) ) ;
#65752=CARTESIAN_POINT ( 'NONE',  ( -27.08429572838383947, 2.089332284968718145, 0.9410937941433747955 ) ) ;
#65755=VECTOR ( 'NONE', #38883, 1000.000000000000000 ) ;
#65757=CARTESIAN_POINT ( 'NONE',  ( 0.000000000000000000, 4.915517050588409376, 4.717154614762108622 ) ) ;
#65763=CARTESIAN_POINT ( 'NONE',  ( -27.04788180060269198, -2.923150379392646325, 1.373100113388785237 ) ) ;
#65769=ORIENTED_EDGE ( 'NONE', *, *, #4155, .F. ) ;
#65770=DIRECTION ( 'NONE',  ( -1.000000000000000000, 0.000000000000000000, 0.000000000000000000 ) ) ;
#65775=CARTESIAN_POINT ( 'NONE',  ( -27.20164183316781248, 2.237540722393175585, -1.409601201084038191 ) ) ;
#65795=ORIENTED_EDGE ( 'NONE', *, *, #54329, .T. ) ;
#65798=ORIENTED_EDGE ( 'NONE', *, *, #3544, .F. ) ;
#65802=B_SPLINE_CURVE_WITH_KNOTS ( 'NONE', 3,
 ( #10873, #4598, #588, #4920, #60765, #19870, #55108, #46448, #41441, #26176, #9539, #5920, #9885, #20850, #55445, #50787, #14526, #21171, #65720 ),
 .UNSPECIFIED., .F., .F.,
 ( 4, 3, 3, 3, 3, 3, 4 ),
 ( 0.000000000000000000, 2.832085443540607455E-05, 4.217789847394679871E-05, 5.603488375046066227E-05, 6.989180858579203070E-05, 9.821094829918603994E-05, 0.0001178165571465128561 ),
 .UNSPECIFIED. ) ;
#65803=ORIENTED_EDGE ( 'NONE', *, *, #16671, .T. ) ;
#65804=CARTESIAN_POINT ( 'NONE',  ( 1.000000000000000888, -2.315790869867006219, -7.133520354428148025 ) ) ;
ENDSEC;
END-ISO-10303-21;
